ISO-10303-21;
HEADER;
FILE_DESCRIPTION (('STEP AP203'),
    '1' );
FILE_NAME ('Aloris-BXA-Center-Rod.step',
    '2026-10-07T20:09:13',
    ( '' ),
    ( '' ),
    'SwSTEP 2.0',
    'SolidWorks 2024',
    '' );
FILE_SCHEMA (( 'AUTOMOTIVE_DESIGN' ));
ENDSEC;

DATA;
#3=CARTESIAN_POINT ( 'NONE',  ( 1.910449006669871087E-17, 0.1986111111111107386, -0.3119999999999999996 ) ) ;
#4=CARTESIAN_POINT ( 'NONE',  ( 0.1993543840281267465, 4.595916666742532186, 0.1993543840281266633 ) ) ;
#6=CARTESIAN_POINT ( 'NONE',  ( -0.3119999999999999996, 4.772999999999998799, 0.000000000000000000 ) ) ;
#8=CARTESIAN_POINT ( 'NONE',  ( -0.1167790944451422702, 0.4555555554796890116, -0.2819296736111110424 ) ) ;
#9=ORIENTED_EDGE ( 'NONE', *, *, #4852, .T. ) ;
#11=CARTESIAN_POINT ( 'NONE',  ( -0.1993543840281266633, 0.1256944443685777957, -0.1993543840281266910 ) ) ;
#13=CARTESIAN_POINT ( 'NONE',  ( 0.000000000000000000, 5.384999999999999787, 0.000000000000000000 ) ) ;
#19=CARTESIAN_POINT ( 'NONE',  ( -0.1167790944451422702, 0.2194444443685778234, -0.2819296736111110979 ) ) ;
#20=CARTESIAN_POINT ( 'NONE',  ( 0.1993543840281266355, 0.02847222214635558926, 0.1993543840281267465 ) ) ;
#22=CARTESIAN_POINT ( 'NONE',  ( -1.726321361862525858E-17, 4.575083333409199149, -0.2819296736111110979 ) ) ;
#25=CARTESIAN_POINT ( 'NONE',  ( 0.1993543840281266633, 5.179250000075866112, -0.1993543840281266910 ) ) ;
#26=CARTESIAN_POINT ( 'NONE',  ( -0.2819296736111110979, 4.349388888964754507, -0.1167790944451422980 ) ) ;
#27=CARTESIAN_POINT ( 'NONE',  ( 0.3137165877996647145, 3.752159157235426701, 0.001669988021508127815 ) ) ;
#30=ADVANCED_FACE ( 'NONE', ( #19654 ), #17708, .T. ) ;
#31=CARTESIAN_POINT ( 'NONE',  ( -0.1292346314604057023, 4.123694444596177178, 0.3119999999999998885 ) ) ;
#32=CARTESIAN_POINT ( 'NONE',  ( -0.2819296736111110979, 4.533416666742532186, 0.000000000000000000 ) ) ;
#33=DIRECTION ( 'NONE',  ( 0.000000000000000000, 0.7071067811865497932, 0.7071067811865452413 ) ) ;
#34=EDGE_CURVE ( 'NONE', #12593, #3702, #6524, .T. ) ;
#40=FACE_OUTER_BOUND ( 'NONE', #1469, .T. ) ;
#44=CARTESIAN_POINT ( 'NONE',  ( -0.3119999999999999996, 0.4277777776260448528, -3.820898013339742174E-17 ) ) ;
#47=CARTESIAN_POINT ( 'NONE',  ( -0.3140464948364212194, 3.723602166599303764, -0.02909203108594766995 ) ) ;
#49=CARTESIAN_POINT ( 'NONE',  ( 0.1916168258699956772, 3.966268988801258555, 0.2495847059250467792 ) ) ;
#50=ORIENTED_EDGE ( 'NONE', *, *, #21102, .T. ) ;
#55=CARTESIAN_POINT ( 'NONE',  ( 0.1167790944451422702, 4.279944444520310753, -0.2819296736111110424 ) ) ;
#56=CARTESIAN_POINT ( 'NONE',  ( 5.178964085587577574E-17, 5.033416666742532186, 0.2819296736111110979 ) ) ;
#60=CARTESIAN_POINT ( 'NONE',  ( -0.1292346314604057023, 3.894527777777776478, 0.3119999999999998885 ) ) ;
#62=ADVANCED_FACE ( 'NONE', ( #18066 ), #7215, .T. ) ;
#63=CARTESIAN_POINT ( 'NONE',  ( 0.1292346314604056190, 4.707027777929510215, -0.3119999999999999996 ) ) ;
#64=CARTESIAN_POINT ( 'NONE',  ( 0.1337853507730711877, 4.797771151123610522, 0.2837542960833542294 ) ) ;
#65=CARTESIAN_POINT ( 'NONE',  ( 0.2206173157302028232, 0.4138888888888885287, -0.2206173157302028232 ) ) ;
#70=VERTEX_POINT ( 'NONE', #16487 ) ;
#73=CARTESIAN_POINT ( 'NONE',  ( -0.2819296736111110424, 5.134111111186975940, 0.1167790944451424923 ) ) ;
#74=CARTESIAN_POINT ( 'NONE',  ( -0.2819296736111110979, 3.866750000075866112, 0.000000000000000000 ) ) ;
#79=CARTESIAN_POINT ( 'NONE',  ( 0.1993543840281266910, 0.1673611110352444808, -0.1993543840281266910 ) ) ;
#81=CARTESIAN_POINT ( 'NONE',  ( -0.1167790944451423257, 5.023000000075867000, -0.2819296736111110424 ) ) ;
#82=CARTESIAN_POINT ( 'NONE',  ( 0.1572276619573833301, 4.465128489813300128, 0.2725687012519474872 ) ) ;
#83=CARTESIAN_POINT ( 'NONE',  ( -0.2819296736111110424, 4.960500000075865223, -0.1167790944451423119 ) ) ;
#87=DIRECTION ( 'NONE',  ( 0.000000000000000000, 0.000000000000000000, -1.000000000000000000 ) ) ;
#88=CARTESIAN_POINT ( 'NONE',  ( 0.2206173157302028787, 4.460499999999998799, 0.2206173157302027954 ) ) ;
#90=CARTESIAN_POINT ( 'NONE',  ( 0.2819296736111110979, 3.773000000075866112, -0.1167790944451423396 ) ) ;
#92=CARTESIAN_POINT ( 'NONE',  ( 0.01188239640610571149, 4.043514080066898053, -0.3119999715909181903 ) ) ;
#93=CARTESIAN_POINT ( 'NONE',  ( -0.01999320810728339587, 3.737730494582271579, 0.3119999990119339817 ) ) ;
#94=ORIENTED_EDGE ( 'NONE', *, *, #21035, .F. ) ;
#99=AXIS2_PLACEMENT_3D ( 'NONE', #2316, #21202, #17426 ) ;
#101=( BOUNDED_CURVE ( )  B_SPLINE_CURVE ( 2, ( #22373, #3964, #5909, #11408, #18841, #2137, #22623, #13366, #20787 ),
 .UNSPECIFIED., .F., .F. ) 
 B_SPLINE_CURVE_WITH_KNOTS ( ( 3, 2, 2, 2, 3 ),
 ( 0.2767857142857141350, 0.2812499999999998335, 0.2857142857142855319, 0.2901785714285712858, 0.2946428571428569843 ),
 .UNSPECIFIED. ) 
 CURVE ( )  GEOMETRIC_REPRESENTATION_ITEM ( )  RATIONAL_B_SPLINE_CURVE ( ( 1.000000000000002887, 0.9238795325112838519, 1.000000000000000000, 0.9238795325112867385, 1.000000000000000000, 0.9238795325112867385, 1.000000000000000000, 0.9238795325112896251, 0.9999999999999971134 ) ) 
 REPRESENTATION_ITEM ( '' )  );
#103=CARTESIAN_POINT ( 'NONE',  ( -0.1292346314604058410, 0.3895833333333330040, 0.3119999999999998885 ) ) ;
#107=CARTESIAN_POINT ( 'NONE',  ( 1.726321361862525858E-17, 0.3270833332574666907, -0.2819296736111110979 ) ) ;
#110=CARTESIAN_POINT ( 'NONE',  ( -0.3119999999999999996, 0.1569444444444440812, -3.820898013339742174E-17 ) ) ;
#115=CARTESIAN_POINT ( 'NONE',  ( -0.3119999999999999996, 0.1013888888888885564, -3.820898013339742174E-17 ) ) ;
#116=CARTESIAN_POINT ( 'NONE',  ( -0.1292346314604057023, 5.061194444444443441, 0.3119999999999998885 ) ) ;
#119=CARTESIAN_POINT ( 'NONE',  ( -0.1167790944451423535, 4.210500000075866112, 0.2819296736111110424 ) ) ;
#120=CARTESIAN_POINT ( 'NONE',  ( 0.3119999999999998885, 0.1187499998482670627, 0.1292346314604058410 ) ) ;
#125=CARTESIAN_POINT ( 'NONE',  ( -0.1167790944451423257, 5.009111111186976828, -0.2819296736111110424 ) ) ;
#129=CARTESIAN_POINT ( 'NONE',  ( 0.001964067453944123073, 3.710447205286024897, -0.3119947023668593333 ) ) ;
#130=DIRECTION ( 'NONE',  ( 0.000000000000000000, 0.000000000000000000, -1.000000000000000000 ) ) ;
#131=CARTESIAN_POINT ( 'NONE',  ( 0.1167790944451422702, 4.613277777853643791, -0.2819296736111110979 ) ) ;
#135=CARTESIAN_POINT ( 'NONE',  ( -0.2819296736111110979, 0.4138888888130222155, 0.1167790944451422425 ) ) ;
#137=CARTESIAN_POINT ( 'NONE',  ( 0.2819296736111110979, 0.2715277777019111660, 0.000000000000000000 ) ) ;
#138=CARTESIAN_POINT ( 'NONE',  ( -0.1797761229313996068, 4.715880237781718165, -0.2556404866186153257 ) ) ;
#144=CARTESIAN_POINT ( 'NONE',  ( 1.726321361862525858E-17, 0.3270833332574666907, -0.2819296736111110979 ) ) ;
#146=CARTESIAN_POINT ( 'NONE',  ( 0.1167790944451422702, 4.293833333409199149, -0.2819296736111110424 ) ) ;
#148=CARTESIAN_POINT ( 'NONE',  ( -0.1167790944451423535, 4.766055555631421470, 0.2819296736111110424 ) ) ;
#151=CARTESIAN_POINT ( 'NONE',  ( -0.1167790944451423119, 4.453555555631420582, -0.2819296736111110979 ) ) ;
#153=EDGE_LOOP ( 'NONE', ( #3116, #23568, #3841, #12769 ) ) ;
#154=CARTESIAN_POINT ( 'NONE',  ( -0.07966834441866296745, 4.768317572005395633, -0.3042764398256994629 ) ) ;
#155=CARTESIAN_POINT ( 'NONE',  ( -1.910449006669871087E-17, 4.154944444596176290, -0.3119999999999999996 ) ) ;
#159=EDGE_LOOP ( 'NONE', ( #9188, #6198, #17290, #20083, #1245, #14099, #50 ) ) ;
#161=CARTESIAN_POINT ( 'NONE',  ( -0.3119999999999998885, 4.276472222222222008, 0.1292346314604058410 ) ) ;
#162=EDGE_LOOP ( 'NONE', ( #18983, #19188, #20187, #19564 ) ) ;
#163=CARTESIAN_POINT ( 'NONE',  ( -0.1953777901228682112, 4.843409774179208149, 0.2460124067163272643 ) ) ;
#167=CARTESIAN_POINT ( 'NONE',  ( 0.2206173157302027676, 0.3930555554038225874, 0.2206173157302028787 ) ) ;
#168=ORIENTED_EDGE ( 'NONE', *, *, #11879, .F. ) ;
#170=CARTESIAN_POINT ( 'NONE',  ( 0.2903256038615220636, 4.748660027621867563, 0.1207610085887053653 ) ) ;
#172=CARTESIAN_POINT ( 'NONE',  ( 0.3119530872320841475, 3.973196682663843848, 0.04116800644467977222 ) ) ;
#177=CARTESIAN_POINT ( 'NONE',  ( -0.3070879998666070088, 4.670587574863169777, 0.05874933755621322695 ) ) ;
#180=CARTESIAN_POINT ( 'NONE',  ( 5.178964085587577574E-17, 4.144527777853642903, 0.2819296736111110979 ) ) ;
#183=CARTESIAN_POINT ( 'NONE',  ( -0.2206173157302027676, 3.891055555555554601, 0.2206173157302028787 ) ) ;
#184=CARTESIAN_POINT ( 'NONE',  ( 0.1292346314604058410, 4.686194444596177178, 0.3119999999999998885 ) ) ;
#185=CARTESIAN_POINT ( 'NONE',  ( 0.07199389927938498746, 4.795915137278597307, 0.3053389904577915592 ) ) ;
#186=CARTESIAN_POINT ( 'NONE',  ( 0.1993543840281267465, 4.373694444520309865, 0.1993543840281266633 ) ) ;
#191=CARTESIAN_POINT ( 'NONE',  ( -0.03922876767354999128, 0.06005265186466097332, 0.3076901691082670753 ) ) ;
#196=CARTESIAN_POINT ( 'NONE',  ( -1.726321361862525858E-17, 5.172305555631420582, -0.2819296736111110979 ) ) ;
#198=CARTESIAN_POINT ( 'NONE',  ( -0.2819296736111110424, 3.925777777853644235, 0.1167790944451424923 ) ) ;
#200=CARTESIAN_POINT ( 'NONE',  ( -6.389700406101856968E-07, 4.404919069638722817, 0.3119999999986028949 ) ) ;
#202=ORIENTED_EDGE ( 'NONE', *, *, #20793, .T. ) ;
#204=CARTESIAN_POINT ( 'NONE',  ( 0.1167790944451423535, 0.5944444443685777957, 0.2819296736111110979 ) ) ;
#206=CARTESIAN_POINT ( 'NONE',  ( 0.2819296736111110424, 4.898000000075866112, -0.1167790944451423396 ) ) ;
#210=CARTESIAN_POINT ( 'NONE',  ( 0.1167790944451422702, 4.946611111186975940, -0.2819296736111110424 ) ) ;
#212=CARTESIAN_POINT ( 'NONE',  ( 0.2409776823595090323, 4.857164591472093562, 0.1984146367410583867 ) ) ;
#215=CARTESIAN_POINT ( 'NONE',  ( 5.731347020009612645E-17, 4.453555555555555046, 0.3119999999999999996 ) ) ;
#217=CARTESIAN_POINT ( 'NONE',  ( 0.1292346314604056745, 0.3548611109593781676, -0.3119999999999999996 ) ) ;
#218=CARTESIAN_POINT ( 'NONE',  ( 0.0007558196063935046592, 4.988256100791213399, -0.3119993132609195641 ) ) ;
#219=CARTESIAN_POINT ( 'NONE',  ( -0.1042511535495848213, 3.735277012539861108, 0.2940678913504243819 ) ) ;
#221=CARTESIAN_POINT ( 'NONE',  ( 0.3010133589939812948, 4.583146549113322976, 0.08341395606948878716 ) ) ;
#224=AXIS2_PLACEMENT_3D ( 'NONE', #22932, #10391, #12107 ) ;
#225=CARTESIAN_POINT ( 'NONE',  ( 0.1785406736446525644, 4.649568862857817564, -0.2599013730876763573 ) ) ;
#234=CARTESIAN_POINT ( 'NONE',  ( 0.1993543840281266355, 0.4173611110352444808, 0.1993543840281267465 ) ) ;
#237=CARTESIAN_POINT ( 'NONE',  ( -0.3120000000000000551, 0.1604166666666663188, 0.1292346314604056190 ) ) ;
#239=EDGE_CURVE ( 'NONE', #8265, #17235, #2483, .T. ) ;
#240=CARTESIAN_POINT ( 'NONE',  ( -0.3003085958321041748, 5.103171429360789269, -0.08162789287472543842 ) ) ;
#242=CARTESIAN_POINT ( 'NONE',  ( 0.1292346314604056745, 0.2506944444444441089, -0.3119999999999999996 ) ) ;
#243=CARTESIAN_POINT ( 'NONE',  ( -1.910449006669871087E-17, 5.092444444444443441, -0.3119999999999999996 ) ) ;
#245=CARTESIAN_POINT ( 'NONE',  ( 0.2819296736111110979, 4.279944444520310753, 0.1167790944451422425 ) ) ;
#246=CARTESIAN_POINT ( 'NONE',  ( -0.3119999999999999996, 3.825083333333333169, -0.1292346314604056468 ) ) ;
#250=CARTESIAN_POINT ( 'NONE',  ( 0.1167790944451424368, 4.981333333409198261, 0.2819296736111110424 ) ) ;
#253=CARTESIAN_POINT ( 'NONE',  ( -5.731347020009612645E-17, 0.6083333331816004330, 0.3119999999999999996 ) ) ;
#254=CARTESIAN_POINT ( 'NONE',  ( 0.2819296736111111534, 4.599388888964754507, 0.1167790944451422563 ) ) ;
#256=CARTESIAN_POINT ( 'NONE',  ( 0.1292346314604058410, 4.290361111111110404, 0.3119999999999998885 ) ) ;
#258=CARTESIAN_POINT ( 'NONE',  ( 0.1993543840281266910, 0.5006944443685779067, -0.1993543840281266910 ) ) ;
#259=ORIENTED_EDGE ( 'NONE', *, *, #15539, .F. ) ;
#260=CARTESIAN_POINT ( 'NONE',  ( -0.2819296736111110424, 0.1291666665908000611, -0.1167790944451423396 ) ) ;
#268=CARTESIAN_POINT ( 'NONE',  ( 0.1167790944451423535, 0.1916666665908000056, 0.2819296736111110979 ) ) ;
#269=CARTESIAN_POINT ( 'NONE',  ( 0.2819296736111110979, 0.1465277777019111383, 0.000000000000000000 ) ) ;
#270=CARTESIAN_POINT ( 'NONE',  ( -0.1167790944451423535, 4.321611111186976828, 0.2819296736111110424 ) ) ;
#272=CARTESIAN_POINT ( 'NONE',  ( -1.726321361862525858E-17, 4.852861111186976828, -0.2819296736111110979 ) ) ;
#273=CARTESIAN_POINT ( 'NONE',  ( 0.2819296736111111534, 4.377166666742532186, 0.1167790944451422563 ) ) ;
#274=CARTESIAN_POINT ( 'NONE',  ( -6.528214817076446933E-07, 5.071585437816050757, 0.3119999999985565986 ) ) ;
#275=AXIS2_PLACEMENT_3D ( 'NONE', #1586, #7436, #11218 ) ;
#276=DIRECTION ( 'NONE',  ( 0.000000000000000000, 0.000000000000000000, -1.000000000000000000 ) ) ;
#277=CARTESIAN_POINT ( 'NONE',  ( 0.2206173157302027954, 4.092444444596176290, -0.2206173157302028232 ) ) ;
#284=CARTESIAN_POINT ( 'NONE',  ( -0.1566814371109810367, 4.992845198620254443, -0.2728731690866343929 ) ) ;
#286=CARTESIAN_POINT ( 'NONE',  ( 0.2206173157302028232, 0.5180555554038226429, -0.2206173157302028232 ) ) ;
#291=CARTESIAN_POINT ( 'NONE',  ( -0.3120000000000000551, 0.5493055555555551583, 0.1292346314604056190 ) ) ;
#296=EDGE_LOOP ( 'NONE', ( #12056, #1155, #20586, #17433 ) ) ;
#299=CARTESIAN_POINT ( 'NONE',  ( 5.731347020009612645E-17, 4.064666666666665762, 0.3119999999999999996 ) ) ;
#300=CARTESIAN_POINT ( 'NONE',  ( 0.1167790944451422702, 4.057722222298087544, -0.2819296736111110424 ) ) ;
#303=CARTESIAN_POINT ( 'NONE',  ( -0.2206173157302028232, 3.932722222222221120, -0.2206173157302028232 ) ) ;
#304=CARTESIAN_POINT ( 'NONE',  ( 0.1292346314604056190, 4.762583333485065573, -0.3119999999999999996 ) ) ;
#305=CARTESIAN_POINT ( 'NONE',  ( -0.2819296736111110979, 4.863277777853643791, -0.1167790944451422980 ) ) ;
#308=CARTESIAN_POINT ( 'NONE',  ( 0.1167790944451422702, 4.335500000075866112, -0.2819296736111110424 ) ) ;
#313=ORIENTED_EDGE ( 'NONE', *, *, #4837, .T. ) ;
#316=SPHERICAL_SURFACE ( 'NONE', #20439, 0.3119999999999999996 ) ;
#317=CARTESIAN_POINT ( 'NONE',  ( -0.1167790944451423257, 5.120222222298088433, -0.2819296736111110424 ) ) ;
#318=CARTESIAN_POINT ( 'NONE',  ( -0.2819296736111110424, 3.814666666742532630, 0.1167790944451424923 ) ) ;
#319=CARTESIAN_POINT ( 'NONE',  ( 0.04075291810813885807, 4.431559223094041045, -0.3099974353593557552 ) ) ;
#324=CARTESIAN_POINT ( 'NONE',  ( 0.2819296736111110979, 0.6083333332574668573, -0.1167790944451422980 ) ) ;
#326=CARTESIAN_POINT ( 'NONE',  ( -0.2819296736111110979, 4.977861111186976828, 0.000000000000000000 ) ) ;
#327=CARTESIAN_POINT ( 'NONE',  ( -1.910449006669871087E-17, 3.925777777777776922, -0.3119999999999999996 ) ) ;
#328=CARTESIAN_POINT ( 'NONE',  ( 0.2819296736111110979, 4.654944444520309865, 0.1167790944451422425 ) ) ;
#330=CARTESIAN_POINT ( 'NONE',  ( 0.08682016143536398778, 4.851954871454551288, 0.3004229350962410172 ) ) ;
#333=CARTESIAN_POINT ( 'NONE',  ( -0.3119999999999998885, 4.609805555555555046, 0.1292346314604058410 ) ) ;
#334=CARTESIAN_POINT ( 'NONE',  ( -0.1167790944451423535, 3.807722222298087988, 0.2819296736111110979 ) ) ;
#335=CARTESIAN_POINT ( 'NONE',  ( -1.910449006669871087E-17, 4.203555555555555046, -0.3119999999999999996 ) ) ;
#338=CARTESIAN_POINT ( 'NONE',  ( 0.03916719867818912321, 4.598255416773466386, -0.3119999648250499358 ) ) ;
#342=EDGE_CURVE ( 'NONE', #14624, #11367, #6577, .T. ) ;
#343=CARTESIAN_POINT ( 'NONE',  ( 0.3131180815194534173, 4.641677528921063889, -0.02196450506224391711 ) ) ;
#346=CARTESIAN_POINT ( 'NONE',  ( 0.3119529355813799310, 4.306505973446880020, 0.04122820550216244745 ) ) ;
#347=CARTESIAN_POINT ( 'NONE',  ( 0.1344534248014218336, 5.134761163306762910, 0.2754137591327791013 ) ) ;
#350=CARTESIAN_POINT ( 'NONE',  ( 0.1993543840281266355, 0.5840277777019111660, 0.1993543840281267465 ) ) ;
#357=CARTESIAN_POINT ( 'NONE',  ( 1.910449006669871087E-17, 0.1986111111111107386, -0.3119999999999999996 ) ) ;
#358=CARTESIAN_POINT ( 'NONE',  ( -0.3119999999999999996, 5.213972222222221120, -0.1292346314604056468 ) ) ;
#360=CARTESIAN_POINT ( 'NONE',  ( -0.2819296736111110424, 4.148000000075866112, 0.1167790944451424923 ) ) ;
#361=CARTESIAN_POINT ( 'NONE',  ( -0.2493918854782433692, 4.341271243197787122, 0.1918690073863245360 ) ) ;
#366=CARTESIAN_POINT ( 'NONE',  ( -0.1167790944451423257, 4.953555555631421470, -0.2819296736111110424 ) ) ;
#368=CARTESIAN_POINT ( 'NONE',  ( -0.3009367667953548597, 5.155896567499441474, 0.01723797010695745854 ) ) ;
#369=EDGE_CURVE ( 'NONE', #17235, #19258, #1125, .T. ) ;
#371=CARTESIAN_POINT ( 'NONE',  ( 8.973317209400627124E-05, 3.710497589222864434, -0.3120000002591014066 ) ) ;
#374=CARTESIAN_POINT ( 'NONE',  ( 0.1993543840281267465, 4.387583333409199149, 0.1993543840281266633 ) ) ;
#378=CARTESIAN_POINT ( 'NONE',  ( 0.2819296736111110424, 0.4902777777019112215, 0.1167790944451424923 ) ) ;
#379=CARTESIAN_POINT ( 'NONE',  ( 0.1167790944451423257, 0.5597222221463555858, -0.2819296736111110424 ) ) ;
#387=CARTESIAN_POINT ( 'NONE',  ( 0.1167790944451423535, 0.4694444443685777957, 0.2819296736111110979 ) ) ;
#388=CARTESIAN_POINT ( 'NONE',  ( -0.2819296736111110979, 0.1743055554796889284, -3.452642723725051716E-17 ) ) ;
#390=CARTESIAN_POINT ( 'NONE',  ( -0.2819296736111110424, 4.370222222298088433, 0.1167790944451424923 ) ) ;
#392=CARTESIAN_POINT ( 'NONE',  ( -0.1167790944451423535, 4.932722222298088433, 0.2819296736111110424 ) ) ;
#393=CARTESIAN_POINT ( 'NONE',  ( 0.2819296736111110979, 4.550777777853643791, -0.1167790944451423396 ) ) ;
#399=CARTESIAN_POINT ( 'NONE',  ( -0.2206173157302028232, 3.995222222373953969, -0.2206173157302028232 ) ) ;
#400=CARTESIAN_POINT ( 'NONE',  ( 1.910449006669871087E-17, 0.1430555555555552139, -0.3119999999999999996 ) ) ;
#402=EDGE_LOOP ( 'NONE', ( #17001, #2878, #11780, #16230 ) ) ;
#410=CARTESIAN_POINT ( 'NONE',  ( -0.3119999999999999996, 0.4833333331816003775, -3.820898013339742174E-17 ) ) ;
#413=CARTESIAN_POINT ( 'NONE',  ( 3.820898013339742174E-17, 5.384999999999999787, 0.3119999999999999996 ) ) ;
#414=DIRECTION ( 'NONE',  ( -0.000000000000000000, -1.000000000000000000, -0.000000000000000000 ) ) ;
#415=CARTESIAN_POINT ( 'NONE',  ( -0.3119999999999999996, 0.5423611111111107386, -0.1292346314604056745 ) ) ;
#417=CARTESIAN_POINT ( 'NONE',  ( 0.1469174392757871539, 5.171225737096911246, 0.2578308252673338630 ) ) ;
#418=ORIENTED_EDGE ( 'NONE', *, *, #12814, .T. ) ;
#422=CARTESIAN_POINT ( 'NONE',  ( 0.1993543840281266633, 4.054250000075865223, -0.1993543840281266910 ) ) ;
#426=CARTESIAN_POINT ( 'NONE',  ( -0.3119999999999999996, 4.668833333485065573, 0.000000000000000000 ) ) ;
#427=CARTESIAN_POINT ( 'NONE',  ( -1.726321361862525858E-17, 5.019527777853643791, -0.2819296736111110979 ) ) ;
#430=CARTESIAN_POINT ( 'NONE',  ( -1.726321361862525858E-17, 4.283416666742532186, -0.2819296736111110979 ) ) ;
#433=ADVANCED_FACE ( 'NONE', ( #11974 ), #14262, .T. ) ;
#440=CARTESIAN_POINT ( 'NONE',  ( -0.1167790944451423119, 3.856333333409199149, -0.2819296736111110979 ) ) ;
#441=CARTESIAN_POINT ( 'NONE',  ( 0.1058512031593883823, 4.429673085808546240, -0.2934957001599620141 ) ) ;
#442=CARTESIAN_POINT ( 'NONE',  ( 0.2206173157302027954, 4.641055555555554157, -0.2206173157302028232 ) ) ;
#445=CARTESIAN_POINT ( 'NONE',  ( 0.2819296736111110979, 0.5527777777019112770, -0.1167790944451422980 ) ) ;
#448=CARTESIAN_POINT ( 'NONE',  ( 0.1993543840281266633, 4.734805555631421470, -0.1993543840281266910 ) ) ;
#450=CARTESIAN_POINT ( 'NONE',  ( -0.1167790944451423257, 4.731333333409198261, -0.2819296736111110424 ) ) ;
#452=CARTESIAN_POINT ( 'NONE',  ( 0.2588148980552389400, 4.857971016408025200, 0.1753205476218995251 ) ) ;
#455=CARTESIAN_POINT ( 'NONE',  ( -0.2206173157302028232, 4.488277777777776478, -0.2206173157302028232 ) ) ;
#456=CARTESIAN_POINT ( 'NONE',  ( -0.2819296736111110979, 3.793833333409199149, -0.1167790944451422980 ) ) ;
#457=CARTESIAN_POINT ( 'NONE',  ( -0.1292346314604106428, 4.005638888888888083, 0.3119999999999950036 ) ) ;
#459=ORIENTED_EDGE ( 'NONE', *, *, #15967, .F. ) ;
#461=ORIENTED_EDGE ( 'NONE', *, *, #3849, .T. ) ;
#462=CARTESIAN_POINT ( 'NONE',  ( 0.3118815705390921011, 4.695382381602317245, 0.04185132024466815120 ) ) ;
#463=CARTESIAN_POINT ( 'NONE',  ( 3.887228417612631703E-07, 4.154944433789834690, -0.3119999999997578044 ) ) ;
#466=ORIENTED_EDGE ( 'NONE', *, *, #1277, .F. ) ;
#469=CARTESIAN_POINT ( 'NONE',  ( 0.2819296736111110424, 0.4277777777019111105, -0.1167790944451423119 ) ) ;
#471=CARTESIAN_POINT ( 'NONE',  ( 3.820898013339742174E-17, 5.384999999999999787, 0.3119999999999999996 ) ) ;
#472=CARTESIAN_POINT ( 'NONE',  ( 1.910449006669871087E-17, 0.1430555555555552139, -0.3119999999999999996 ) ) ;
#474=CARTESIAN_POINT ( 'NONE',  ( -0.2361897315408544862, 4.619585270958687317, 0.2066264843407155938 ) ) ;
#475=CARTESIAN_POINT ( 'NONE',  ( 1.910449006669871087E-17, 0.08749999999999966138, -0.3119999999999999996 ) ) ;
#477=CARTESIAN_POINT ( 'NONE',  ( 1.910449006669871087E-17, 0.3097222222222218435, -0.3119999999999999996 ) ) ;
#478=CARTESIAN_POINT ( 'NONE',  ( -0.3119999999999999996, 5.106333333333332725, 0.000000000000000000 ) ) ;
#480=CARTESIAN_POINT ( 'NONE',  ( 0.1167790944451422702, 4.127166666742532186, -0.2819296736111110424 ) ) ;
#481=CARTESIAN_POINT ( 'NONE',  ( -0.1571792371097448515, 4.326278488575934666, -0.2725945807372967544 ) ) ;
#484=ORIENTED_EDGE ( 'NONE', *, *, #13372, .F. ) ;
#486=CARTESIAN_POINT ( 'NONE',  ( -0.2819296736111110424, 4.800777777853643791, 0.1167790944451424923 ) ) ;
#489=CARTESIAN_POINT ( 'NONE',  ( -0.02861657392953457710, 4.515272125417114424, 0.3106861733379689405 ) ) ;
#491=CARTESIAN_POINT ( 'NONE',  ( 0.3119999999999998885, 0.6187499998482670627, 0.1292346314604058410 ) ) ;
#492=CARTESIAN_POINT ( 'NONE',  ( 0.1167790944451424506, 4.217444444520309865, 0.2819296736111110424 ) ) ;
#494=CARTESIAN_POINT ( 'NONE',  ( -0.2031932902514208272, 4.050132635743126208, -0.2367657278459141534 ) ) ;
#497=CARTESIAN_POINT ( 'NONE',  ( 0.2819296736111110424, 0.4416666665908000056, -0.1167790944451423119 ) ) ;
#505=CARTESIAN_POINT ( 'NONE',  ( -5.178964085587577574E-17, 0.5215277777019111660, 0.2819296736111110979 ) ) ;
#506=CARTESIAN_POINT ( 'NONE',  ( 0.2819296736111110424, 0.1430555554796889284, 0.1167790944451424923 ) ) ;
#507=CARTESIAN_POINT ( 'NONE',  ( 0.1167790944451424368, 4.384111111186976828, 0.2819296736111110424 ) ) ;
#510=CARTESIAN_POINT ( 'NONE',  ( -0.1167790944451423257, 4.800777777853643791, -0.2819296736111110424 ) ) ;
#511=CARTESIAN_POINT ( 'NONE',  ( 5.178964085587577574E-17, 4.144527777853642903, 0.2819296736111110979 ) ) ;
#514=CARTESIAN_POINT ( 'NONE',  ( 0.2206173157302027954, 3.870222222373954413, -0.2206173157302028232 ) ) ;
#518=ORIENTED_EDGE ( 'NONE', *, *, #538, .F. ) ;
#522=CARTESIAN_POINT ( 'NONE',  ( -0.2740748391469606249, 5.006672122428321714, 0.1502628184871280526 ) ) ;
#524=CARTESIAN_POINT ( 'NONE',  ( 1.726321361862525858E-17, 0.06319444436857780956, -0.2819296736111110979 ) ) ;
#525=EDGE_CURVE ( 'NONE', #11560, #14350, #13656, .T. ) ;
#530=CARTESIAN_POINT ( 'NONE',  ( 0.002608860322658908878, 4.765981492550016796, -0.3119906577544150905 ) ) ;
#532=CARTESIAN_POINT ( 'NONE',  ( 0.2898213196250513102, 5.180044785969154297, -0.04452301891601496975 ) ) ;
#536=CARTESIAN_POINT ( 'NONE',  ( -0.3119999999999998885, 4.054249999999999687, 0.1292346314604058410 ) ) ;
#538=EDGE_CURVE ( 'NONE', #12392, #3340, #18037, .T. ) ;
#539=CARTESIAN_POINT ( 'NONE',  ( 0.1993543840281267465, 4.040361111186976828, 0.1993543840281266633 ) ) ;
#541=CARTESIAN_POINT ( 'NONE',  ( 8.984713656453739555E-13, 5.162518060853549251, -0.2988821118451543968 ) ) ;
#542=CARTESIAN_POINT ( 'NONE',  ( -0.1292346314604056745, 4.825083333485066461, -0.3119999999999999996 ) ) ;
#543=CARTESIAN_POINT ( 'NONE',  ( -0.1167790944451423119, 4.967444444520310753, -0.2819296736111110979 ) ) ;
#545=CARTESIAN_POINT ( 'NONE',  ( 0.1993543840281266633, 4.276472222298087544, -0.1993543840281266910 ) ) ;
#551=VECTOR ( 'NONE', #33, 39.37007874015748143 ) ;
#552=FACE_OUTER_BOUND ( 'NONE', #3950, .T. ) ;
#554=CARTESIAN_POINT ( 'NONE',  ( -0.3119999999999999996, 0.09791666651493373397, 0.1292346314604056190 ) ) ;
#555=CARTESIAN_POINT ( 'NONE',  ( 0.1698237203583192467, 4.427710968560108817, -0.2637982107419344358 ) ) ;
#560=CARTESIAN_POINT ( 'NONE',  ( -0.2819296736111110979, 0.4624999999241333759, -0.1167790944451423396 ) ) ;
#564=CARTESIAN_POINT ( 'NONE',  ( -0.2819296736111110424, 4.641055555631422358, -0.1167790944451423119 ) ) ;
#567=CARTESIAN_POINT ( 'NONE',  ( 5.178964085587577574E-17, 4.644527777853642903, 0.2819296736111110979 ) ) ;
#569=CYLINDRICAL_SURFACE ( 'NONE', #13680, 0.3119999999999999996 ) ;
#572=CARTESIAN_POINT ( 'NONE',  ( 0.2206173157302027954, 4.252166666666665762, -0.2206173157302028232 ) ) ;
#573=CARTESIAN_POINT ( 'NONE',  ( -0.2819296736111110979, 3.797305555631421470, 0.000000000000000000 ) ) ;
#575=DIRECTION ( 'NONE',  ( -0.000000000000000000, -1.000000000000000000, -0.000000000000000000 ) ) ;
#579=ORIENTED_EDGE ( 'NONE', *, *, #18990, .T. ) ;
#580=( BOUNDED_CURVE ( )  B_SPLINE_CURVE ( 2, ( #15781, #4678, #899, #4561, #19800, #3097, #781, #8211, #8694 ),
 .UNSPECIFIED., .F., .T. ) 
 B_SPLINE_CURVE_WITH_KNOTS ( ( 3, 2, 2, 2, 3 ),
 ( 0.1041666666666666713, 0.1145833333333333287, 0.1250000000000000000, 0.1354166666666666574, 0.1458333333333333426 ),
 .UNSPECIFIED. ) 
 CURVE ( )  GEOMETRIC_REPRESENTATION_ITEM ( )  RATIONAL_B_SPLINE_CURVE ( ( 1.000000000000000000, 0.9238795325112867385, 1.000000000000000000, 0.9238795325112867385, 1.000000000000000000, 0.9238795325112867385, 1.000000000000000000, 0.9238795325112867385, 1.000000000000000000 ) ) 
 REPRESENTATION_ITEM ( '' )  );
#583=CARTESIAN_POINT ( 'NONE',  ( 0.3035962428291631987, 4.694232598334442841, 0.08277057684829301765 ) ) ;
#586=VECTOR ( 'NONE', #16991, 39.37007874015748143 ) ;
#587=CARTESIAN_POINT ( 'NONE',  ( 0.1914943533321577518, 4.299605383836522243, 0.2496738231090171456 ) ) ;
#588=EDGE_LOOP ( 'NONE', ( #11742, #10987, #11274, #3654 ) ) ;
#590=CARTESIAN_POINT ( 'NONE',  ( -0.1167790944451422702, 0.4416666665908000611, -0.2819296736111110424 ) ) ;
#591=CARTESIAN_POINT ( 'NONE',  ( -0.1048218097661234444, 5.206640035683669510, 0.2619026841321052124 ) ) ;
#596=CARTESIAN_POINT ( 'NONE',  ( -0.1635002882892696296, 4.622259302225510069, 0.2657784613148136410 ) ) ;
#600=CARTESIAN_POINT ( 'NONE',  ( -5.731347020009612645E-17, 0.1708333333333330040, 0.3119999999999999996 ) ) ;
#601=CARTESIAN_POINT ( 'NONE',  ( 0.2206173157302027954, 4.974388888888888083, -0.2206173157302028232 ) ) ;
#602=CARTESIAN_POINT ( 'NONE',  ( -0.1993543840281266355, 4.095916666742533074, 0.1993543840281267465 ) ) ;
#606=VERTEX_POINT ( 'NONE', #6943 ) ;
#609=CARTESIAN_POINT ( 'NONE',  ( 0.2819296736111110424, 4.773000000075865223, -0.1167790944451423396 ) ) ;
#613=CARTESIAN_POINT ( 'NONE',  ( 5.463034709641816805E-17, 5.167344860100310910, 0.2973937581265823082 ) ) ;
#616=CARTESIAN_POINT ( 'NONE',  ( 0.3119999999999999996, 0.6222222220704892726, 0.000000000000000000 ) ) ;
#618=CARTESIAN_POINT ( 'NONE',  ( 0.1167790944451422702, 4.349388888964754507, -0.2819296736111110979 ) ) ;
#624=CARTESIAN_POINT ( 'NONE',  ( -0.2819296736111110979, 0.3583333332574666907, 0.1167790944451422425 ) ) ;
#625=CARTESIAN_POINT ( 'NONE',  ( 4.282505654011733572E-07, 3.932722210548942776, -0.3119999999997061790 ) ) ;
#629=CARTESIAN_POINT ( 'NONE',  ( 0.3119999999999999996, 3.970916666666665318, -0.1292346314604056745 ) ) ;
#630=CARTESIAN_POINT ( 'NONE',  ( 0.2206173157302028787, 5.016055555555554157, 0.2206173157302027954 ) ) ;
#631=CARTESIAN_POINT ( 'NONE',  ( -0.2819296736111110979, 0.5597222221463555858, -0.1167790944451423396 ) ) ;
#632=CARTESIAN_POINT ( 'NONE',  ( -0.2819296736111110424, 0.2819444443685777957, -0.1167790944451423396 ) ) ;
#633=CARTESIAN_POINT ( 'NONE',  ( -0.1993543840281266355, 4.207027777853643791, 0.1993543840281267465 ) ) ;
#635=CARTESIAN_POINT ( 'NONE',  ( -0.1167790944451423257, 4.856333333409199149, -0.2819296736111110424 ) ) ;
#640=CARTESIAN_POINT ( 'NONE',  ( 0.2206173157302028787, 3.745222222373954413, 0.2206173157302027954 ) ) ;
#646=EDGE_CURVE ( 'NONE', #2198, #7226, #16693, .T. ) ;
#648=CARTESIAN_POINT ( 'NONE',  ( -0.2300939842550158432, 5.008739598255579573, 0.2107150241362776288 ) ) ;
#650=CARTESIAN_POINT ( 'NONE',  ( -0.1167790944451424368, 0.1430555554796889284, 0.2819296736111110424 ) ) ;
#656=CARTESIAN_POINT ( 'NONE',  ( 0.03852464118876493954, 5.189404391384640824, -0.2870586899848421303 ) ) ;
#660=CARTESIAN_POINT ( 'NONE',  ( -0.2499225477423614450, 4.674556910496129980, 0.1869683874588545791 ) ) ;
#661=CARTESIAN_POINT ( 'NONE',  ( -0.1167790944451423257, 4.009111111186976828, -0.2819296736111110424 ) ) ;
#662=CARTESIAN_POINT ( 'NONE',  ( 2.064578755398029967E-15, 5.043833333485014947, -0.3119999999999999996 ) ) ;
#663=CARTESIAN_POINT ( 'NONE',  ( -0.07624758732758733781, 5.194631950919444741, 0.2776879540135884228 ) ) ;
#664=CARTESIAN_POINT ( 'NONE',  ( 0.3119999999999999996, 4.422305555707287894, -0.1292346314604056745 ) ) ;
#665=CARTESIAN_POINT ( 'NONE',  ( -0.1993543840281266910, 4.970916666742532186, -0.1993543840281266910 ) ) ;
#666=EDGE_CURVE ( 'NONE', #787, #19238, #18451, .T. ) ;
#669=CARTESIAN_POINT ( 'NONE',  ( 0.2819296736111110424, 3.995222222298087544, -0.1167790944451423396 ) ) ;
#670=EDGE_CURVE ( 'NONE', #23659, #6065, #12081, .T. ) ;
#678=ORIENTED_EDGE ( 'NONE', *, *, #19419, .T. ) ;
#681=CARTESIAN_POINT ( 'NONE',  ( -0.3119999999999999996, 0.1465277776260448805, -0.1292346314604056745 ) ) ;
#682=CARTESIAN_POINT ( 'NONE',  ( 0.07114610157022679959, 4.406947439583936088, 0.3037810326460302912 ) ) ;
#686=CARTESIAN_POINT ( 'NONE',  ( 0.1167790944451423535, 0.4833333332574666907, 0.2819296736111110979 ) ) ;
#689=CARTESIAN_POINT ( 'NONE',  ( 0.2819296736111110979, 4.724388888964754507, 0.1167790944451422425 ) ) ;
#691=CARTESIAN_POINT ( 'NONE',  ( 0.2819296736111110424, 4.717444444520309865, -0.1167790944451423396 ) ) ;
#693=CARTESIAN_POINT ( 'NONE',  ( 0.2906999326536478523, 4.866559060925098379, -0.1133051895180592905 ) ) ;
#696=CARTESIAN_POINT ( 'NONE',  ( -0.2206173157302028232, 4.321611111111110404, -0.2206173157302028232 ) ) ;
#697=AXIS2_PLACEMENT_3D ( 'NONE', #16054, #6536, #19464 ) ;
#698=CARTESIAN_POINT ( 'NONE',  ( -0.2206173157302027676, 5.120222222373953969, 0.2206173157302028787 ) ) ;
#699=EDGE_LOOP ( 'NONE', ( #23726, #16988, #20171, #18010 ) ) ;
#701=CARTESIAN_POINT ( 'NONE',  ( 0.1608054620978590921, 4.576414215844414990, 0.2688593698499974205 ) ) ;
#702=ORIENTED_EDGE ( 'NONE', *, *, #20635, .F. ) ;
#705=CARTESIAN_POINT ( 'NONE',  ( -3.990790521751304672E-07, 4.654944455680286808, -0.3119999999997447038 ) ) ;
#708=CARTESIAN_POINT ( 'NONE',  ( 0.08172490057555677201, 4.319272503786364403, -0.3038674704060840281 ) ) ;
#711=CARTESIAN_POINT ( 'NONE',  ( -5.178964085587577574E-17, 0.4104166665908000056, 0.2819296736111110979 ) ) ;
#712=FACE_OUTER_BOUND ( 'NONE', #6881, .T. ) ;
#714=FACE_OUTER_BOUND ( 'NONE', #18143, .T. ) ;
#716=ORIENTED_EDGE ( 'NONE', *, *, #14992, .F. ) ;
#720=CARTESIAN_POINT ( 'NONE',  ( 0.3119999999999998885, 0.2368055555555552416, 0.1292346314604058410 ) ) ;
#721=CARTESIAN_POINT ( 'NONE',  ( -0.3119999999999998885, 4.943138888888888083, 0.1292346314604058410 ) ) ;
#722=CARTESIAN_POINT ( 'NONE',  ( 5.178964085587577574E-17, 3.880638888964754951, 0.2819296736111110979 ) ) ;
#725=CARTESIAN_POINT ( 'NONE',  ( 0.3109237511666488318, 4.807014546080258910, 0.02589370761429525894 ) ) ;
#726=( BOUNDED_CURVE ( )  B_SPLINE_CURVE ( 2, ( #21271, #14984, #20582, #13399, #3879, #22405, #13842, #217, #15222 ),
 .UNSPECIFIED., .F., .F. ) 
 B_SPLINE_CURVE_WITH_KNOTS ( ( 3, 2, 2, 2, 3 ),
 ( 0.4791666666666666852, 0.4895833333333333148, 0.5000000000000000000, 0.5104166666666666297, 0.5208333333333333703 ),
 .UNSPECIFIED. ) 
 CURVE ( )  GEOMETRIC_REPRESENTATION_ITEM ( )  RATIONAL_B_SPLINE_CURVE ( ( 1.000000000000000000, 0.9238795325112867385, 1.000000000000000000, 0.9238795325112867385, 1.000000000000000000, 0.9238795325112867385, 1.000000000000000000, 0.9238795325112867385, 1.000000000000000000 ) ) 
 REPRESENTATION_ITEM ( '' )  );
#730=CARTESIAN_POINT ( 'NONE',  ( -0.2819296736111110424, 4.793833333409199149, -0.1167790944451423119 ) ) ;
#735=CARTESIAN_POINT ( 'NONE',  ( 0.2206173157302028232, 0.6291666665149338034, -0.2206173157302028232 ) ) ;
#737=CARTESIAN_POINT ( 'NONE',  ( 5.178964085587577574E-17, 4.269527777853643791, 0.2819296736111110979 ) ) ;
#738=CARTESIAN_POINT ( 'NONE',  ( -0.1962930875501540939, 4.049869897624702730, -0.2425499489820887034 ) ) ;
#742=CARTESIAN_POINT ( 'NONE',  ( 0.1167790944451423535, 0.4833333332574667462, 0.2819296736111110424 ) ) ;
#744=CARTESIAN_POINT ( 'NONE',  ( 0.1292346314604105595, 4.477861111111109516, -0.3119999999999950591 ) ) ;
#749=CARTESIAN_POINT ( 'NONE',  ( -0.1993543840281267465, 0.4590277777019111105, 0.1993543840281266633 ) ) ;
#750=CARTESIAN_POINT ( 'NONE',  ( -0.1993543840281266633, 0.2784722221463555858, -0.1993543840281266910 ) ) ;
#751=CARTESIAN_POINT ( 'NONE',  ( 0.1167790944451422702, 3.960500000075866556, -0.2819296736111110424 ) ) ;
#753=CARTESIAN_POINT ( 'NONE',  ( 0.1167790944451424368, 4.550777777853644679, 0.2819296736111110424 ) ) ;
#754=CARTESIAN_POINT ( 'NONE',  ( 1.910449006669871087E-17, 0.1361111109593781676, -0.3119999999999999996 ) ) ;
#757=CARTESIAN_POINT ( 'NONE',  ( 0.3119999999999999996, 3.859805555707287450, 0.1292346314604056190 ) ) ;
#762=DIRECTION ( 'NONE',  ( -0.000000000000000000, -1.000000000000000000, -0.000000000000000000 ) ) ;
#766=CARTESIAN_POINT ( 'NONE',  ( -0.2338183013878962213, 5.008588309138786165, 0.2066192498384957776 ) ) ;
#768=CARTESIAN_POINT ( 'NONE',  ( -0.1993543840281266633, 0.1812499999241333482, -0.1993543840281266910 ) ) ;
#770=CARTESIAN_POINT ( 'NONE',  ( 0.2842112554124473500, 4.255934241376375660, -0.1287169935595789960 ) ) ;
#772=CARTESIAN_POINT ( 'NONE',  ( 7.699581739047377146E-15, 4.099388889040679551, -0.3119999999999999996 ) ) ;
#774=CARTESIAN_POINT ( 'NONE',  ( 0.1938699776224440674, 5.185072709559078064, -0.2174650966580584655 ) ) ;
#780=CARTESIAN_POINT ( 'NONE',  ( -0.1167790944451423535, 4.085500000075865223, 0.2819296736111110424 ) ) ;
#781=CARTESIAN_POINT ( 'NONE',  ( -0.2206173157302028787, 0.1013888887371559577, 0.2206173157302027954 ) ) ;
#782=CARTESIAN_POINT ( 'NONE',  ( -0.1792825390751967840, 5.189912767811706296, 0.2278189856582707729 ) ) ;
#784=CARTESIAN_POINT ( 'NONE',  ( 0.3119999999999999996, 4.526472222373955745, 0.1292346314604056190 ) ) ;
#786=CARTESIAN_POINT ( 'NONE',  ( 0.1167790944451422702, 4.904944444520310753, -0.2819296736111110979 ) ) ;
#787=VERTEX_POINT ( 'NONE', #705 ) ;
#788=CARTESIAN_POINT ( 'NONE',  ( 0.1167790944451424368, 4.092444444520309865, 0.2819296736111110424 ) ) ;
#789=VERTEX_POINT ( 'NONE', #11944 ) ;
#798=CARTESIAN_POINT ( 'NONE',  ( -0.3119999999999999996, 0.03541666651493374784, -0.1292346314604056745 ) ) ;
#799=LINE ( 'NONE', #7545, #21796 ) ;
#800=LINE ( 'NONE', #23333, #4506 ) ;
#802=CARTESIAN_POINT ( 'NONE',  ( -0.3119999999999999996, 4.936194444444443441, -0.1292346314604056468 ) ) ;
#803=FACE_OUTER_BOUND ( 'NONE', #402, .T. ) ;
#804=CARTESIAN_POINT ( 'NONE',  ( 0.1167790944451423119, 0.6152777777019110550, -0.2819296736111110979 ) ) ;
#807=CARTESIAN_POINT ( 'NONE',  ( 1.726321361862525858E-17, 0.6187499999241333759, -0.2819296736111110979 ) ) ;
#808=CARTESIAN_POINT ( 'NONE',  ( -0.1993543840281266910, 4.679250000075866112, -0.1993543840281266910 ) ) ;
#814=CARTESIAN_POINT ( 'NONE',  ( 0.3119999999999999996, 4.359805555555555046, -0.1292346314604056745 ) ) ;
#816=CARTESIAN_POINT ( 'NONE',  ( 0.3119999999999999996, 5.082027777929511103, 0.1292346314604056190 ) ) ;
#818=CARTESIAN_POINT ( 'NONE',  ( 0.3108786273261404665, 4.973666332255019640, 0.02642876375196673636 ) ) ;
#820=CARTESIAN_POINT ( 'NONE',  ( 0.2556444780738587608, 4.580106500439447892, 0.1804377530121719919 ) ) ;
#822=CARTESIAN_POINT ( 'NONE',  ( 5.022068824175014099E-06, 4.710499865219635929, -0.3120000000021129760 ) ) ;
#823=CARTESIAN_POINT ( 'NONE',  ( 0.1907856466924852668, 4.133017441549366566, 0.2468700812986916737 ) ) ;
#824=ADVANCED_FACE ( 'NONE', ( #40 ), #14572, .T. ) ;
#828=EDGE_CURVE ( 'NONE', #4354, #12796, #17702, .T. ) ;
#831=CARTESIAN_POINT ( 'NONE',  ( 0.1167790944451423119, 0.05972222214635558579, -0.2819296736111110979 ) ) ;
#840=CARTESIAN_POINT ( 'NONE',  ( 0.1292346314604057023, 0.5631944444444441089, 0.3119999999999998885 ) ) ;
#841=CARTESIAN_POINT ( 'NONE',  ( 0.1292346314604056190, 4.977861111111110404, -0.3119999999999999996 ) ) ;
#842=CARTESIAN_POINT ( 'NONE',  ( -0.2819296736111110424, 4.092444444520309865, 0.1167790944451424923 ) ) ;
#848=VERTEX_POINT ( 'NONE', #8395 ) ;
#850=CARTESIAN_POINT ( 'NONE',  ( -0.1993543840281266910, 4.734805555631420582, -0.1993543840281266910 ) ) ;
#855=CARTESIAN_POINT ( 'NONE',  ( 0.1167790944451422702, 4.238277777853643791, -0.2819296736111110979 ) ) ;
#860=CARTESIAN_POINT ( 'NONE',  ( 0.1993543840281266910, 0.5006944443685777957, -0.1993543840281266910 ) ) ;
#866=CARTESIAN_POINT ( 'NONE',  ( -0.001104081132507200120, 3.766085226183863099, -0.3119983319538429667 ) ) ;
#867=CARTESIAN_POINT ( 'NONE',  ( -0.1993543840281266633, 0.4451388888130222710, -0.1993543840281266910 ) ) ;
#868=CARTESIAN_POINT ( 'NONE',  ( 0.1993543840281266355, 0.5284722221463555858, 0.1993543840281267465 ) ) ;
#869=CARTESIAN_POINT ( 'NONE',  ( -0.2819296736111110424, 4.036888888964754507, 0.1167790944451424923 ) ) ;
#873=CARTESIAN_POINT ( 'NONE',  ( 0.2819296736111110979, 4.672305555631421470, -3.452642723725051716E-17 ) ) ;
#876=CARTESIAN_POINT ( 'NONE',  ( 0.3085878716108892972, 5.079831059683014516, -0.04768157464158169490 ) ) ;
#879=CARTESIAN_POINT ( 'NONE',  ( -0.1292346314604057023, 3.845916666818398610, 0.3119999999999998885 ) ) ;
#881=CARTESIAN_POINT ( 'NONE',  ( 0.01440321200433056920, 0.03242967361111057795, 0.2819296736110772916 ) ) ;
#882=CARTESIAN_POINT ( 'NONE',  ( -7.892860322346445127E-13, 5.206640035683665957, 0.2819296736111106538 ) ) ;
#885=CARTESIAN_POINT ( 'NONE',  ( -0.2255988601820826389, 5.107692461630542802, -0.2129516302912839998 ) ) ;
#888=CARTESIAN_POINT ( 'NONE',  ( -5.178964085587577574E-17, 0.1465277777019111383, 0.2819296736111110979 ) ) ;
#889=ORIENTED_EDGE ( 'NONE', *, *, #5537, .F. ) ;
#890=CARTESIAN_POINT ( 'NONE',  ( 0.3039227669911347962, 4.254450600140130767, -0.08153721476616594688 ) ) ;
#891=CARTESIAN_POINT ( 'NONE',  ( -0.2206173157302027954, 0.3166666666666663188, -0.2206173157302028232 ) ) ;
#894=CARTESIAN_POINT ( 'NONE',  ( 0.2934402123939894302, 5.178655305724935154, 0.01285040835610953142 ) ) ;
#898=CARTESIAN_POINT ( 'NONE',  ( 0.2819296736111110979, 5.224388888964754507, 0.1167790944451422425 ) ) ;
#899=CARTESIAN_POINT ( 'NONE',  ( -0.2206173157302027954, 0.08749999984826707655, -0.2206173157302028232 ) ) ;
#901=CARTESIAN_POINT ( 'NONE',  ( -0.2064834833177447981, 4.787537442838174506, 0.2372672924203171607 ) ) ;
#902=CARTESIAN_POINT ( 'NONE',  ( 5.731347020009612645E-17, 4.460500000151732536, 0.3119999999999999996 ) ) ;
#903=VECTOR ( 'NONE', #18861, 39.37007874015748143 ) ;
#904=CARTESIAN_POINT ( 'NONE',  ( 0.1167790944451422702, 4.682722222298088433, -0.2819296736111110979 ) ) ;
#907=CARTESIAN_POINT ( 'NONE',  ( -0.2819296736111110424, 4.134111111186976828, 0.1167790944451424923 ) ) ;
#908=EDGE_LOOP ( 'NONE', ( #16306, #2151, #2824, #8426 ) ) ;
#915=CARTESIAN_POINT ( 'NONE',  ( -0.2206173157302028787, 0.1013888887371559577, 0.2206173157302027954 ) ) ;
#919=CYLINDRICAL_SURFACE ( 'NONE', #3731, 0.3119999999999999996 ) ;
#920=CYLINDRICAL_SURFACE ( 'NONE', #12495, 0.3119999999999999996 ) ;
#924=CARTESIAN_POINT ( 'NONE',  ( -0.1167790944451423535, 4.529944444520309865, 0.2819296736111110424 ) ) ;
#925=CYLINDRICAL_SURFACE ( 'NONE', #11464, 0.3119999999999999996 ) ;
#929=CARTESIAN_POINT ( 'NONE',  ( 0.1292346314604056190, 4.200083333333332725, -0.3119999999999999996 ) ) ;
#930=CARTESIAN_POINT ( 'NONE',  ( 0.3109914489913703228, 4.973703627688673912, 0.02508773589508955792 ) ) ;
#933=CARTESIAN_POINT ( 'NONE',  ( 0.1311265150379480604, 4.706765840712305859, -0.2838643453171283970 ) ) ;
#937=CARTESIAN_POINT ( 'NONE',  ( 0.2287940570885543812, 4.134455149918617956, 0.2125776350808679938 ) ) ;
#939=FACE_OUTER_BOUND ( 'NONE', #20791, .T. ) ;
#942=CARTESIAN_POINT ( 'NONE',  ( 0.1993543840281266355, 0.04236111103524448085, 0.1993543840281267465 ) ) ;
#948=CARTESIAN_POINT ( 'NONE',  ( -0.1492859955951554296, 4.622732444181830047, 0.2739670279635503802 ) ) ;
#949=CARTESIAN_POINT ( 'NONE',  ( -0.2443338556138178186, 4.273966251018599394, -0.1950947543421605312 ) ) ;
#951=CARTESIAN_POINT ( 'NONE',  ( -0.2206173157302028787, 0.3861111111111107386, 0.2206173157302027954 ) ) ;
#952=CARTESIAN_POINT ( 'NONE',  ( -0.2206173157302027676, 4.946611111111110404, 0.2206173157302028787 ) ) ;
#953=CARTESIAN_POINT ( 'NONE',  ( -0.1167790944451423119, 4.286888888964754507, -0.2819296736111110979 ) ) ;
#954=CARTESIAN_POINT ( 'NONE',  ( 0.2819296736111110979, 4.057722222298088433, 0.1167790944451422425 ) ) ;
#959=ORIENTED_EDGE ( 'NONE', *, *, #12477, .F. ) ;
#962=CARTESIAN_POINT ( 'NONE',  ( -0.04084074333279361091, 4.014960638875646914, 0.3119999946968434190 ) ) ;
#963=CARTESIAN_POINT ( 'NONE',  ( -0.1993543840281266910, 4.790361111186976828, -0.1993543840281266910 ) ) ;
#965=CARTESIAN_POINT ( 'NONE',  ( -0.02574519130974469924, 4.515352010847526465, 0.3109365854241030735 ) ) ;
#967=EDGE_CURVE ( 'NONE', #9981, #22483, #2651, .T. ) ;
#973=CARTESIAN_POINT ( 'NONE',  ( 0.1167790944451424506, 3.995222222298087988, 0.2819296736111110424 ) ) ;
#980=CARTESIAN_POINT ( 'NONE',  ( -0.2819296736111110979, 0.1187499999241333620, -3.452642723725051716E-17 ) ) ;
#983=CARTESIAN_POINT ( 'NONE',  ( 0.1292346314604107538, 4.457027777777777366, 0.3119999999999950036 ) ) ;
#987=CARTESIAN_POINT ( 'NONE',  ( -0.08166736493278629883, 3.791608634910940800, 0.3038790671151373468 ) ) ;
#988=CARTESIAN_POINT ( 'NONE',  ( -0.1917386267986692094, 3.843661969516976917, 0.2494960182609696486 ) ) ;
#989=CARTESIAN_POINT ( 'NONE',  ( -0.1167790944451424368, 0.4069444443685779067, 0.2819296736111110424 ) ) ;
#990=CARTESIAN_POINT ( 'NONE',  ( 0.2819296736111110979, 4.113277777853643791, 0.1167790944451422425 ) ) ;
#993=CARTESIAN_POINT ( 'NONE',  ( 5.178964085587577574E-17, 4.713972222298088433, 0.2819296736111110979 ) ) ;
#994=DIRECTION ( 'NONE',  ( -0.000000000000000000, -1.000000000000000000, -0.000000000000000000 ) ) ;
#998=CARTESIAN_POINT ( 'NONE',  ( 0.1292346314604019553, 4.811194444444444329, -0.3120000000000036633 ) ) ;
#999=CARTESIAN_POINT ( 'NONE',  ( -1.910449006669871087E-17, 3.877166666818399055, -0.3119999999999999996 ) ) ;
#1003=CARTESIAN_POINT ( 'NONE',  ( 0.2413337927286317020, 0.03242967361111052244, 0.1464648618589436124 ) ) ;
#1004=B_SPLINE_CURVE_WITH_KNOTS ( 'NONE', 3,
 ( #1700, #12703, #23874, #24003, #22299, #16701, #7315, #20118, #7194, #5481, #12946, #5596, #13061, #11217, #20479, #18646, #12822, #1939, #9386, #18767, #14639, #16826, #22423, #2062, #22062, #9503, #5356, #13542, #2546, #19014 ),
 .UNSPECIFIED., .F., .F.,
 ( 4, 2, 1, 1, 1, 1, 1, 1, 2, 2, 2, 2, 2, 2, 2, 2, 2, 4 ),
 ( 0.8863390212757288333, 0.8863434829168148621, 0.8863479445579008908, 0.8863568678400728373, 0.8863747144044168413, 0.8864104075331049604, 0.8864817937904809764, 0.8866245663052331194, 0.8869101113347374055, 0.8874812013937460886, 0.8886233815117632329, 0.8909077417477977434, 0.8931921019838321429, 0.8954764622198666535, 0.8977608224559010530, 0.9000451826919354525, 0.9023295429279699631, 0.9046139031640043626 ),
 .UNSPECIFIED. ) ;
#1005=CARTESIAN_POINT ( 'NONE',  ( -0.1167790944451423535, 4.918833333409199149, 0.2819296736111110979 ) ) ;
#1007=ORIENTED_EDGE ( 'NONE', *, *, #22448, .T. ) ;
#1010=ORIENTED_EDGE ( 'NONE', *, *, #1279, .T. ) ;
#1011=CARTESIAN_POINT ( 'NONE',  ( 0.1993543840281266910, 0.0006944443685778149775, -0.1993543840281266910 ) ) ;
#1013=CARTESIAN_POINT ( 'NONE',  ( 0.2819296736111110424, 0.1083333332574667046, -0.1167790944451423119 ) ) ;
#1014=CARTESIAN_POINT ( 'NONE',  ( -0.2222495215503474397, 4.717448722450788168, -0.2199230339716857219 ) ) ;
#1017=CARTESIAN_POINT ( 'NONE',  ( -0.1292346314604007618, 4.484805555555555046, -0.3120000000000049400 ) ) ;
#1021=CARTESIAN_POINT ( 'NONE',  ( 0.1993543840281267465, 3.873694444520310309, 0.1993543840281266633 ) ) ;
#1022=CARTESIAN_POINT ( 'NONE',  ( 0.04846562453573687035, 5.017398224273947882, 0.3082233696503673959 ) ) ;
#1023=CARTESIAN_POINT ( 'NONE',  ( 0.1353437200857772471, 0.04934356402903733452, 0.2678729552212573695 ) ) ;
#1024=CARTESIAN_POINT ( 'NONE',  ( -0.2450396070443827401, 4.773971645789902851, -0.1971973324235511971 ) ) ;
#1025=CARTESIAN_POINT ( 'NONE',  ( 0.1292346314604058410, 4.519527777929509327, 0.3119999999999998885 ) ) ;
#1027=CARTESIAN_POINT ( 'NONE',  ( -0.1993543840281266355, 4.818138888964754507, 0.1993543840281267465 ) ) ;
#1029=CARTESIAN_POINT ( 'NONE',  ( -0.1993543840281266910, 4.123694444520309865, -0.1993543840281266910 ) ) ;
#1030=ORIENTED_EDGE ( 'NONE', *, *, #7036, .F. ) ;
#1031=( BOUNDED_CURVE ( )  B_SPLINE_CURVE ( 2, ( #17601, #8571, #891, #6616, #21494, #10531, #6501, #19665, #8322 ),
 .UNSPECIFIED., .F., .F. ) 
 B_SPLINE_CURVE_WITH_KNOTS ( ( 3, 2, 2, 2, 3 ),
 ( 0.5208333333333333703, 0.5312500000000000000, 0.5416666666666666297, 0.5520833333333333703, 0.5625000000000000000 ),
 .UNSPECIFIED. ) 
 CURVE ( )  GEOMETRIC_REPRESENTATION_ITEM ( )  RATIONAL_B_SPLINE_CURVE ( ( 1.000000000000000000, 0.9238795325112867385, 1.000000000000000000, 0.9238795325112867385, 1.000000000000000000, 0.9238795325112867385, 1.000000000000000000, 0.9238795325112867385, 1.000000000000000000 ) ) 
 REPRESENTATION_ITEM ( '' )  );
#1036=EDGE_CURVE ( 'NONE', #11353, #11100, #8248, .T. ) ;
#1038=CARTESIAN_POINT ( 'NONE',  ( 0.2206173157302028232, 0.4694444444444441089, -0.2206173157302028232 ) ) ;
#1041=CARTESIAN_POINT ( 'NONE',  ( -0.1246144517033525162, 4.380716919267113596, -0.2867501499782466046 ) ) ;
#1050=CARTESIAN_POINT ( 'NONE',  ( 0.1993543840281266633, 4.498694444520309865, -0.1993543840281266910 ) ) ;
#1053=PLANE ( 'NONE',  #15689 ) ;
#1055=CARTESIAN_POINT ( 'NONE',  ( 0.1292346314604056190, 4.311194444444443441, -0.3119999999999999996 ) ) ;
#1056=CARTESIAN_POINT ( 'NONE',  ( 0.1292346314604058410, 5.130638889040620931, 0.3119999999999998885 ) ) ;
#1057=CARTESIAN_POINT ( 'NONE',  ( 0.2831239686220249907, 4.970529875428314703, 0.1329317239649490667 ) ) ;
#1060=CARTESIAN_POINT ( 'NONE',  ( 0.2065268859206847996, 4.578017556304259550, 0.2355640099602401283 ) ) ;
#1061=CARTESIAN_POINT ( 'NONE',  ( -0.2728548680617166600, 4.886493481094341895, -0.1567155967314854681 ) ) ;
#1062=CARTESIAN_POINT ( 'NONE',  ( 0.2190263280134926160, 4.134062133123920901, 0.2226461969101928007 ) ) ;
#1064=CARTESIAN_POINT ( 'NONE',  ( -0.2819296736111110424, 5.238277777853643791, -0.1167790944451423119 ) ) ;
#1065=CARTESIAN_POINT ( 'NONE',  ( 0.08166541343684949328, 3.819386461530409616, -0.3038794602980067205 ) ) ;
#1074=DIRECTION ( 'NONE',  ( -0.000000000000000000, -1.000000000000000000, -0.000000000000000000 ) ) ;
#1077=CARTESIAN_POINT ( 'NONE',  ( -5.731347020009612645E-17, 0.4486111111111107386, 0.3119999999999999996 ) ) ;
#1078=CARTESIAN_POINT ( 'NONE',  ( -0.1292346314604057023, 5.005638888888888083, 0.3119999999999998885 ) ) ;
#1079=CARTESIAN_POINT ( 'NONE',  ( -0.1167790944451423535, 4.252166666742533074, 0.2819296736111110979 ) ) ;
#1080=CARTESIAN_POINT ( 'NONE',  ( -0.2819296736111110424, 4.029944444520309865, -0.1167790944451423119 ) ) ;
#1081=CARTESIAN_POINT ( 'NONE',  ( 1.910449006669871087E-17, 0.5805555554038225319, -0.3119999999999999996 ) ) ;
#1086=ORIENTED_EDGE ( 'NONE', *, *, #17053, .F. ) ;
#1087=CARTESIAN_POINT ( 'NONE',  ( -0.3038794811195862922, 4.004552013912318742, 0.08166531675456255301 ) ) ;
#1088=CARTESIAN_POINT ( 'NONE',  ( -1.726321361862525858E-17, 4.450083333409198261, -0.2819296736111110979 ) ) ;
#1089=EDGE_CURVE ( 'NONE', #10194, #22245, #14393, .T. ) ;
#1090=CARTESIAN_POINT ( 'NONE',  ( -0.3103119043768812757, 4.501276256218609717, -0.03246517880612528190 ) ) ;
#1091=AXIS2_PLACEMENT_3D ( 'NONE', #21137, #18954, #19068 ) ;
#1092=DIRECTION ( 'NONE',  ( 0.000000000000000000, 1.000000000000000000, 0.000000000000000000 ) ) ;
#1095=CARTESIAN_POINT ( 'NONE',  ( -0.2819296736111110979, 4.200083333409199149, 0.000000000000000000 ) ) ;
#1096=CARTESIAN_POINT ( 'NONE',  ( -0.0006228004652524621668, 4.821629233683148108, -0.3119995338756686443 ) ) ;
#1097=DIRECTION ( 'NONE',  ( 0.000000000000000000, 0.000000000000000000, -1.000000000000000000 ) ) ;
#1100=CARTESIAN_POINT ( 'NONE',  ( -0.1167790944451422702, 0.5666666665908001166, -0.2819296736111110424 ) ) ;
#1102=CARTESIAN_POINT ( 'NONE',  ( -2.336494862270849996E-07, 3.904935224540334815, 0.3119999999998144258 ) ) ;
#1106=VERTEX_POINT ( 'NONE', #23229 ) ;
#1108=CARTESIAN_POINT ( 'NONE',  ( -0.1571128864003343839, 3.770594504772994071, -0.2726305689577052660 ) ) ;
#1109=CARTESIAN_POINT ( 'NONE',  ( 1.910449006669871087E-17, 0.3097222222222218435, -0.3119999999999999996 ) ) ;
#1110=CARTESIAN_POINT ( 'NONE',  ( 0.1993543840281266355, 0.4729166665908000611, 0.1993543840281267465 ) ) ;
#1112=CARTESIAN_POINT ( 'NONE',  ( 0.1167790944451424368, 4.161888888964755395, 0.2819296736111110424 ) ) ;
#1116=CARTESIAN_POINT ( 'NONE',  ( -0.2819296736111110424, 4.703555555631421470, 0.1167790944451424923 ) ) ;
#1117=CARTESIAN_POINT ( 'NONE',  ( 0.3012075971199598134, 5.132458837216917757, -0.05814740050211916755 ) ) ;
#1121=CARTESIAN_POINT ( 'NONE',  ( -0.1993543840281266910, 5.234805555631421470, -0.1993543840281266910 ) ) ;
#1125=LINE ( 'NONE', #17800, #18154 ) ;
#1127=CARTESIAN_POINT ( 'NONE',  ( -0.1167790944451423535, 4.807722222298087544, 0.2819296736111110979 ) ) ;
#1130=CARTESIAN_POINT ( 'NONE',  ( -0.02013615247613211728, 5.100645930978458864, -0.3102850255878896735 ) ) ;
#1132=CARTESIAN_POINT ( 'NONE',  ( -0.03138891603827507343, 4.570755570789335920, 0.3104503094740446723 ) ) ;
#1134=CARTESIAN_POINT ( 'NONE',  ( 1.726321361862525858E-17, 0.2298611110352444531, -0.2819296736111110979 ) ) ;
#1135=FACE_OUTER_BOUND ( 'NONE', #23601, .T. ) ;
#1136=DIRECTION ( 'NONE',  ( 0.000000000000000000, 0.000000000000000000, -1.000000000000000000 ) ) ;
#1139=CARTESIAN_POINT ( 'NONE',  ( -0.2860141851659954160, 5.054083271882030104, -0.1246764997512364026 ) ) ;
#1142=CARTESIAN_POINT ( 'NONE',  ( -1.726321361862525858E-17, 4.797305555631421470, -0.2819296736111110979 ) ) ;
#1144=CARTESIAN_POINT ( 'NONE',  ( -0.2819296736111110424, 3.745222222298088433, 0.1167790944451424923 ) ) ;
#1145=CARTESIAN_POINT ( 'NONE',  ( -0.04924783737072570278, 0.04405018457464146553, -0.2895592137998864168 ) ) ;
#1146=CARTESIAN_POINT ( 'NONE',  ( 0.01963288055412146585, 5.016555562292845494, 0.3115338482637666218 ) ) ;
#1150=CARTESIAN_POINT ( 'NONE',  ( -0.2206173157302027676, 4.453555555707287894, 0.2206173157302028787 ) ) ;
#1151=CARTESIAN_POINT ( 'NONE',  ( -0.1993543840281266910, 4.804250000075865223, -0.1993543840281266910 ) ) ;
#1153=CARTESIAN_POINT ( 'NONE',  ( -0.1167790944451423535, 4.029944444520309865, 0.2819296736111110424 ) ) ;
#1155=ORIENTED_EDGE ( 'NONE', *, *, #10547, .T. ) ;
#1156=ORIENTED_EDGE ( 'NONE', *, *, #22775, .F. ) ;
#1161=CARTESIAN_POINT ( 'NONE',  ( 0.2206173157302027676, 0.3374999998482670627, 0.2206173157302028787 ) ) ;
#1162=AXIS2_PLACEMENT_3D ( 'NONE', #6725, #19531, #11999 ) ;
#1164=CARTESIAN_POINT ( 'NONE',  ( 1.910449006669871087E-17, 0.4694444442927115380, -0.3119999999999999996 ) ) ;
#1167=CARTESIAN_POINT ( 'NONE',  ( 0.3119999999999999996, 0.2333333331816004053, 0.000000000000000000 ) ) ;
#1168=CARTESIAN_POINT ( 'NONE',  ( -0.2819296736111111534, 0.06666666659080003332, 0.1167790944451422563 ) ) ;
#1170=ORIENTED_EDGE ( 'NONE', *, *, #22862, .T. ) ;
#1171=CARTESIAN_POINT ( 'NONE',  ( -0.2819296736111110979, 4.519527777853643791, 0.000000000000000000 ) ) ;
#1176=CARTESIAN_POINT ( 'NONE',  ( -0.2206173157302028232, 4.154944444444443441, -0.2206173157302028232 ) ) ;
#1179=CARTESIAN_POINT ( 'NONE',  ( 0.2474824800886665510, 4.968567478400213844, 0.1919644361720711512 ) ) ;
#1182=VECTOR ( 'NONE', #18082, 39.37007874015748143 ) ;
#1185=CARTESIAN_POINT ( 'NONE',  ( -0.007181820806740507948, 4.877369323082827002, -0.3121677187871257364 ) ) ;
#1193=CARTESIAN_POINT ( 'NONE',  ( 0.1993543840281266355, 0.09791666659080004720, 0.1993543840281267465 ) ) ;
#1196=CARTESIAN_POINT ( 'NONE',  ( -0.1167790944451423535, 5.154944444520309865, 0.2819296736111110424 ) ) ;
#1199=CARTESIAN_POINT ( 'NONE',  ( -0.07953501818328695405, 4.601699271391998636, -0.3023590498254824510 ) ) ;
#1201=CARTESIAN_POINT ( 'NONE',  ( -0.2310837057929944205, 4.286504077376945610, 0.2125035569942567704 ) ) ;
#1203=CARTESIAN_POINT ( 'NONE',  ( -0.3119999999999999996, 0.4902777777777773682, -3.820898013339742174E-17 ) ) ;
#1204=CARTESIAN_POINT ( 'NONE',  ( 0.1292346314604056190, 4.755638888888888083, -0.3119999999999999996 ) ) ;
#1205=CARTESIAN_POINT ( 'NONE',  ( 0.1167790944451424506, 4.203555555631420582, 0.2819296736111110424 ) ) ;
#1206=CARTESIAN_POINT ( 'NONE',  ( 0.2819296736111110979, 4.002166666742532186, 0.1167790944451422425 ) ) ;
#1207=CARTESIAN_POINT ( 'NONE',  ( -0.3119999999999999996, 0.5944444442927114824, -3.820898013339742174E-17 ) ) ;
#1209=CARTESIAN_POINT ( 'NONE',  ( 0.000000000000000000, 0.000000000000000000, 0.000000000000000000 ) ) ;
#1211=CARTESIAN_POINT ( 'NONE',  ( 0.1167790944451422702, 4.613277777853643791, -0.2819296736111110424 ) ) ;
#1213=CARTESIAN_POINT ( 'NONE',  ( -1.910449006669871087E-17, 3.814666666666665762, -0.3119999999999999996 ) ) ;
#1218=CARTESIAN_POINT ( 'NONE',  ( -0.1167790944451423119, 4.134111111186977716, -0.2819296736111110979 ) ) ;
#1219=CARTESIAN_POINT ( 'NONE',  ( -0.3116075380362458014, 4.835063446295903233, -0.01613731598427003630 ) ) ;
#1224=CARTESIAN_POINT ( 'NONE',  ( 0.1167790944451423535, 0.02499999992413337591, 0.2819296736111110424 ) ) ;
#1227=DIRECTION ( 'NONE',  ( -0.000000000000000000, -1.000000000000000000, -0.000000000000000000 ) ) ;
#1230=EDGE_CURVE ( 'NONE', #22245, #3381, #5918, .T. ) ;
#1234=CARTESIAN_POINT ( 'NONE',  ( -0.3038792844419939687, 3.837724674714062090, 0.08166605555175254771 ) ) ;
#1235=CARTESIAN_POINT ( 'NONE',  ( 0.1167790944451423257, 0.4347222221463555858, -0.2819296736111110424 ) ) ;
#1236=CARTESIAN_POINT ( 'NONE',  ( -0.2819296736111110424, 3.974388888964754507, -0.1167790944451423119 ) ) ;
#1238=CARTESIAN_POINT ( 'NONE',  ( -0.1167790944451423257, 4.578555555631421470, -0.2819296736111110424 ) ) ;
#1239=CARTESIAN_POINT ( 'NONE',  ( 0.2095071056370220175, 5.124394802682457950, 0.2256314019847080743 ) ) ;
#1240=CARTESIAN_POINT ( 'NONE',  ( 0.3104426192702163245, 5.079437309436282355, -0.03361595017585427420 ) ) ;
#1243=CARTESIAN_POINT ( 'NONE',  ( -0.2819296736111110979, 5.075083333409198261, 0.000000000000000000 ) ) ;
#1244=CARTESIAN_POINT ( 'NONE',  ( 0.06767679649697184996, 4.208568552395559159, -0.3050095114520465778 ) ) ;
#1245=ORIENTED_EDGE ( 'NONE', *, *, #16907, .T. ) ;
#1246=CARTESIAN_POINT ( 'NONE',  ( 0.2819296736111111534, 4.877166666742532186, 0.1167790944451422563 ) ) ;
#1249=CARTESIAN_POINT ( 'NONE',  ( -0.2206173157302027954, 0.3097222220704892726, -0.2206173157302028232 ) ) ;
#1250=CARTESIAN_POINT ( 'NONE',  ( -0.2206173157302027954, 0.1986111109593781676, -0.2206173157302028232 ) ) ;
#1252=CARTESIAN_POINT ( 'NONE',  ( -0.1167790944451424368, 0.3652777777019110550, 0.2819296736111110424 ) ) ;
#1256=CARTESIAN_POINT ( 'NONE',  ( 0.3016947543841931867, 4.083248925189674416, 0.07952538849869711379 ) ) ;
#1262=CARTESIAN_POINT ( 'NONE',  ( 0.1993543840281266633, 4.790361111186976828, -0.1993543840281266910 ) ) ;
#1266=CARTESIAN_POINT ( 'NONE',  ( 0.1167790944451422702, 3.779944444520310309, -0.2819296736111110424 ) ) ;
#1267=CARTESIAN_POINT ( 'NONE',  ( -0.2818086106116773903, 0.05407526412938527122, 0.1133068594113698230 ) ) ;
#1268=CARTESIAN_POINT ( 'NONE',  ( 0.04618426000566567408, 5.017331032664509749, 0.3085723143962725290 ) ) ;
#1269=CARTESIAN_POINT ( 'NONE',  ( 0.1095210610625794029, 0.04736867464127668403, 0.2773152020650166416 ) ) ;
#1271=CARTESIAN_POINT ( 'NONE',  ( 0.3119999999999999996, 4.311194444596176290, -0.1292346314604056745 ) ) ;
#1272=CARTESIAN_POINT ( 'NONE',  ( -0.1167790944451423119, 4.745222222298088433, -0.2819296736111110979 ) ) ;
#1274=CARTESIAN_POINT ( 'NONE',  ( 5.178964085587577574E-17, 3.811194444520309865, 0.2819296736111110979 ) ) ;
#1275=VECTOR ( 'NONE', #8120, 39.37007874015748143 ) ;
#1277=EDGE_CURVE ( 'NONE', #16112, #4354, #2064, .T. ) ;
#1279=EDGE_CURVE ( 'NONE', #14020, #4825, #1031, .T. ) ;
#1284=CARTESIAN_POINT ( 'NONE',  ( -0.1292346314604058410, 0.3826388887371559022, 0.3119999999999998885 ) ) ;
#1285=CARTESIAN_POINT ( 'NONE',  ( -0.3037470199460711728, 4.393456864127093908, 0.08219764244668044395 ) ) ;
#1286=CARTESIAN_POINT ( 'NONE',  ( 0.1292346314604057300, 0.1673611109593781676, 0.3119999999999998885 ) ) ;
#1291=CARTESIAN_POINT ( 'NONE',  ( 0.2819296736111110424, 0.08749999992413336203, 0.1167790944451424923 ) ) ;
#1294=CARTESIAN_POINT ( 'NONE',  ( -0.1993543840281266910, 4.512583333409199149, -0.1993543840281266910 ) ) ;
#1296=CARTESIAN_POINT ( 'NONE',  ( 5.731347020009612645E-17, 4.397999999999999687, 0.3119999999999999996 ) ) ;
#1297=CARTESIAN_POINT ( 'NONE',  ( -0.2206173157302027954, 0.3652777776260448528, -0.2206173157302028232 ) ) ;
#1298=CARTESIAN_POINT ( 'NONE',  ( 0.1292346314604056190, 4.088972222222221120, -0.3119999999999999996 ) ) ;
#1300=CARTESIAN_POINT ( 'NONE',  ( 0.1292346314604056190, 4.873694444596176290, -0.3119999999999999996 ) ) ;
#1302=ORIENTED_EDGE ( 'NONE', *, *, #8448, .T. ) ;
#1310=CARTESIAN_POINT ( 'NONE',  ( -0.3119999999999999996, 4.436194444444443441, -0.1292346314604056468 ) ) ;
#1311=ADVANCED_FACE ( 'NONE', ( #19789 ), #15889, .T. ) ;
#1313=CARTESIAN_POINT ( 'NONE',  ( -5.178964085587577574E-17, 0.1465277777019111383, 0.2819296736111110979 ) ) ;
#1315=CARTESIAN_POINT ( 'NONE',  ( -0.1993543840281266910, 5.248694444520310753, -0.1993543840281266910 ) ) ;
#1318=CARTESIAN_POINT ( 'NONE',  ( -0.2205053451214862847, 4.606340970039537908, -0.2212367656121000947 ) ) ;
#1319=CARTESIAN_POINT ( 'NONE',  ( -0.2905792868698985343, 4.276554290496439314, -0.1163786327526087350 ) ) ;
#1321=CARTESIAN_POINT ( 'NONE',  ( 0.3119999999999998885, 0.4590277777777774793, 0.1292346314604058410 ) ) ;
#1322=CARTESIAN_POINT ( 'NONE',  ( -0.3119999999999999996, 4.658416666666666650, -0.1292346314604056468 ) ) ;
#1323=CARTESIAN_POINT ( 'NONE',  ( 0.1993543840281267465, 3.929250000075865668, 0.1993543840281266633 ) ) ;
#1325=CARTESIAN_POINT ( 'NONE',  ( -5.731347020009612645E-17, 0.6083333331816004330, 0.3119999999999999996 ) ) ;
#1327=CARTESIAN_POINT ( 'NONE',  ( 0.000000000000000000, 5.072999999999999510, 0.000000000000000000 ) ) ;
#1330=CARTESIAN_POINT ( 'NONE',  ( 0.1993543840281267465, 4.595916666742532186, 0.1993543840281266633 ) ) ;
#1331=CARTESIAN_POINT ( 'NONE',  ( -0.3134171556598066011, 4.502164757452278288, -0.0009694151472935294252 ) ) ;
#1335=CARTESIAN_POINT ( 'NONE',  ( -1.726321361862525858E-17, 4.186194444520309865, -0.2819296736111110979 ) ) ;
#1341=CARTESIAN_POINT ( 'NONE',  ( 0.1167790944451423535, 0.08055555547968892838, 0.2819296736111110424 ) ) ;
#1347=EDGE_LOOP ( 'NONE', ( #11006, #21584, #11418, #2986 ) ) ;
#1351=CARTESIAN_POINT ( 'NONE',  ( 0.1993543840281266910, 0.4312499999241333759, -0.1993543840281266910 ) ) ;
#1352=CARTESIAN_POINT ( 'NONE',  ( -0.2819296736111110979, 3.811194444520310309, 0.000000000000000000 ) ) ;
#1354=CARTESIAN_POINT ( 'NONE',  ( -0.2819296736111110424, 4.363277777853643791, -0.1167790944451423119 ) ) ;
#1356=CARTESIAN_POINT ( 'NONE',  ( 0.2236628504143657326, 5.124892759571328504, 0.2114858233200252735 ) ) ;
#1358=CARTESIAN_POINT ( 'NONE',  ( -0.1292346314604058410, 0.1604166665149337478, 0.3119999999999998885 ) ) ;
#1360=CARTESIAN_POINT ( 'NONE',  ( 0.1292346314604070623, 4.790361111111110404, 0.3119999999999986673 ) ) ;
#1361=CARTESIAN_POINT ( 'NONE',  ( 0.2819296736111110424, 5.161888888964753619, -0.1167790944451423396 ) ) ;
#1363=CARTESIAN_POINT ( 'NONE',  ( 0.08265232788921492157, 4.208131977080836528, -0.3012013616566489027 ) ) ;
#1367=( BOUNDED_CURVE ( )  B_SPLINE_CURVE ( 2, ( #2710, #998, #15874, #17831, #23291, #23415, #8309, #1360, #15760 ),
 .UNSPECIFIED., .F., .F. ) 
 B_SPLINE_CURVE_WITH_KNOTS ( ( 3, 2, 2, 2, 3 ),
 ( 0.2946428571428569843, 0.2991071428571426827, 0.3035714285714284366, 0.3080357142857141906, 0.3124999999999999445 ),
 .UNSPECIFIED. ) 
 CURVE ( )  GEOMETRIC_REPRESENTATION_ITEM ( )  RATIONAL_B_SPLINE_CURVE ( ( 1.000000000000002887, 0.9238795325112838519, 1.000000000000000000, 0.9238795325112867385, 1.000000000000000000, 0.9238795325112867385, 1.000000000000000000, 0.9238795325112877377, 0.9999999999999990008 ) ) 
 REPRESENTATION_ITEM ( '' )  );
#1369=CARTESIAN_POINT ( 'NONE',  ( 0.1167790944451424506, 4.870222222298087544, 0.2819296736111110424 ) ) ;
#1372=CARTESIAN_POINT ( 'NONE',  ( -0.1292346314604058410, 0.2159722220704893003, 0.3119999999999998885 ) ) ;
#1374=CARTESIAN_POINT ( 'NONE',  ( -0.1993543840281266633, 0.3479166665908000056, -0.1993543840281266910 ) ) ;
#1376=CARTESIAN_POINT ( 'NONE',  ( -0.1993543840281267465, 0.02847222214635559273, 0.1993543840281266633 ) ) ;
#1380=CARTESIAN_POINT ( 'NONE',  ( -0.2146400242025152671, 5.064908869111506284, 0.2268182928792843722 ) ) ;
#1382=CARTESIAN_POINT ( 'NONE',  ( 0.1988757138996042617, 3.752970977545328157, -0.2404006040361021113 ) ) ;
#1384=CARTESIAN_POINT ( 'NONE',  ( 0.1167790944451422702, 4.571611111186976828, -0.2819296736111110424 ) ) ;
#1385=CARTESIAN_POINT ( 'NONE',  ( 0.2608937378291124043, 4.524766547629808677, 0.1723236813421265556 ) ) ;
#1386=CARTESIAN_POINT ( 'NONE',  ( -0.2819296736111110979, 3.741750000075865668, 0.000000000000000000 ) ) ;
#1388=CARTESIAN_POINT ( 'NONE',  ( 0.08162334319253711223, 4.907349590646077786, 0.3038879386963563856 ) ) ;
#1392=ADVANCED_FACE ( 'NONE', ( #2964 ), #17845, .T. ) ;
#1393=CARTESIAN_POINT ( 'NONE',  ( -0.1292346314604057023, 4.401472222373953080, 0.3119999999999998885 ) ) ;
#1394=CARTESIAN_POINT ( 'NONE',  ( 0.1993543840281266633, 4.679250000075866112, -0.1993543840281266910 ) ) ;
#1395=CARTESIAN_POINT ( 'NONE',  ( -0.1993543840281266355, 3.915361111186976384, 0.1993543840281267465 ) ) ;
#1404=ORIENTED_EDGE ( 'NONE', *, *, #20695, .T. ) ;
#1405=CARTESIAN_POINT ( 'NONE',  ( -5.731347020009612645E-17, 0.2194444442927115380, 0.3119999999999999996 ) ) ;
#1406=CARTESIAN_POINT ( 'NONE',  ( -0.0001215146640037667272, 4.377169931752053600, -0.3119999823201240474 ) ) ;
#1407=CARTESIAN_POINT ( 'NONE',  ( -0.1884418442843545372, 5.123706002978354768, 0.2436494946675597795 ) ) ;
#1413=CARTESIAN_POINT ( 'NONE',  ( 0.2338198238642340554, 5.079091233363342006, 0.2073940069782997664 ) ) ;
#1414=CARTESIAN_POINT ( 'NONE',  ( -0.1993543840281267465, 0.1812499999241333759, 0.1993543840281266633 ) ) ;
#1417=CARTESIAN_POINT ( 'NONE',  ( 5.178964085587577574E-17, 4.477861111186976828, 0.2819296736111110979 ) ) ;
#1422=CARTESIAN_POINT ( 'NONE',  ( 0.3119999999999999996, 4.137583333333332725, -0.1292346314604056745 ) ) ;
#1424=CARTESIAN_POINT ( 'NONE',  ( -0.1292346314604057023, 5.012583333485065573, 0.3119999999999998885 ) ) ;
#1425=CARTESIAN_POINT ( 'NONE',  ( -0.2933322049817026489, 5.157132068594114216, 0.06571910644767618714 ) ) ;
#1427=CARTESIAN_POINT ( 'NONE',  ( 5.731347020009612645E-17, 4.175777777777776478, 0.3119999999999999996 ) ) ;
#1428=EDGE_CURVE ( 'NONE', #4057, #606, #2731, .T. ) ;
#1429=CARTESIAN_POINT ( 'NONE',  ( -0.09925723254180866817, 4.880039691319455031, -0.2961790094676920448 ) ) ;
#1436=CARTESIAN_POINT ( 'NONE',  ( -0.2819296736111110979, 0.3548611110352444808, -3.452642723725051716E-17 ) ) ;
#1438=CARTESIAN_POINT ( 'NONE',  ( 0.2819296736111110979, 5.113277777853642903, 0.1167790944451422425 ) ) ;
#1443=CARTESIAN_POINT ( 'NONE',  ( -0.1292346314604056745, 4.762583333333332725, -0.3119999999999999996 ) ) ;
#1445=CARTESIAN_POINT ( 'NONE',  ( 5.178964085587577574E-17, 4.088972222298087544, 0.2819296736111110979 ) ) ;
#1446=CARTESIAN_POINT ( 'NONE',  ( 0.2819296736111110979, 3.779944444520310309, 0.1167790944451422425 ) ) ;
#1447=CARTESIAN_POINT ( 'NONE',  ( 0.1777386203871747228, 4.021449974115596682, 0.2564743595758844918 ) ) ;
#1448=MANIFOLD_SOLID_BREP ( 'Thread2', #11535 ) ;
#1450=ORIENTED_EDGE ( 'NONE', *, *, #8496, .T. ) ;
#1452=CARTESIAN_POINT ( 'NONE',  ( 5.178964085587577574E-17, 4.477861111186976828, 0.2819296736111110979 ) ) ;
#1453=EDGE_CURVE ( 'NONE', #11367, #8566, #16136, .T. ) ;
#1454=CARTESIAN_POINT ( 'NONE',  ( -0.02716817033992858718, 4.489059518347089828, -0.3108624770087871081 ) ) ;
#1458=CARTESIAN_POINT ( 'NONE',  ( -0.1167790944451423119, 4.189666666742533074, -0.2819296736111110979 ) ) ;
#1463=CARTESIAN_POINT ( 'NONE',  ( -0.2819296736111110424, 0.3374999999241334314, -0.1167790944451423396 ) ) ;
#1469=EDGE_LOOP ( 'NONE', ( #23951, #8778, #23474, #3762 ) ) ;
#1472=CARTESIAN_POINT ( 'NONE',  ( -0.1167790944451424368, 0.5736111110352444253, 0.2819296736111110424 ) ) ;
#1473=CARTESIAN_POINT ( 'NONE',  ( -1.726321361862525858E-17, 3.852861111186976828, -0.2819296736111110979 ) ) ;
#1476=CARTESIAN_POINT ( 'NONE',  ( 0.1167790944451424368, 4.495222222298088433, 0.2819296736111110424 ) ) ;
#1478=CARTESIAN_POINT ( 'NONE',  ( -0.1292346314604105872, 4.373694444444443441, -0.3119999999999950591 ) ) ;
#1481=CARTESIAN_POINT ( 'NONE',  ( 0.000000000000000000, 5.072999999999999510, 0.000000000000000000 ) ) ;
#1483=CARTESIAN_POINT ( 'NONE',  ( -0.2206173157302028232, 3.717444444596176734, -0.2206173157302028232 ) ) ;
#1487=CARTESIAN_POINT ( 'NONE',  ( 0.1993543840281267465, 4.929250000075866112, 0.1993543840281266633 ) ) ;
#1492=CARTESIAN_POINT ( 'NONE',  ( 0.2819296736111110979, 0.2159722221463555858, 0.000000000000000000 ) ) ;
#1499=CARTESIAN_POINT ( 'NONE',  ( -0.3119999999999999996, 4.495222222222221120, 0.000000000000000000 ) ) ;
#1500=CARTESIAN_POINT ( 'NONE',  ( -0.1292346314604032043, 3.762583333333332281, -0.3120000000000024420 ) ) ;
#1503=CARTESIAN_POINT ( 'NONE',  ( 0.1993543840281266633, 4.457027777853643791, -0.1993543840281266910 ) ) ;
#1505=CARTESIAN_POINT ( 'NONE',  ( 0.007400005122092102351, 4.543623246078921873, -0.3119247507460371494 ) ) ;
#1506=CARTESIAN_POINT ( 'NONE',  ( 0.1167790944451424368, 5.161888888964753619, 0.2819296736111110424 ) ) ;
#1508=CARTESIAN_POINT ( 'NONE',  ( -0.3015329647789626311, 0.05188409045955083565, -0.002760744269507171226 ) ) ;
#1509=CARTESIAN_POINT ( 'NONE',  ( 0.1920553804271201426, 4.926912892342040884, -0.2492488320715855465 ) ) ;
#1510=CARTESIAN_POINT ( 'NONE',  ( 0.05498706736770282016, 0.04336109282094929851, 0.2879801573640842216 ) ) ;
#1512=CARTESIAN_POINT ( 'NONE',  ( -0.3119999999999999996, 4.279944444596176290, 0.000000000000000000 ) ) ;
#1513=CARTESIAN_POINT ( 'NONE',  ( 0.1993543840281267465, 4.443138888964754507, 0.1993543840281266633 ) ) ;
#1516=CARTESIAN_POINT ( 'NONE',  ( 0.1167790944451424368, 3.814666666742532630, 0.2819296736111110424 ) ) ;
#1517=VECTOR ( 'NONE', #7020, 39.37007874015748143 ) ;
#1519=VERTEX_POINT ( 'NONE', #20271 ) ;
#1522=CARTESIAN_POINT ( 'NONE',  ( -0.3119999999999999996, 4.272999999999998799, 0.000000000000000000 ) ) ;
#1524=CARTESIAN_POINT ( 'NONE',  ( -5.731347020009612645E-17, 0.1638888887371559577, 0.3119999999999999996 ) ) ;
#1525=ADVANCED_FACE ( 'NONE', ( #14674 ), #3439, .T. ) ;
#1526=VERTEX_POINT ( 'NONE', #9290 ) ;
#1527=CARTESIAN_POINT ( 'NONE',  ( -0.2206173157302027954, 0.3097222220704892726, -0.2206173157302028232 ) ) ;
#1529=CARTESIAN_POINT ( 'NONE',  ( -0.2454434631267384259, 5.121228990971889772, 0.1867560419929801541 ) ) ;
#1530=DIRECTION ( 'NONE',  ( 0.000000000000000000, 0.000000000000000000, -1.000000000000000000 ) ) ;
#1537=CARTESIAN_POINT ( 'NONE',  ( -0.2819296736111110979, 4.130638888964754507, 0.000000000000000000 ) ) ;
#1538=CARTESIAN_POINT ( 'NONE',  ( -0.2819296736111110424, 5.078555555631420582, 0.1167790944451424923 ) ) ;
#1541=CARTESIAN_POINT ( 'NONE',  ( 0.2206173157302027954, 4.085499999999999687, -0.2206173157302028232 ) ) ;
#1542=CARTESIAN_POINT ( 'NONE',  ( -0.3119999999999999996, 4.943138889040621820, -0.1292346314604056468 ) ) ;
#1543=CARTESIAN_POINT ( 'NONE',  ( -0.2819296736111110424, 5.092444444520309865, 0.1167790944451424923 ) ) ;
#1545=CARTESIAN_POINT ( 'NONE',  ( 0.03417713022414695795, 4.683645677618572201, 0.3101606497207352042 ) ) ;
#1553=CARTESIAN_POINT ( 'NONE',  ( 0.2819296736111110424, 0.2124999999241334037, 0.1167790944451424923 ) ) ;
#1555=CARTESIAN_POINT ( 'NONE',  ( -0.2819296736111110424, 5.148000000075865223, 0.1167790944451424923 ) ) ;
#1559=CARTESIAN_POINT ( 'NONE',  ( -0.04084116025059186111, 3.792736021511474487, 0.3120000000000012208 ) ) ;
#1561=CARTESIAN_POINT ( 'NONE',  ( 0.1311510126959312961, 4.873430014960409729, -0.2838723230971368916 ) ) ;
#1562=CARTESIAN_POINT ( 'NONE',  ( 3.820898013339742174E-17, 5.384999999999999787, 0.3119999999999999996 ) ) ;
#1564=CARTESIAN_POINT ( 'NONE',  ( 5.731347020009612645E-17, 4.731333333333332725, 0.3119999999999999996 ) ) ;
#1566=CARTESIAN_POINT ( 'NONE',  ( -0.2819296736111110979, 4.016055555631421470, -0.1167790944451422980 ) ) ;
#1567=CARTESIAN_POINT ( 'NONE',  ( 0.1167790944451424368, 3.773000000075866112, 0.2819296736111110424 ) ) ;
#1568=CARTESIAN_POINT ( 'NONE',  ( 0.2008485455641423334, 4.022270167221941861, 0.2388045284289016523 ) ) ;
#1572=CARTESIAN_POINT ( 'NONE',  ( -0.1167790944451423257, 4.453555555631420582, -0.2819296736111110424 ) ) ;
#1573=CARTESIAN_POINT ( 'NONE',  ( -0.1494206241407597668, 4.511765937384295100, 0.2773182096705338884 ) ) ;
#1574=CARTESIAN_POINT ( 'NONE',  ( 0.3119999999999998885, 0.07013888888888854256, 0.1292346314604058410 ) ) ;
#1579=CARTESIAN_POINT ( 'NONE',  ( 0.2819296736111110979, 3.842444444520310309, -0.1167790944451423396 ) ) ;
#1581=CARTESIAN_POINT ( 'NONE',  ( -6.528214817076446933E-07, 5.071585437816050757, 0.3119999999985565986 ) ) ;
#1584=CARTESIAN_POINT ( 'NONE',  ( 0.1167790944451423535, 0.2472222221463555303, 0.2819296736111110424 ) ) ;
#1586=CARTESIAN_POINT ( 'NONE',  ( 0.000000000000000000, 5.384999999999999787, 0.000000000000000000 ) ) ;
#1591=ORIENTED_EDGE ( 'NONE', *, *, #8432, .T. ) ;
#1595=CARTESIAN_POINT ( 'NONE',  ( 0.3119999999999999996, 0.01805555555555522079, 0.000000000000000000 ) ) ;
#1596=CARTESIAN_POINT ( 'NONE',  ( -0.1167790944451423535, 3.877166666742531742, 0.2819296736111110424 ) ) ;
#1599=CARTESIAN_POINT ( 'NONE',  ( -0.2819296736111110979, 4.366750000075866112, 0.000000000000000000 ) ) ;
#1600=CARTESIAN_POINT ( 'NONE',  ( 0.3120000000000000551, 4.963972222222222008, 0.1292346314604056190 ) ) ;
#1601=CARTESIAN_POINT ( 'NONE',  ( 3.820898013339742174E-17, 5.384999999999999787, 0.3119999999999999996 ) ) ;
#1603=ORIENTED_EDGE ( 'NONE', *, *, #21096, .T. ) ;
#1604=CARTESIAN_POINT ( 'NONE',  ( 0.3119999999999999996, 4.693138888888888971, -0.1292346314604056745 ) ) ;
#1605=CARTESIAN_POINT ( 'NONE',  ( -0.1292346314604056745, 3.713972222373953525, -0.3119999999999999996 ) ) ;
#1606=CARTESIAN_POINT ( 'NONE',  ( 0.2581855260733656454, 4.201935345941767430, -0.1757379818918752279 ) ) ;
#1609=CARTESIAN_POINT ( 'NONE',  ( 0.1993543840281267465, 4.707027777853643791, 0.1993543840281266633 ) ) ;
#1611=CARTESIAN_POINT ( 'NONE',  ( -0.1543006097263451837, 4.067011077438127842, 0.2711740475169042153 ) ) ;
#1613=CARTESIAN_POINT ( 'NONE',  ( 0.1167790944451423257, 0.3374999999241334314, -0.2819296736111110424 ) ) ;
#1614=CARTESIAN_POINT ( 'NONE',  ( -5.178964085587577574E-17, 0.2020833332574667185, 0.2819296736111110979 ) ) ;
#1616=CARTESIAN_POINT ( 'NONE',  ( -0.1292346314604057300, 4.338972222222222008, 0.3119999999999998885 ) ) ;
#1617=CARTESIAN_POINT ( 'NONE',  ( -0.2340349472341747006, 5.197103598887514941, -0.1654092351966998387 ) ) ;
#1619=CARTESIAN_POINT ( 'NONE',  ( 5.731347020009612645E-17, 4.675777777777777366, 0.3119999999999999996 ) ) ;
#1620=CARTESIAN_POINT ( 'NONE',  ( -1.910449006669871087E-17, 3.759111111111109960, -0.3119999999999999996 ) ) ;
#1621=CARTESIAN_POINT ( 'NONE',  ( -0.2561990078798795922, 3.885650447666386675, -0.1780621544523601218 ) ) ;
#1622=FACE_OUTER_BOUND ( 'NONE', #20306, .T. ) ;
#1623=CARTESIAN_POINT ( 'NONE',  ( -0.1167790944451423257, 4.467444444520309865, -0.2819296736111110424 ) ) ;
#1625=CARTESIAN_POINT ( 'NONE',  ( 0.3035782676821786041, 4.527778441137987109, 0.07531847786364795350 ) ) ;
#1626=CARTESIAN_POINT ( 'NONE',  ( 0.2819296736111110424, 5.175777777853644679, -0.1167790944451423396 ) ) ;
#1628=CARTESIAN_POINT ( 'NONE',  ( 0.3047183941458634915, 3.750271769757703932, 0.06756532177053888033 ) ) ;
#1631=CARTESIAN_POINT ( 'NONE',  ( 0.1292346314604058410, 4.241750000151731648, 0.3119999999999998885 ) ) ;
#1632=CARTESIAN_POINT ( 'NONE',  ( 5.178964085587577574E-17, 4.547305555631421470, 0.2819296736111110979 ) ) ;
#1633=CARTESIAN_POINT ( 'NONE',  ( -0.1167790944451423535, 3.752166666742532630, 0.2819296736111110424 ) ) ;
#1637=CARTESIAN_POINT ( 'NONE',  ( -0.2206173157302028232, 4.266055555555555046, -0.2206173157302028232 ) ) ;
#1638=CARTESIAN_POINT ( 'NONE',  ( -0.1568435058878248078, 4.955841575901558826, 0.2727737269072668114 ) ) ;
#1641=CARTESIAN_POINT ( 'NONE',  ( 1.910449006669871087E-17, 0.3027777776260448528, -0.3119999999999999996 ) ) ;
#1643=CARTESIAN_POINT ( 'NONE',  ( -0.2325997273933552156, 5.121856475730185210, 0.2023777655239332174 ) ) ;
#1649=CARTESIAN_POINT ( 'NONE',  ( 0.2931105832524772969, 5.082463614296739429, 0.1082669822925051151 ) ) ;
#1651=CARTESIAN_POINT ( 'NONE',  ( -0.1993543840281266910, 4.179250000075865223, -0.1993543840281266910 ) ) ;
#1652=CARTESIAN_POINT ( 'NONE',  ( 0.1167790944451424506, 5.148000000075865223, 0.2819296736111110424 ) ) ;
#1654=CARTESIAN_POINT ( 'NONE',  ( -0.2990811592642881878, 4.226951744488065543, 0.09065860205554784890 ) ) ;
#1655=CARTESIAN_POINT ( 'NONE',  ( 0.3119999999999999996, 3.963972222222221564, 0.1292346314604056190 ) ) ;
#1656=CARTESIAN_POINT ( 'NONE',  ( 0.3119999999999999996, 4.915361111262843252, 0.1292346314604056190 ) ) ;
#1658=CARTESIAN_POINT ( 'NONE',  ( 0.2819296736111111534, 5.057722222298088433, 0.1167790944451422563 ) ) ;
#1663=CARTESIAN_POINT ( 'NONE',  ( -0.2056020336012781280, 0.05660050360928185753, 0.2269839081635093292 ) ) ;
#1664=EDGE_LOOP ( 'NONE', ( #16964, #17985, #11126, #20437 ) ) ;
#1667=CARTESIAN_POINT ( 'NONE',  ( 0.1167790944451422702, 5.168833333409199149, -0.2819296736111110424 ) ) ;
#1670=CARTESIAN_POINT ( 'NONE',  ( 0.000000000000000000, 5.384999999999999787, -0.3119999999999999996 ) ) ;
#1671=CARTESIAN_POINT ( 'NONE',  ( 0.1993543840281266355, 0.2645833332574666907, 0.1993543840281267465 ) ) ;
#1673=CARTESIAN_POINT ( 'NONE',  ( 0.1993543840281267465, 5.165361111186976828, 0.1993543840281266633 ) ) ;
#1676=CARTESIAN_POINT ( 'NONE',  ( -0.1167790944451423535, 4.807722222298087544, 0.2819296736111110424 ) ) ;
#1677=CARTESIAN_POINT ( 'NONE',  ( -0.2724619974122192700, 4.164101067513843901, -0.1574067719271113330 ) ) ;
#1681=CARTESIAN_POINT ( 'NONE',  ( 0.3119999999999999996, 4.634111111111110404, -3.820898013339742174E-17 ) ) ;
#1682=CARTESIAN_POINT ( 'NONE',  ( -0.2819296736111110979, 3.960500000075865668, -0.1167790944451422980 ) ) ;
#1683=CARTESIAN_POINT ( 'NONE',  ( -1.726321361862525858E-17, 3.741750000075865668, -0.2819296736111110979 ) ) ;
#1684=CARTESIAN_POINT ( 'NONE',  ( 0.2591841582727462123, 4.035241130471740156, -0.1755254409656935577 ) ) ;
#1688=EDGE_LOOP ( 'NONE', ( #15767, #21825, #18890, #22350 ) ) ;
#1690=CARTESIAN_POINT ( 'NONE',  ( 5.178964085587577574E-17, 4.311194444520309865, 0.2819296736111110979 ) ) ;
#1699=CARTESIAN_POINT ( 'NONE',  ( 0.2819296736111110424, 0.2611111110352444808, -0.1167790944451423119 ) ) ;
#1700=CARTESIAN_POINT ( 'NONE',  ( -3.268767525105149064E-07, 3.877166675600695722, -0.3119999999998287477 ) ) ;
#1701=CARTESIAN_POINT ( 'NONE',  ( -5.731347020009612645E-17, 0.5597222222222218990, 0.3119999999999999996 ) ) ;
#1702=FACE_OUTER_BOUND ( 'NONE', #19122, .T. ) ;
#1707=CARTESIAN_POINT ( 'NONE',  ( -0.1888797109280974940, 5.097681916776925171, -0.2473108602307070025 ) ) ;
#1709=CARTESIAN_POINT ( 'NONE',  ( 1.726321361862525858E-17, 0.6048611110352445364, -0.2819296736111110979 ) ) ;
#1710=CARTESIAN_POINT ( 'NONE',  ( -0.1167790944451423535, 3.932722222298087544, 0.2819296736111110424 ) ) ;
#1712=CARTESIAN_POINT ( 'NONE',  ( 0.1993543840281266633, 4.345916666742532186, -0.1993543840281266910 ) ) ;
#1714=CARTESIAN_POINT ( 'NONE',  ( 0.000000000000000000, 5.384999999999999787, -0.3119999999999999996 ) ) ;
#1715=VERTEX_POINT ( 'NONE', #2091 ) ;
#1716=ADVANCED_FACE ( 'NONE', ( #5984 ), #10027, .T. ) ;
#1718=CARTESIAN_POINT ( 'NONE',  ( -0.2819296736111110424, 4.856333333409198261, 0.1167790944451424923 ) ) ;
#1719=CARTESIAN_POINT ( 'NONE',  ( 0.2730705943700247329, 4.192115419233818585, 0.1511490652758342157 ) ) ;
#1724=CARTESIAN_POINT ( 'NONE',  ( -0.1993543840281266355, 4.582027777853642903, 0.1993543840281267465 ) ) ;
#1728=CARTESIAN_POINT ( 'NONE',  ( -0.1167790944451422702, 0.5111111110352446474, -0.2819296736111110424 ) ) ;
#1731=CARTESIAN_POINT ( 'NONE',  ( 0.2819296736111110424, 0.1638888888130222432, -0.1167790944451423119 ) ) ;
#1732=CARTESIAN_POINT ( 'NONE',  ( -0.1655462978948334940, 4.715401455808697406, -0.2649287660789821919 ) ) ;
#1737=CARTESIAN_POINT ( 'NONE',  ( -0.2620303320828955007, 3.885945015255288126, -0.1694884108109906695 ) ) ;
#1739=CARTESIAN_POINT ( 'NONE',  ( 0.2819296736111110979, 4.450083333409199149, -3.452642723725051716E-17 ) ) ;
#1741=CARTESIAN_POINT ( 'NONE',  ( -0.1292346314604056190, 0.2506944442927114824, -0.3119999999999999996 ) ) ;
#1743=CARTESIAN_POINT ( 'NONE',  ( 0.2819296736111110424, 5.064666666742533074, -0.1167790944451423396 ) ) ;
#1744=CARTESIAN_POINT ( 'NONE',  ( 0.1167790944451422702, 4.391055555631420582, -0.2819296736111110979 ) ) ;
#1745=CARTESIAN_POINT ( 'NONE',  ( 0.1573838318022541261, 3.761421851761045154, -0.2699628318548333850 ) ) ;
#1746=CARTESIAN_POINT ( 'NONE',  ( -5.731347020009612645E-17, 0.4972222220704892726, 0.3119999999999999996 ) ) ;
#1748=CARTESIAN_POINT ( 'NONE',  ( -0.1292346314604056745, 4.102861111262843252, -0.3119999999999999996 ) ) ;
#1749=CARTESIAN_POINT ( 'NONE',  ( 0.1167790944451424506, 4.495222222298088433, 0.2819296736111110424 ) ) ;
#1751=CARTESIAN_POINT ( 'NONE',  ( 0.2819296736111110979, 3.932722222298087544, 0.1167790944451422425 ) ) ;
#1758=EDGE_LOOP ( 'NONE', ( #14412, #12025, #21999, #8230 ) ) ;
#1759=CARTESIAN_POINT ( 'NONE',  ( 0.1292346314604057023, 0.3895833331816003775, 0.3119999999999998885 ) ) ;
#1763=CARTESIAN_POINT ( 'NONE',  ( 0.1919009159517996166, 3.982454885862982685, -0.2493777159950087974 ) ) ;
#1767=ORIENTED_EDGE ( 'NONE', *, *, #23255, .F. ) ;
#1768=CARTESIAN_POINT ( 'NONE',  ( 0.3114906597041430802, 5.086078164599575402, -0.01551821721983479528 ) ) ;
#1770=CARTESIAN_POINT ( 'NONE',  ( 0.2819296736111110979, 4.213972222298087544, -3.452642723725051716E-17 ) ) ;
#1771=CARTESIAN_POINT ( 'NONE',  ( -0.1167790944451423119, 5.120222222298088433, -0.2819296736111110979 ) ) ;
#1773=CARTESIAN_POINT ( 'NONE',  ( 1.910449006669871087E-17, 0.3583333331816003775, -0.3119999999999999996 ) ) ;
#1775=CARTESIAN_POINT ( 'NONE',  ( 5.731347020009612645E-17, 4.904944444596176290, 0.3119999999999999996 ) ) ;
#1777=CARTESIAN_POINT ( 'NONE',  ( 0.3039826620300027926, 4.805727411070424893, 0.07105243237910956189 ) ) ;
#1780=EDGE_CURVE ( 'NONE', #23361, #1879, #11797, .T. ) ;
#1783=ORIENTED_EDGE ( 'NONE', *, *, #12175, .T. ) ;
#1785=CARTESIAN_POINT ( 'NONE',  ( 0.1993543840281267465, 5.151472222298087544, 0.1993543840281266633 ) ) ;
#1790=CARTESIAN_POINT ( 'NONE',  ( 0.1167790944451423535, 0.2611111110352444808, 0.2819296736111110979 ) ) ;
#1792=CARTESIAN_POINT ( 'NONE',  ( 0.2819296736111110979, 5.002166666742532186, 0.1167790944451422425 ) ) ;
#1794=CARTESIAN_POINT ( 'NONE',  ( 0.1993543840281267465, 4.984805555631420582, 0.1993543840281266633 ) ) ;
#1795=DIRECTION ( 'NONE',  ( -0.000000000000000000, -1.000000000000000000, -0.000000000000000000 ) ) ;
#1799=CARTESIAN_POINT ( 'NONE',  ( 0.1292346314604058410, 4.401472222222221120, 0.3119999999999998885 ) ) ;
#1800=CARTESIAN_POINT ( 'NONE',  ( 0.1993543840281266633, 4.054250000075865223, -0.1993543840281266910 ) ) ;
#1802=CARTESIAN_POINT ( 'NONE',  ( 0.05402694832707571893, 4.042351412354395990, -0.3076319426930580470 ) ) ;
#1805=LINE ( 'NONE', #18392, #19451 ) ;
#1807=CARTESIAN_POINT ( 'NONE',  ( 0.3114133620982494355, 4.640484927562076756, 0.02096553565331283828 ) ) ;
#1810=CARTESIAN_POINT ( 'NONE',  ( -0.08089845032000375635, 4.435061056889780140, -0.3020206211261280971 ) ) ;
#1815=CARTESIAN_POINT ( 'NONE',  ( 0.1167790944451423257, 0.1569444443685778234, -0.2819296736111110424 ) ) ;
#1822=CARTESIAN_POINT ( 'NONE',  ( -0.2689956684658347807, 5.109708706941876066, 0.1540837381399228490 ) ) ;
#1824=CARTESIAN_POINT ( 'NONE',  ( 0.2206173157302028232, 0.02499999999999966485, -0.2206173157302028232 ) ) ;
#1825=CARTESIAN_POINT ( 'NONE',  ( -0.2819296736111110979, 3.866750000075866112, 0.000000000000000000 ) ) ;
#1828=CARTESIAN_POINT ( 'NONE',  ( 0.1993543840281266633, 4.512583333409199149, -0.1993543840281266910 ) ) ;
#1829=CYLINDRICAL_SURFACE ( 'NONE', #13178, 0.3119999999999999996 ) ;
#1833=CARTESIAN_POINT ( 'NONE',  ( -1.726321361862525858E-17, 5.061194444520309865, -0.2819296736111110979 ) ) ;
#1834=CARTESIAN_POINT ( 'NONE',  ( -0.01961490578657244105, 5.143841740609819801, -0.3033781769544516838 ) ) ;
#1839=CARTESIAN_POINT ( 'NONE',  ( 0.1167790944451422702, 4.724388888964754507, -0.2819296736111110979 ) ) ;
#1840=CARTESIAN_POINT ( 'NONE',  ( -0.3119999999999998885, 4.776472222222222008, 0.1292346314604058410 ) ) ;
#1841=CARTESIAN_POINT ( 'NONE',  ( 1.910449006669871087E-17, 0.4138888887371559577, -0.3119999999999999996 ) ) ;
#1842=CARTESIAN_POINT ( 'NONE',  ( -0.2819296736111110979, 0.5249999999241332649, 0.1167790944451422425 ) ) ;
#1846=CARTESIAN_POINT ( 'NONE',  ( 0.1993543840281266355, 0.1534722221463556135, 0.1993543840281267465 ) ) ;
#1852=CARTESIAN_POINT ( 'NONE',  ( -0.2912517187485964554, 3.894337629471870788, 0.1144103805008772345 ) ) ;
#1853=CARTESIAN_POINT ( 'NONE',  ( 0.2819296736111110979, 0.3166666665908000056, -0.1167790944451422980 ) ) ;
#1854=CARTESIAN_POINT ( 'NONE',  ( -0.2819296736111110424, 0.05972222214635559273, -0.1167790944451423396 ) ) ;
#1855=CARTESIAN_POINT ( 'NONE',  ( -0.1167790944451423257, 4.578555555631421470, -0.2819296736111110424 ) ) ;
#1860=CARTESIAN_POINT ( 'NONE',  ( 0.1993543840281266633, 5.012583333409199149, -0.1993543840281266910 ) ) ;
#1862=CARTESIAN_POINT ( 'NONE',  ( 0.2819296736111110979, 4.547305555631421470, -3.452642723725051716E-17 ) ) ;
#1863=CARTESIAN_POINT ( 'NONE',  ( 0.000000000000000000, 5.384999999999999787, 0.000000000000000000 ) ) ;
#1866=CARTESIAN_POINT ( 'NONE',  ( 0.04950202671021954742, 3.931318200535246277, -0.3090077374095805962 ) ) ;
#1867=CARTESIAN_POINT ( 'NONE',  ( 0.1292346314604056190, 3.984805555707287894, -0.3119999999999999996 ) ) ;
#1868=CARTESIAN_POINT ( 'NONE',  ( -0.1167790944451423119, 4.578555555631421470, -0.2819296736111110979 ) ) ;
#1872=ORIENTED_EDGE ( 'NONE', *, *, #18577, .F. ) ;
#1874=ORIENTED_EDGE ( 'NONE', *, *, #12510, .F. ) ;
#1879=VERTEX_POINT ( 'NONE', #7932 ) ;
#1880=CARTESIAN_POINT ( 'NONE',  ( 0.1292346314604056745, 0.5770833331816004330, -0.3119999999999999996 ) ) ;
#1883=CARTESIAN_POINT ( 'NONE',  ( -0.2034396455339492205, 3.716810070265228028, -0.2365585480272117402 ) ) ;
#1885=CARTESIAN_POINT ( 'NONE',  ( 0.04088039599977719152, 3.987110618275341523, -0.3119999999999992779 ) ) ;
#1892=CARTESIAN_POINT ( 'NONE',  ( 0.2819296736111110979, 4.269527777853643791, -3.452642723725051716E-17 ) ) ;
#1893=CARTESIAN_POINT ( 'NONE',  ( 0.1993543840281267465, 5.040361111186975940, 0.1993543840281266633 ) ) ;
#1896=CARTESIAN_POINT ( 'NONE',  ( -0.3119999999999998885, 3.776472222222221564, 0.1292346314604058410 ) ) ;
#1898=CARTESIAN_POINT ( 'NONE',  ( -1.910449006669871087E-17, 4.766055555707287894, -0.3119999999999999996 ) ) ;
#1899=CARTESIAN_POINT ( 'NONE',  ( 0.1993543840281267465, 5.109805555631420582, 0.1993543840281266633 ) ) ;
#1900=CARTESIAN_POINT ( 'NONE',  ( 1.995346317926969793E-07, 4.516063323326865664, 0.3119999999998666063 ) ) ;
#1903=CARTESIAN_POINT ( 'NONE',  ( 0.04544327613271605115, 0.04227586460901846394, -0.2884427797219447087 ) ) ;
#1906=CARTESIAN_POINT ( 'NONE',  ( -0.1993543840281266910, 5.068138888964754507, -0.1993543840281266910 ) ) ;
#1911=CARTESIAN_POINT ( 'NONE',  ( 0.2819296736111110979, 0.3270833332574666907, 0.000000000000000000 ) ) ;
#1913=EDGE_CURVE ( 'NONE', #6274, #11233, #22814, .T. ) ;
#1914=CARTESIAN_POINT ( 'NONE',  ( 0.1167790944451422702, 4.904944444520311642, -0.2819296736111110424 ) ) ;
#1915=CARTESIAN_POINT ( 'NONE',  ( 0.04944919563260133377, 5.072983550597543356, 0.3080590098858524417 ) ) ;
#1917=CARTESIAN_POINT ( 'NONE',  ( 0.1993543840281267465, 4.929250000075866112, 0.1993543840281266633 ) ) ;
#1918=CARTESIAN_POINT ( 'NONE',  ( 0.000000000000000000, 5.384999999999999787, 0.000000000000000000 ) ) ;
#1922=CARTESIAN_POINT ( 'NONE',  ( -0.2206173157302028232, 4.543833333333332725, -0.2206173157302028232 ) ) ;
#1924=CARTESIAN_POINT ( 'NONE',  ( 0.2673609140411699059, 4.025085253908718741, 0.1646236954874195357 ) ) ;
#1925=CARTESIAN_POINT ( 'NONE',  ( -0.06562929165342790139, 3.736422086006603749, 0.3053604199167166411 ) ) ;
#1929=CARTESIAN_POINT ( 'NONE',  ( -0.1491676245034612991, 4.122732337806922942, 0.2741778922001768537 ) ) ;
#1932=CARTESIAN_POINT ( 'NONE',  ( -0.1917207807845848766, 4.454768623156928342, 0.2495099228813656700 ) ) ;
#1934=VERTEX_POINT ( 'NONE', #625 ) ;
#1935=AXIS2_PLACEMENT_3D ( 'NONE', #18041, #14031, #19753 ) ;
#1938=CARTESIAN_POINT ( 'NONE',  ( -0.2819296736111110424, 0.2819444443685777957, -0.1167790944451423396 ) ) ;
#1939=CARTESIAN_POINT ( 'NONE',  ( 0.2495004542431085715, 3.869004524374595189, -0.1917331026496484903 ) ) ;
#1944=CARTESIAN_POINT ( 'NONE',  ( -1.906863420619159052E-17, 5.092106365077719410, -0.3114144293598434809 ) ) ;
#1945=CARTESIAN_POINT ( 'NONE',  ( -0.2206173157302027676, 4.724388888888888083, 0.2206173157302028787 ) ) ;
#1946=CARTESIAN_POINT ( 'NONE',  ( 0.1292346314604056745, 0.08402777777777743762, -0.3119999999999999996 ) ) ;
#1947=CARTESIAN_POINT ( 'NONE',  ( 5.731347020009612645E-17, 5.064666666666665762, 0.3119999999999999996 ) ) ;
#1950=CARTESIAN_POINT ( 'NONE',  ( 5.178964085587577574E-17, 4.269527777853643791, 0.2819296736111110979 ) ) ;
#1955=ORIENTED_EDGE ( 'NONE', *, *, #7094, .F. ) ;
#1956=CARTESIAN_POINT ( 'NONE',  ( 0.2712357692916257390, 4.358675636220367799, 0.1542604503148356232 ) ) ;
#1957=CARTESIAN_POINT ( 'NONE',  ( -0.1993543840281266355, 4.970916666742532186, 0.1993543840281267465 ) ) ;
#1959=CARTESIAN_POINT ( 'NONE',  ( 0.008702674981888494643, 5.198088336626264017, 0.2858269518860258041 ) ) ;
#1961=ADVANCED_FACE ( 'NONE', ( #22931 ), #20624, .T. ) ;
#1963=VECTOR ( 'NONE', #18895, 39.37007874015748143 ) ;
#1965=CARTESIAN_POINT ( 'NONE',  ( 0.07134304080793986425, 3.708532704952418602, -0.3042648351956888098 ) ) ;
#1967=CARTESIAN_POINT ( 'NONE',  ( 0.2819296736111110979, 4.717444444520309865, -0.1167790944451423396 ) ) ;
#1972=CARTESIAN_POINT ( 'NONE',  ( -0.2819296736111110979, 0.5805555554796888451, 0.1167790944451422425 ) ) ;
#1974=ORIENTED_EDGE ( 'NONE', *, *, #2134, .F. ) ;
#1975=CARTESIAN_POINT ( 'NONE',  ( -0.1993543840281267465, 0.2506944443685777957, 0.1993543840281266633 ) ) ;
#1977=DIRECTION ( 'NONE',  ( -0.000000000000000000, -1.000000000000000000, -0.000000000000000000 ) ) ;
#1983=CARTESIAN_POINT ( 'NONE',  ( -0.2819296736111111534, 0.2888888888130223265, 0.1167790944451422563 ) ) ;
#1984=CARTESIAN_POINT ( 'NONE',  ( -0.1993543840281266633, 0.05624999992413336897, -0.1993543840281266910 ) ) ;
#1986=CARTESIAN_POINT ( 'NONE',  ( 0.1167790944451422702, 4.238277777853643791, -0.2819296736111110424 ) ) ;
#1988=CARTESIAN_POINT ( 'NONE',  ( -0.1167790944451423257, 5.078555555631421470, -0.2819296736111110424 ) ) ;
#1989=CARTESIAN_POINT ( 'NONE',  ( 0.1993543840281267465, 4.484805555631420582, 0.1993543840281266633 ) ) ;
#1993=CARTESIAN_POINT ( 'NONE',  ( 0.2206173157302028787, 4.078555555707287894, 0.2206173157302027954 ) ) ;
#1996=EDGE_LOOP ( 'NONE', ( #8675, #6494, #19229, #22769 ) ) ;
#2002=CARTESIAN_POINT ( 'NONE',  ( -0.1383363854359150602, 4.845312163550097750, 0.2796553313559969056 ) ) ;
#2004=VERTEX_POINT ( 'NONE', #2695 ) ;
#2005=CARTESIAN_POINT ( 'NONE',  ( -0.1292346314604058410, 0.4381944442927114824, 0.3119999999999998885 ) ) ;
#2006=ORIENTED_EDGE ( 'NONE', *, *, #15547, .F. ) ;
#2008=CARTESIAN_POINT ( 'NONE',  ( 0.1683412523880292166, 4.743237864158165173, 0.2653294386633363033 ) ) ;
#2010=CARTESIAN_POINT ( 'NONE',  ( 0.08174464492498181856, 3.985945071896700664, -0.3038634887636957882 ) ) ;
#2014=VERTEX_POINT ( 'NONE', #1102 ) ;
#2016=CARTESIAN_POINT ( 'NONE',  ( -0.3058739907781938272, 4.667087298452083921, -0.06261323344678072778 ) ) ;
#2017=CARTESIAN_POINT ( 'NONE',  ( 0.1993543840281267465, 4.207027777853643791, 0.1993543840281266633 ) ) ;
#2020=CARTESIAN_POINT ( 'NONE',  ( 0.2206173157302027954, 3.807722222222221564, -0.2206173157302028232 ) ) ;
#2021=CARTESIAN_POINT ( 'NONE',  ( -0.2206173157302027676, 4.731333333485065573, 0.2206173157302028787 ) ) ;
#2022=CARTESIAN_POINT ( 'NONE',  ( 0.3091789633153798067, 4.806552312893038525, 0.04229410102701547380 ) ) ;
#2023=EDGE_CURVE ( 'NONE', #11875, #11539, #20335, .T. ) ;
#2024=CARTESIAN_POINT ( 'NONE',  ( -2.336494862270849996E-07, 3.904935224540334815, 0.3119999999998144258 ) ) ;
#2026=CARTESIAN_POINT ( 'NONE',  ( 0.2787925280157932950, 0.03555950194956544741, -0.06367239110606161268 ) ) ;
#2032=CARTESIAN_POINT ( 'NONE',  ( 0.1993543840281266633, 5.109805555631420582, -0.1993543840281266910 ) ) ;
#2033=CARTESIAN_POINT ( 'NONE',  ( 0.2819296736111110979, 3.838972222298087544, -3.452642723725051716E-17 ) ) ;
#2034=LINE ( 'NONE', #9471, #14651 ) ;
#2037=CARTESIAN_POINT ( 'NONE',  ( 1.726321361862525858E-17, 0.3965277777019111105, -0.2819296736111110979 ) ) ;
#2039=CARTESIAN_POINT ( 'NONE',  ( 5.178964085587577574E-17, 5.047305555631421470, 0.2819296736111110979 ) ) ;
#2042=CARTESIAN_POINT ( 'NONE',  ( -0.1993543840281266355, 4.804250000075865223, 0.1993543840281267465 ) ) ;
#2043=CARTESIAN_POINT ( 'NONE',  ( -0.02036395251267785617, 4.182136029502010466, 0.3120000006060605902 ) ) ;
#2044=CARTESIAN_POINT ( 'NONE',  ( -0.2206173157302028232, 5.043833333333332725, -0.2206173157302028232 ) ) ;
#2047=CARTESIAN_POINT ( 'NONE',  ( -0.3119999999999998885, 4.554249999999999687, 0.1292346314604058410 ) ) ;
#2048=CARTESIAN_POINT ( 'NONE',  ( -0.2819296736111110979, 3.738277777853643791, -0.1167790944451422980 ) ) ;
#2049=CARTESIAN_POINT ( 'NONE',  ( -0.3119999999999999996, 4.217444444444443441, 0.000000000000000000 ) ) ;
#2050=CARTESIAN_POINT ( 'NONE',  ( 0.001511429766296307989, 4.988234430213637438, -0.3119965677994301356 ) ) ;
#2051=CARTESIAN_POINT ( 'NONE',  ( -0.1036374797578168139, 3.735295676787865116, 0.2942854964279391639 ) ) ;
#2055=EDGE_CURVE ( 'NONE', #19443, #11353, #12456, .T. ) ;
#2061=CARTESIAN_POINT ( 'NONE',  ( -0.1167790944451424368, 0.4069444443685779067, 0.2819296736111110424 ) ) ;
#2062=CARTESIAN_POINT ( 'NONE',  ( 0.2726200149141687623, 3.858738252036598482, 0.1571313599304320630 ) ) ;
#2064=LINE ( 'NONE', #5248, #23992 ) ;
#2068=FACE_OUTER_BOUND ( 'NONE', #162, .T. ) ;
#2069=CARTESIAN_POINT ( 'NONE',  ( -0.2206173157302028787, 0.3305555555555552139, 0.2206173157302027954 ) ) ;
#2070=CARTESIAN_POINT ( 'NONE',  ( 0.3119999999999999996, 5.248694444444444329, -0.1292346314604056745 ) ) ;
#2072=CARTESIAN_POINT ( 'NONE',  ( 0.2819296736111110424, 4.120222222298087544, -0.1167790944451423396 ) ) ;
#2075=B_SPLINE_CURVE_WITH_KNOTS ( 'NONE', 3,
 ( #21997, #18105, #23812, #1638, #14456, #20177, #18344, #7254, #23939, #5046, #8956, #3344, #7134, #12759, #14574, #7370, #12516, #14820 ),
 .UNSPECIFIED., .F., .F.,
 ( 4, 2, 2, 2, 2, 2, 2, 2, 4 ),
 ( 0.1736046203853397751, 0.1758900224122931233, 0.1781754244392464714, 0.1804608264661998196, 0.1827462284931531677, 0.1850316305201065159, 0.1873170325470598641, 0.1896024345740132122, 0.1918878366009665604 ),
 .UNSPECIFIED. ) ;
#2079=CARTESIAN_POINT ( 'NONE',  ( -0.2819296736111110979, 4.908416666742532186, 0.000000000000000000 ) ) ;
#2080=CARTESIAN_POINT ( 'NONE',  ( -1.861236469537744314E-17, 5.143359825938298435, -0.3039629827691722741 ) ) ;
#2084=CARTESIAN_POINT ( 'NONE',  ( -0.1167790944451423535, 4.641055555631421470, 0.2819296736111110979 ) ) ;
#2086=CARTESIAN_POINT ( 'NONE',  ( -0.004140126504927462738, 4.043944831220694702, -0.3119764910025323856 ) ) ;
#2088=CARTESIAN_POINT ( 'NONE',  ( 0.1167790944451423535, 0.5388888888130223265, 0.2819296736111110424 ) ) ;
#2090=CARTESIAN_POINT ( 'NONE',  ( 0.2819296736111110424, 0.3305555554796888451, -0.1167790944451423119 ) ) ;
#2091=CARTESIAN_POINT ( 'NONE',  ( 1.910449006669871087E-17, 0.3583333331816003775, -0.3119999999999999996 ) ) ;
#2097=CARTESIAN_POINT ( 'NONE',  ( -1.910449006669871087E-17, 5.036888888888888971, -0.3119999999999999996 ) ) ;
#2098=CARTESIAN_POINT ( 'NONE',  ( 1.726321361862525858E-17, 0.2159722221463555858, -0.2819296736111110979 ) ) ;
#2099=CARTESIAN_POINT ( 'NONE',  ( 0.1993543840281266355, 0.1951388888130222155, 0.1993543840281267465 ) ) ;
#2100=CARTESIAN_POINT ( 'NONE',  ( -1.726321361862525858E-17, 4.297305555631421470, -0.2819296736111110979 ) ) ;
#2103=CARTESIAN_POINT ( 'NONE',  ( -0.1167790944451423257, 4.911888888964755395, -0.2819296736111110424 ) ) ;
#2104=CARTESIAN_POINT ( 'NONE',  ( -0.2819296736111110424, 4.467444444520309865, 0.1167790944451424923 ) ) ;
#2106=ORIENTED_EDGE ( 'NONE', *, *, #8432, .F. ) ;
#2109=CARTESIAN_POINT ( 'NONE',  ( 0.3119999999999999996, 3.977861111262842808, -0.1292346314604056745 ) ) ;
#2113=ORIENTED_EDGE ( 'NONE', *, *, #9831, .T. ) ;
#2116=CARTESIAN_POINT ( 'NONE',  ( 7.515426412127797749E-07, 4.849418923572540230, 0.3119999999980542227 ) ) ;
#2117=CARTESIAN_POINT ( 'NONE',  ( -0.2722822261173367120, 4.997487659248541547, -0.1577061459665719811 ) ) ;
#2119=B_SPLINE_CURVE_WITH_KNOTS ( 'NONE', 3,
 ( #4000, #15110, #7783, #5586, #18758, #5471, #1929, #14989, #5828, #20347, #24113, #7305, #18884, #9251, #22658, #14875, #20469, #13052, #5946, #2184, #9374, #9128, #20231, #3520, #10971, #11328, #16928, #3637, #3768, #7660, #13291, #16815, #7541, #18395 ),
 .UNSPECIFIED., .F., .F.,
 ( 4, 2, 2, 2, 1, 1, 1, 2, 2, 1, 2, 2, 2, 2, 2, 2, 2, 2, 4 ),
 ( 0.7232422263945339491, 0.7242982534508761727, 0.7248262669790472845, 0.7250902737431328404, 0.7252222771251756184, 0.7252552779706863406, 0.7252717783934417017, 0.7252759034991305143, 0.7252800286048193268, 0.7252882788161969518, 0.7253542805072183963, 0.7274663346199028435, 0.7295783887325872907, 0.7316904428452717379, 0.7327464699016139615, 0.7338024969579561851, 0.7359145510706406323, 0.7380266051833250796, 0.7401386592960095268 ),
 .UNSPECIFIED. ) ;
#2120=CARTESIAN_POINT ( 'NONE',  ( -0.3119999999999999996, 0.5909722220704892726, -0.1292346314604056745 ) ) ;
#2123=CARTESIAN_POINT ( 'NONE',  ( -1.910449006669871087E-17, 4.481333333333331836, -0.3119999999999999996 ) ) ;
#2127=CARTESIAN_POINT ( 'NONE',  ( 0.2493652384627738638, 3.968578555994963786, 0.1919023481737216208 ) ) ;
#2128=ORIENTED_EDGE ( 'NONE', *, *, #6335, .F. ) ;
#2133=CARTESIAN_POINT ( 'NONE',  ( -0.2901014048727216799, 4.672287041779367378, 0.1163490317311436512 ) ) ;
#2134=EDGE_CURVE ( 'NONE', #14350, #20423, #5074, .T. ) ;
#2135=CARTESIAN_POINT ( 'NONE',  ( -0.2819296736111110979, 3.908416666742532630, 0.000000000000000000 ) ) ;
#2136=CARTESIAN_POINT ( 'NONE',  ( 0.1675091558324258156, 5.038924456986563882, -0.2640337788857253787 ) ) ;
#2137=CARTESIAN_POINT ( 'NONE',  ( -0.3119999999999999996, 4.825083333333331836, -0.1292346314604056468 ) ) ;
#2139=CARTESIAN_POINT ( 'NONE',  ( -0.2206173157302028232, 3.877166666666666206, -0.2206173157302028232 ) ) ;
#2141=CARTESIAN_POINT ( 'NONE',  ( -0.1292346314604057023, 4.679250000151732536, 0.3119999999999998885 ) ) ;
#2143=CARTESIAN_POINT ( 'NONE',  ( -0.2819296736111110979, 5.033416666742532186, 0.000000000000000000 ) ) ;
#2145=CARTESIAN_POINT ( 'NONE',  ( 0.1993543840281266633, 4.387583333409199149, -0.1993543840281266910 ) ) ;
#2146=CARTESIAN_POINT ( 'NONE',  ( -0.2229596387321840234, 3.897916385485626911, 0.2198564724305951679 ) ) ;
#2151=ORIENTED_EDGE ( 'NONE', *, *, #1913, .T. ) ;
#2154=( BOUNDED_CURVE ( )  B_SPLINE_CURVE ( 2, ( #4765, #6723, #21596, #23529, #6363, #17584, #6482, #13703, #11874 ),
 .UNSPECIFIED., .F., .T. ) 
 B_SPLINE_CURVE_WITH_KNOTS ( ( 3, 2, 2, 2, 3 ),
 ( 0.5625000000000000000, 0.5729166666666666297, 0.5833333333333333703, 0.5937500000000000000, 0.6041666666666666297 ),
 .UNSPECIFIED. ) 
 CURVE ( )  GEOMETRIC_REPRESENTATION_ITEM ( )  RATIONAL_B_SPLINE_CURVE ( ( 1.000000000000000000, 0.9238795325112867385, 1.000000000000000000, 0.9238795325112867385, 1.000000000000000000, 0.9238795325112867385, 1.000000000000000000, 0.9238795325112867385, 1.000000000000000000 ) ) 
 REPRESENTATION_ITEM ( '' )  );
#2156=CARTESIAN_POINT ( 'NONE',  ( 0.2819296736111110979, 5.099388888964754507, 0.1167790944451422425 ) ) ;
#2159=CARTESIAN_POINT ( 'NONE',  ( 0.1993543840281267465, 3.887583333409199149, 0.1993543840281266633 ) ) ;
#2161=CARTESIAN_POINT ( 'NONE',  ( -0.2206173157302027676, 4.946611111111110404, 0.2206173157302028787 ) ) ;
#2165=CARTESIAN_POINT ( 'NONE',  ( -0.2819296736111111534, 0.4694444443685776847, 0.1167790944451422563 ) ) ;
#2167=CARTESIAN_POINT ( 'NONE',  ( 0.1167790944451422702, 4.849388888964755395, -0.2819296736111110424 ) ) ;
#2170=CARTESIAN_POINT ( 'NONE',  ( -0.2819296736111110424, 4.578555555631421470, 0.1167790944451424923 ) ) ;
#2172=CARTESIAN_POINT ( 'NONE',  ( 0.2874075015922078480, 4.866815774503709946, -0.1215004182914477260 ) ) ;
#2175=CARTESIAN_POINT ( 'NONE',  ( 5.731347020009612645E-17, 4.564666666666665762, 0.3119999999999999996 ) ) ;
#2176=CARTESIAN_POINT ( 'NONE',  ( -0.1167790944451423119, 3.842444444520309865, -0.2819296736111110979 ) ) ;
#2179=CARTESIAN_POINT ( 'NONE',  ( 0.02106080771364779100, 4.987673659226542711, -0.3113894394960690093 ) ) ;
#2184=CARTESIAN_POINT ( 'NONE',  ( -0.2777741477604763753, 4.117533257858705831, 0.1469810680412119430 ) ) ;
#2186=CARTESIAN_POINT ( 'NONE',  ( 0.0007708829432935857895, 4.654922335358357088, -0.3119992858245870804 ) ) ;
#2189=CARTESIAN_POINT ( 'NONE',  ( 0.3028046083902323216, 5.145323248153195195, 0.02283065314510586419 ) ) ;
#2193=CARTESIAN_POINT ( 'NONE',  ( -5.178964085587577574E-17, 0.5770833332574667462, 0.2819296736111110979 ) ) ;
#2198=VERTEX_POINT ( 'NONE', #1701 ) ;
#2201=CARTESIAN_POINT ( 'NONE',  ( 0.3119999999999999996, 0.3548611111111107386, -0.1292346314604056468 ) ) ;
#2202=CARTESIAN_POINT ( 'NONE',  ( 5.731347020009612645E-17, 5.231333333333332725, 0.3119999999999999996 ) ) ;
#2205=CARTESIAN_POINT ( 'NONE',  ( -1.726321361862525858E-17, 4.297305555631421470, -0.2819296736111110979 ) ) ;
#2206=CARTESIAN_POINT ( 'NONE',  ( -0.08161796258724582365, 4.347022020324052605, 0.3038890204011986951 ) ) ;
#2207=CYLINDRICAL_SURFACE ( 'NONE', #5585, 0.3119999999999999996 ) ;
#2210=CARTESIAN_POINT ( 'NONE',  ( 0.1993543840281267465, 4.929250000075866112, 0.1993543840281266633 ) ) ;
#2213=CARTESIAN_POINT ( 'NONE',  ( -0.2504139486751147947, 5.150879149016799552, -0.1698805244519268065 ) ) ;
#2214=( NAMED_UNIT ( * ) PLANE_ANGLE_UNIT ( ) SI_UNIT ( $, .RADIAN. ) );
#2217=AXIS2_PLACEMENT_3D ( 'NONE', #5357, #10982, #8773 ) ;
#2218=CARTESIAN_POINT ( 'NONE',  ( 0.2819296736111111534, 4.391055555631421470, 0.1167790944451422563 ) ) ;
#2219=CARTESIAN_POINT ( 'NONE',  ( -0.3136059260014000261, 4.058353895888922480, 0.02336461472333654921 ) ) ;
#2221=CARTESIAN_POINT ( 'NONE',  ( -5.178964085587577574E-17, 0.5354166665908000056, 0.2819296736111110979 ) ) ;
#2223=CARTESIAN_POINT ( 'NONE',  ( -0.1167790944451424368, 0.5319444443685777957, 0.2819296736111110424 ) ) ;
#2224=CARTESIAN_POINT ( 'NONE',  ( 0.2206173157302028787, 4.127166666666665762, 0.2206173157302027954 ) ) ;
#2225=CARTESIAN_POINT ( 'NONE',  ( 0.000000000000000000, 5.384999999999999787, 0.000000000000000000 ) ) ;
#2230=CARTESIAN_POINT ( 'NONE',  ( 0.1167790944451423119, 0.4902777777019112215, -0.2819296736111110979 ) ) ;
#2231=CARTESIAN_POINT ( 'NONE',  ( -0.1993543840281267465, 0.2923611110352445364, 0.1993543840281266633 ) ) ;
#2232=CARTESIAN_POINT ( 'NONE',  ( 0.2819296736111110424, 4.231333333409199149, -0.1167790944451423396 ) ) ;
#2234=CARTESIAN_POINT ( 'NONE',  ( 0.1993543840281266633, 4.901472222298088433, -0.1993543840281266910 ) ) ;
#2235=EDGE_CURVE ( 'NONE', #19908, #12402, #24004, .T. ) ;
#2236=CARTESIAN_POINT ( 'NONE',  ( -0.1167790944451423119, 4.509111111186976828, -0.2819296736111110979 ) ) ;
#2240=CARTESIAN_POINT ( 'NONE',  ( 0.1292346314604056190, 4.040361111262843252, -0.3119999999999999996 ) ) ;
#2241=CARTESIAN_POINT ( 'NONE',  ( 3.820898013339742174E-17, 5.384999999999999787, 0.3119999999999999996 ) ) ;
#2242=CARTESIAN_POINT ( 'NONE',  ( 0.000000000000000000, 5.384999999999999787, -0.3119999999999999996 ) ) ;
#2247=CARTESIAN_POINT ( 'NONE',  ( 1.910449006669871087E-17, 0.5319444444444439979, -0.3119999999999999996 ) ) ;
#2249=CARTESIAN_POINT ( 'NONE',  ( 0.1292346314604057023, 0.5006944442927115935, 0.3119999999999998885 ) ) ;
#2251=CARTESIAN_POINT ( 'NONE',  ( 0.1852222081618724869, 4.260541747846676941, -0.2521104950801930089 ) ) ;
#2255=CARTESIAN_POINT ( 'NONE',  ( 0.2895852664652339703, 5.177710075864474071, 0.05112040707668003697 ) ) ;
#2261=CARTESIAN_POINT ( 'NONE',  ( 0.2819296736111110424, 3.939666666742531742, -0.1167790944451423396 ) ) ;
#2263=CARTESIAN_POINT ( 'NONE',  ( 0.02013700421290525247, 5.118816490325227342, 0.3086180630080335718 ) ) ;
#2265=CARTESIAN_POINT ( 'NONE',  ( -0.3119999999999998885, 4.838972222373953969, 0.1292346314604058410 ) ) ;
#2266=CARTESIAN_POINT ( 'NONE',  ( 0.1993543840281266633, 4.957027777853642903, -0.1993543840281266910 ) ) ;
#2267=ORIENTED_EDGE ( 'NONE', *, *, #3707, .T. ) ;
#2268=CARTESIAN_POINT ( 'NONE',  ( 0.2819296736111110979, 4.325083333409198261, -3.452642723725051716E-17 ) ) ;
#2277=CARTESIAN_POINT ( 'NONE',  ( -0.1993543840281266355, 3.929250000075865668, 0.1993543840281267465 ) ) ;
#2278=CARTESIAN_POINT ( 'NONE',  ( 0.07073318196858055518, 4.430697953807255729, -0.3040470679591011915 ) ) ;
#2281=B_SPLINE_CURVE_WITH_KNOTS ( 'NONE', 1,
 ( #17512, #807 ),
 .UNSPECIFIED., .F., .F.,
 ( 2, 2 ),
 ( 0.000000000000000000, 1.000000000000000000 ),
 .UNSPECIFIED. ) ;
#2285=CARTESIAN_POINT ( 'NONE',  ( 0.1993543840281266355, 0.5423611110352445364, 0.1993543840281267465 ) ) ;
#2287=CARTESIAN_POINT ( 'NONE',  ( -0.1167790944451423257, 4.689666666742532186, -0.2819296736111110424 ) ) ;
#2288=CARTESIAN_POINT ( 'NONE',  ( -0.3119999999999999996, 3.939666666666666206, 0.000000000000000000 ) ) ;
#2289=CARTESIAN_POINT ( 'NONE',  ( 0.1167790944451424368, 4.759111111186977716, 0.2819296736111110424 ) ) ;
#2294=CARTESIAN_POINT ( 'NONE',  ( 0.2206173157302028787, 4.516055555555555046, 0.2206173157302027954 ) ) ;
#2295=CARTESIAN_POINT ( 'NONE',  ( 0.2819296736111111534, 3.821611111186975940, 0.1167790944451422563 ) ) ;
#2296=CARTESIAN_POINT ( 'NONE',  ( 0.01055874796617838236, 4.987974962125321987, -0.3118467276096589247 ) ) ;
#2299=ORIENTED_EDGE ( 'NONE', *, *, #3851, .F. ) ;
#2300=( BOUNDED_CURVE ( )  B_SPLINE_CURVE ( 2, ( #20741, #15500, #9528, #19150, #16961, #17326, #7927, #256, #5860 ),
 .UNSPECIFIED., .F., .F. ) 
 B_SPLINE_CURVE_WITH_KNOTS ( ( 3, 2, 2, 2, 3 ),
 ( 0.6160714285714284921, 0.6205357142857141906, 0.6250000000000000000, 0.6294642857142856984, 0.6339285714285713969 ),
 .UNSPECIFIED. ) 
 CURVE ( )  GEOMETRIC_REPRESENTATION_ITEM ( )  RATIONAL_B_SPLINE_CURVE ( ( 1.000000000000001998, 0.9238795325112848511, 1.000000000000000000, 0.9238795325112867385, 1.000000000000000000, 0.9238795325112867385, 1.000000000000000000, 0.9238795325112867385, 1.000000000000000000 ) ) 
 REPRESENTATION_ITEM ( '' )  );
#2301=( BOUNDED_CURVE ( )  B_SPLINE_CURVE ( 2, ( #12414, #18366, #14475, #14597, #24085, #7035, #8978, #9093, #14349 ),
 .UNSPECIFIED., .F., .F. ) 
 B_SPLINE_CURVE_WITH_KNOTS ( ( 3, 2, 2, 2, 3 ),
 ( 0.2589285714285712303, 0.2633928571428569287, 0.2678571428571426827, 0.2723214285714283811, 0.2767857142857141350 ),
 .UNSPECIFIED. ) 
 CURVE ( )  GEOMETRIC_REPRESENTATION_ITEM ( )  RATIONAL_B_SPLINE_CURVE ( ( 1.000000000000003775, 0.9238795325112829637, 1.000000000000000000, 0.9238795325112867385, 1.000000000000000000, 0.9238795325112867385, 1.000000000000000000, 0.9238795325112896251, 0.9999999999999971134 ) ) 
 REPRESENTATION_ITEM ( '' )  );
#2302=CARTESIAN_POINT ( 'NONE',  ( 0.2874800067704069706, 4.700142690845275695, -0.1212674689108930587 ) ) ;
#2305=CARTESIAN_POINT ( 'NONE',  ( -0.04074214740764643683, 3.933880325120055144, -0.3094968904035911850 ) ) ;
#2306=EDGE_CURVE ( 'NONE', #2198, #11353, #16778, .T. ) ;
#2309=CARTESIAN_POINT ( 'NONE',  ( -0.2819296736111110424, 0.5597222221463555858, -0.1167790944451423396 ) ) ;
#2312=DIRECTION ( 'NONE',  ( -0.000000000000000000, -1.000000000000000000, -0.000000000000000000 ) ) ;
#2314=CARTESIAN_POINT ( 'NONE',  ( -0.3002551575529973094, 4.610724490433781853, -0.08857506410196538948 ) ) ;
#2316=CARTESIAN_POINT ( 'NONE',  ( 0.000000000000000000, 5.072999999999999510, 0.000000000000000000 ) ) ;
#2317=CARTESIAN_POINT ( 'NONE',  ( 1.910449006669871087E-17, 0.2541666666666663188, -0.3119999999999999996 ) ) ;
#2318=CARTESIAN_POINT ( 'NONE',  ( -0.1292346314604057023, 5.116749999999999687, 0.3119999999999998885 ) ) ;
#2320=CARTESIAN_POINT ( 'NONE',  ( -0.1167790944451423535, 4.154944444520309865, 0.2819296736111110424 ) ) ;
#2321=CARTESIAN_POINT ( 'NONE',  ( -0.2725090806957128353, 4.340125742647720664, 0.1573274259844539558 ) ) ;
#2323=EDGE_CURVE ( 'NONE', #11539, #7602, #3410, .T. ) ;
#2327=CARTESIAN_POINT ( 'NONE',  ( 0.1167790944451424368, 4.648000000075865223, 0.2819296736111110424 ) ) ;
#2329=ADVANCED_FACE ( 'NONE', ( #8900 ), #15083, .T. ) ;
#2331=EDGE_CURVE ( 'NONE', #9441, #10582, #7669, .T. ) ;
#2332=ADVANCED_FACE ( 'NONE', ( #16702 ), #14396, .T. ) ;
#2337=CARTESIAN_POINT ( 'NONE',  ( -0.2819296736111110424, 4.203555555631421470, 0.1167790944451424923 ) ) ;
#2340=CARTESIAN_POINT ( 'NONE',  ( -0.01317391978361341122, 4.044190193732460692, -0.3117386529996676869 ) ) ;
#2343=CARTESIAN_POINT ( 'NONE',  ( -0.1167790944451422702, 0.3444444443685777402, -0.2819296736111110424 ) ) ;
#2345=CARTESIAN_POINT ( 'NONE',  ( -0.2272226533539420668, 5.205980271775564105, 0.1697100602738888242 ) ) ;
#2348=CARTESIAN_POINT ( 'NONE',  ( -1.906863420619159052E-17, 5.092106365077719410, -0.3114144293598434809 ) ) ;
#2350=CARTESIAN_POINT ( 'NONE',  ( 0.2819296736111110424, 0.5874999999241333759, 0.1167790944451424923 ) ) ;
#2351=CARTESIAN_POINT ( 'NONE',  ( 0.2819296736111110979, 0.2576388888130222155, 0.000000000000000000 ) ) ;
#2352=CARTESIAN_POINT ( 'NONE',  ( -0.1993543840281266355, 4.373694444520309865, 0.1993543840281267465 ) ) ;
#2354=CARTESIAN_POINT ( 'NONE',  ( -0.2819296736111110979, 4.811194444520309865, 0.000000000000000000 ) ) ;
#2355=CARTESIAN_POINT ( 'NONE',  ( 0.1167790944451424506, 4.259111111186976828, 0.2819296736111110424 ) ) ;
#2360=CARTESIAN_POINT ( 'NONE',  ( -0.1292346314604056745, 3.880638889040620931, -0.3119999999999999996 ) ) ;
#2361=CARTESIAN_POINT ( 'NONE',  ( 0.2206173157302027676, 0.1222222222222218990, 0.2206173157302028787 ) ) ;
#2366=VERTEX_POINT ( 'NONE', #16226 ) ;
#2369=CARTESIAN_POINT ( 'NONE',  ( -0.01584329491212002269, 0.03242967361111059876, 0.2819296736111481794 ) ) ;
#2372=CARTESIAN_POINT ( 'NONE',  ( -0.2819296736111110424, 0.1291666665908000611, -0.1167790944451423396 ) ) ;
#2375=CARTESIAN_POINT ( 'NONE',  ( 0.06082884619916966579, 4.264387106092869750, -0.3064377004203949206 ) ) ;
#2380=ORIENTED_EDGE ( 'NONE', *, *, #12493, .F. ) ;
#2384=CARTESIAN_POINT ( 'NONE',  ( 0.1993543840281267465, 3.984805555631421470, 0.1993543840281266633 ) ) ;
#2386=CARTESIAN_POINT ( 'NONE',  ( -0.1295556563484780987, 5.167372147454906361, -0.2683632288998299420 ) ) ;
#2387=CARTESIAN_POINT ( 'NONE',  ( -0.1292346314604057023, 4.845916666818398610, 0.3119999999999998885 ) ) ;
#2388=CARTESIAN_POINT ( 'NONE',  ( -0.1167790944451423535, 4.988277777853643791, 0.2819296736111110979 ) ) ;
#2389=ORIENTED_EDGE ( 'NONE', *, *, #11086, .F. ) ;
#2391=CARTESIAN_POINT ( 'NONE',  ( -0.2819296736111110979, 4.186194444520309865, 0.000000000000000000 ) ) ;
#2395=ORIENTED_EDGE ( 'NONE', *, *, #5929, .T. ) ;
#2397=DIRECTION ( 'NONE',  ( 0.000000000000000000, 0.000000000000000000, 1.000000000000000000 ) ) ;
#2398=CARTESIAN_POINT ( 'NONE',  ( 0.2206173157302027676, 0.2888888888888885287, 0.2206173157302028787 ) ) ;
#2399=CARTESIAN_POINT ( 'NONE',  ( -0.2819296736111110424, 3.870222222298087988, 0.1167790944451424923 ) ) ;
#2400=CARTESIAN_POINT ( 'NONE',  ( 0.1066988909913641620, 4.429648004107447967, -0.2931885909852042782 ) ) ;
#2404=CARTESIAN_POINT ( 'NONE',  ( 0.1993543840281266910, 0.4451388888130222710, -0.1993543840281266910 ) ) ;
#2406=ORIENTED_EDGE ( 'NONE', *, *, #20795, .T. ) ;
#2407=CARTESIAN_POINT ( 'NONE',  ( -0.2819296736111110979, 4.644527777853643791, 0.000000000000000000 ) ) ;
#2408=CARTESIAN_POINT ( 'NONE',  ( -0.3119999999999998885, 3.943138888888888083, 0.1292346314604058410 ) ) ;
#2409=CARTESIAN_POINT ( 'NONE',  ( -0.1167790944451423535, 4.696611111186976828, 0.2819296736111110424 ) ) ;
#2413=CARTESIAN_POINT ( 'NONE',  ( 0.3119999999999999996, 4.304249999999999687, -0.1292346314604056745 ) ) ;
#2418=ORIENTED_EDGE ( 'NONE', *, *, #18544, .F. ) ;
#2421=CARTESIAN_POINT ( 'NONE',  ( 0.2719451416848666647, 4.691957884589568195, 0.1583271517010935991 ) ) ;
#2426=VERTEX_POINT ( 'NONE', #3776 ) ;
#2428=CARTESIAN_POINT ( 'NONE',  ( -0.1993543840281266633, 0.3895833332574667462, -0.1993543840281266910 ) ) ;
#2431=CARTESIAN_POINT ( 'NONE',  ( 0.2206173157302028232, 0.5249999999999996891, -0.2206173157302028232 ) ) ;
#2433=CARTESIAN_POINT ( 'NONE',  ( -0.02046452715226480465, 5.117794691263952700, 0.3082562737412080089 ) ) ;
#2434=CARTESIAN_POINT ( 'NONE',  ( 0.000000000000000000, 0.000000000000000000, 0.000000000000000000 ) ) ;
#2436=CARTESIAN_POINT ( 'NONE',  ( 0.1292346314604056745, 0.1951388888888886397, -0.3119999999999999996 ) ) ;
#2437=CARTESIAN_POINT ( 'NONE',  ( 0.1292346314604056190, 5.088972222222220232, -0.3119999999999999996 ) ) ;
#2439=CARTESIAN_POINT ( 'NONE',  ( 0.1993543840281267465, 4.220916666742532186, 0.1993543840281266633 ) ) ;
#2443=( BOUNDED_CURVE ( )  B_SPLINE_CURVE ( 2, ( #17108, #19173, #19055, #7715, #6120, #13588, #21000, #9914, #22595 ),
 .UNSPECIFIED., .F., .F. ) 
 B_SPLINE_CURVE_WITH_KNOTS ( ( 3, 2, 2, 2, 3 ),
 ( 0.4732142857142858094, 0.4776785714285715079, 0.4821428571428570953, 0.4866071428571427382, 0.4910714285714283811 ),
 .UNSPECIFIED. ) 
 CURVE ( )  GEOMETRIC_REPRESENTATION_ITEM ( )  RATIONAL_B_SPLINE_CURVE ( ( 0.9999999999999981126, 0.9238795325112886259, 1.000000000000000000, 0.9238795325112867385, 1.000000000000000000, 0.9238795325112867385, 1.000000000000000000, 0.9238795325112896251, 0.9999999999999971134 ) ) 
 REPRESENTATION_ITEM ( '' )  );
#2446=CARTESIAN_POINT ( 'NONE',  ( 0.000000000000000000, 5.072999999999999510, 0.000000000000000000 ) ) ;
#2447=CARTESIAN_POINT ( 'NONE',  ( -0.1167790944451423257, 4.675777777853642903, -0.2819296736111110424 ) ) ;
#2448=AXIS2_PLACEMENT_3D ( 'NONE', #23614, #18147, #14366 ) ;
#2449=EDGE_CURVE ( 'NONE', #4057, #9930, #4129, .T. ) ;
#2455=CARTESIAN_POINT ( 'NONE',  ( 5.178964085587577574E-17, 4.380638888964754507, 0.2819296736111110979 ) ) ;
#2457=CARTESIAN_POINT ( 'NONE',  ( -0.2917836889767269626, 4.054536616146934946, -0.1122327437212481960 ) ) ;
#2459=LINE ( 'NONE', #19271, #16491 ) ;
#2460=CARTESIAN_POINT ( 'NONE',  ( -0.1167790944451424368, 0.3652777777019111105, 0.2819296736111110424 ) ) ;
#2461=CARTESIAN_POINT ( 'NONE',  ( 0.1292346314604080892, 4.144527777777776478, -0.3119999999999975016 ) ) ;
#2463=LINE ( 'NONE', #6228, #4103 ) ;
#2469=CARTESIAN_POINT ( 'NONE',  ( 0.2819296736111110979, 0.4833333332574666907, -0.1167790944451422980 ) ) ;
#2470=CARTESIAN_POINT ( 'NONE',  ( 0.1993543840281266910, 0.2645833332574666907, -0.1993543840281266910 ) ) ;
#2473=CARTESIAN_POINT ( 'NONE',  ( 0.1167790944451424368, 4.217444444520310753, 0.2819296736111110424 ) ) ;
#2476=CARTESIAN_POINT ( 'NONE',  ( -0.1993543840281266355, 4.818138888964754507, 0.1993543840281267465 ) ) ;
#2480=CARTESIAN_POINT ( 'NONE',  ( -0.1292346314604056745, 3.936194444596176290, -0.3119999999999999996 ) ) ;
#2483=B_SPLINE_CURVE_WITH_KNOTS ( 'NONE', 3,
 ( #22803, #371, #22684, #15254, #6095, #129, #13084, #20499, #13566, #20975, #11239, #5974, #1965, #16956, #13437, #9403, #15020 ),
 .UNSPECIFIED., .F., .F.,
 ( 4, 2, 1, 1, 1, 1, 1, 2, 2, 2, 4 ),
 ( 0.9959891374116947027, 0.9959969711276874804, 0.9960048048436802581, 0.9960204722756658136, 0.9960518071396369244, 0.9961144768675792571, 0.9962398163234638115, 0.9964904952352329204, 0.9969918530587710270, 0.9979945687058473514, 1.000000000000000000 ),
 .UNSPECIFIED. ) ;
#2489=CARTESIAN_POINT ( 'NONE',  ( -0.3070897238531018481, 5.003920639348050869, 0.05874023563891096061 ) ) ;
#2491=CARTESIAN_POINT ( 'NONE',  ( -0.1167790944451422702, 0.1777777777019111383, -0.2819296736111110424 ) ) ;
#2496=CARTESIAN_POINT ( 'NONE',  ( 0.1473522029762736330, 5.186493960802011749, -0.2512293203370171701 ) ) ;
#2498=CARTESIAN_POINT ( 'NONE',  ( -3.268767525105149064E-07, 3.877166675600695722, -0.3119999999998287477 ) ) ;
#2501=CARTESIAN_POINT ( 'NONE',  ( -0.2819296736111110424, 4.023000000075866112, 0.1167790944451424923 ) ) ;
#2502=CARTESIAN_POINT ( 'NONE',  ( -0.03226549977394326668, 0.03723082898989394512, 0.2853644822618193744 ) ) ;
#2503=CARTESIAN_POINT ( 'NONE',  ( -0.1929987219779752405, 5.170199845349932488, -0.2252547127343075273 ) ) ;
#2504=CARTESIAN_POINT ( 'NONE',  ( 0.2206173157302027954, 4.425777777929510215, -0.2206173157302028232 ) ) ;
#2505=CARTESIAN_POINT ( 'NONE',  ( -0.1167790944451423535, 4.877166666742532186, 0.2819296736111110979 ) ) ;
#2507=CARTESIAN_POINT ( 'NONE',  ( 0.1993543840281267465, 4.040361111186976828, 0.1993543840281266633 ) ) ;
#2510=ORIENTED_EDGE ( 'NONE', *, *, #6776, .F. ) ;
#2512=AXIS2_PLACEMENT_3D ( 'NONE', #7170, #1795, #18868 ) ;
#2513=ORIENTED_EDGE ( 'NONE', *, *, #19139, .F. ) ;
#2516=CARTESIAN_POINT ( 'NONE',  ( 0.2206173157302028232, 0.07361111095937818150, -0.2206173157302028232 ) ) ;
#2517=CARTESIAN_POINT ( 'NONE',  ( 0.06630425240443300894, 4.406804897824915024, 0.3048872720155125227 ) ) ;
#2519=CARTESIAN_POINT ( 'NONE',  ( -0.3119999999999998885, 4.943138888888888083, 0.1292346314604058410 ) ) ;
#2521=CARTESIAN_POINT ( 'NONE',  ( -0.2819296736111110979, 0.5736111110352443143, -0.1167790944451423396 ) ) ;
#2524=CARTESIAN_POINT ( 'NONE',  ( -0.1167790944451423257, 4.745222222298088433, -0.2819296736111110424 ) ) ;
#2526=CARTESIAN_POINT ( 'NONE',  ( 0.1167790944451422702, 4.613277777853643791, -0.2819296736111110424 ) ) ;
#2527=CARTESIAN_POINT ( 'NONE',  ( 1.910449006669871087E-17, 0.3027777776260448528, -0.3119999999999999996 ) ) ;
#2528=CARTESIAN_POINT ( 'NONE',  ( 0.2694814359950223892, 4.858521671012855592, 0.1585249534160457774 ) ) ;
#2531=CARTESIAN_POINT ( 'NONE',  ( 5.731347020009612645E-17, 4.175777777777776478, 0.3119999999999999996 ) ) ;
#2532=CARTESIAN_POINT ( 'NONE',  ( -0.1292346314604056745, 5.213972222373953969, -0.3119999999999999996 ) ) ;
#2534=CARTESIAN_POINT ( 'NONE',  ( 5.731347020009612645E-17, 4.009111111111109516, 0.3119999999999999996 ) ) ;
#2539=CARTESIAN_POINT ( 'NONE',  ( 0.09844450058468011411, 4.685553096116148453, 0.2967704092508852698 ) ) ;
#2542=CARTESIAN_POINT ( 'NONE',  ( 0.1572347947908322718, 4.316939703013657592, -0.2725648881498895504 ) ) ;
#2545=CARTESIAN_POINT ( 'NONE',  ( 1.726321361862525858E-17, 0.3826388888130222710, -0.2819296736111110979 ) ) ;
#2546=CARTESIAN_POINT ( 'NONE',  ( 0.04084064317332824351, 3.850486187038780095, 0.3119999999999971685 ) ) ;
#2550=ORIENTED_EDGE ( 'NONE', *, *, #21102, .F. ) ;
#2551=CARTESIAN_POINT ( 'NONE',  ( -0.1890277917641698391, 5.112901531185110926, 0.2452034757534968523 ) ) ;
#2553=CARTESIAN_POINT ( 'NONE',  ( 1.910449006669871087E-17, 0.1361111109593781676, -0.3119999999999999996 ) ) ;
#2555=CARTESIAN_POINT ( 'NONE',  ( 0.1292346314604070623, 4.734805555555555046, 0.3119999999999986673 ) ) ;
#2556=CARTESIAN_POINT ( 'NONE',  ( -0.3119999999999999996, 0.2645833333333330040, -0.1292346314604056745 ) ) ;
#2557=CARTESIAN_POINT ( 'NONE',  ( 0.2206173157302028787, 5.016055555555554157, 0.2206173157302027954 ) ) ;
#2558=CARTESIAN_POINT ( 'NONE',  ( 0.1167790944451424368, 3.884111111186977272, 0.2819296736111110424 ) ) ;
#2559=CARTESIAN_POINT ( 'NONE',  ( -1.910449006669871087E-17, 4.981333333333332725, -0.3119999999999999996 ) ) ;
#2564=CARTESIAN_POINT ( 'NONE',  ( -0.2819296736111110424, 4.689666666742532186, 0.1167790944451424923 ) ) ;
#2567=CARTESIAN_POINT ( 'NONE',  ( -0.3119999999999999996, 4.102861111111110404, -0.1292346314604056468 ) ) ;
#2571=CARTESIAN_POINT ( 'NONE',  ( -0.1167790944451423535, 4.321611111186976828, 0.2819296736111110979 ) ) ;
#2573=CARTESIAN_POINT ( 'NONE',  ( -0.1703658285323327304, 4.048932979482113836, -0.2616358941182676534 ) ) ;
#2578=CARTESIAN_POINT ( 'NONE',  ( 0.2819296736111110424, 0.3861111110352444808, -0.1167790944451423119 ) ) ;
#2582=DIRECTION ( 'NONE',  ( -0.000000000000000000, -1.000000000000000000, -0.000000000000000000 ) ) ;
#2587=CARTESIAN_POINT ( 'NONE',  ( -0.3038758835458211238, 3.777719410249359200, -0.08167920987076236761 ) ) ;
#2588=CARTESIAN_POINT ( 'NONE',  ( -0.1993543840281267465, 0.4034722221463555858, 0.1993543840281266633 ) ) ;
#2589=CARTESIAN_POINT ( 'NONE',  ( 0.2819296736111110424, 0.1986111110352444253, 0.1167790944451424923 ) ) ;
#2590=CARTESIAN_POINT ( 'NONE',  ( -0.2819296736111110979, 4.088972222298088433, 0.000000000000000000 ) ) ;
#2592=CARTESIAN_POINT ( 'NONE',  ( 0.2819296736111110979, 4.561194444520310753, -3.452642723725051716E-17 ) ) ;
#2597=CARTESIAN_POINT ( 'NONE',  ( -0.2206173157302027676, 3.953555555707287894, 0.2206173157302028787 ) ) ;
#2605=( BOUNDED_CURVE ( )  B_SPLINE_CURVE ( 2, ( #3662, #20131, #16597, #24017, #3786, #1600, #7327, #12717, #5369 ),
 .UNSPECIFIED., .F., .F. ) 
 B_SPLINE_CURVE_WITH_KNOTS ( ( 3, 2, 2, 2, 3 ),
 ( 0.1874999999999997224, 0.1919642857142855319, 0.1964285714285713413, 0.2008928571428571508, 0.2053571428571429325 ),
 .UNSPECIFIED. ) 
 CURVE ( )  GEOMETRIC_REPRESENTATION_ITEM ( )  RATIONAL_B_SPLINE_CURVE ( ( 1.000000000000004663, 0.9238795325112819645, 1.000000000000000000, 0.9238795325112867385, 1.000000000000000000, 0.9238795325112867385, 1.000000000000000000, 0.9238795325112852952, 1.000000000000001332 ) ) 
 REPRESENTATION_ITEM ( '' )  );
#2608=CARTESIAN_POINT ( 'NONE',  ( -0.2819296736111110979, 0.1361111110352444808, 0.1167790944451422425 ) ) ;
#2610=CARTESIAN_POINT ( 'NONE',  ( 0.2366305250842039298, 4.258541195428815485, -0.2048919769568291471 ) ) ;
#2612=CARTESIAN_POINT ( 'NONE',  ( 0.2779822102558559549, 4.089747752421554416, -0.1478112815533153268 ) ) ;
#2618=CARTESIAN_POINT ( 'NONE',  ( -1.726321361862525858E-17, 4.061194444520309865, -0.2819296736111110979 ) ) ;
#2620=CARTESIAN_POINT ( 'NONE',  ( -0.1704140045665936964, 5.169151437939198956, -0.2432099552469337289 ) ) ;
#2622=CARTESIAN_POINT ( 'NONE',  ( 0.1292346314604056190, 4.595916666818398610, -0.3119999999999999996 ) ) ;
#2623=CARTESIAN_POINT ( 'NONE',  ( 0.1993543840281267465, 5.054250000075865223, 0.1993543840281266633 ) ) ;
#2625=CARTESIAN_POINT ( 'NONE',  ( -0.2819296736111110424, 4.016055555631421470, -0.1167790944451423119 ) ) ;
#2626=ORIENTED_EDGE ( 'NONE', *, *, #11276, .T. ) ;
#2632=CARTESIAN_POINT ( 'NONE',  ( -0.2206173157302028787, 0.1569444442927115102, 0.2206173157302027954 ) ) ;
#2633=CARTESIAN_POINT ( 'NONE',  ( 0.2003325403190083509, 5.154788576413611878, -0.2249901030001114077 ) ) ;
#2639=CARTESIAN_POINT ( 'NONE',  ( -5.178964085587577574E-17, 0.07708333325746669074, 0.2819296736111110979 ) ) ;
#2642=CARTESIAN_POINT ( 'NONE',  ( 0.1993543840281266633, 4.679250000075866112, -0.1993543840281266910 ) ) ;
#2644=CARTESIAN_POINT ( 'NONE',  ( 0.1167790944451422702, 4.724388888964754507, -0.2819296736111110424 ) ) ;
#2645=CARTESIAN_POINT ( 'NONE',  ( 0.1292346314604057300, 0.2784722220704892726, 0.3119999999999998885 ) ) ;
#2648=CARTESIAN_POINT ( 'NONE',  ( -0.1292346314604056745, 4.262583333333332725, -0.3119999999999999996 ) ) ;
#2650=CARTESIAN_POINT ( 'NONE',  ( -0.1292346314604057023, 5.179250000151732536, 0.3119999999999998885 ) ) ;
#2651=LINE ( 'NONE', #6663, #9593 ) ;
#2653=CARTESIAN_POINT ( 'NONE',  ( 0.000000000000000000, 0.000000000000000000, 0.2495000000000007212 ) ) ;
#2657=CARTESIAN_POINT ( 'NONE',  ( 0.2940001360523776808, 4.144101130514563636, -0.1069869603560802546 ) ) ;
#2661=CARTESIAN_POINT ( 'NONE',  ( 5.731347020009612645E-17, 4.453555555555555046, 0.3119999999999999996 ) ) ;
#2663=CARTESIAN_POINT ( 'NONE',  ( -0.09380593400082881672, 0.03242967361111052244, 0.2658661084243340578 ) ) ;
#2666=DIRECTION ( 'NONE',  ( -0.000000000000000000, -1.000000000000000000, -0.000000000000000000 ) ) ;
#2669=CARTESIAN_POINT ( 'NONE',  ( -0.2651997416066034785, 4.618152273832173194, 0.1652184020648941043 ) ) ;
#2672=CARTESIAN_POINT ( 'NONE',  ( -0.3119999999999999996, 0.4937499999999996336, 0.1292346314604056190 ) ) ;
#2673=CARTESIAN_POINT ( 'NONE',  ( 0.3119999999999999996, 4.908416666666665762, 0.1292346314604056190 ) ) ;
#2674=CARTESIAN_POINT ( 'NONE',  ( -1.726321361862525858E-17, 4.019527777853643791, -0.2819296736111110979 ) ) ;
#2682=CARTESIAN_POINT ( 'NONE',  ( 0.1167790944451424368, 4.703555555631420582, 0.2819296736111110424 ) ) ;
#2684=CARTESIAN_POINT ( 'NONE',  ( -0.1754560956303653774, 5.162608100474836981, 0.2421305434278448743 ) ) ;
#2688=CARTESIAN_POINT ( 'NONE',  ( 0.2819296736111111534, 4.279944444520310753, 0.1167790944451422563 ) ) ;
#2694=CARTESIAN_POINT ( 'NONE',  ( 0.1993543840281266910, 0.4451388888130222710, -0.1993543840281266910 ) ) ;
#2695=CARTESIAN_POINT ( 'NONE',  ( -1.910449006669871087E-17, 3.759111111111109960, -0.3119999999999999996 ) ) ;
#2699=DIRECTION ( 'NONE',  ( -0.000000000000000000, -1.000000000000000000, -0.000000000000000000 ) ) ;
#2700=CARTESIAN_POINT ( 'NONE',  ( -0.2726255772188902471, 3.784483688608106799, 0.1571220562871406545 ) ) ;
#2701=CARTESIAN_POINT ( 'NONE',  ( -0.1993543840281267465, 0.5701388888130222155, 0.1993543840281266633 ) ) ;
#2703=CARTESIAN_POINT ( 'NONE',  ( 0.2819296736111110424, 0.4277777777019111105, -0.1167790944451423119 ) ) ;
#2704=CARTESIAN_POINT ( 'NONE',  ( -0.1167790944451423535, 3.988277777853643347, 0.2819296736111110424 ) ) ;
#2706=CARTESIAN_POINT ( 'NONE',  ( 0.1167790944451422702, 4.627166666742533074, -0.2819296736111110424 ) ) ;
#2710=CARTESIAN_POINT ( 'NONE',  ( -1.910449006669871087E-17, 4.814666666666665762, -0.3119999999999999996 ) ) ;
#2711=CARTESIAN_POINT ( 'NONE',  ( -0.2206173157302027676, 3.898000000151732092, 0.2206173157302028787 ) ) ;
#2716=EDGE_LOOP ( 'NONE', ( #17071, #14816, #13647, #3130 ) ) ;
#2719=CARTESIAN_POINT ( 'NONE',  ( -0.3071179979379754510, 4.559663454061065657, 0.06789499495992476485 ) ) ;
#2721=CARTESIAN_POINT ( 'NONE',  ( -0.1993543840281267465, 0.02847222214635559273, 0.1993543840281266633 ) ) ;
#2722=ORIENTED_EDGE ( 'NONE', *, *, #15876, .T. ) ;
#2723=CARTESIAN_POINT ( 'NONE',  ( 0.01239007739188290914, 4.265721496431039483, -0.3117902882241837537 ) ) ;
#2724=CARTESIAN_POINT ( 'NONE',  ( -0.2932070754709316107, 4.721180316163950508, -0.1095533496861972739 ) ) ;
#2725=CARTESIAN_POINT ( 'NONE',  ( 0.3014967569398348535, 4.083227540263434818, 0.08027429777791007803 ) ) ;
#2727=CARTESIAN_POINT ( 'NONE',  ( 0.03846423745654679177, 5.168284486722195759, 0.2947504553715781239 ) ) ;
#2731=B_SPLINE_CURVE_WITH_KNOTS ( 'NONE', 3,
 ( #13951, #14305, #15773, #17719, #4669, #21739, #5024, #4551, #12014, #16255, #23667, #19426, #10178, #2724, #12138, #19545, #2837, #1014, #9050, #138, #1732, #9414, #12734, #11009, #16732, #18200, #13096, #22329 ),
 .UNSPECIFIED., .F., .F.,
 ( 4, 2, 2, 2, 2, 2, 2, 2, 2, 2, 2, 2, 2, 4 ),
 ( 0.3125972154215642673, 0.3141903899697943703, 0.3157835645180244732, 0.3173767390662545762, 0.3189699136144846792, 0.3205630881627147821, 0.3221562627109448851, 0.3237494372591749325, 0.3253426118074050355, 0.3269357863556351385, 0.3285289609038652414, 0.3317153100003254473, 0.3349016590967856533, 0.3380880081932458592 ),
 .UNSPECIFIED. ) ;
#2733=CARTESIAN_POINT ( 'NONE',  ( -0.2819296736111110424, 3.849388888964754063, -0.1167790944451423119 ) ) ;
#2734=CARTESIAN_POINT ( 'NONE',  ( 0.2827533054146886271, 5.033813457600698982, -0.1318886379381357665 ) ) ;
#2735=CARTESIAN_POINT ( 'NONE',  ( -0.01917769073881700828, 5.163168389804723368, -0.2986873320831633927 ) ) ;
#2737=CARTESIAN_POINT ( 'NONE',  ( -0.3119999999999998885, 4.505638889040620931, 0.1292346314604058410 ) ) ;
#2738=CARTESIAN_POINT ( 'NONE',  ( -0.1993543840281266910, 4.748694444520309865, -0.1993543840281266910 ) ) ;
#2740=CARTESIAN_POINT ( 'NONE',  ( 0.1167790944451422702, 4.057722222298087544, -0.2819296736111110424 ) ) ;
#2748=CARTESIAN_POINT ( 'NONE',  ( -5.731347020009612645E-17, 0.2819444444444441089, 0.3119999999999999996 ) ) ;
#2749=CARTESIAN_POINT ( 'NONE',  ( -0.3119999999999999996, 0.09444444429271151020, -3.820898013339742174E-17 ) ) ;
#2750=CARTESIAN_POINT ( 'NONE',  ( 0.2634381141838555429, 5.151414792010848842, -0.1489582081906541955 ) ) ;
#2758=CARTESIAN_POINT ( 'NONE',  ( 0.1993543840281267465, 4.373694444520309865, 0.1993543840281266633 ) ) ;
#2762=CARTESIAN_POINT ( 'NONE',  ( 0.1292346314604057300, 0.4451388887371560132, 0.3119999999999998885 ) ) ;
#2763=CARTESIAN_POINT ( 'NONE',  ( -1.910449006669871087E-17, 4.370222222222221120, -0.3119999999999999996 ) ) ;
#2765=CARTESIAN_POINT ( 'NONE',  ( 0.2098724675597480049, 4.981782548361976204, -0.2345071763989569069 ) ) ;
#2768=CARTESIAN_POINT ( 'NONE',  ( 0.03691426518906104626, 4.709496014152167120, -0.3099139152953400700 ) ) ;
#2769=ORIENTED_EDGE ( 'NONE', *, *, #17414, .T. ) ;
#2775=CARTESIAN_POINT ( 'NONE',  ( -0.1167790944451422702, 0.06666666659080003332, -0.2819296736111110979 ) ) ;
#2778=DIRECTION ( 'NONE',  ( 0.000000000000000000, 0.000000000000000000, -1.000000000000000000 ) ) ;
#2780=VERTEX_POINT ( 'NONE', #8207 ) ;
#2781=CARTESIAN_POINT ( 'NONE',  ( -0.1094414729302275041, 5.115363257335545200, 0.2892685870146211591 ) ) ;
#2783=CYLINDRICAL_SURFACE ( 'NONE', #17237, 0.3119999999999999996 ) ;
#2784=CARTESIAN_POINT ( 'NONE',  ( 0.3119999999999999996, 0.5770833333333330595, -0.1292346314604056468 ) ) ;
#2785=CARTESIAN_POINT ( 'NONE',  ( -0.1292346314604057023, 4.950083333333331836, 0.3119999999999998885 ) ) ;
#2786=CARTESIAN_POINT ( 'NONE',  ( -0.2819296736111110979, 4.238277777853642903, -0.1167790944451422980 ) ) ;
#2787=CARTESIAN_POINT ( 'NONE',  ( -1.726321361862525858E-17, 3.963972222298087988, -0.2819296736111110979 ) ) ;
#2790=CARTESIAN_POINT ( 'NONE',  ( 0.1437411428072669917, 4.817336466253104632, -0.2795564064785391878 ) ) ;
#2791=VERTEX_POINT ( 'NONE', #2498 ) ;
#2794=CARTESIAN_POINT ( 'NONE',  ( -0.1167790944451423257, 4.620222222298087544, -0.2819296736111110424 ) ) ;
#2796=CARTESIAN_POINT ( 'NONE',  ( -0.02386323619205392085, 4.515404379429468484, 0.3110906963637425360 ) ) ;
#2800=CARTESIAN_POINT ( 'NONE',  ( 0.2819296736111110979, 4.005638888964754507, -3.452642723725051716E-17 ) ) ;
#2803=DIRECTION ( 'NONE',  ( -0.000000000000000000, -1.000000000000000000, -0.000000000000000000 ) ) ;
#2806=CARTESIAN_POINT ( 'NONE',  ( -0.1993543840281266633, 0.1118055554796889145, -0.1993543840281266910 ) ) ;
#2808=CARTESIAN_POINT ( 'NONE',  ( -0.2206173157302028787, 0.4416666666666662633, 0.2206173157302027954 ) ) ;
#2809=CARTESIAN_POINT ( 'NONE',  ( -1.910449006669871087E-17, 3.925777777777776922, -0.3119999999999999996 ) ) ;
#2810=CARTESIAN_POINT ( 'NONE',  ( 8.984713656453739555E-13, 5.162518060853549251, -0.2988821118451543968 ) ) ;
#2813=CARTESIAN_POINT ( 'NONE',  ( 0.2206173157302027954, 3.974388888888888083, -0.2206173157302028232 ) ) ;
#2815=CARTESIAN_POINT ( 'NONE',  ( -0.08166012297515250207, 3.823835601340495494, -0.3038808721544720148 ) ) ;
#2816=CARTESIAN_POINT ( 'NONE',  ( -0.2819296736111110424, 0.5041666665908000056, -0.1167790944451423396 ) ) ;
#2817=CARTESIAN_POINT ( 'NONE',  ( -0.1993543840281266355, 4.095916666742533074, 0.1993543840281267465 ) ) ;
#2820=CARTESIAN_POINT ( 'NONE',  ( 0.2819296736111110979, 4.616750000075865223, -3.452642723725051716E-17 ) ) ;
#2821=CARTESIAN_POINT ( 'NONE',  ( 0.2908167028465252213, 5.128327494763021299, 0.1005549492768820219 ) ) ;
#2822=CARTESIAN_POINT ( 'NONE',  ( 0.1864859647049422198, 5.086573399267850348, -0.2501715381927130388 ) ) ;
#2824=ORIENTED_EDGE ( 'NONE', *, *, #9965, .F. ) ;
#2826=CARTESIAN_POINT ( 'NONE',  ( 0.3119999999999999996, 3.748694444596176734, 0.1292346314604056190 ) ) ;
#2832=CARTESIAN_POINT ( 'NONE',  ( -0.2450385544630677703, 4.551749392525340276, -0.1971986354532856700 ) ) ;
#2834=CARTESIAN_POINT ( 'NONE',  ( 1.726321361862525858E-17, 0.007638888813022257952, -0.2819296736111110979 ) ) ;
#2835=CARTESIAN_POINT ( 'NONE',  ( 0.2819296736111110424, 0.1013888888130222432, 0.1167790944451424923 ) ) ;
#2837=CARTESIAN_POINT ( 'NONE',  ( -0.2490186137998644522, 4.718604494521838610, -0.1890786097946130784 ) ) ;
#2838=CARTESIAN_POINT ( 'NONE',  ( 0.3072473562388144397, 4.087380897120025836, -0.06871205321792885068 ) ) ;
#2840=CARTESIAN_POINT ( 'NONE',  ( -0.2206173157302028232, 4.488277777777776478, -0.2206173157302028232 ) ) ;
#2843=CARTESIAN_POINT ( 'NONE',  ( 0.1993543840281266633, 3.887583333409198705, -0.1993543840281266910 ) ) ;
#2845=CARTESIAN_POINT ( 'NONE',  ( 0.1553973393617723575, 5.020657948710086416, 0.2736341191248760629 ) ) ;
#2848=CARTESIAN_POINT ( 'NONE',  ( -0.3119999999999999996, 4.557722222373954857, 0.000000000000000000 ) ) ;
#2850=CARTESIAN_POINT ( 'NONE',  ( -0.1993543840281266910, 4.637583333409199149, -0.1993543840281266910 ) ) ;
#2852=CARTESIAN_POINT ( 'NONE',  ( 0.2819296736111110424, 4.106333333409199149, -0.1167790944451423396 ) ) ;
#2853=EDGE_LOOP ( 'NONE', ( #10665, #14476, #21486, #12136, #16151 ) ) ;
#2857=CARTESIAN_POINT ( 'NONE',  ( 0.3119999999999999996, 0.4624999999999996336, 0.000000000000000000 ) ) ;
#2858=CARTESIAN_POINT ( 'NONE',  ( 0.3119999999999999996, 0.1222222220704892864, 0.000000000000000000 ) ) ;
#2865=CARTESIAN_POINT ( 'NONE',  ( 0.1292346314604056745, 0.2437499998482670904, -0.3119999999999999996 ) ) ;
#2866=FACE_OUTER_BOUND ( 'NONE', #22246, .T. ) ;
#2870=CARTESIAN_POINT ( 'NONE',  ( 0.1167790944451422702, 4.335500000075866112, -0.2819296736111110424 ) ) ;
#2875=CARTESIAN_POINT ( 'NONE',  ( 0.2206173157302028787, 4.349388888888888083, 0.2206173157302027954 ) ) ;
#2876=CARTESIAN_POINT ( 'NONE',  ( 0.1292346314604056190, 5.207027777929509327, -0.3119999999999999996 ) ) ;
#2877=CARTESIAN_POINT ( 'NONE',  ( 0.04104138843526779906, 4.961624887611388424, 0.3099691146773075334 ) ) ;
#2878=ORIENTED_EDGE ( 'NONE', *, *, #646, .T. ) ;
#2882=CARTESIAN_POINT ( 'NONE',  ( 0.01963551970466389379, 4.683222298665006278, 0.3115337314451123718 ) ) ;
#2883=CARTESIAN_POINT ( 'NONE',  ( 0.2540558108961654682, 4.146614437982985457, -0.1864098413859918979 ) ) ;
#2889=CARTESIAN_POINT ( 'NONE',  ( 0.000000000000000000, 5.384999999999999787, 0.000000000000000000 ) ) ;
#2891=CARTESIAN_POINT ( 'NONE',  ( 0.2819296736111110979, 0.1048611110352444808, 0.000000000000000000 ) ) ;
#2900=CARTESIAN_POINT ( 'NONE',  ( -0.2574330024693365915, 4.274579109818574807, -0.1777445644304753436 ) ) ;
#2902=CARTESIAN_POINT ( 'NONE',  ( 0.3119999999999998885, 0.5145833333333330595, 0.1292346314604058410 ) ) ;
#2903=CARTESIAN_POINT ( 'NONE',  ( -1.910449006669871087E-17, 4.981333333333332725, -0.3119999999999999996 ) ) ;
#2904=CARTESIAN_POINT ( 'NONE',  ( 0.2819296736111110979, 4.161888888964754507, -0.1167790944451423396 ) ) ;
#2905=CARTESIAN_POINT ( 'NONE',  ( 0.2819296736111110424, 3.953555555631421914, -0.1167790944451423396 ) ) ;
#2908=CARTESIAN_POINT ( 'NONE',  ( 0.3110098031160312138, 4.807043492563579434, 0.02485275949016588215 ) ) ;
#2910=ORIENTED_EDGE ( 'NONE', *, *, #10241, .F. ) ;
#2911=ORIENTED_EDGE ( 'NONE', *, *, #8092, .F. ) ;
#2912=CARTESIAN_POINT ( 'NONE',  ( -0.04087474790194534774, 3.989444776327029096, -0.3120000000000006657 ) ) ;
#2913=CARTESIAN_POINT ( 'NONE',  ( 5.178964085587577574E-17, 4.422305555631421470, 0.2819296736111110979 ) ) ;
#2916=CARTESIAN_POINT ( 'NONE',  ( -0.2608208652903403757, 4.496968897623760064, -0.1766640260429742371 ) ) ;
#2921=CARTESIAN_POINT ( 'NONE',  ( -0.1167790944451423535, 3.988277777853643347, 0.2819296736111110979 ) ) ;
#2924=( BOUNDED_CURVE ( )  B_SPLINE_CURVE ( 2, ( #12500, #12863, #4494, #8268, #15481, #20843, #22789, #2555, #10002 ),
 .UNSPECIFIED., .F., .T. ) 
 B_SPLINE_CURVE_WITH_KNOTS ( ( 3, 2, 2, 2, 3 ),
 ( 0.3303571428571427937, 0.3348214285714284921, 0.3392857142857142461, 0.3437499999999999445, 0.3482142857142856429 ),
 .UNSPECIFIED. ) 
 CURVE ( )  GEOMETRIC_REPRESENTATION_ITEM ( )  RATIONAL_B_SPLINE_CURVE ( ( 1.000000000000000888, 0.9238795325112857393, 1.000000000000000000, 0.9238795325112867385, 1.000000000000000000, 0.9238795325112867385, 1.000000000000000000, 0.9238795325112877377, 0.9999999999999990008 ) ) 
 REPRESENTATION_ITEM ( '' )  );
#2929=CARTESIAN_POINT ( 'NONE',  ( 0.1993543840281266355, 0.08402777770191115214, 0.1993543840281267465 ) ) ;
#2939=CARTESIAN_POINT ( 'NONE',  ( -0.2819296736111110979, 0.3965277777019111660, -3.452642723725051716E-17 ) ) ;
#2940=CARTESIAN_POINT ( 'NONE',  ( -0.1167790944451423257, 4.023000000075866112, -0.2819296736111110424 ) ) ;
#2944=CARTESIAN_POINT ( 'NONE',  ( -1.726321361862525858E-17, 4.686194444520309865, -0.2819296736111110979 ) ) ;
#2945=CARTESIAN_POINT ( 'NONE',  ( 0.2905596657203107225, 5.133515633311446003, -0.09673461593479984466 ) ) ;
#2949=CARTESIAN_POINT ( 'NONE',  ( 0.2819296736111110979, 5.099388888964754507, 0.1167790944451422425 ) ) ;
#2954=CARTESIAN_POINT ( 'NONE',  ( 0.2819296736111110979, 4.995222222298087544, -0.1167790944451423396 ) ) ;
#2957=CARTESIAN_POINT ( 'NONE',  ( -0.2040850575673537060, 5.106812889253229848, -0.2344380848128326533 ) ) ;
#2958=CARTESIAN_POINT ( 'NONE',  ( 0.2206173157302027676, 0.2333333333333330040, 0.2206173157302028787 ) ) ;
#2960=CARTESIAN_POINT ( 'NONE',  ( 0.1993543840281266355, 0.3756944443685777957, 0.1993543840281267465 ) ) ;
#2963=ADVANCED_FACE ( 'NONE', ( #12142 ), #10781, .T. ) ;
#2964=FACE_OUTER_BOUND ( 'NONE', #20175, .T. ) ;
#2965=CARTESIAN_POINT ( 'NONE',  ( 0.2201042859353726511, 4.078604825199830586, 0.2219247941868362495 ) ) ;
#2967=CARTESIAN_POINT ( 'NONE',  ( -0.2781420133907471781, 5.053541304894200614, -0.1415874665319149239 ) ) ;
#2970=DIRECTION ( 'NONE',  ( -0.000000000000000000, -1.000000000000000000, -0.000000000000000000 ) ) ;
#2971=FACE_OUTER_BOUND ( 'NONE', #4503, .T. ) ;
#2972=ORIENTED_EDGE ( 'NONE', *, *, #1279, .F. ) ;
#2973=CARTESIAN_POINT ( 'NONE',  ( 0.2819296736111110979, 3.766055555631420582, 0.1167790944451422425 ) ) ;
#2974=CARTESIAN_POINT ( 'NONE',  ( -0.07848227395379105131, 0.04462176029470379945, -0.2841493449351579215 ) ) ;
#2975=CARTESIAN_POINT ( 'NONE',  ( -4.760580627680044823E-09, 4.932722222506802368, -0.3119999999999999996 ) ) ;
#2976=CARTESIAN_POINT ( 'NONE',  ( 0.01377311677012589726, 0.04044221366775575116, 0.2899422136677570205 ) ) ;
#2980=CARTESIAN_POINT ( 'NONE',  ( 0.1292346314604056190, 4.484805555707287006, -0.3119999999999999996 ) ) ;
#2981=CARTESIAN_POINT ( 'NONE',  ( -0.2819296736111110424, 4.759111111186977716, 0.1167790944451424923 ) ) ;
#2982=ORIENTED_EDGE ( 'NONE', *, *, #17351, .T. ) ;
#2983=CARTESIAN_POINT ( 'NONE',  ( -0.1993543840281266355, 4.137583333409199149, 0.1993543840281267465 ) ) ;
#2986=ORIENTED_EDGE ( 'NONE', *, *, #17379, .T. ) ;
#2992=EDGE_LOOP ( 'NONE', ( #18075, #2910, #10313, #3605 ) ) ;
#2993=CARTESIAN_POINT ( 'NONE',  ( -0.3119999999999999996, 0.09097222207048931419, -0.1292346314604056745 ) ) ;
#2995=CARTESIAN_POINT ( 'NONE',  ( -0.003434916545333202738, 4.377259052997221289, -0.3119838150564986368 ) ) ;
#2999=ORIENTED_EDGE ( 'NONE', *, *, #1089, .T. ) ;
#3001=DIRECTION ( 'NONE',  ( -0.000000000000000000, -1.000000000000000000, -0.000000000000000000 ) ) ;
#3003=CARTESIAN_POINT ( 'NONE',  ( -1.726321361862525858E-17, 4.505638888964754507, -0.2819296736111110979 ) ) ;
#3004=FACE_OUTER_BOUND ( 'NONE', #15519, .T. ) ;
#3007=CARTESIAN_POINT ( 'NONE',  ( 0.1292346314604058410, 3.957027777777776478, 0.3119999999999998885 ) ) ;
#3008=CARTESIAN_POINT ( 'NONE',  ( -0.2206173157302028232, 5.106333333485065573, -0.2206173157302028232 ) ) ;
#3009=CARTESIAN_POINT ( 'NONE',  ( -0.3119999999999998885, 4.665361111111110404, 0.1292346314604058410 ) ) ;
#3019=CARTESIAN_POINT ( 'NONE',  ( -0.2206173157302027676, 4.446611111111110404, 0.2206173157302028787 ) ) ;
#3022=CARTESIAN_POINT ( 'NONE',  ( 0.1167790944451423535, 0.03888888881302225708, 0.2819296736111110979 ) ) ;
#3025=CARTESIAN_POINT ( 'NONE',  ( -0.1993543840281266910, 5.193138888964755395, -0.1993543840281266910 ) ) ;
#3028=CARTESIAN_POINT ( 'NONE',  ( 0.3119999999999999996, 3.859805555555554601, -0.1292346314604056745 ) ) ;
#3029=CARTESIAN_POINT ( 'NONE',  ( -8.048972922423762964E-05, 4.293831062076359117, 0.3119999997849208784 ) ) ;
#3031=CARTESIAN_POINT ( 'NONE',  ( 0.2206173157302028232, 0.5249999999999996891, -0.2206173157302028232 ) ) ;
#3032=CARTESIAN_POINT ( 'NONE',  ( -0.1292346314604057023, 4.672305555555554157, 0.3119999999999998885 ) ) ;
#3033=CARTESIAN_POINT ( 'NONE',  ( 0.1167790944451424506, 4.314666666742532186, 0.2819296736111110424 ) ) ;
#3034=CARTESIAN_POINT ( 'NONE',  ( 0.1167790944451422702, 3.904944444520310753, -0.2819296736111110424 ) ) ;
#3035=CARTESIAN_POINT ( 'NONE',  ( 3.820898013339742174E-17, 5.384999999999999787, 0.3119999999999999996 ) ) ;
#3038=CARTESIAN_POINT ( 'NONE',  ( -0.3038794704804686497, 3.999912589447470079, -0.08166535634033041113 ) ) ;
#3039=CARTESIAN_POINT ( 'NONE',  ( 0.1993543840281266633, 4.609805555631420582, -0.1993543840281266910 ) ) ;
#3046=CARTESIAN_POINT ( 'NONE',  ( -0.1993543840281266355, 4.040361111186976828, 0.1993543840281267465 ) ) ;
#3047=CARTESIAN_POINT ( 'NONE',  ( -0.3120000000000000551, 0.3826388888888884732, 0.1292346314604056190 ) ) ;
#3048=CARTESIAN_POINT ( 'NONE',  ( 0.000000000000000000, 5.384999999999999787, 0.000000000000000000 ) ) ;
#3051=CARTESIAN_POINT ( 'NONE',  ( -0.2819296736111110979, 0.5805555554796888451, 0.1167790944451422425 ) ) ;
#3054=CARTESIAN_POINT ( 'NONE',  ( 5.731347020009612645E-17, 4.231333333333332725, 0.3119999999999999996 ) ) ;
#3061=CARTESIAN_POINT ( 'NONE',  ( -0.2819296736111110424, 0.3374999999241334314, -0.1167790944451423396 ) ) ;
#3062=CARTESIAN_POINT ( 'NONE',  ( 5.178964085587577574E-17, 4.158416666742532186, 0.2819296736111110979 ) ) ;
#3066=CARTESIAN_POINT ( 'NONE',  ( 0.1167790944451424368, 4.717444444520309865, 0.2819296736111110424 ) ) ;
#3067=CARTESIAN_POINT ( 'NONE',  ( 0.2660021697418833431, 5.126719186317235000, 0.1552671348293162834 ) ) ;
#3069=CARTESIAN_POINT ( 'NONE',  ( 0.2382335091060892029, 5.084669797853266893, -0.2016295426171259009 ) ) ;
#3072=CARTESIAN_POINT ( 'NONE',  ( -0.2819296736111110424, 5.071611111186976828, -0.1167790944451423119 ) ) ;
#3073=CARTESIAN_POINT ( 'NONE',  ( 0.2645723224789517936, 4.191640340208213189, 0.1653647831739661345 ) ) ;
#3075=( BOUNDED_CURVE ( )  B_SPLINE_CURVE ( 2, ( #14722, #7510, #22137, #16542, #16660, #5556, #16777, #5437, #3852, #12903, #22376, #13142, #23963, #13259, #14596, #7626, #5794, #18724, #10818, #18606, #20555, #3603, #11054, #7390, #22260, #13020, #20435, #3732, #1899, #9461, #16893, #20674, #18246, #1543, #8975, #3486, #23833, #22018, #5315, #12778, #20198, #10936, #18364, #1658, #2623, #11905, #23084, #4204, #21028, #9701, #2143, #15311, #17140, #11658, #427, #19081, #22627, #8215, #15189, #8094, #11538, #7979, #15548, #2388, #9580, #20911, #13844, #22739, #665, #543, #19325, #9825, #2266, #6027, #18969, #5912, #22969, #11775, #3967, #11412, #13496, #10066, #17260, #19196, #15430, #17491, #13370, #786, #18845, #15664, #17375, #17012, #7746, #22857, #6147, #2505, #13613, #6392, #9945, #305, #20790, #7861, #4320, #4081, #6270, #13728, #21151, #4438, #8335, #10308, #14199, #21632, #1027, #8589, #8457, #23683, #1151, #12263, #15900, #23565, #10662, #6880, #19678, #21754, #16150, #18093, #6630, #19804, #6515, #2981, #19438, #14078, #2738, #1272, #21507, #4924, #7004, #4799, #16026, #14321, #21393, #10435, #23442, #3101, #23322, #5040, #17859, #8699, #10548, #19559, #21274, #904, #1394, #16271, #12507, #4565, #12388, #17981, #4682, #6754, #19929, #3215, #8825, #12024, #2850, #10190, #17613, #15786, #23204, #13963, #12152, #17732, #16396, #5285, #3457, #18578, #9192, #12873, #7480, #23804, #14927, #1868, #3700, #22347, #9066, #11028, #21990, #12629, #20169, #12753, #1632, #10908, #16514, #18219, #32, #10791, #14813, #7125, #14567, #22230, #14447, #20045, #23928, #21871, #7247, #1749, #18337, #3334, #14693, #22111, #5406, #20290, #3575, #8948, #5163, #18455, #9308, #16634, #24052, #16750, #1513, #5529, #7362, #12993, #20408, #11147, #15378, #4391, #17323, #11978, #5976, #17564, #20738, #19390, #10020, #2218, #374, #8048, #2455, #19267, #6221, #13568, #22925, #23150, #15256, #11605, #13685, #618, #22807, #11481, #15737, #4031, #8285, #7924, #22686, #2571, #11726, #6098, #4153, #21101, #11851, #19148, #20976, #23037, #10141, #6461, #17083, #2688, #21222, #9893, #737, #17208, #17443, #4273, #9648, #15498, #8166, #15620, #6341, #855, #18916, #13793, #4512, #7815, #20859, #492, #13440, #19035, #9773, #2337, #1095, #14143, #10381, #1458, #1335, #14264, #4984, #4744, #12215, #8402, #15970, #10610, #14030, #23391, #19868, #8765, #6698, #19749, #3160, #1218, #19624, #21572, #14386, #18039, #12449, #21701, #5103, #8646, #19989, #10493, #4866, #16094, #8893, #6580, #16336, #12569, #6948, #3277, #23747, #10255, #10730, #21814, #12333, #16218, #17803, #23630, #3046, #19507, #17923, #23508, #18161, #6823, #13914, #21342, #4629, #12097, #2800, #21460, #8526, #973, #17682, #2921, #15852, #23269, #7639, #3863, #19092, #18979, #7757, #22637, #22388, #7871, #7071, #15201, #4092, #7517, #16904, #13381, #2277, #198, #13269, #20804, #18858, #5689, #15088, #15320, #11549, #5922, #9713, #22751, #2159, #18736, #6042, #17150, #9592, #2399, #74, #9838, #13508, #440, #22510, #21928, #4215, #1579, #2033, #17270, #20922, #10853, #17024, #11668, #13152, #318, #14509, #11426, #5221, #12694, #20111, #5804, #3403, #20685, #18281, #16792, #9014, #3976, #14966, #20565, #11305, #9470, #15556, #11784, #12160, #13972, #6159, #4333, #12037 ),
 .UNSPECIFIED., .F., .T. ) 
 B_SPLINE_CURVE_WITH_KNOTS ( ( 3, 2, 2, 2, 2, 2, 2, 2, 2, 2, 2, 2, 2, 2, 2, 2, 2, 2, 2, 2, 2, 2, 2, 2, 2, 2, 2, 2, 2, 2, 2, 2, 2, 2, 2, 2, 2, 2, 2, 2, 2, 2, 2, 2, 2, 2, 2, 2, 2, 2, 2, 2, 2, 2, 2, 2, 2, 2, 2, 2, 2, 2, 2, 2, 2, 2, 2, 2, 2, 2, 2, 2, 2, 2, 2, 2, 2, 2, 2, 2, 2, 2, 2, 2, 2, 2, 2, 2, 2, 2, 2, 2, 2, 2, 2, 2, 2, 2, 2, 2, 2, 2, 2, 2, 2, 2, 2, 2, 2, 2, 2, 2, 2, 2, 2, 2, 2, 2, 2, 2, 2, 2, 2, 2, 2, 2, 2, 2, 2, 2, 2, 2, 2, 2, 2, 2, 2, 2, 2, 2, 2, 2, 2, 2, 2, 2, 2, 2, 2, 2, 2, 2, 2, 2, 2, 2, 2, 2, 2, 2, 2, 2, 2, 2, 2, 2, 2, 2, 2, 2, 2, 2, 2, 2, 2, 2, 2, 2, 2, 2, 2, 2, 2, 2, 2, 2, 2, 2, 2, 2, 2, 2, 2, 2, 2, 2, 2, 2, 2, 2, 2, 2, 2, 2, 2, 2, 2, 2, 2, 2, 2, 2, 3 ),
 ( 0.03225371760371920082, 0.03655005604694450128, 0.04111881305281361171, 0.04568757005868272214, 0.05025632706455182563, 0.05482508407042094301, 0.05939384107629005344, 0.06396259808215916387, 0.06853135508802826736, 0.07310011209389738474, 0.07766886909976648823, 0.08223762610563560560, 0.08680638311150470909, 0.09137514011737382646, 0.09594389712324292996, 0.1005126541291120335, 0.1050814111349811369, 0.1096501681408502543, 0.1142189251467193856, 0.1187876821525884752, 0.1233564391584576064, 0.1279251961643266822, 0.1324939531701957995, 0.1370627101760649169, 0.1416314671819340343, 0.1462002241878031239, 0.1507689811936722690, 0.1553377381995413309, 0.1599064952054104760, 0.1644752522112795934, 0.1690440092171486830, 0.1736127662230178004, 0.1781815232288868900, 0.1827502802347560074, 0.1873190372406251247, 0.1918877942464942421, 0.1964565512523633317, 0.2010253082582324491, 0.2055940652641015665, 0.2101628222699706838, 0.2147315792758397734, 0.2193003362817088908, 0.2238690932875780082, 0.2284378502934471256, 0.2330066072993162152, 0.2375753643051853325, 0.2421441213110544499, 0.2467128783169235673, 0.2512816353227926292, 0.2558503923286618020, 0.2604191493345308639, 0.2649879063404000368, 0.2695566633462690986, 0.2741254203521382160, 0.2786941773580072779, 0.2832629343638764507, 0.2878316913697455126, 0.2924004483756146300, 0.2969692053814838029, 0.3015379623873529202, 0.3061067193932219821, 0.3106754763990910995, 0.3152442334049602168, 0.3198129904108292787, 0.3243817474166983961, 0.3289505044225675690, 0.3335192614284366308, 0.3380880184343057482, 0.3426567754401748656, 0.3472255324460440384, 0.3517942894519130448, 0.3563630464577821622, 0.3609318034636513350, 0.3655005604695203969, 0.3700693174753895143, 0.3746380744812586316, 0.3792068314871278045, 0.3837755884929968664, 0.3883443454988659282, 0.3929131025047351011, 0.3974818595106041630, 0.4020506165164732804, 0.4066193735223423977, 0.4111881305282115706, 0.4157568875340806325, 0.4203256445399497498, 0.4248944015458188672, 0.4294631585516879291, 0.4340319155575570464, 0.4386006725634261638, 0.4431694295692952812, 0.4477381865751643986, 0.4523069435810335159, 0.4568757005869026888, 0.4614444575927716952, 0.4660132145986408125, 0.4705819716045099299, 0.4751507286103790473, 0.4797194856162481646, 0.4842882426221172820, 0.4888569996279864549, 0.4934257566338555168, 0.4979945136397245786, 0.5025632706455936960, 0.5071320276514628134, 0.5117007846573319307, 0.5162695416632010481, 0.5208382986690700545, 0.5254070556749392829, 0.5299758126808085112, 0.5345445696866775176, 0.5391133266925466350, 0.5436820836984157523, 0.5482508407042848697, 0.5528195977101539871, 0.5573883547160231045, 0.5619571117218922218, 0.5665258687277613392, 0.5710946257336304566, 0.5756633827394995739, 0.5802321397453686913, 0.5848008967512376977, 0.5893696537571068150, 0.5939384107629760434, 0.5985071677688450498, 0.6030759247747142782, 0.6076446817805832845, 0.6122134387864524019, 0.6167821957923215193, 0.6213509527981906366, 0.6259197098040597540, 0.6304884668099288714, 0.6350572238157979887, 0.6396259808216669951, 0.6441947378275362235, 0.6487634948334052298, 0.6533322518392744582, 0.6579010088451435756, 0.6624697658510125819, 0.6670385228568818103, 0.6716072798627508167, 0.6761760368686199341, 0.6807447938744890514, 0.6853135508803581688, 0.6898823078862272862, 0.6944510648920965146, 0.6990198218979655209, 0.7035885789038345273, 0.7081573359097037557, 0.7127260929155727620, 0.7172948499214418794, 0.7218636069273111078, 0.7264323639331802251, 0.7310011209390493425, 0.7355698779449183489, 0.7401386349507874662, 0.7447073919566565836, 0.7492761489625257010, 0.7538449059683948184, 0.7584136629742640467, 0.7629824199801330531, 0.7675511769860021705, 0.7721199339918712878, 0.7766886909977402942, 0.7812574480036094116, 0.7858262050094786400, 0.7903949620153477573, 0.7949637190212168747, 0.7995324760270859921, 0.8041012330329549984, 0.8086699900388241158, 0.8132387470446932332, 0.8178075040505623505, 0.8223762610564315789, 0.8269450180623005853, 0.8315137750681697026, 0.8360825320740388200, 0.8406512890799079374, 0.8452200460857769437, 0.8497888030916461721, 0.8543575600975152895, 0.8589263171033842958, 0.8634950741092535242, 0.8680638311151225306, 0.8726325881209917590, 0.8772013451268607653, 0.8817701021327298827, 0.8863388591385991111, 0.8909076161444681174, 0.8954763731503372348, 0.9000451301562063522, 0.9046138871620754696, 0.9091826441679444759, 0.9137514011738138153, 0.9183201581796828217, 0.9228889151855518280, 0.9274576721914210564, 0.9320264291972900628, 0.9365951862031591801, 0.9411639432090282975, 0.9457327002148975259, 0.9503014572207666433, 0.9548702142266356496, 0.9594389712325047670, 0.9640077282383738844, 0.9685764852442430017, 0.9731452422501120081, 0.9777139992559813475, 0.9822827562618503539, 0.9868515132677194712, 0.9914202702735885886, 0.9959890272794575949, 1.000000000000000000 ),
 .UNSPECIFIED. ) 
 CURVE ( )  GEOMETRIC_REPRESENTATION_ITEM ( )  RATIONAL_B_SPLINE_CURVE ( ( 0.9914636835865273667, 0.9284183224522731814, 1.000000000000000000, 0.9238795325112867385, 1.000000000000000000, 0.9238795325112867385, 1.000000000000000000, 0.9238795325112867385, 1.000000000000000000, 0.9238795325112867385, 1.000000000000000000, 0.9238795325112867385, 1.000000000000000000, 0.9238795325112867385, 1.000000000000000000, 0.9238795325112867385, 1.000000000000000000, 0.9238795325112867385, 1.000000000000000000, 0.9238795325112867385, 1.000000000000000000, 0.9238795325112867385, 1.000000000000000000, 0.9238795325112867385, 1.000000000000000000, 0.9238795325112867385, 1.000000000000000000, 0.9238795325112867385, 1.000000000000000000, 0.9238795325112867385, 1.000000000000000000, 0.9238795325112867385, 1.000000000000000000, 0.9238795325112867385, 1.000000000000000000, 0.9238795325112867385, 1.000000000000000000, 0.9238795325112867385, 1.000000000000000000, 0.9238795325112867385, 1.000000000000000000, 0.9238795325112867385, 1.000000000000000000, 0.9238795325112867385, 1.000000000000000000, 0.9238795325112867385, 1.000000000000000000, 0.9238795325112867385, 1.000000000000000000, 0.9238795325112867385, 1.000000000000000000, 0.9238795325112867385, 1.000000000000000000, 0.9238795325112867385, 1.000000000000000000, 0.9238795325112867385, 1.000000000000000000, 0.9238795325112867385, 1.000000000000000000, 0.9238795325112867385, 1.000000000000000000, 0.9238795325112867385, 1.000000000000000000, 0.9238795325112867385, 1.000000000000000000, 0.9238795325112867385, 1.000000000000000000, 0.9238795325112867385, 1.000000000000000000, 0.9238795325112867385, 1.000000000000000000, 0.9238795325112867385, 1.000000000000000000, 0.9238795325112867385, 1.000000000000000000, 0.9238795325112867385, 1.000000000000000000, 0.9238795325112867385, 1.000000000000000000, 0.9238795325112867385, 1.000000000000000000, 0.9238795325112867385, 1.000000000000000000, 0.9238795325112867385, 1.000000000000000000, 0.9238795325112867385, 1.000000000000000000, 0.9238795325112867385, 1.000000000000000000, 0.9238795325112867385, 1.000000000000000000, 0.9238795325112867385, 1.000000000000000000, 0.9238795325112867385, 1.000000000000000000, 0.9238795325112867385, 1.000000000000000000, 0.9238795325112867385, 1.000000000000000000, 0.9238795325112867385, 1.000000000000000000, 0.9238795325112867385, 1.000000000000000000, 0.9238795325112867385, 1.000000000000000000, 0.9238795325112867385, 1.000000000000000000, 0.9238795325112867385, 1.000000000000000000, 0.9238795325112867385, 1.000000000000000000, 0.9238795325112867385, 1.000000000000000000, 0.9238795325112867385, 1.000000000000000000, 0.9238795325112867385, 1.000000000000000000, 0.9238795325112867385, 1.000000000000000000, 0.9238795325112867385, 1.000000000000000000, 0.9238795325112867385, 1.000000000000000000, 0.9238795325112867385, 1.000000000000000000, 0.9238795325112867385, 1.000000000000000000, 0.9238795325112867385, 1.000000000000000000, 0.9238795325112867385, 1.000000000000000000, 0.9238795325112867385, 1.000000000000000000, 0.9238795325112867385, 1.000000000000000000, 0.9238795325112867385, 1.000000000000000000, 0.9238795325112867385, 1.000000000000000000, 0.9238795325112867385, 1.000000000000000000, 0.9238795325112867385, 1.000000000000000000, 0.9238795325112867385, 1.000000000000000000, 0.9238795325112867385, 1.000000000000000000, 0.9238795325112867385, 1.000000000000000000, 0.9238795325112867385, 1.000000000000000000, 0.9238795325112867385, 1.000000000000000000, 0.9238795325112867385, 1.000000000000000000, 0.9238795325112867385, 1.000000000000000000, 0.9238795325112867385, 1.000000000000000000, 0.9238795325112867385, 1.000000000000000000, 0.9238795325112867385, 1.000000000000000000, 0.9238795325112867385, 1.000000000000000000, 0.9238795325112867385, 1.000000000000000000, 0.9238795325112867385, 1.000000000000000000, 0.9238795325112867385, 1.000000000000000000, 0.9238795325112867385, 1.000000000000000000, 0.9238795325112867385, 1.000000000000000000, 0.9238795325112867385, 1.000000000000000000, 0.9238795325112867385, 1.000000000000000000, 0.9238795325112867385, 1.000000000000000000, 0.9238795325112867385, 1.000000000000000000, 0.9238795325112867385, 1.000000000000000000, 0.9238795325112867385, 1.000000000000000000, 0.9238795325112867385, 1.000000000000000000, 0.9238795325112867385, 1.000000000000000000, 0.9238795325112867385, 1.000000000000000000, 0.9238795325112867385, 1.000000000000000000, 0.9238795325112867385, 1.000000000000000000, 0.9238795325112867385, 1.000000000000000000, 0.9238795325112867385, 1.000000000000000000, 0.9238795325112867385, 1.000000000000000000, 0.9238795325112867385, 1.000000000000000000, 0.9238795325112867385, 1.000000000000000000, 0.9238795325112867385, 1.000000000000000000, 0.9238795325112867385, 1.000000000000000000, 0.9238795325112867385, 1.000000000000000000, 0.9238795325112867385, 1.000000000000000000, 0.9238795325112867385, 1.000000000000000000, 0.9238795325112867385, 1.000000000000000000, 0.9238795325112867385, 1.000000000000000000, 0.9238795325112867385, 1.000000000000000000, 0.9238795325112867385, 1.000000000000000000, 0.9238795325112867385, 1.000000000000000000, 0.9238795325112867385, 1.000000000000000000, 0.9238795325112867385, 1.000000000000000000, 0.9238795325112867385, 1.000000000000000000, 0.9238795325112867385, 1.000000000000000000, 0.9238795325112867385, 1.000000000000000000, 0.9238795325112867385, 1.000000000000000000, 0.9238795325112867385, 1.000000000000000000, 0.9238795325112867385, 1.000000000000000000, 0.9238795325112867385, 1.000000000000000000, 0.9238795325112867385, 1.000000000000000000, 0.9238795325112867385, 1.000000000000000000, 0.9238795325112867385, 1.000000000000000000, 0.9238795325112867385, 1.000000000000000000, 0.9238795325112867385, 1.000000000000000000, 0.9238795325112867385, 1.000000000000000000, 0.9238795325112867385, 1.000000000000000000, 0.9238795325112867385, 1.000000000000000000, 0.9238795325112867385, 1.000000000000000000, 0.9238795325112867385, 1.000000000000000000, 0.9238795325112867385, 1.000000000000000000, 0.9238795325112867385, 1.000000000000000000, 0.9238795325112867385, 1.000000000000000000, 0.9238795325112867385, 1.000000000000000000, 0.9238795325112867385, 1.000000000000000000, 0.9238795325112867385, 1.000000000000000000, 0.9238795325112867385, 1.000000000000000000, 0.9238795325112867385, 1.000000000000000000, 0.9238795325112867385, 1.000000000000000000, 0.9238795325112867385, 1.000000000000000000, 0.9238795325112867385, 1.000000000000000000, 0.9238795325112867385, 1.000000000000000000, 0.9238795325112867385, 1.000000000000000000, 0.9238795325112867385, 1.000000000000000000, 0.9238795325112867385, 1.000000000000000000, 0.9238795325112867385, 1.000000000000000000, 0.9238795325112867385, 1.000000000000000000, 0.9238795325112867385, 1.000000000000000000, 0.9238795325112867385, 1.000000000000000000, 0.9238795325112867385, 1.000000000000000000, 0.9238795325112867385, 1.000000000000000000, 0.9238795325112867385, 1.000000000000000000, 0.9238795325112867385, 1.000000000000000000, 0.9238795325112867385, 1.000000000000000000, 0.9238795325112867385, 1.000000000000000000, 0.9238795325112867385, 1.000000000000000000, 0.9238795325112867385, 1.000000000000000000, 0.9238795325112867385, 1.000000000000000000, 0.9238795325112867385, 1.000000000000000000, 0.9238795325112867385, 1.000000000000000000, 0.9238795325112867385, 1.000000000000000000, 0.9238795325112867385, 1.000000000000000000, 0.9238795325112867385, 1.000000000000000000, 0.9238795325112867385, 1.000000000000000000, 0.9238795325112867385, 1.000000000000000000, 0.9238795325112867385, 1.000000000000000000, 0.9238795325112867385, 1.000000000000000000, 0.9238795325112867385, 1.000000000000000000, 0.9238795325112867385, 1.000000000000000000, 0.9238795325112867385, 1.000000000000000000, 0.9238795325112867385, 1.000000000000000000, 0.9238795325112867385, 1.000000000000000000, 0.9238795325112867385, 1.000000000000000000, 0.9238795325112867385, 1.000000000000000000, 0.9238795325112867385, 1.000000000000000000, 0.9238795325112867385, 1.000000000000000000, 0.9238795325112867385, 1.000000000000000000, 0.9238795325112867385, 1.000000000000000000, 0.9238795325112867385, 1.000000000000000000, 0.9238795325112867385, 1.000000000000000000, 0.9238795325112867385, 1.000000000000000000, 0.9238795325112867385, 1.000000000000000000, 0.9238795325112867385, 1.000000000000000000, 0.9238795325112867385, 1.000000000000000000, 0.9238795325112867385, 1.000000000000000000, 0.9238795325112867385, 1.000000000000000000, 0.9238795325112867385, 1.000000000000000000, 0.9238795325112867385, 1.000000000000000000, 0.9238795325112867385, 1.000000000000000000, 0.9238795325112867385, 1.000000000000000000, 0.9238795325112867385, 1.000000000000000000, 0.9238795325112867385, 1.000000000000000000, 0.9238795325112867385, 1.000000000000000000, 0.9238795325112867385, 1.000000000000000000, 0.9238795325112867385, 1.000000000000000000, 0.9238795325112867385, 1.000000000000000000, 0.9238795325112867385, 1.000000000000000000, 0.9238795325112867385, 1.000000000000000000, 0.9238795325112867385, 1.000000000000000000, 0.9238795325112867385, 1.000000000000000000, 0.9238795325112867385, 1.000000000000000000, 0.9238795325112867385, 1.000000000000000000, 0.9238795325112867385, 1.000000000000000000, 0.9238795325112867385, 1.000000000000000000, 0.9238795325112867385, 1.000000000000000000, 0.9238795325112867385, 1.000000000000000000, 0.9238795325112867385, 1.000000000000000000, 0.9238795325112867385, 1.000000000000000000, 0.9238795325112867385, 1.000000000000000000, 0.9331728261800869006, 0.9836825870399050764 ) ) 
 REPRESENTATION_ITEM ( '' )  );
#3076=CARTESIAN_POINT ( 'NONE',  ( 0.07168957172816003975, 0.03242967361111057795, 0.2730421076994219431 ) ) ;
#3077=( BOUNDED_CURVE ( )  B_SPLINE_CURVE ( 2, ( #23861, #8755, #7422, #12562, #5344, #5583, #20345, #14376, #12808 ),
 .UNSPECIFIED., .F., .T. ) 
 B_SPLINE_CURVE_WITH_KNOTS ( ( 3, 2, 2, 2, 3 ),
 ( 0.8660714285714284921, 0.8705357142857141906, 0.8750000000000000000, 0.8794642857142856984, 0.8839285714285713969 ),
 .UNSPECIFIED. ) 
 CURVE ( )  GEOMETRIC_REPRESENTATION_ITEM ( )  RATIONAL_B_SPLINE_CURVE ( ( 1.000000000000001998, 0.9238795325112848511, 1.000000000000000000, 0.9238795325112867385, 1.000000000000000000, 0.9238795325112867385, 1.000000000000000000, 0.9238795325112867385, 1.000000000000000000 ) ) 
 REPRESENTATION_ITEM ( '' )  );
#3079=CARTESIAN_POINT ( 'NONE',  ( 0.1167790944451424506, 4.925777777853642903, 0.2819296736111110424 ) ) ;
#3082=CARTESIAN_POINT ( 'NONE',  ( -0.08027973808803456901, 5.102470732942563814, -0.3007383443984451565 ) ) ;
#3083=CARTESIAN_POINT ( 'NONE',  ( -0.3119999999999999996, 0.2055555554038226151, -3.820898013339742174E-17 ) ) ;
#3084=B_SPLINE_CURVE_WITH_KNOTS ( 'NONE', 3,
 ( #23763, #19521, #8908, #16233, #988, #6595, #6838, #1234, #14403, #4999, #14523, #5117, #21946, #5238, #4882, #2815, #8417, #8659 ),
 .UNSPECIFIED., .F., .F.,
 ( 4, 2, 2, 2, 2, 2, 2, 2, 4 ),
 ( 0.9046139031640043626, 0.9068982821206797995, 0.9091826610773552364, 0.9114670400340306733, 0.9137514189907061102, 0.9160357979473815471, 0.9183201769040569840, 0.9206045558607324208, 0.9228889348174078577 ),
 .UNSPECIFIED. ) ;
#3086=CARTESIAN_POINT ( 'NONE',  ( -0.2819296736111110979, 0.1916666665908000333, 0.1167790944451422425 ) ) ;
#3087=CARTESIAN_POINT ( 'NONE',  ( 0.2819296736111110979, 0.04930555547968892144, 0.000000000000000000 ) ) ;
#3088=CARTESIAN_POINT ( 'NONE',  ( 0.000000000000000000, 5.384999999999999787, 0.000000000000000000 ) ) ;
#3089=CARTESIAN_POINT ( 'NONE',  ( 7.515426412127797749E-07, 4.849418923572540230, 0.3119999999980542227 ) ) ;
#3091=CARTESIAN_POINT ( 'NONE',  ( -0.2882663752280904546, 5.054250704846746878, -0.1193744778696609748 ) ) ;
#3094=CARTESIAN_POINT ( 'NONE',  ( -0.1167790944451423535, 4.821611111186976828, 0.2819296736111110424 ) ) ;
#3096=CARTESIAN_POINT ( 'NONE',  ( -0.2819296736111110424, 3.800777777853643347, 0.1167790944451424923 ) ) ;
#3097=CARTESIAN_POINT ( 'NONE',  ( -0.3120000000000000551, 0.09791666651493373397, 0.1292346314604056190 ) ) ;
#3100=CARTESIAN_POINT ( 'NONE',  ( 0.1292346314604056190, 4.318138889040620931, -0.3119999999999999996 ) ) ;
#3101=CARTESIAN_POINT ( 'NONE',  ( -0.1167790944451423535, 4.710500000075865223, 0.2819296736111110979 ) ) ;
#3103=CARTESIAN_POINT ( 'NONE',  ( 0.1167790944451424368, 3.759111111186976828, 0.2819296736111110424 ) ) ;
#3111=CARTESIAN_POINT ( 'NONE',  ( -0.3119999999999999996, 0.3756944442927114824, 0.1292346314604056190 ) ) ;
#3113=CARTESIAN_POINT ( 'NONE',  ( -0.08648628660923504685, 4.379571832817274135, -0.3004572054626405420 ) ) ;
#3116=ORIENTED_EDGE ( 'NONE', *, *, #670, .T. ) ;
#3120=CARTESIAN_POINT ( 'NONE',  ( 0.2819296736111110424, 4.384111111186976828, -0.1167790944451423396 ) ) ;
#3124=CARTESIAN_POINT ( 'NONE',  ( -0.04077505786994410630, 4.211656132442665346, -0.3119997438092615427 ) ) ;
#3125=CARTESIAN_POINT ( 'NONE',  ( 0.3119999999999999996, 4.026472222222221120, -0.1292346314604056745 ) ) ;
#3126=CARTESIAN_POINT ( 'NONE',  ( 0.1292346314604058410, 5.075083333485064685, 0.3119999999999998885 ) ) ;
#3129=CARTESIAN_POINT ( 'NONE',  ( 1.059513921322799533E-10, 3.821611107313654720, -0.3119999999999999996 ) ) ;
#3130=ORIENTED_EDGE ( 'NONE', *, *, #5798, .T. ) ;
#3139=CARTESIAN_POINT ( 'NONE',  ( -0.1167790944451424506, 0.1430555554796889284, 0.2819296736111110424 ) ) ;
#3146=CARTESIAN_POINT ( 'NONE',  ( -0.3119999999999999996, 0.5458333333333329485, -3.820898013339742174E-17 ) ) ;
#3147=CARTESIAN_POINT ( 'NONE',  ( 0.3119999999999999996, 4.686194444444444329, 0.1292346314604056190 ) ) ;
#3149=CARTESIAN_POINT ( 'NONE',  ( -0.2819296736111110979, 4.293833333409199149, -0.1167790944451422980 ) ) ;
#3152=CARTESIAN_POINT ( 'NONE',  ( 0.2206173157302028232, 0.5180555554038226429, -0.2206173157302028232 ) ) ;
#3154=CARTESIAN_POINT ( 'NONE',  ( 5.178964085587577574E-17, 4.588972222298087544, 0.2819296736111110979 ) ) ;
#3155=CARTESIAN_POINT ( 'NONE',  ( -0.2344453928311062418, 4.508576492912489186, 0.2058803838101449790 ) ) ;
#3160=CARTESIAN_POINT ( 'NONE',  ( -0.1993543840281266910, 4.137583333409199149, -0.1993543840281266910 ) ) ;
#3161=CARTESIAN_POINT ( 'NONE',  ( -0.001245755308147351035, 4.821647350372675334, -0.3119976684412342216 ) ) ;
#3165=CARTESIAN_POINT ( 'NONE',  ( 1.726321361862525858E-17, 0.04930555547968892144, -0.2819296736111110979 ) ) ;
#3176=CARTESIAN_POINT ( 'NONE',  ( 0.2819296736111110424, 0.4763888888130222710, 0.1167790944451424923 ) ) ;
#3177=CARTESIAN_POINT ( 'NONE',  ( -0.1993543840281266355, 3.929250000075865668, 0.1993543840281267465 ) ) ;
#3180=CARTESIAN_POINT ( 'NONE',  ( -0.1167790944451423257, 4.356333333409199149, -0.2819296736111110424 ) ) ;
#3181=CARTESIAN_POINT ( 'NONE',  ( 0.2661418463900624420, 5.135117573705075600, -0.1518351709947930450 ) ) ;
#3183=VERTEX_POINT ( 'NONE', #12860 ) ;
#3184=CARTESIAN_POINT ( 'NONE',  ( 5.731347020009612645E-17, 4.009111111111109516, 0.3119999999999999996 ) ) ;
#3185=CARTESIAN_POINT ( 'NONE',  ( -0.2819296736111110424, 5.182722222298088433, -0.1167790944451423119 ) ) ;
#3186=CARTESIAN_POINT ( 'NONE',  ( 0.2476760547999725393, 4.190764322939071640, 0.1908289239165902873 ) ) ;
#3187=DIRECTION ( 'NONE',  ( -0.000000000000000000, -1.000000000000000000, -0.000000000000000000 ) ) ;
#3188=CARTESIAN_POINT ( 'NONE',  ( -1.726321361862525858E-17, 4.894527777853642903, -0.2819296736111110979 ) ) ;
#3191=CARTESIAN_POINT ( 'NONE',  ( -0.1292346314604058410, 0.3270833331816004330, 0.3119999999999998885 ) ) ;
#3193=CARTESIAN_POINT ( 'NONE',  ( -0.3009857094490465679, 4.555141368925776924, -0.09131701761149857433 ) ) ;
#3194=ORIENTED_EDGE ( 'NONE', *, *, #2449, .F. ) ;
#3195=CARTESIAN_POINT ( 'NONE',  ( 0.2819296736111110979, 0.2715277777019111660, 0.000000000000000000 ) ) ;
#3196=ADVANCED_FACE ( 'NONE', ( #1622 ), #18625, .T. ) ;
#3197=ORIENTED_EDGE ( 'NONE', *, *, #19594, .T. ) ;
#3198=CARTESIAN_POINT ( 'NONE',  ( -0.2819296736111110424, 0.01805555547968892838, -0.1167790944451423396 ) ) ;
#3202=CARTESIAN_POINT ( 'NONE',  ( -0.2299564775410312401, 5.051042695534824212, -0.2131007688933645450 ) ) ;
#3206=CARTESIAN_POINT ( 'NONE',  ( -0.2819296736111110979, 4.477861111186976828, 0.000000000000000000 ) ) ;
#3207=CARTESIAN_POINT ( 'NONE',  ( -0.3119999999999999996, 0.2611111109593781676, -3.820898013339742174E-17 ) ) ;
#3209=CARTESIAN_POINT ( 'NONE',  ( 0.2819296736111110979, 5.227861111186977716, -3.452642723725051716E-17 ) ) ;
#3210=CARTESIAN_POINT ( 'NONE',  ( -0.01965242898639488894, 0.04348884421539742084, -0.2924957164008217814 ) ) ;
#3211=CARTESIAN_POINT ( 'NONE',  ( 0.3007072963801942223, 3.754733255434872241, -0.08834097405045530926 ) ) ;
#3212=LINE ( 'NONE', #8945, #20293 ) ;
#3213=CARTESIAN_POINT ( 'NONE',  ( -0.06344583501299609629, 4.792058108258712146, 0.3056432983527924696 ) ) ;
#3214=CARTESIAN_POINT ( 'NONE',  ( 0.2206173157302028787, 4.300777777929509327, 0.2206173157302027954 ) ) ;
#3215=CARTESIAN_POINT ( 'NONE',  ( -0.2819296736111110424, 4.648000000075866112, 0.1167790944451424923 ) ) ;
#3217=CARTESIAN_POINT ( 'NONE',  ( 0.2819296736111110979, 3.877166666742531742, 0.1167790944451422425 ) ) ;
#3218=ORIENTED_EDGE ( 'NONE', *, *, #967, .F. ) ;
#3226=CARTESIAN_POINT ( 'NONE',  ( -0.2206173157302028787, 0.2124999998482670627, 0.2206173157302027954 ) ) ;
#3227=CARTESIAN_POINT ( 'NONE',  ( -0.009913296964756498908, 4.377433935782568675, -0.3118490548042810451 ) ) ;
#3231=CYLINDRICAL_SURFACE ( 'NONE', #4887, 0.3119999999999999996 ) ;
#3232=CARTESIAN_POINT ( 'NONE',  ( -0.2819296736111110979, 0.2298611110352444808, -3.452642723725051716E-17 ) ) ;
#3238=CARTESIAN_POINT ( 'NONE',  ( -0.1167790944451423257, 4.342444444520310753, -0.2819296736111110424 ) ) ;
#3239=CARTESIAN_POINT ( 'NONE',  ( 0.2206173157302028232, 0.1916666666666663466, -0.2206173157302028232 ) ) ;
#3241=CARTESIAN_POINT ( 'NONE',  ( -0.08757809820678906509, 4.235785868357317518, 0.3004240109509383472 ) ) ;
#3242=CARTESIAN_POINT ( 'NONE',  ( 0.3119999999999999996, 4.082027777777776478, -0.1292346314604056745 ) ) ;
#3243=CARTESIAN_POINT ( 'NONE',  ( 0.2206173157302028787, 4.856333333485065573, 0.2206173157302027954 ) ) ;
#3247=CARTESIAN_POINT ( 'NONE',  ( -0.1426465030096581710, 4.881379615490812007, -0.2780736469684209622 ) ) ;
#3253=CARTESIAN_POINT ( 'NONE',  ( -0.1167790944451424506, 0.1986111110352444808, 0.2819296736111110424 ) ) ;
#3255=CARTESIAN_POINT ( 'NONE',  ( 0.1167790944451422702, 5.127166666742532186, -0.2819296736111110424 ) ) ;
#3256=CARTESIAN_POINT ( 'NONE',  ( 0.2295400061202557962, 4.481090041848301730, -0.2126894043619363961 ) ) ;
#3257=ORIENTED_EDGE ( 'NONE', *, *, #21842, .F. ) ;
#3260=CARTESIAN_POINT ( 'NONE',  ( -0.01726427071093490639, 4.293343159678996379, 0.3115899811169826616 ) ) ;
#3262=CARTESIAN_POINT ( 'NONE',  ( 0.2206173157302028232, 0.5805555555555552694, -0.2206173157302028232 ) ) ;
#3263=CARTESIAN_POINT ( 'NONE',  ( -0.1292346314604056745, 4.707027777777777366, -0.3119999999999999996 ) ) ;
#3264=CARTESIAN_POINT ( 'NONE',  ( -0.1167790944451423119, 3.898000000075865223, -0.2819296736111110979 ) ) ;
#3266=CARTESIAN_POINT ( 'NONE',  ( 0.1993543840281266633, 3.845916666742533074, -0.1993543840281266910 ) ) ;
#3268=CARTESIAN_POINT ( 'NONE',  ( -5.731347020009612645E-17, 0.4972222220704892726, 0.3119999999999999996 ) ) ;
#3269=EDGE_LOOP ( 'NONE', ( #6569, #418, #1170, #13342 ) ) ;
#3271=CARTESIAN_POINT ( 'NONE',  ( -0.1993543840281266910, 4.568138888964754507, -0.1993543840281266910 ) ) ;
#3272=CARTESIAN_POINT ( 'NONE',  ( -0.02174346296206112333, 4.488903266706190109, -0.3112889508319767740 ) ) ;
#3274=DIRECTION ( 'NONE',  ( 0.000000000000000000, 0.000000000000000000, -1.000000000000000000 ) ) ;
#3276=B_SPLINE_CURVE_WITH_KNOTS ( 'NONE', 3,
 ( #9465, #5441, #10941, #1903, #9227, #3606, #7277, #13025, #11182, #18730, #16898, #18369, #16664, #20440, #14960, #24087, #5683, #22380, #2026, #11059, #9346, #18489, #22022, #7397, #14849, #16787 ),
 .UNSPECIFIED., .F., .F.,
 ( 4, 2, 2, 2, 2, 2, 2, 2, 2, 2, 2, 2, 4 ),
 ( 0.02660920303947646864, 0.02748246392853086195, 0.02835572481758525526, 0.03010224659569404188, 0.03097550748474843518, 0.03184876837380282849, 0.03272202926285722180, 0.03359529015191161511, 0.03534181193002039478, 0.03708833370812918140, 0.03796159459718358165, 0.03883485548623796801, 0.04058137726434675463 ),
 .UNSPECIFIED. ) ;
#3277=CARTESIAN_POINT ( 'NONE',  ( 0.1167790944451422702, 4.071611111186977716, -0.2819296736111110979 ) ) ;
#3280=CARTESIAN_POINT ( 'NONE',  ( 0.01995244822899069209, 5.161835221482045988, -0.2985861170655538799 ) ) ;
#3283=CARTESIAN_POINT ( 'NONE',  ( 0.2819296736111110979, 0.03541666659080003332, 0.000000000000000000 ) ) ;
#3291=FACE_OUTER_BOUND ( 'NONE', #3269, .T. ) ;
#3292=CARTESIAN_POINT ( 'NONE',  ( 7.459700445346810805E-07, 4.043833313442511290, -0.3119999999991081574 ) ) ;
#3293=CARTESIAN_POINT ( 'NONE',  ( -0.3119999999999999996, -0.006250000000000336016, 0.1292346314604056190 ) ) ;
#3294=CARTESIAN_POINT ( 'NONE',  ( -0.1993543840281266910, 3.859805555631421470, -0.1993543840281266910 ) ) ;
#3296=CARTESIAN_POINT ( 'NONE',  ( 0.1993543840281266633, 4.457027777853643791, -0.1993543840281266910 ) ) ;
#3301=CARTESIAN_POINT ( 'NONE',  ( 0.1915320766489893856, 4.355118862228665400, 0.2496463631673534467 ) ) ;
#3302=CARTESIAN_POINT ( 'NONE',  ( -0.1167790944451423257, 5.175777777853644679, -0.2819296736111110424 ) ) ;
#3303=CARTESIAN_POINT ( 'NONE',  ( 0.2335926053540489100, 4.203040725598064853, -0.2068301295312730270 ) ) ;
#3305=EDGE_CURVE ( 'NONE', #7226, #12971, #6944, .T. ) ;
#3307=CARTESIAN_POINT ( 'NONE',  ( -0.1993543840281266355, 4.804250000075865223, 0.1993543840281267465 ) ) ;
#3311=CARTESIAN_POINT ( 'NONE',  ( -0.3120000000000000551, 0.3201388887371559577, 0.1292346314604056190 ) ) ;
#3314=CARTESIAN_POINT ( 'NONE',  ( 0.2819296736111110424, 0.2194444443685777957, -0.1167790944451423119 ) ) ;
#3315=CARTESIAN_POINT ( 'NONE',  ( 0.2819296736111110424, -0.002777777853644409004, -0.1167790944451423119 ) ) ;
#3316=CARTESIAN_POINT ( 'NONE',  ( 0.000000000000000000, 5.384999999999999787, 0.000000000000000000 ) ) ;
#3320=CARTESIAN_POINT ( 'NONE',  ( 5.731347020009612645E-17, 4.509111111111110404, 0.3119999999999999996 ) ) ;
#3321=CARTESIAN_POINT ( 'NONE',  ( 5.731347020009612645E-17, 4.175777777777776478, 0.3119999999999999996 ) ) ;
#3322=CARTESIAN_POINT ( 'NONE',  ( -0.02020282852508829483, 3.877718746106461278, -0.3119025878752364478 ) ) ;
#3324=CARTESIAN_POINT ( 'NONE',  ( 0.1993543840281266633, 4.401472222298088433, -0.1993543840281266910 ) ) ;
#3327=CARTESIAN_POINT ( 'NONE',  ( -0.2819296736111110979, 5.033416666742532186, 0.000000000000000000 ) ) ;
#3328=CARTESIAN_POINT ( 'NONE',  ( -0.3011022955695156211, 0.05170836598878657958, -0.01273678397337616591 ) ) ;
#3329=CARTESIAN_POINT ( 'NONE',  ( 2.570936052289255124E-07, 3.738287934957344127, 0.3119999999997750129 ) ) ;
#3331=CARTESIAN_POINT ( 'NONE',  ( 0.06877731076760502937, 0.04436119539538452977, 0.2860349230690588107 ) ) ;
#3333=CARTESIAN_POINT ( 'NONE',  ( -1.910449006669871087E-17, 4.377166666818398610, -0.3119999999999999996 ) ) ;
#3334=CARTESIAN_POINT ( 'NONE',  ( -0.1167790944451423535, 4.488277777853643791, 0.2819296736111110979 ) ) ;
#3335=B_SPLINE_CURVE_WITH_KNOTS ( 'NONE', 3,
 ( #15236, #11585, #17184, #13768, #21075, #591, #8260, #22665, #22547, #21194, #15592, #20957, #13301 ),
 .UNSPECIFIED., .F., .F.,
 ( 4, 2, 2, 2, 1, 2, 4 ),
 ( 0.000000000000000000, 0.001498478264507173679, 0.002996956529014346490, 0.003746195661267932679, 0.004495434793521518868, 0.005244673925775105057, 0.005993913058028690378 ),
 .UNSPECIFIED. ) ;
#3336=CARTESIAN_POINT ( 'NONE',  ( -0.1993543840281266910, 3.901472222298087544, -0.1993543840281266910 ) ) ;
#3340=VERTEX_POINT ( 'NONE', #5207 ) ;
#3343=EDGE_CURVE ( 'NONE', #11560, #8700, #7354, .T. ) ;
#3344=CARTESIAN_POINT ( 'NONE',  ( -0.2727962046151662934, 4.942087318129531504, -0.1568363485577166649 ) ) ;
#3345=CARTESIAN_POINT ( 'NONE',  ( 1.910449006669871087E-17, 0.3652777777777774237, -0.3119999999999999996 ) ) ;
#3347=ORIENTED_EDGE ( 'NONE', *, *, #18731, .F. ) ;
#3348=CARTESIAN_POINT ( 'NONE',  ( 0.3119999999999999996, 0.3444444442927114824, 0.000000000000000000 ) ) ;
#3349=CARTESIAN_POINT ( 'NONE',  ( -0.2263603714153657742, 4.384333806754304064, -0.2147221485470059144 ) ) ;
#3350=CARTESIAN_POINT ( 'NONE',  ( -0.2115755794123815592, 5.122769419632757781, 0.2240629809752085200 ) ) ;
#3351=CARTESIAN_POINT ( 'NONE',  ( -0.1292346314604058410, 0.2784722222222218435, 0.3119999999999998885 ) ) ;
#3355=CARTESIAN_POINT ( 'NONE',  ( 0.3080438441126990279, 5.084176856567461655, 0.05194822647866765425 ) ) ;
#3358=CARTESIAN_POINT ( 'NONE',  ( 0.2819296736111110424, 4.217444444520310753, -0.1167790944451423396 ) ) ;
#3359=CARTESIAN_POINT ( 'NONE',  ( -0.1167790944451423535, 5.085500000075866112, 0.2819296736111110979 ) ) ;
#3362=CARTESIAN_POINT ( 'NONE',  ( -0.2612101927628759923, 4.229576235931883588, 0.1754577556920814685 ) ) ;
#3363=CARTESIAN_POINT ( 'NONE',  ( 5.731347020009612645E-17, 4.120222222222221120, 0.3119999999999999996 ) ) ;
#3364=CARTESIAN_POINT ( 'NONE',  ( 0.2206173157302028787, 4.967444444596176290, 0.2206173157302027954 ) ) ;
#3365=CARTESIAN_POINT ( 'NONE',  ( 0.2943229328651665866, 4.810734450191622713, -0.1059385550757641070 ) ) ;
#3368=ADVANCED_FACE ( 'NONE', ( #3990 ), #17166, .T. ) ;
#3371=CARTESIAN_POINT ( 'NONE',  ( -0.3039836006089354226, 4.888818180532651603, -0.08126209352896139604 ) ) ;
#3377=CARTESIAN_POINT ( 'NONE',  ( 0.2819296736111110979, 0.2749999999241334314, -0.1167790944451422980 ) ) ;
#3379=CARTESIAN_POINT ( 'NONE',  ( 0.1167790944451422702, 5.182722222298088433, -0.2819296736111110424 ) ) ;
#3380=DIRECTION ( 'NONE',  ( -0.000000000000000000, -1.000000000000000000, -0.000000000000000000 ) ) ;
#3381=VERTEX_POINT ( 'NONE', #13165 ) ;
#3382=CARTESIAN_POINT ( 'NONE',  ( -0.0001469343572505705023, 3.766059503595236446, -0.3119999755966755828 ) ) ;
#3383=CARTESIAN_POINT ( 'NONE',  ( 0.1292346314604031765, 3.866750000000000131, -0.3120000000000024420 ) ) ;
#3384=CARTESIAN_POINT ( 'NONE',  ( 0.1128137788402567426, 4.873987063709920520, -0.2914807742742103192 ) ) ;
#3385=CARTESIAN_POINT ( 'NONE',  ( 5.731347020009612645E-17, 4.564666666666665762, 0.3119999999999999996 ) ) ;
#3387=CARTESIAN_POINT ( 'NONE',  ( -0.2206173157302027676, 4.835499999999999687, 0.2206173157302028787 ) ) ;
#3389=CARTESIAN_POINT ( 'NONE',  ( 0.1993543840281267465, 4.095916666742532186, 0.1993543840281266633 ) ) ;
#3390=CARTESIAN_POINT ( 'NONE',  ( -1.726321361862525858E-17, 3.797305555631421470, -0.2819296736111110979 ) ) ;
#3391=CARTESIAN_POINT ( 'NONE',  ( 0.2100805295423999741, 4.037387642597302317, -0.2317816973857660945 ) ) ;
#3393=B_SPLINE_CURVE_WITH_KNOTS ( 'NONE', 3,
 ( #15864, #1559, #987, #8416, #17818, #23048, #2700, #23280, #6594, #22935, #2587, #14042, #12228, #8176, #1108, #10835, #5202, #8542, #10152, #21237, #15984, #6356, #23405, #11990, #866, #6713, #14158, #3382, #18263, #6231 ),
 .UNSPECIFIED., .F., .F.,
 ( 4, 2, 2, 2, 2, 2, 2, 2, 2, 2, 1, 1, 1, 1, 1, 1, 2, 4 ),
 ( 0.9411639604301500484, 0.9434483960034079075, 0.9457328315766656557, 0.9480172671499235149, 0.9503017027231813740, 0.9525861382964391222, 0.9548705738696969814, 0.9571550094429547295, 0.9582972272295836591, 0.9588683361228981239, 0.9591538905695553563, 0.9592966677928840280, 0.9593680564045482528, 0.9594037507103804208, 0.9594215978632965047, 0.9594305214397546022, 0.9594349832279835955, 0.9594394450162125887 ),
 .UNSPECIFIED. ) ;
#3397=CARTESIAN_POINT ( 'NONE',  ( -0.1167790944451423257, 4.509111111186976828, -0.2819296736111110424 ) ) ;
#3398=CARTESIAN_POINT ( 'NONE',  ( 0.2206173157302028787, 3.793833333333332725, 0.2206173157302027954 ) ) ;
#3403=CARTESIAN_POINT ( 'NONE',  ( 0.1993543840281266633, 3.790361111186977272, -0.1993543840281266910 ) ) ;
#3404=CARTESIAN_POINT ( 'NONE',  ( -8.183246661411124563E-08, 3.960496777434589610, 0.3119999999999772400 ) ) ;
#3405=CARTESIAN_POINT ( 'NONE',  ( 0.1347543868356496644, 5.157564342225265719, -0.2691372244021535964 ) ) ;
#3408=CARTESIAN_POINT ( 'NONE',  ( 0.2819296736111110424, 0.3652777777019111105, 0.1167790944451424923 ) ) ;
#3410=LINE ( 'NONE', #5482, #13147 ) ;
#3418=CARTESIAN_POINT ( 'NONE',  ( -5.731347020009612645E-17, 0.05972222222222188515, 0.3119999999999999996 ) ) ;
#3419=CARTESIAN_POINT ( 'NONE',  ( -0.2819296736111110424, 3.807722222298089321, -0.1167790944451423119 ) ) ;
#3421=CARTESIAN_POINT ( 'NONE',  ( -0.2819296736111110424, 4.481333333409199149, 0.1167790944451424923 ) ) ;
#3423=CARTESIAN_POINT ( 'NONE',  ( -0.2206173157302028232, 4.377166666666665762, -0.2206173157302028232 ) ) ;
#3426=CARTESIAN_POINT ( 'NONE',  ( 0.3120000000000000551, 4.686194444444444329, 0.1292346314604056190 ) ) ;
#3427=CARTESIAN_POINT ( 'NONE',  ( 0.1167790944451422702, 5.113277777853642903, -0.2819296736111110424 ) ) ;
#3428=CARTESIAN_POINT ( 'NONE',  ( 0.2354754176334847293, 4.202962126866166770, -0.2046859565788392565 ) ) ;
#3430=CARTESIAN_POINT ( 'NONE',  ( 0.2819296736111111534, 4.654944444520309865, 0.1167790944451422563 ) ) ;
#3432=CARTESIAN_POINT ( 'NONE',  ( -0.1196036944483439418, 4.068140768160333209, 0.2893420950190842000 ) ) ;
#3434=ORIENTED_EDGE ( 'NONE', *, *, #20904, .F. ) ;
#3435=CARTESIAN_POINT ( 'NONE',  ( -0.1167790944451424368, 0.3097222221463555303, 0.2819296736111110424 ) ) ;
#3438=CARTESIAN_POINT ( 'NONE',  ( -0.2819296736111110424, 0.2402777777019111938, -0.1167790944451423396 ) ) ;
#3439=CYLINDRICAL_SURFACE ( 'NONE', #13509, 0.3119999999999999996 ) ;
#3440=CARTESIAN_POINT ( 'NONE',  ( -0.2258351564880545503, 5.196761101924514570, -0.1766745448178271560 ) ) ;
#3444=ADVANCED_FACE ( 'NONE', ( #22525 ), #7772, .T. ) ;
#3445=CARTESIAN_POINT ( 'NONE',  ( 0.2819296736111110979, 0.09097222214635558579, 0.000000000000000000 ) ) ;
#3446=CARTESIAN_POINT ( 'NONE',  ( 5.178964085587577574E-17, 4.491750000075866112, 0.2819296736111110979 ) ) ;
#3448=CARTESIAN_POINT ( 'NONE',  ( 0.03357672467717862097, 4.542878599828895858, -0.3103008995289400218 ) ) ;
#3449=CARTESIAN_POINT ( 'NONE',  ( 0.1993543840281266633, 5.068138888964754507, -0.1993543840281266910 ) ) ;
#3451=CARTESIAN_POINT ( 'NONE',  ( 0.2062776401250031866, 3.759720860179437629, -0.2349803605453861244 ) ) ;
#3455=CARTESIAN_POINT ( 'NONE',  ( 0.1292346314604056190, 4.373694444596176290, -0.3119999999999999996 ) ) ;
#3457=CARTESIAN_POINT ( 'NONE',  ( 5.178964085587577574E-17, 4.602861111186976828, 0.2819296736111110979 ) ) ;
#3458=CARTESIAN_POINT ( 'NONE',  ( -0.2819296736111110424, 3.793833333409199149, -0.1167790944451423119 ) ) ;
#3461=ORIENTED_EDGE ( 'NONE', *, *, #12779, .F. ) ;
#3466=VERTEX_POINT ( 'NONE', #8006 ) ;
#3468=CARTESIAN_POINT ( 'NONE',  ( -0.3119999999999999996, 0.3131944442927114824, -0.1292346314604056745 ) ) ;
#3477=CARTESIAN_POINT ( 'NONE',  ( 0.2843522314373275739, 5.089490977768033275, -0.1277081573576893947 ) ) ;
#3479=CARTESIAN_POINT ( 'NONE',  ( 0.1167790944451422702, 4.113277777853642903, -0.2819296736111110424 ) ) ;
#3480=CARTESIAN_POINT ( 'NONE',  ( 0.2819296736111110979, 5.158416666742532186, -3.452642723725051716E-17 ) ) ;
#3482=CARTESIAN_POINT ( 'NONE',  ( -0.3120000000000000551, 0.3756944442927115380, 0.1292346314604056190 ) ) ;
#3483=CARTESIAN_POINT ( 'NONE',  ( -0.3119999999999999996, 4.158416666666665762, -0.1292346314604056468 ) ) ;
#3484=CARTESIAN_POINT ( 'NONE',  ( 0.1292346314604056190, 4.929250000151730760, -0.3119999999999999996 ) ) ;
#3486=CARTESIAN_POINT ( 'NONE',  ( -0.2819296736111110979, 5.085500000075866112, -0.1167790944451422980 ) ) ;
#3488=CARTESIAN_POINT ( 'NONE',  ( -0.1831105892130123203, 0.05713127989799830081, 0.2461514306801097784 ) ) ;
#3492=CARTESIAN_POINT ( 'NONE',  ( 0.2819296736111110979, 5.047305555631421470, -3.452642723725051716E-17 ) ) ;
#3499=CARTESIAN_POINT ( 'NONE',  ( -0.2819296736111110979, 0.2437499999241333759, -3.452642723725051716E-17 ) ) ;
#3503=VERTEX_POINT ( 'NONE', #19108 ) ;
#3504=CARTESIAN_POINT ( 'NONE',  ( -0.2819296736111110979, 4.963972222298087544, 0.000000000000000000 ) ) ;
#3508=CARTESIAN_POINT ( 'NONE',  ( 0.2597743206613019606, 0.06249999999999967387, 0.1775648204224116178 ) ) ;
#3509=CARTESIAN_POINT ( 'NONE',  ( 0.3119999999999999996, 4.745222222222221120, -3.820898013339742174E-17 ) ) ;
#3511=CARTESIAN_POINT ( 'NONE',  ( 0.1167790944451422702, 4.002166666742532186, -0.2819296736111110979 ) ) ;
#3514=CARTESIAN_POINT ( 'NONE',  ( 0.2824272245982780150, 4.025992211338290439, 0.1357506634668411982 ) ) ;
#3519=CARTESIAN_POINT ( 'NONE',  ( 0.2819296736111110979, 4.377166666742532186, 0.1167790944451422425 ) ) ;
#3520=CARTESIAN_POINT ( 'NONE',  ( -0.3076502150634595201, 4.111722031579642334, -0.05522520306492269965 ) ) ;
#3525=CARTESIAN_POINT ( 'NONE',  ( -0.3038794998734477004, 3.948928095230931135, 0.08166525255517291526 ) ) ;
#3529=CARTESIAN_POINT ( 'NONE',  ( 0.2819296736111110979, 0.2020833332574666907, 0.000000000000000000 ) ) ;
#3531=CARTESIAN_POINT ( 'NONE',  ( 0.2206173157302028232, 0.5805555555555552694, -0.2206173157302028232 ) ) ;
#3534=EDGE_LOOP ( 'NONE', ( #13556, #12311, #8856, #16838 ) ) ;
#3537=CARTESIAN_POINT ( 'NONE',  ( 0.1292346314604057023, 0.06319444444444410891, 0.3119999999999998885 ) ) ;
#3538=CARTESIAN_POINT ( 'NONE',  ( 0.1167790944451424368, 3.773000000075866112, 0.2819296736111110424 ) ) ;
#3540=CARTESIAN_POINT ( 'NONE',  ( 0.2819296736111110424, 4.398000000075866112, -0.1167790944451423396 ) ) ;
#3542=LINE ( 'NONE', #1714, #10249 ) ;
#3545=CARTESIAN_POINT ( 'NONE',  ( 0.09743210712940192364, 4.374395042175329706, -0.2968164557725501140 ) ) ;
#3546=CARTESIAN_POINT ( 'NONE',  ( 0.1993543840281267465, 4.873694444520309865, 0.1993543840281266633 ) ) ;
#3547=CARTESIAN_POINT ( 'NONE',  ( 0.3100836462667937998, 4.197804898758246139, -0.04106420197143005602 ) ) ;
#3548=CARTESIAN_POINT ( 'NONE',  ( 6.614309848781084774E-13, 0.03242967361111062652, 0.2819296736111109869 ) ) ;
#3550=CARTESIAN_POINT ( 'NONE',  ( -1.726321361862525858E-17, 4.672305555631421470, -0.2819296736111110979 ) ) ;
#3553=DIRECTION ( 'NONE',  ( 0.000000000000000000, 0.000000000000000000, -1.000000000000000000 ) ) ;
#3557=CARTESIAN_POINT ( 'NONE',  ( 0.1167790944451423535, 0.1499999999241333759, 0.2819296736111110424 ) ) ;
#3563=CARTESIAN_POINT ( 'NONE',  ( -0.04794410370418378947, 3.878501262280343198, -0.3084350945838093550 ) ) ;
#3564=CARTESIAN_POINT ( 'NONE',  ( -0.1167790944451422702, -0.002777777853644409437, -0.2819296736111110424 ) ) ;
#3565=CARTESIAN_POINT ( 'NONE',  ( -0.1993543840281266355, 4.484805555631421470, 0.1993543840281267465 ) ) ;
#3567=CARTESIAN_POINT ( 'NONE',  ( 0.0009234384475589447160, 4.543807118310973614, -0.3119988299807083254 ) ) ;
#3568=CARTESIAN_POINT ( 'NONE',  ( -0.1993543840281266910, 5.137583333409199149, -0.1993543840281266910 ) ) ;
#3570=CARTESIAN_POINT ( 'NONE',  ( -0.1167790944451423535, 4.418833333409199149, 0.2819296736111110979 ) ) ;
#3571=CARTESIAN_POINT ( 'NONE',  ( 0.2701949539277979651, 3.747486037583882101, 0.1592585331144268646 ) ) ;
#3574=CARTESIAN_POINT ( 'NONE',  ( -0.1292346314604057023, 4.234805555707287894, 0.3119999999999998885 ) ) ;
#3575=CARTESIAN_POINT ( 'NONE',  ( -0.1993543840281266910, 4.470916666742532186, -0.1993543840281266910 ) ) ;
#3576=CARTESIAN_POINT ( 'NONE',  ( 0.1993543840281267465, 3.929250000075865668, 0.1993543840281266633 ) ) ;
#3577=ORIENTED_EDGE ( 'NONE', *, *, #5971, .F. ) ;
#3581=CARTESIAN_POINT ( 'NONE',  ( -0.1292346314604056745, 4.262583333333332725, -0.3119999999999999996 ) ) ;
#3582=CARTESIAN_POINT ( 'NONE',  ( 0.3119999999999999996, 4.245222222222222008, -3.820898013339742174E-17 ) ) ;
#3584=VERTEX_POINT ( 'NONE', #10097 ) ;
#3585=CARTESIAN_POINT ( 'NONE',  ( 0.1292346314604056745, 0.2993055554038226429, -0.3119999999999999996 ) ) ;
#3587=CARTESIAN_POINT ( 'NONE',  ( -0.1096552380901288787, 3.735110229336745746, 0.2921016150509060383 ) ) ;
#3589=CARTESIAN_POINT ( 'NONE',  ( 0.000000000000000000, 5.384999999999999787, -0.3119999999999999996 ) ) ;
#3596=CARTESIAN_POINT ( 'NONE',  ( 0.1993543840281267465, 4.318138888964754507, 0.1993543840281266633 ) ) ;
#3597=CARTESIAN_POINT ( 'NONE',  ( 5.178964085587577574E-17, 5.144527777853643791, 0.2819296736111110979 ) ) ;
#3599=CARTESIAN_POINT ( 'NONE',  ( -0.3036941569096411331, 4.222036648323082453, -0.08231831230607603023 ) ) ;
#3600=CARTESIAN_POINT ( 'NONE',  ( -0.2206173157302027676, 3.946611111111110404, 0.2206173157302028787 ) ) ;
#3601=CARTESIAN_POINT ( 'NONE',  ( -0.3119999999999998885, 5.005638889040620931, 0.1292346314604058410 ) ) ;
#3603=CARTESIAN_POINT ( 'NONE',  ( -0.1167790944451423119, 5.134111111186977716, -0.2819296736111110979 ) ) ;
#3605=ORIENTED_EDGE ( 'NONE', *, *, #4937, .T. ) ;
#3606=CARTESIAN_POINT ( 'NONE',  ( 0.09006919403515362132, 0.04138265269501665428, -0.2775327652233305353 ) ) ;
#3610=CARTESIAN_POINT ( 'NONE',  ( -1.726321361862525858E-17, 5.116750000075865223, -0.2819296736111110979 ) ) ;
#3611=ORIENTED_EDGE ( 'NONE', *, *, #22582, .T. ) ;
#3616=VERTEX_POINT ( 'NONE', #19581 ) ;
#3617=CARTESIAN_POINT ( 'NONE',  ( -0.1167790944451424506, 0.3097222221463555303, 0.2819296736111110424 ) ) ;
#3619=CARTESIAN_POINT ( 'NONE',  ( -1.726321361862525858E-17, 5.019527777853643791, -0.2819296736111110979 ) ) ;
#3622=CARTESIAN_POINT ( 'NONE',  ( -0.1993543840281266355, 4.915361111186976828, 0.1993543840281267465 ) ) ;
#3624=CARTESIAN_POINT ( 'NONE',  ( -0.3119999999999999996, 5.050777777777776478, 0.000000000000000000 ) ) ;
#3626=CARTESIAN_POINT ( 'NONE',  ( 0.1292346314604056745, 0.5840277777777773682, -0.3119999999999999996 ) ) ;
#3627=CARTESIAN_POINT ( 'NONE',  ( 0.2206173157302028787, 4.404944444444443441, 0.2206173157302027954 ) ) ;
#3628=CARTESIAN_POINT ( 'NONE',  ( -0.1167790944451423535, 4.029944444520309865, 0.2819296736111110979 ) ) ;
#3630=CARTESIAN_POINT ( 'NONE',  ( 0.1383926702065426950, 4.020153189153055528, 0.2803734965809290824 ) ) ;
#3637=CARTESIAN_POINT ( 'NONE',  ( -0.2592333949642908197, 4.108027434044173809, -0.1776828664482337783 ) ) ;
#3640=CARTESIAN_POINT ( 'NONE',  ( 0.09694982473845883963, 0.06249891840240667101, 0.2965547697865978938 ) ) ;
#3647=CARTESIAN_POINT ( 'NONE',  ( -5.178964085587577574E-17, 0.2993055554796889561, 0.2819296736111110979 ) ) ;
#3649=CARTESIAN_POINT ( 'NONE',  ( -5.731347020009612645E-17, 0.5597222222222218990, 0.3119999999999999996 ) ) ;
#3653=EDGE_LOOP ( 'NONE', ( #6556, #19153, #18472, #12719 ) ) ;
#3654=ORIENTED_EDGE ( 'NONE', *, *, #9559, .F. ) ;
#3655=CARTESIAN_POINT ( 'NONE',  ( -0.2786000101406610474, 5.109152158301237812, 0.1360994231350151629 ) ) ;
#3657=CARTESIAN_POINT ( 'NONE',  ( 0.3119999999999999996, 0.02152777777777744109, -0.1292346314604056468 ) ) ;
#3658=CARTESIAN_POINT ( 'NONE',  ( -0.1167790944451423257, 3.911888888964754507, -0.2819296736111110424 ) ) ;
#3660=ORIENTED_EDGE ( 'NONE', *, *, #15494, .T. ) ;
#3661=CARTESIAN_POINT ( 'NONE',  ( 0.2819296736111110424, 4.509111111186976828, -0.1167790944451423396 ) ) ;
#3662=CARTESIAN_POINT ( 'NONE',  ( -1.910449006669871087E-17, 4.981333333333332725, -0.3119999999999999996 ) ) ;
#3665=CARTESIAN_POINT ( 'NONE',  ( 5.731347020009612645E-17, 4.675777777777777366, 0.3119999999999999996 ) ) ;
#3666=CARTESIAN_POINT ( 'NONE',  ( -0.1993543840281266910, 4.901472222298087544, -0.1993543840281266910 ) ) ;
#3667=( BOUNDED_CURVE ( )  B_SPLINE_CURVE ( 2, ( #18228, #15794, #6522, #21402, #2857, #17743, #1038, #8467, #15908 ),
 .UNSPECIFIED., .F., .F. ) 
 B_SPLINE_CURVE_WITH_KNOTS ( ( 3, 2, 2, 2, 3 ),
 ( 0.7291666666666666297, 0.7395833333333333703, 0.7500000000000000000, 0.7604166666666666297, 0.7708333333333333703 ),
 .UNSPECIFIED. ) 
 CURVE ( )  GEOMETRIC_REPRESENTATION_ITEM ( )  RATIONAL_B_SPLINE_CURVE ( ( 1.000000000000000000, 0.9238795325112867385, 1.000000000000000000, 0.9238795325112867385, 1.000000000000000000, 0.9238795325112867385, 1.000000000000000000, 0.9238795325112867385, 1.000000000000000000 ) ) 
 REPRESENTATION_ITEM ( '' )  );
#3669=LINE ( 'NONE', #3792, #11079 ) ;
#3671=SHAPE_REPRESENTATION_RELATIONSHIP ( 'NONE' , 'NONE' ,  #7952, #12638 ) ;
#3673=CARTESIAN_POINT ( 'NONE',  ( -0.1993543840281266355, 4.693138888964754507, 0.1993543840281267465 ) ) ;
#3678=CARTESIAN_POINT ( 'NONE',  ( -0.2819296736111110424, 0.5180555554796888451, -0.1167790944451423396 ) ) ;
#3679=ORIENTED_EDGE ( 'NONE', *, *, #6592, .T. ) ;
#3681=CARTESIAN_POINT ( 'NONE',  ( 0.2819296736111110424, 0.2124999999241334314, 0.1167790944451424923 ) ) ;
#3682=CARTESIAN_POINT ( 'NONE',  ( -0.3119999999999998885, 4.332027777777777366, 0.1292346314604058410 ) ) ;
#3683=CARTESIAN_POINT ( 'NONE',  ( -0.2839807072535898147, 5.201861426142459166, 0.01683923060391288168 ) ) ;
#3687=CARTESIAN_POINT ( 'NONE',  ( -0.2173539347745672701, 3.883923987474912298, -0.2247910917580860646 ) ) ;
#3688=CARTESIAN_POINT ( 'NONE',  ( -0.2819296736111111534, 0.2333333332574667185, 0.1167790944451422563 ) ) ;
#3689=CARTESIAN_POINT ( 'NONE',  ( -0.2819296736111110979, 0.007638888813022256218, -3.452642723725051716E-17 ) ) ;
#3690=CARTESIAN_POINT ( 'NONE',  ( -0.1167790944451423257, 4.411888888964754507, -0.2819296736111110424 ) ) ;
#3694=CARTESIAN_POINT ( 'NONE',  ( -0.2819296736111110424, 5.203555555631421470, 0.1167790944451424923 ) ) ;
#3695=CARTESIAN_POINT ( 'NONE',  ( 5.178964085587577574E-17, 4.422305555631421470, 0.2819296736111110979 ) ) ;
#3696=CARTESIAN_POINT ( 'NONE',  ( 0.3088587430578357274, 3.750936470065025841, 0.04450246037814264283 ) ) ;
#3698=CARTESIAN_POINT ( 'NONE',  ( 0.3003959655288142017, 3.916143348187413498, 0.09367083608899910707 ) ) ;
#3699=CARTESIAN_POINT ( 'NONE',  ( 0.3119999999999999996, 4.082027777929511103, 0.1292346314604056190 ) ) ;
#3700=CARTESIAN_POINT ( 'NONE',  ( -1.726321361862525858E-17, 4.575083333409199149, -0.2819296736111110979 ) ) ;
#3702=VERTEX_POINT ( 'NONE', #8358 ) ;
#3704=ADVANCED_FACE ( 'NONE', ( #23227 ), #21658, .T. ) ;
#3707=EDGE_CURVE ( 'NONE', #7602, #22848, #22539, .T. ) ;
#3709=DIRECTION ( 'NONE',  ( 0.000000000000000000, 0.000000000000000000, 1.000000000000000000 ) ) ;
#3711=CARTESIAN_POINT ( 'NONE',  ( 0.3119999999999999996, 0.4590277776260447973, -0.1292346314604056468 ) ) ;
#3713=CYLINDRICAL_SURFACE ( 'NONE', #22592, 0.3119999999999999996 ) ;
#3714=CARTESIAN_POINT ( 'NONE',  ( -0.2767634618065506480, 3.728737891010954542, 0.1512181958280439387 ) ) ;
#3715=CARTESIAN_POINT ( 'NONE',  ( -0.3120000000000000551, 0.2715277777777774793, 0.1292346314604056190 ) ) ;
#3717=( BOUNDED_CURVE ( )  B_SPLINE_CURVE ( 2, ( #6409, #12526, #17998, #17507, #1167, #14215, #17629, #2865, #23460 ),
 .UNSPECIFIED., .F., .F. ) 
 B_SPLINE_CURVE_WITH_KNOTS ( ( 3, 2, 2, 2, 3 ),
 ( 0.3125000000000000000, 0.3229166666666666852, 0.3333333333333333148, 0.3437500000000000000, 0.3541666666666666852 ),
 .UNSPECIFIED. ) 
 CURVE ( )  GEOMETRIC_REPRESENTATION_ITEM ( )  RATIONAL_B_SPLINE_CURVE ( ( 1.000000000000000000, 0.9238795325112867385, 1.000000000000000000, 0.9238795325112867385, 1.000000000000000000, 0.9238795325112867385, 1.000000000000000000, 0.9238795325112867385, 1.000000000000000000 ) ) 
 REPRESENTATION_ITEM ( '' )  );
#3719=ORIENTED_EDGE ( 'NONE', *, *, #23371, .F. ) ;
#3723=CARTESIAN_POINT ( 'NONE',  ( 0.3110505074677553661, 5.085000275326436281, 0.02324247747823024457 ) ) ;
#3725=CARTESIAN_POINT ( 'NONE',  ( 0.1993543840281266633, 4.165361111186975940, -0.1993543840281266910 ) ) ;
#3726=CARTESIAN_POINT ( 'NONE',  ( -1.726321361862525858E-17, 5.116750000075865223, -0.2819296736111110979 ) ) ;
#3729=CARTESIAN_POINT ( 'NONE',  ( -1.910449006669871087E-17, 3.870222222222221564, -0.3119999999999999996 ) ) ;
#3730=CARTESIAN_POINT ( 'NONE',  ( -0.1292346314604056745, 4.769527777929509327, -0.3119999999999999996 ) ) ;
#3731=AXIS2_PLACEMENT_3D ( 'NONE', #15801, #13980, #21408 ) ;
#3732=CARTESIAN_POINT ( 'NONE',  ( 0.2819296736111111534, 5.113277777853642903, 0.1167790944451422563 ) ) ;
#3733=CARTESIAN_POINT ( 'NONE',  ( 0.2206173157302027676, 0.3999999999999996336, 0.2206173157302028787 ) ) ;
#3741=CARTESIAN_POINT ( 'NONE',  ( 0.2819296736111110979, 5.158416666742532186, -3.452642723725051716E-17 ) ) ;
#3744=B_SPLINE_CURVE_WITH_KNOTS ( 'NONE', 3,
 ( #23433, #4672, #10648, #6741, #6865, #16380, #14185, #8687, #1380, #12141, #21619, #19548, #18080, #4912, #14308, #13954, #12374, #16135, #8809, #6619, #10423, #19792, #5027, #17723, #17848, #16258, #23670, #10299, #14070, #3091, #10534, #1139, #8574, #2967, #15892, #23312, #3202, #21497, #16015, #12492, #6989, #21742, #19913, #12254, #14431 ),
 .UNSPECIFIED., .F., .F.,
 ( 4, 2, 2, 2, 2, 1, 1, 1, 2, 2, 1, 2, 2, 2, 2, 2, 1, 2, 2, 2, 2, 2, 2, 2, 4 ),
 ( 0.09617319050982510442, 0.09758660992310271010, 0.09900002933638030189, 0.1018268681629354994, 0.1046537069894907107, 0.1050070618428101121, 0.1051837392694698059, 0.1052720779827996528, 0.1053162473394645832, 0.1053383320177970345, 0.1053604166961294997, 0.1060671264027681776, 0.1074805458160455335, 0.1088939652293229032, 0.1103073846426002591, 0.1117208040558776150, 0.1118974814825372810, 0.1119858201958671140, 0.1120741589091969470, 0.1124275137625162929, 0.1131342234691549709, 0.1145476428824323267, 0.1159610622957096826, 0.1173744817089870524, 0.1187879011222644082 ),
 .UNSPECIFIED. ) ;
#3746=CARTESIAN_POINT ( 'NONE',  ( 1.726321361862525858E-17, 0.1743055554796889284, -0.2819296736111110979 ) ) ;
#3748=CARTESIAN_POINT ( 'NONE',  ( -0.2819296736111110424, 4.925777777853643791, 0.1167790944451424923 ) ) ;
#3749=CARTESIAN_POINT ( 'NONE',  ( 0.1661407850955833043, 4.483412766610799238, -0.2646232894162082183 ) ) ;
#3750=CARTESIAN_POINT ( 'NONE',  ( -1.726321361862525858E-17, 4.950083333409199149, -0.2819296736111110979 ) ) ;
#3755=CARTESIAN_POINT ( 'NONE',  ( 0.2206173157302027954, 4.085499999999999687, -0.2206173157302028232 ) ) ;
#3757=CARTESIAN_POINT ( 'NONE',  ( -0.2206173157302028232, 4.432722222222222008, -0.2206173157302028232 ) ) ;
#3758=CARTESIAN_POINT ( 'NONE',  ( 0.2819296736111111534, 3.932722222298087988, 0.1167790944451422563 ) ) ;
#3760=CARTESIAN_POINT ( 'NONE',  ( 0.04088167920887831458, 4.017269169224574554, 0.3120000053084774350 ) ) ;
#3761=DIRECTION ( 'NONE',  ( 0.000000000000000000, 0.000000000000000000, -1.000000000000000000 ) ) ;
#3762=ORIENTED_EDGE ( 'NONE', *, *, #4520, .F. ) ;
#3766=( BOUNDED_CURVE ( )  B_SPLINE_CURVE ( 2, ( #14387, #15853, #14145, #21461, #19751, #3047, #3886, #103, #5592 ),
 .UNSPECIFIED., .F., .F. ) 
 B_SPLINE_CURVE_WITH_KNOTS ( ( 3, 2, 2, 2, 3 ),
 ( 0.6041666666666666297, 0.6145833333333333703, 0.6250000000000000000, 0.6354166666666666297, 0.6458333333333333703 ),
 .UNSPECIFIED. ) 
 CURVE ( )  GEOMETRIC_REPRESENTATION_ITEM ( )  RATIONAL_B_SPLINE_CURVE ( ( 1.000000000000000000, 0.9238795325112867385, 1.000000000000000000, 0.9238795325112867385, 1.000000000000000000, 0.9238795325112867385, 1.000000000000000000, 0.9238795325112867385, 1.000000000000000000 ) ) 
 REPRESENTATION_ITEM ( '' )  );
#3768=CARTESIAN_POINT ( 'NONE',  ( -0.2356117178940455303, 4.106961824400430672, -0.2079910394304901600 ) ) ;
#3774=CARTESIAN_POINT ( 'NONE',  ( 0.2819296736111110979, 0.2576388888130222155, 0.000000000000000000 ) ) ;
#3776=CARTESIAN_POINT ( 'NONE',  ( -5.308788303787306404E-17, 0.03949697488198145034, 0.2889969748819818385 ) ) ;
#3780=CARTESIAN_POINT ( 'NONE',  ( 0.1292346314604007063, 4.366749999999999687, -0.3120000000000049400 ) ) ;
#3781=CARTESIAN_POINT ( 'NONE',  ( -0.2819296736111110979, 0.5631944443685777957, -3.452642723725051716E-17 ) ) ;
#3782=CARTESIAN_POINT ( 'NONE',  ( 0.2206173157302028787, 5.071611111111109516, 0.2206173157302027954 ) ) ;
#3785=CARTESIAN_POINT ( 'NONE',  ( -0.2819296736111110979, 4.311194444520309865, 0.000000000000000000 ) ) ;
#3786=CARTESIAN_POINT ( 'NONE',  ( 0.3119999999999999996, 4.967444444444443441, -3.820898013339742174E-17 ) ) ;
#3788=ORIENTED_EDGE ( 'NONE', *, *, #3849, .F. ) ;
#3789=CARTESIAN_POINT ( 'NONE',  ( 0.2677646337359513851, 4.358477931348908818, 0.1602620551619879097 ) ) ;
#3790=CARTESIAN_POINT ( 'NONE',  ( -0.2819296736111110424, 5.016055555631420582, -0.1167790944451423119 ) ) ;
#3792=CARTESIAN_POINT ( 'NONE',  ( 3.820898013339742174E-17, 0.06249999999999967387, -0.3119999999999999996 ) ) ;
#3795=DIRECTION ( 'NONE',  ( -0.000000000000000000, -1.000000000000000000, -0.000000000000000000 ) ) ;
#3796=B_SPLINE_CURVE_WITH_KNOTS ( 'NONE', 3,
 ( #5158, #10432, #14195, #23561, #19925, #10305 ),
 .UNSPECIFIED., .F., .F.,
 ( 4, 2, 4 ),
 ( 0.3494352842492303157, 0.4117316744839973897, 0.4740280647187645191 ),
 .UNSPECIFIED. ) ;
#3797=CARTESIAN_POINT ( 'NONE',  ( 0.2819296736111110979, 4.773000000075865223, -0.1167790944451423396 ) ) ;
#3800=DIRECTION ( 'NONE',  ( -0.000000000000000000, -1.000000000000000000, -0.000000000000000000 ) ) ;
#3801=CARTESIAN_POINT ( 'NONE',  ( -0.2819296736111110979, 0.4659722221463555303, -3.452642723725051716E-17 ) ) ;
#3803=ORIENTED_EDGE ( 'NONE', *, *, #8915, .T. ) ;
#3804=CARTESIAN_POINT ( 'NONE',  ( 0.1167790944451423257, 0.1708333332574666907, -0.2819296736111110424 ) ) ;
#3810=CARTESIAN_POINT ( 'NONE',  ( 0.3120000000000000551, 5.019527777777777366, 0.1292346314604056190 ) ) ;
#3811=CARTESIAN_POINT ( 'NONE',  ( 0.2819296736111110424, 0.1986111110352444531, 0.1167790944451424923 ) ) ;
#3815=CARTESIAN_POINT ( 'NONE',  ( 0.2819296736111110979, 4.279944444520310753, 0.1167790944451422425 ) ) ;
#3818=CARTESIAN_POINT ( 'NONE',  ( -0.2819296736111110424, 5.085500000075866112, -0.1167790944451423119 ) ) ;
#3819=CARTESIAN_POINT ( 'NONE',  ( 0.1167790944451424506, 4.536888888964754507, 0.2819296736111110424 ) ) ;
#3823=CARTESIAN_POINT ( 'NONE',  ( -0.3119999999999999996, 4.054250000151732536, -0.1292346314604056468 ) ) ;
#3825=CARTESIAN_POINT ( 'NONE',  ( -1.726321361862525858E-17, 3.727861111186976384, -0.2819296736111110979 ) ) ;
#3834=ORIENTED_EDGE ( 'NONE', *, *, #23371, .T. ) ;
#3835=CARTESIAN_POINT ( 'NONE',  ( 0.1292346314604057023, 0.5562499998482671737, 0.3119999999999998885 ) ) ;
#3836=ORIENTED_EDGE ( 'NONE', *, *, #12285, .F. ) ;
#3838=CARTESIAN_POINT ( 'NONE',  ( 0.2697513640123151979, 4.756947486709429462, -0.1629237773733702710 ) ) ;
#3840=CARTESIAN_POINT ( 'NONE',  ( 1.910449006669871087E-17, 0.4763888888888885287, -0.3119999999999999996 ) ) ;
#3841=ORIENTED_EDGE ( 'NONE', *, *, #1780, .F. ) ;
#3844=CARTESIAN_POINT ( 'NONE',  ( -0.2206173157302028232, 4.043833333333332725, -0.2206173157302028232 ) ) ;
#3845=CARTESIAN_POINT ( 'NONE',  ( -0.2819296736111110979, 4.241750000075865223, 0.000000000000000000 ) ) ;
#3846=CARTESIAN_POINT ( 'NONE',  ( 1.910449006669871087E-17, 0.3027777776260448528, -0.3119999999999999996 ) ) ;
#3848=CARTESIAN_POINT ( 'NONE',  ( 5.731347020009612645E-17, 3.842444444444443441, 0.3119999999999999996 ) ) ;
#3849=EDGE_CURVE ( 'NONE', #1715, #11042, #21758, .T. ) ;
#3850=CARTESIAN_POINT ( 'NONE',  ( 0.2206173157302028787, 4.634111111262843252, 0.2206173157302027954 ) ) ;
#3851=EDGE_CURVE ( 'NONE', #21992, #12983, #5009, .T. ) ;
#3852=CARTESIAN_POINT ( 'NONE',  ( 0.1993543840281266633, 5.179250000075866112, -0.1993543840281266910 ) ) ;
#3853=CARTESIAN_POINT ( 'NONE',  ( 0.1292346314604056745, 0.4173611111111109051, -0.3119999999999999996 ) ) ;
#3855=CARTESIAN_POINT ( 'NONE',  ( 7.256325792998745354E-13, 0.06073895945496885634, 0.3102389594549692098 ) ) ;
#3856=ORIENTED_EDGE ( 'NONE', *, *, #6472, .T. ) ;
#3861=CARTESIAN_POINT ( 'NONE',  ( 0.1167790944451424368, 5.148000000075865223, 0.2819296736111110424 ) ) ;
#3863=CARTESIAN_POINT ( 'NONE',  ( -0.2819296736111110979, 3.974388888964754951, -0.1167790944451422980 ) ) ;
#3865=CARTESIAN_POINT ( 'NONE',  ( 0.2999766478522543633, 4.416353878536761535, 0.08855854222874144643 ) ) ;
#3868=CARTESIAN_POINT ( 'NONE',  ( 0.2819296736111110424, 0.4347222221463555858, 0.1167790944451424923 ) ) ;
#3870=CARTESIAN_POINT ( 'NONE',  ( 5.178964085587577574E-17, 4.991750000075866112, 0.2819296736111110979 ) ) ;
#3872=CARTESIAN_POINT ( 'NONE',  ( 0.1167790944451422702, 4.891055555631421470, -0.2819296736111110424 ) ) ;
#3873=FACE_OUTER_BOUND ( 'NONE', #2853, .T. ) ;
#3874=CARTESIAN_POINT ( 'NONE',  ( 0.006049195330367759457, 4.877003847587220164, -0.3119499012820716177 ) ) ;
#3877=CARTESIAN_POINT ( 'NONE',  ( -0.1292346314604056745, 4.540361111111110404, -0.3119999999999999996 ) ) ;
#3878=CARTESIAN_POINT ( 'NONE',  ( -0.2819296736111110424, 3.856333333409199149, 0.1167790944451424923 ) ) ;
#3879=CARTESIAN_POINT ( 'NONE',  ( 0.3119999999999999996, 0.3444444442927114824, 0.000000000000000000 ) ) ;
#3880=CARTESIAN_POINT ( 'NONE',  ( 0.002644507750069672973, 4.988201934502406232, -0.3119903920917703743 ) ) ;
#3883=CARTESIAN_POINT ( 'NONE',  ( 0.3109270811063121753, 4.584793454335284402, 0.02585305464956524218 ) ) ;
#3886=CARTESIAN_POINT ( 'NONE',  ( -0.2206173157302028787, 0.3861111111111107386, 0.2206173157302027954 ) ) ;
#3892=CARTESIAN_POINT ( 'NONE',  ( -0.1167790944451422702, 0.2194444443685777957, -0.2819296736111110424 ) ) ;
#3901=CARTESIAN_POINT ( 'NONE',  ( 0.2206173157302028232, 0.2472222222222218435, -0.2206173157302028232 ) ) ;
#3902=CARTESIAN_POINT ( 'NONE',  ( -1.910449006669871087E-17, 5.259111111111110404, -0.3119999999999999996 ) ) ;
#3904=ORIENTED_EDGE ( 'NONE', *, *, #22862, .F. ) ;
#3905=CARTESIAN_POINT ( 'NONE',  ( -0.1993543840281266910, 4.137583333409199149, -0.1993543840281266910 ) ) ;
#3909=DIRECTION ( 'NONE',  ( 1.000000000000000000, 0.000000000000000000, 0.000000000000000000 ) ) ;
#3910=CARTESIAN_POINT ( 'NONE',  ( -0.1993543840281266910, 4.957027777853642903, -0.1993543840281266910 ) ) ;
#3911=AXIS2_PLACEMENT_3D ( 'NONE', #14887, #18652, #22306 ) ;
#3912=CARTESIAN_POINT ( 'NONE',  ( 0.08148075347861075124, 4.184984852033682756, 0.3039166203302874902 ) ) ;
#3914=( NAMED_UNIT ( * ) SI_UNIT ( $, .STERADIAN. ) SOLID_ANGLE_UNIT ( ) );
#3917=CARTESIAN_POINT ( 'NONE',  ( -1.726321361862525858E-17, 4.727861111186976828, -0.2819296736111110979 ) ) ;
#3919=CARTESIAN_POINT ( 'NONE',  ( -8.893442360197089595E-05, 4.043835722953997625, -0.3120000002135276396 ) ) ;
#3921=CARTESIAN_POINT ( 'NONE',  ( -0.1167790944451424368, 0.5874999999241333759, 0.2819296736111110424 ) ) ;
#3923=CARTESIAN_POINT ( 'NONE',  ( 0.2819296736111110979, 0.3270833332574666907, 0.000000000000000000 ) ) ;
#3924=CARTESIAN_POINT ( 'NONE',  ( 0.000000000000000000, 5.384999999999999787, 0.000000000000000000 ) ) ;
#3932=CARTESIAN_POINT ( 'NONE',  ( -0.2819296736111110979, 0.1743055554796889284, -3.452642723725051716E-17 ) ) ;
#3933=CARTESIAN_POINT ( 'NONE',  ( -0.2819296736111110979, 0.06319444436857780956, -3.452642723725051716E-17 ) ) ;
#3935=CARTESIAN_POINT ( 'NONE',  ( -0.2819296736111110424, 4.363277777853643791, -0.1167790944451423119 ) ) ;
#3937=CARTESIAN_POINT ( 'NONE',  ( 0.1993543840281267465, 4.832027777853643791, 0.1993543840281266633 ) ) ;
#3938=CARTESIAN_POINT ( 'NONE',  ( -0.1993543840281266910, 4.345916666742532186, -0.1993543840281266910 ) ) ;
#3941=CARTESIAN_POINT ( 'NONE',  ( 0.1292346314604058410, 4.075083333485065573, 0.3119999999999998885 ) ) ;
#3950=EDGE_LOOP ( 'NONE', ( #19649, #1450, #14644, #15470 ) ) ;
#3951=CARTESIAN_POINT ( 'NONE',  ( 1.910449006669871087E-17, 0.4138888887371559577, -0.3119999999999999996 ) ) ;
#3962=CARTESIAN_POINT ( 'NONE',  ( 0.1167790944451422702, 4.002166666742532186, -0.2819296736111110424 ) ) ;
#3963=CARTESIAN_POINT ( 'NONE',  ( -0.07891297495569016274, 0.03366361305084811933, 0.2724293070475350964 ) ) ;
#3964=CARTESIAN_POINT ( 'NONE',  ( -0.1292346314604020385, 4.838972222222222008, 0.3120000000000036078 ) ) ;
#3965=CARTESIAN_POINT ( 'NONE',  ( 5.731347020009612645E-17, 3.897999999999999243, 0.3119999999999999996 ) ) ;
#3966=CARTESIAN_POINT ( 'NONE',  ( 0.2206173157302027954, 4.759111111262843252, -0.2206173157302028232 ) ) ;
#3967=CARTESIAN_POINT ( 'NONE',  ( 5.178964085587577574E-17, 4.936194444520309865, 0.2819296736111110979 ) ) ;
#3968=CARTESIAN_POINT ( 'NONE',  ( -0.1167790944451423535, 4.363277777853642903, 0.2819296736111110424 ) ) ;
#3969=CARTESIAN_POINT ( 'NONE',  ( -0.1547861949055390485, 3.900357038476919058, 0.2724574402709006860 ) ) ;
#3975=CARTESIAN_POINT ( 'NONE',  ( 5.178964085587577574E-17, 5.033416666742532186, 0.2819296736111110979 ) ) ;
#3976=CARTESIAN_POINT ( 'NONE',  ( 0.1167790944451424506, 3.773000000075866112, 0.2819296736111110424 ) ) ;
#3977=CARTESIAN_POINT ( 'NONE',  ( 0.04072223948701583079, 4.406056745573514455, 0.3100004575725601730 ) ) ;
#3981=CARTESIAN_POINT ( 'NONE',  ( 0.1993543840281266910, 0.5562499999241333759, -0.1993543840281266910 ) ) ;
#3983=CARTESIAN_POINT ( 'NONE',  ( -0.1993543840281266910, 4.859805555631421470, -0.1993543840281266910 ) ) ;
#3986=CARTESIAN_POINT ( 'NONE',  ( -1.726321361862525858E-17, 4.838972222298088433, -0.2819296736111110979 ) ) ;
#3988=CARTESIAN_POINT ( 'NONE',  ( 0.2249574224929273558, 4.856505608673026053, 0.2162428277538668564 ) ) ;
#3990=FACE_OUTER_BOUND ( 'NONE', #11301, .T. ) ;
#3991=CARTESIAN_POINT ( 'NONE',  ( 0.3119999999999999996, 4.526472222222221120, -0.1292346314604056745 ) ) ;
#3992=CARTESIAN_POINT ( 'NONE',  ( 0.1993543840281266633, 3.776472222298087988, -0.1993543840281266910 ) ) ;
#3994=DIRECTION ( 'NONE',  ( 0.000000000000000000, 0.000000000000000000, -1.000000000000000000 ) ) ;
#3999=( BOUNDED_CURVE ( )  B_SPLINE_CURVE ( 2, ( #17152, #12163, #442, #7873, #15323, #22753, #20924, #6044, #4218 ),
 .UNSPECIFIED., .F., .F. ) 
 B_SPLINE_CURVE_WITH_KNOTS ( ( 3, 2, 2, 2, 3 ),
 ( 0.4017857142857142461, 0.4062500000000000000, 0.4107142857142856984, 0.4151785714285715079, 0.4196428571428572063 ),
 .UNSPECIFIED. ) 
 CURVE ( )  GEOMETRIC_REPRESENTATION_ITEM ( )  RATIONAL_B_SPLINE_CURVE ( ( 1.000000000000000888, 0.9238795325112857393, 1.000000000000000000, 0.9238795325112867385, 1.000000000000000000, 0.9238795325112867385, 1.000000000000000000, 0.9238795325112857393, 1.000000000000000888 ) ) 
 REPRESENTATION_ITEM ( '' )  );
#4000=CARTESIAN_POINT ( 'NONE',  ( -2.918002456435568987E-09, 4.127166543308980806, 0.3119999999999999996 ) ) ;
#4002=CARTESIAN_POINT ( 'NONE',  ( 0.0003241969039724112056, 4.654935146396195655, -0.3120000004149252049 ) ) ;
#4006=CARTESIAN_POINT ( 'NONE',  ( 0.3039609707416114359, 4.309972269864218219, -0.08137645367071676128 ) ) ;
#4007=CARTESIAN_POINT ( 'NONE',  ( 0.2072783878431551374, 5.137695445002894878, 0.2242608243709702798 ) ) ;
#4011=CARTESIAN_POINT ( 'NONE',  ( -0.2819296736111110979, 0.3999999999241333759, 0.1167790944451422425 ) ) ;
#4014=CARTESIAN_POINT ( 'NONE',  ( 3.820898013339742174E-17, 5.384999999999999787, 0.3119999999999999996 ) ) ;
#4016=CARTESIAN_POINT ( 'NONE',  ( 0.000000000000000000, 5.072999999999999510, 0.000000000000000000 ) ) ;
#4017=DIRECTION ( 'NONE',  ( -0.000000000000000000, -1.000000000000000000, -0.000000000000000000 ) ) ;
#4018=CARTESIAN_POINT ( 'NONE',  ( 0.2206173157302027676, 0.3444444444444440534, 0.2206173157302028787 ) ) ;
#4019=CARTESIAN_POINT ( 'NONE',  ( -0.2206173157302027676, 5.224388888888887195, 0.2206173157302028787 ) ) ;
#4021=CARTESIAN_POINT ( 'NONE',  ( 0.1167790944451422702, 4.238277777853643791, -0.2819296736111110424 ) ) ;
#4027=CARTESIAN_POINT ( 'NONE',  ( 0.1993543840281266633, 5.054250000075865223, -0.1993543840281266910 ) ) ;
#4028=CARTESIAN_POINT ( 'NONE',  ( 0.04074832584215749842, 4.183841529647392754, 0.3119999987872715264 ) ) ;
#4031=CARTESIAN_POINT ( 'NONE',  ( 0.2819296736111111534, 4.335500000075866112, 0.1167790944451422563 ) ) ;
#4035=CARTESIAN_POINT ( 'NONE',  ( -0.1167790944451424368, 0.4208333332574665797, 0.2819296736111110424 ) ) ;
#4037=CARTESIAN_POINT ( 'NONE',  ( 0.2819296736111110424, 0.5458333332574666352, 0.1167790944451424923 ) ) ;
#4039=DIRECTION ( 'NONE',  ( 0.000000000000000000, 0.000000000000000000, -1.000000000000000000 ) ) ;
#4044=CARTESIAN_POINT ( 'NONE',  ( 0.2819296736111110979, 0.2020833332574666907, 0.000000000000000000 ) ) ;
#4045=CARTESIAN_POINT ( 'NONE',  ( 0.1993543840281266910, 0.3201388888130222710, -0.1993543840281266910 ) ) ;
#4046=CARTESIAN_POINT ( 'NONE',  ( -0.1993543840281266910, 4.359805555631421470, -0.1993543840281266910 ) ) ;
#4048=CARTESIAN_POINT ( 'NONE',  ( 0.2819296736111110979, 4.950083333409199149, -3.452642723725051716E-17 ) ) ;
#4049=CARTESIAN_POINT ( 'NONE',  ( 0.2819296736111110979, 4.439666666742532186, -0.1167790944451423396 ) ) ;
#4053=CARTESIAN_POINT ( 'NONE',  ( 0.1292346314604056190, 4.095916666818398610, -0.3119999999999999996 ) ) ;
#4057=VERTEX_POINT ( 'NONE', #17009 ) ;
#4061=CARTESIAN_POINT ( 'NONE',  ( -1.054647954922321762E-07, 4.988277780858759947, -0.3119999999999820695 ) ) ;
#4063=CARTESIAN_POINT ( 'NONE',  ( -0.1292346314604058410, 0.6048611109593783342, 0.3119999999999998885 ) ) ;
#4065=CARTESIAN_POINT ( 'NONE',  ( 0.000000000000000000, 5.384999999999999787, 0.000000000000000000 ) ) ;
#4066=CARTESIAN_POINT ( 'NONE',  ( -1.910449006669871087E-17, 4.647999999999998799, -0.3119999999999999996 ) ) ;
#4067=CARTESIAN_POINT ( 'NONE',  ( 0.3146586916146184576, 4.752112305768198652, 0.001375812536115708813 ) ) ;
#4074=CARTESIAN_POINT ( 'NONE',  ( -0.2284009101814420406, 4.675474525268722203, 0.2125530810637378254 ) ) ;
#4075=CARTESIAN_POINT ( 'NONE',  ( -0.1167790944451423535, 3.974388888964754063, 0.2819296736111110424 ) ) ;
#4077=CARTESIAN_POINT ( 'NONE',  ( -1.062695237341364068E-12, 5.118312382271687611, 0.3086920601714014945 ) ) ;
#4078=EDGE_CURVE ( 'NONE', #16166, #13675, #101, .T. ) ;
#4079=CARTESIAN_POINT ( 'NONE',  ( 0.4035778243552766709, 3.745586516788660170, -0.07105710959332679766 ) ) ;
#4080=CARTESIAN_POINT ( 'NONE',  ( 0.2206173157302028787, 4.745222222373954857, 0.2206173157302027954 ) ) ;
#4081=CARTESIAN_POINT ( 'NONE',  ( 0.1167790944451422702, 4.849388888964755395, -0.2819296736111110979 ) ) ;
#4083=CARTESIAN_POINT ( 'NONE',  ( -0.2819296736111110424, 4.245222222298087544, 0.1167790944451424923 ) ) ;
#4084=ORIENTED_EDGE ( 'NONE', *, *, #22172, .F. ) ;
#4085=EDGE_CURVE ( 'NONE', #9548, #6543, #16466, .T. ) ;
#4086=EDGE_LOOP ( 'NONE', ( #10118, #5738, #15930, #16495 ) ) ;
#4092=CARTESIAN_POINT ( 'NONE',  ( 0.1993543840281267465, 3.943138888964754951, 0.1993543840281266633 ) ) ;
#4093=CARTESIAN_POINT ( 'NONE',  ( 0.2839364041945253159, 4.422813250354537651, -0.1344124572274522367 ) ) ;
#4096=B_SPLINE_CURVE_WITH_KNOTS ( 'NONE', 3,
 ( #18823, #2369, #5535, #20890, #18948, #11156 ),
 .UNSPECIFIED., .F., .F.,
 ( 4, 2, 4 ),
 ( 0.008885579728328409088, 0.01010732856524649767, 0.01132907740216458452 ),
 .UNSPECIFIED. ) ;
#4097=CARTESIAN_POINT ( 'NONE',  ( 0.01630689377124411657, 0.06101829741696308818, 0.3105182974169249932 ) ) ;
#4099=CARTESIAN_POINT ( 'NONE',  ( 0.1993543840281266355, 0.4312499999241333759, 0.1993543840281267465 ) ) ;
#4101=CARTESIAN_POINT ( 'NONE',  ( 0.1993543840281267465, 5.054250000075865223, 0.1993543840281266633 ) ) ;
#4103=VECTOR ( 'NONE', #9902, 39.37007874015748143 ) ;
#4104=CARTESIAN_POINT ( 'NONE',  ( 0.1993543840281266633, 4.609805555631420582, -0.1993543840281266910 ) ) ;
#4106=CARTESIAN_POINT ( 'NONE',  ( 0.2148596022118366422, 4.856116452778191928, 0.2262407900182530907 ) ) ;
#4110=CARTESIAN_POINT ( 'NONE',  ( -0.1292346314604056745, 4.484805555555555046, -0.3119999999999999996 ) ) ;
#4112=CARTESIAN_POINT ( 'NONE',  ( -0.2819296736111110424, 3.800777777853643347, 0.1167790944451424923 ) ) ;
#4116=EDGE_LOOP ( 'NONE', ( #13401, #5666, #20362, #22745 ) ) ;
#4117=FACE_OUTER_BOUND ( 'NONE', #19082, .T. ) ;
#4118=ORIENTED_EDGE ( 'NONE', *, *, #4412, .F. ) ;
#4120=CARTESIAN_POINT ( 'NONE',  ( 0.1129687097031495668, 4.707317419575747230, -0.2914138746359711263 ) ) ;
#4124=ORIENTED_EDGE ( 'NONE', *, *, #21993, .F. ) ;
#4125=CARTESIAN_POINT ( 'NONE',  ( 5.178964085587577574E-17, 4.922305555631420582, 0.2819296736111110979 ) ) ;
#4127=CARTESIAN_POINT ( 'NONE',  ( -0.1167790944451422702, 0.3861111110352444808, -0.2819296736111110424 ) ) ;
#4129=LINE ( 'NONE', #471, #8431 ) ;
#4130=CARTESIAN_POINT ( 'NONE',  ( -0.2206173157302028787, 0.1638888888888885287, 0.2206173157302027954 ) ) ;
#4132=CARTESIAN_POINT ( 'NONE',  ( -0.2124268279052486941, 5.112105532426204135, 0.2253721325002343290 ) ) ;
#4134=CARTESIAN_POINT ( 'NONE',  ( -0.3119999999999999996, 0.2159722222222218713, 0.1292346314604056190 ) ) ;
#4135=CARTESIAN_POINT ( 'NONE',  ( -1.910449006669871087E-17, 5.203555555555554157, -0.3119999999999999996 ) ) ;
#4136=VECTOR ( 'NONE', #20349, 39.37007874015748143 ) ;
#4137=CARTESIAN_POINT ( 'NONE',  ( -0.1993543840281266910, 4.304250000075866112, -0.1993543840281266910 ) ) ;
#4138=CARTESIAN_POINT ( 'NONE',  ( -7.331754493858430024E-07, 4.349360015129621004, 0.3119999999981767358 ) ) ;
#4145=CARTESIAN_POINT ( 'NONE',  ( 0.2819296736111110979, 4.713972222298087544, -3.452642723725051716E-17 ) ) ;
#4146=EDGE_CURVE ( 'NONE', #70, #14521, #19527, .T. ) ;
#4148=CARTESIAN_POINT ( 'NONE',  ( -0.03926412191686881603, 5.144338944773434896, -0.3013481353560393816 ) ) ;
#4151=EDGE_CURVE ( 'NONE', #9842, #14283, #21120, .T. ) ;
#4153=CARTESIAN_POINT ( 'NONE',  ( -0.2819296736111110979, 4.311194444520309865, 0.000000000000000000 ) ) ;
#4157=DIRECTION ( 'NONE',  ( -0.000000000000000000, -1.000000000000000000, -0.000000000000000000 ) ) ;
#4159=CARTESIAN_POINT ( 'NONE',  ( 0.1167790944451423257, 0.3930555554796889561, -0.2819296736111110424 ) ) ;
#4165=CARTESIAN_POINT ( 'NONE',  ( 5.731347020009612645E-17, 5.009111111111110404, 0.3119999999999999996 ) ) ;
#4166=CARTESIAN_POINT ( 'NONE',  ( 0.2819296736111110424, 0.5319444443685777957, 0.1167790944451424923 ) ) ;
#4167=CARTESIAN_POINT ( 'NONE',  ( -0.2819296736111110979, 0.2298611110352444808, -3.452642723725051716E-17 ) ) ;
#4169=CARTESIAN_POINT ( 'NONE',  ( 0.1167790944451424368, 4.273000000075865223, 0.2819296736111110424 ) ) ;
#4171=CARTESIAN_POINT ( 'NONE',  ( 0.1167790944451424368, 4.828555555631421470, 0.2819296736111110424 ) ) ;
#4172=CARTESIAN_POINT ( 'NONE',  ( -0.1167790944451423119, 4.175777777853643791, -0.2819296736111110979 ) ) ;
#4173=DIRECTION ( 'NONE',  ( -0.000000000000000000, -1.000000000000000000, -0.000000000000000000 ) ) ;
#4175=CARTESIAN_POINT ( 'NONE',  ( 5.731347020009612645E-17, 4.071611111262843252, 0.3119999999999999996 ) ) ;
#4176=CARTESIAN_POINT ( 'NONE',  ( 0.3119999999999999996, 0.1326388888888885564, -0.1292346314604056468 ) ) ;
#4184=CARTESIAN_POINT ( 'NONE',  ( -0.2901050598373867695, 5.005620093107005175, 0.1163399601593286398 ) ) ;
#4185=EDGE_CURVE ( 'NONE', #14020, #16668, #23768, .T. ) ;
#4187=CARTESIAN_POINT ( 'NONE',  ( 0.1292346314604056745, 0.6326388887371557912, -0.3119999999999999996 ) ) ;
#4189=ORIENTED_EDGE ( 'NONE', *, *, #666, .F. ) ;
#4200=CARTESIAN_POINT ( 'NONE',  ( -0.1167790944451423535, 4.029944444520309865, 0.2819296736111110424 ) ) ;
#4202=CARTESIAN_POINT ( 'NONE',  ( -0.1469396509590103761, 5.191462283868291117, 0.2486211279754877157 ) ) ;
#4203=CARTESIAN_POINT ( 'NONE',  ( -0.3119999999999999996, 4.776472222373953969, -0.1292346314604056468 ) ) ;
#4204=CARTESIAN_POINT ( 'NONE',  ( -0.1167790944451423535, 5.043833333409199149, 0.2819296736111110979 ) ) ;
#4206=CARTESIAN_POINT ( 'NONE',  ( 0.1167790944451424368, 4.203555555631420582, 0.2819296736111110424 ) ) ;
#4210=ORIENTED_EDGE ( 'NONE', *, *, #4085, .T. ) ;
#4214=CARTESIAN_POINT ( 'NONE',  ( 0.3119999999999999996, 0.2993055555555552139, -0.1292346314604056468 ) ) ;
#4215=CARTESIAN_POINT ( 'NONE',  ( 0.1993543840281266633, 3.845916666742533074, -0.1993543840281266910 ) ) ;
#4217=CARTESIAN_POINT ( 'NONE',  ( 0.1109400265990461154, 4.429522179582135344, -0.2916197229367319954 ) ) ;
#4218=CARTESIAN_POINT ( 'NONE',  ( 5.731347020009612645E-17, 4.620222222222221120, 0.3119999999999999996 ) ) ;
#4222=CARTESIAN_POINT ( 'NONE',  ( 0.2819296736111110424, 0.4902777777019112215, 0.1167790944451424923 ) ) ;
#4225=CARTESIAN_POINT ( 'NONE',  ( -0.2819296736111110424, 4.648000000075866112, 0.1167790944451424923 ) ) ;
#4228=CARTESIAN_POINT ( 'NONE',  ( 0.1993543840281267465, 4.651472222298087544, 0.1993543840281266633 ) ) ;
#4229=CARTESIAN_POINT ( 'NONE',  ( -0.008900482412455170203, 4.155199780624622363, -0.3118911708052335974 ) ) ;
#4230=CARTESIAN_POINT ( 'NONE',  ( 0.2914760784562323015, 4.866496372597516107, -0.1112933579050594812 ) ) ;
#4233=CARTESIAN_POINT ( 'NONE',  ( -0.2206173157302027676, 4.279944444444443441, 0.2206173157302028787 ) ) ;
#4235=CARTESIAN_POINT ( 'NONE',  ( 1.910449006669871087E-17, 0.5249999998482670627, -0.3119999999999999996 ) ) ;
#4237=CARTESIAN_POINT ( 'NONE',  ( 0.2729932625349638098, 4.590067353440807629, -0.1570725860997395085 ) ) ;
#4239=CARTESIAN_POINT ( 'NONE',  ( 0.2829332492628002238, 4.700467745438439593, -0.1315023910696823672 ) ) ;
#4241=CARTESIAN_POINT ( 'NONE',  ( 0.3072406530695101501, 4.639533684784892031, 0.05499356144264888613 ) ) ;
#4244=EDGE_CURVE ( 'NONE', #4444, #22975, #2605, .T. ) ;
#4246=CARTESIAN_POINT ( 'NONE',  ( 0.2492337893549602668, 4.301904822861448707, 0.1920667163975616487 ) ) ;
#4249=CARTESIAN_POINT ( 'NONE',  ( 0.1167790944451423257, 0.4347222221463555858, -0.2819296736111110424 ) ) ;
#4250=DIRECTION ( 'NONE',  ( 0.000000000000000000, 0.000000000000000000, -1.000000000000000000 ) ) ;
#4254=ADVANCED_FACE ( 'NONE', ( #20372 ), #1829, .T. ) ;
#4255=CARTESIAN_POINT ( 'NONE',  ( -0.1501324200702761902, 4.622704549112463646, 0.2735036765724895291 ) ) ;
#4258=CARTESIAN_POINT ( 'NONE',  ( 0.1292346314604057023, 0.2298611111111107663, 0.3119999999999998885 ) ) ;
#4259=CARTESIAN_POINT ( 'NONE',  ( 0.1292346314604056190, 5.144527777777776478, -0.3119999999999999996 ) ) ;
#4261=CARTESIAN_POINT ( 'NONE',  ( 0.2819296736111110979, 4.116750000075866112, -3.452642723725051716E-17 ) ) ;
#4262=CARTESIAN_POINT ( 'NONE',  ( -0.2495581641001925477, 4.329761746715313109, -0.1916607439132450852 ) ) ;
#4263=CARTESIAN_POINT ( 'NONE',  ( -0.1292346314604056190, 0.4729166665149337478, -0.3119999999999999996 ) ) ;
#4268=CARTESIAN_POINT ( 'NONE',  ( -1.726321361862525858E-17, 4.783416666742532186, -0.2819296736111110979 ) ) ;
#4273=CARTESIAN_POINT ( 'NONE',  ( -0.2819296736111110424, 4.259111111186976828, 0.1167790944451424923 ) ) ;
#4275=CARTESIAN_POINT ( 'NONE',  ( -0.01870657908477804665, 4.044342180066220926, -0.3114387789057476708 ) ) ;
#4278=CARTESIAN_POINT ( 'NONE',  ( -0.2819296736111110979, 0.4659722221463555303, -3.452642723725051716E-17 ) ) ;
#4279=CARTESIAN_POINT ( 'NONE',  ( 0.2206173157302027954, 4.141055555555554157, -0.2206173157302028232 ) ) ;
#4285=CARTESIAN_POINT ( 'NONE',  ( 0.1167790944451423119, 0.5458333332574668573, -0.2819296736111110979 ) ) ;
#4286=CARTESIAN_POINT ( 'NONE',  ( 1.726321361862525858E-17, 0.2715277777019111660, -0.2819296736111110979 ) ) ;
#4287=CARTESIAN_POINT ( 'NONE',  ( -0.2819296736111110979, 4.311194444520309865, 0.000000000000000000 ) ) ;
#4289=CARTESIAN_POINT ( 'NONE',  ( 0.2819296736111110979, 4.946611111186976828, 0.1167790944451422425 ) ) ;
#4290=CARTESIAN_POINT ( 'NONE',  ( -0.1993543840281266355, 4.137583333409199149, 0.1993543840281267465 ) ) ;
#4295=CARTESIAN_POINT ( 'NONE',  ( -0.3119999999999999996, 3.887583333485065573, -0.1292346314604056468 ) ) ;
#4301=CARTESIAN_POINT ( 'NONE',  ( -0.3127083509410205631, 5.002075493856721344, -0.005575882147177812359 ) ) ;
#4303=CARTESIAN_POINT ( 'NONE',  ( 0.1167790944451423257, 0.1708333332574666907, -0.2819296736111110424 ) ) ;
#4304=AXIS2_PLACEMENT_3D ( 'NONE', #2225, #11735, #4039 ) ;
#4306=CARTESIAN_POINT ( 'NONE',  ( 0.0003767400161662670839, 4.266045432495603862, -0.3119998056229988936 ) ) ;
#4310=CARTESIAN_POINT ( 'NONE',  ( 0.1707342748200432747, 5.171949696446763944, 0.2418557544016106398 ) ) ;
#4315=CARTESIAN_POINT ( 'NONE',  ( -0.2256633871477300712, 4.675584075455893718, 0.2154820786522459730 ) ) ;
#4316=CARTESIAN_POINT ( 'NONE',  ( 0.1167790944451424368, 4.092444444520309865, 0.2819296736111110424 ) ) ;
#4318=CARTESIAN_POINT ( 'NONE',  ( -0.2931282487914294022, 5.178805443644709072, -0.02438572332841970960 ) ) ;
#4319=CARTESIAN_POINT ( 'NONE',  ( -0.2206173157302028232, 4.550777777929510215, -0.2206173157302028232 ) ) ;
#4320=CARTESIAN_POINT ( 'NONE',  ( -1.726321361862525858E-17, 4.852861111186976828, -0.2819296736111110979 ) ) ;
#4323=CARTESIAN_POINT ( 'NONE',  ( -0.2819296736111110424, 4.356333333409198261, 0.1167790944451424923 ) ) ;
#4332=DIRECTION ( 'NONE',  ( -0.000000000000000000, -1.000000000000000000, -0.000000000000000000 ) ) ;
#4333=CARTESIAN_POINT ( 'NONE',  ( 0.1015009281151166981, 3.738732047420452620, -0.2819296736111110979 ) ) ;
#4334=DIRECTION ( 'NONE',  ( 0.000000000000000000, 0.000000000000000000, -1.000000000000000000 ) ) ;
#4338=CARTESIAN_POINT ( 'NONE',  ( -0.1167790944451422702, 0.5666666665908000056, -0.2819296736111110979 ) ) ;
#4341=CARTESIAN_POINT ( 'NONE',  ( -0.1167790944451423257, 4.634111111186976828, -0.2819296736111110424 ) ) ;
#4343=CARTESIAN_POINT ( 'NONE',  ( -0.1167790944451423257, 4.620222222298087544, -0.2819296736111110424 ) ) ;
#4344=CARTESIAN_POINT ( 'NONE',  ( 0.3119999999999999996, 0.2888888887371559577, 0.000000000000000000 ) ) ;
#4345=CARTESIAN_POINT ( 'NONE',  ( 0.2810189208971028973, 4.867268483421598901, -0.1357210265892402346 ) ) ;
#4348=CARTESIAN_POINT ( 'NONE',  ( -0.2206173157302028232, 4.266055555555555046, -0.2206173157302028232 ) ) ;
#4349=CARTESIAN_POINT ( 'NONE',  ( -0.1993543840281266355, 3.859805555631421026, 0.1993543840281267465 ) ) ;
#4354=VERTEX_POINT ( 'NONE', #22436 ) ;
#4357=DESIGN_CONTEXT ( 'detailed design', #16368, 'design' ) ;
#4359=CARTESIAN_POINT ( 'NONE',  ( 0.1913906330737462635, 4.133038910390919973, 0.2464018815271727947 ) ) ;
#4361=CARTESIAN_POINT ( 'NONE',  ( -8.379073922441706732E-07, 4.293833316950179224, 0.3119999999988748440 ) ) ;
#4364=CARTESIAN_POINT ( 'NONE',  ( -0.2819296736111110979, 0.5631944443685777957, -3.452642723725051716E-17 ) ) ;
#4365=CYLINDRICAL_SURFACE ( 'NONE', #16779, 0.3119999999999999996 ) ;
#4373=CARTESIAN_POINT ( 'NONE',  ( -0.1292346314604056190, 0.3131944444444441089, -0.3119999999999999996 ) ) ;
#4374=CARTESIAN_POINT ( 'NONE',  ( 0.3119999999999999996, 4.967444444444443441, -3.820898013339742174E-17 ) ) ;
#4375=CARTESIAN_POINT ( 'NONE',  ( -0.1167790944451423257, 4.078555555631421470, -0.2819296736111110424 ) ) ;
#4376=CARTESIAN_POINT ( 'NONE',  ( -0.3119777406883143533, 4.336685373751207884, 0.04102447248701817512 ) ) ;
#4378=CARTESIAN_POINT ( 'NONE',  ( 0.3105117338273140071, 4.808796746528941846, -0.03833085760703142109 ) ) ;
#4384=CARTESIAN_POINT ( 'NONE',  ( 0.2819296736111110424, 4.717444444520309865, -0.1167790944451423396 ) ) ;
#4391=CARTESIAN_POINT ( 'NONE',  ( -0.2819296736111110979, 4.418833333409199149, -0.1167790944451422980 ) ) ;
#4392=CARTESIAN_POINT ( 'NONE',  ( -0.3077216217399622589, 4.056174970759743204, -0.05514810450480703979 ) ) ;
#4396=CARTESIAN_POINT ( 'NONE',  ( -5.178964085587577574E-17, 0.3687499999241333204, 0.2819296736111110979 ) ) ;
#4399=LINE ( 'NONE', #11861, #8394 ) ;
#4403=CARTESIAN_POINT ( 'NONE',  ( -7.892860322346445127E-13, 5.206640035683665957, 0.2819296736111106538 ) ) ;
#4404=CARTESIAN_POINT ( 'NONE',  ( 1.726321361862525858E-17, 0.4937499999241333759, -0.2819296736111110979 ) ) ;
#4405=CARTESIAN_POINT ( 'NONE',  ( -5.178964085587577574E-17, 0.1881944443685778512, 0.2819296736111110979 ) ) ;
#4406=ORIENTED_EDGE ( 'NONE', *, *, #14382, .T. ) ;
#4407=CARTESIAN_POINT ( 'NONE',  ( 0.2819296736111110424, 4.175777777853643791, -0.1167790944451423396 ) ) ;
#4409=CARTESIAN_POINT ( 'NONE',  ( 0.2819296736111110979, 4.783416666742532186, -3.452642723725051716E-17 ) ) ;
#4410=EDGE_CURVE ( 'NONE', #16571, #20545, #8035, .T. ) ;
#4411=CARTESIAN_POINT ( 'NONE',  ( 0.3089396748338966714, 5.077109074767299113, 0.05201469694613055500 ) ) ;
#4412=EDGE_CURVE ( 'NONE', #14624, #10770, #6879, .T. ) ;
#4415=CARTESIAN_POINT ( 'NONE',  ( -0.2206173157302028232, 3.828555555707287894, -0.2206173157302028232 ) ) ;
#4422=CARTESIAN_POINT ( 'NONE',  ( -0.03922383558181956331, 5.014860061204379882, 0.3120000079912765845 ) ) ;
#4423=ORIENTED_EDGE ( 'NONE', *, *, #14087, .T. ) ;
#4424=CARTESIAN_POINT ( 'NONE',  ( 0.1167790944451423535, 0.1499999999241333759, 0.2819296736111110424 ) ) ;
#4425=CARTESIAN_POINT ( 'NONE',  ( 0.2723612931040907958, 4.247528608451006882, 0.1575966107290118767 ) ) ;
#4434=CARTESIAN_POINT ( 'NONE',  ( -0.2819296736111110979, 4.075083333409199149, 0.000000000000000000 ) ) ;
#4435=CARTESIAN_POINT ( 'NONE',  ( 0.07786113151988235948, 5.041682425470480844, -0.3026906604598632033 ) ) ;
#4436=CARTESIAN_POINT ( 'NONE',  ( -0.2638604546507810622, 5.184694301399809468, 0.1249839293704117366 ) ) ;
#4437=CARTESIAN_POINT ( 'NONE',  ( -0.3119999999999999996, 4.502166666818398610, 0.000000000000000000 ) ) ;
#4438=CARTESIAN_POINT ( 'NONE',  ( 0.2819296736111111534, 4.835500000075866112, 0.1167790944451422563 ) ) ;
#4439=EDGE_LOOP ( 'NONE', ( #15957, #13604, #16612, #461 ) ) ;
#4440=CARTESIAN_POINT ( 'NONE',  ( -0.2819296736111110424, 3.967444444520310309, 0.1167790944451424923 ) ) ;
#4444=VERTEX_POINT ( 'NONE', #2559 ) ;
#4452=CARTESIAN_POINT ( 'NONE',  ( -0.3119999999999999996, 0.1534722220704892726, 0.1292346314604056190 ) ) ;
#4453=CARTESIAN_POINT ( 'NONE',  ( 0.1764925855509518193, 5.136404133670642302, 0.2495434643755579940 ) ) ;
#4458=CARTESIAN_POINT ( 'NONE',  ( -0.2819296736111111534, 0.1222222221463555719, 0.1167790944451422563 ) ) ;
#4461=CARTESIAN_POINT ( 'NONE',  ( 0.2819296736111110424, 4.675777777853643791, -0.1167790944451423396 ) ) ;
#4463=CARTESIAN_POINT ( 'NONE',  ( 0.2819296736111110979, 4.599388888964753619, 0.1167790944451422425 ) ) ;
#4464=CARTESIAN_POINT ( 'NONE',  ( -0.0006352866450341495630, 4.154962694833915116, -0.3119993937163639264 ) ) ;
#4465=CARTESIAN_POINT ( 'NONE',  ( 0.3080281032009763997, 4.865139504843591034, -0.06764252334466071270 ) ) ;
#4468=CARTESIAN_POINT ( 'NONE',  ( -0.3119999999999999996, 4.272999999999998799, 0.000000000000000000 ) ) ;
#4471=CARTESIAN_POINT ( 'NONE',  ( 0.06396586966202466584, 4.962292326657688157, 0.3053748286811586166 ) ) ;
#4477=CARTESIAN_POINT ( 'NONE',  ( 0.01791502114354955391, 4.710015879029342045, -0.3115078771295382576 ) ) ;
#4478=CARTESIAN_POINT ( 'NONE',  ( 0.1918308770790998485, 4.133054567813140068, 0.2460591670449067125 ) ) ;
#4481=CARTESIAN_POINT ( 'NONE',  ( -0.004466634099735791383, 3.932848888112731700, -0.3119725945497263675 ) ) ;
#4484=CARTESIAN_POINT ( 'NONE',  ( 0.2819296736111110424, 0.4763888888130222710, 0.1167790944451424923 ) ) ;
#4492=LINE ( 'NONE', #9876, #22974 ) ;
#4494=CARTESIAN_POINT ( 'NONE',  ( 0.2206173157302027954, 4.752166666666665762, -0.2206173157302028232 ) ) ;
#4495=CARTESIAN_POINT ( 'NONE',  ( -0.3119999999999999996, 0.5423611111111107386, -0.1292346314604056745 ) ) ;
#4496=CARTESIAN_POINT ( 'NONE',  ( 0.3119999999999999996, 4.963972222222222008, 0.1292346314604056190 ) ) ;
#4498=CARTESIAN_POINT ( 'NONE',  ( -0.1993543840281266355, 3.873694444520310309, 0.1993543840281267465 ) ) ;
#4499=CARTESIAN_POINT ( 'NONE',  ( -0.3119999999999998885, 3.832027777777776922, 0.1292346314604058410 ) ) ;
#4503=EDGE_LOOP ( 'NONE', ( #13855, #19529, #22628, #10807 ) ) ;
#4504=CARTESIAN_POINT ( 'NONE',  ( -0.2494960723420805160, 4.008026183271772958, 0.1917385534842481476 ) ) ;
#4505=CARTESIAN_POINT ( 'NONE',  ( -0.1993543840281266355, 4.748694444520309865, 0.1993543840281267465 ) ) ;
#4506=VECTOR ( 'NONE', #21405, 39.37007874015748143 ) ;
#4507=CARTESIAN_POINT ( 'NONE',  ( -0.03928873229836517267, 5.166389717777303936, 0.2957448058751782627 ) ) ;
#4512=CARTESIAN_POINT ( 'NONE',  ( 0.2819296736111110979, 4.227861111186976828, -3.452642723725051716E-17 ) ) ;
#4513=CARTESIAN_POINT ( 'NONE',  ( -0.1292346314604105872, 4.873694444444444329, -0.3119999999999950591 ) ) ;
#4515=CARTESIAN_POINT ( 'NONE',  ( 0.000000000000000000, 5.384999999999999787, 0.000000000000000000 ) ) ;
#4516=ORIENTED_EDGE ( 'NONE', *, *, #369, .F. ) ;
#4518=CARTESIAN_POINT ( 'NONE',  ( -0.1993543840281266633, 0.5145833332574667462, -0.1993543840281266910 ) ) ;
#4520=EDGE_CURVE ( 'NONE', #11205, #23206, #6006, .T. ) ;
#4528=CARTESIAN_POINT ( 'NONE',  ( -0.2819296736111110979, 0.4486111110352445364, -0.1167790944451423396 ) ) ;
#4529=CARTESIAN_POINT ( 'NONE',  ( -0.1167790944451424368, 0.2958333332574667462, 0.2819296736111110424 ) ) ;
#4530=CARTESIAN_POINT ( 'NONE',  ( -0.1167790944451423257, 3.967444444520310309, -0.2819296736111110424 ) ) ;
#4533=CARTESIAN_POINT ( 'NONE',  ( -0.1993543840281266355, 4.540361111186976828, 0.1993543840281267465 ) ) ;
#4534=CARTESIAN_POINT ( 'NONE',  ( 0.2690855894900002210, 5.073817426067109615, 0.1585580871995575791 ) ) ;
#4535=EDGE_LOOP ( 'NONE', ( #14464, #1404, #12647, #15872 ) ) ;
#4538=CARTESIAN_POINT ( 'NONE',  ( 0.1292346314604058410, 3.852861111262843696, 0.3119999999999998885 ) ) ;
#4541=ORIENTED_EDGE ( 'NONE', *, *, #9010, .T. ) ;
#4545=CARTESIAN_POINT ( 'NONE',  ( -0.2902335162209870867, 4.998847991299789406, -0.1145027670670989706 ) ) ;
#4546=ORIENTED_EDGE ( 'NONE', *, *, #9191, .F. ) ;
#4547=CARTESIAN_POINT ( 'NONE',  ( -0.1993543840281267465, 0.08402777770191115214, 0.1993543840281266633 ) ) ;
#4551=CARTESIAN_POINT ( 'NONE',  ( -0.2832489717015474473, 4.728264267671256960, 0.1346859133935131569 ) ) ;
#4555=B_SPLINE_CURVE_WITH_KNOTS ( 'NONE', 3,
 ( #3404, #9015, #16457, #23869, #5350, #12817, #20234, #3525, #10976, #18401, #13408, #20710, #17415, #22661, #11947, #19121, #19362, #19010, #2305, #8136, #22777, #22542, #4481, #9990, #9498, #17294, #6189, #9620, #9743, #15469 ),
 .UNSPECIFIED., .F., .F.,
 ( 4, 2, 2, 2, 2, 2, 2, 2, 2, 2, 1, 1, 1, 1, 1, 1, 2, 4 ),
 ( 0.8315072053056934420, 0.8337924113469056264, 0.8360776173881179218, 0.8383628234293301063, 0.8406480294705422907, 0.8429332355117545861, 0.8452184415529667705, 0.8475036475941790659, 0.8486462506147851581, 0.8492175521250882042, 0.8495032028802397273, 0.8496460282578154333, 0.8497174409466033973, 0.8497531472909972683, 0.8497710004631943148, 0.8497799270492927270, 0.8497843903423419887, 0.8497888536353912503 ),
 .UNSPECIFIED. ) ;
#4558=ORIENTED_EDGE ( 'NONE', *, *, #4078, .F. ) ;
#4560=CARTESIAN_POINT ( 'NONE',  ( 5.178964085587577574E-17, 3.811194444520309865, 0.2819296736111110979 ) ) ;
#4561=CARTESIAN_POINT ( 'NONE',  ( -0.3119999999999999996, 0.09097222207048930032, -0.1292346314604056745 ) ) ;
#4562=CARTESIAN_POINT ( 'NONE',  ( 5.731347020009612645E-17, 4.342444444444443441, 0.3119999999999999996 ) ) ;
#4563=LINE ( 'NONE', #12022, #5805 ) ;
#4564=CARTESIAN_POINT ( 'NONE',  ( 0.3119999999999999996, 4.470916666818398610, 0.1292346314604056190 ) ) ;
#4565=CARTESIAN_POINT ( 'NONE',  ( 0.2819296736111111534, 4.668833333409200037, 0.1167790944451422563 ) ) ;
#4567=CARTESIAN_POINT ( 'NONE',  ( -0.1993543840281266355, 4.082027777853643791, 0.1993543840281267465 ) ) ;
#4572=ORIENTED_EDGE ( 'NONE', *, *, #6592, .F. ) ;
#4578=CARTESIAN_POINT ( 'NONE',  ( 0.2206173157302028232, 0.01805555540382262902, -0.2206173157302028232 ) ) ;
#4583=CARTESIAN_POINT ( 'NONE',  ( 0.1993543840281266355, 0.08402777770191115214, 0.1993543840281267465 ) ) ;
#4587=EDGE_CURVE ( 'NONE', #12971, #7634, #22825, .T. ) ;
#4588=CARTESIAN_POINT ( 'NONE',  ( -0.1167790944451423535, 4.585500000075865223, 0.2819296736111110424 ) ) ;
#4593=CARTESIAN_POINT ( 'NONE',  ( -0.3119999999999999996, 4.325083333333331836, -0.1292346314604056468 ) ) ;
#4595=CARTESIAN_POINT ( 'NONE',  ( 0.3119999999999999996, 5.193138889040620043, 0.1292346314604056190 ) ) ;
#4596=CARTESIAN_POINT ( 'NONE',  ( 0.3112369449188003290, 4.973790024703991897, 0.02198042532292469528 ) ) ;
#4599=VERTEX_POINT ( 'NONE', #21562 ) ;
#4604=CARTESIAN_POINT ( 'NONE',  ( -0.3119999999999999996, 4.439666666666665762, 0.000000000000000000 ) ) ;
#4606=CARTESIAN_POINT ( 'NONE',  ( -0.2819296736111110979, 0.07708333325746669074, -3.452642723725051716E-17 ) ) ;
#4612=CARTESIAN_POINT ( 'NONE',  ( -0.1432526013158665901, 4.622930756421714804, 0.2772325657423325707 ) ) ;
#4613=CARTESIAN_POINT ( 'NONE',  ( -0.1785261131399872025, 4.288481118505546696, 0.2582360697992498455 ) ) ;
#4615=CARTESIAN_POINT ( 'NONE',  ( 1.910449006669871087E-17, 0.3652777777777774237, -0.3119999999999999996 ) ) ;
#4616=CARTESIAN_POINT ( 'NONE',  ( -0.3119999999999999996, 5.050777777777776478, 0.000000000000000000 ) ) ;
#4617=CARTESIAN_POINT ( 'NONE',  ( 0.2819296736111110424, 4.064666666742532186, -0.1167790944451423396 ) ) ;
#4623=CYLINDRICAL_SURFACE ( 'NONE', #13248, 0.3119999999999999996 ) ;
#4624=CARTESIAN_POINT ( 'NONE',  ( -0.2819296736111110424, 4.627166666742532186, -0.1167790944451423119 ) ) ;
#4625=CARTESIAN_POINT ( 'NONE',  ( 1.995346317926969793E-07, 4.516063323326865664, 0.3119999999998666063 ) ) ;
#4629=CARTESIAN_POINT ( 'NONE',  ( 0.1993543840281266633, 4.012583333409199149, -0.1993543840281266910 ) ) ;
#4632=CARTESIAN_POINT ( 'NONE',  ( 0.03162548898803060199, 5.072453936747297831, 0.3108465394227510337 ) ) ;
#4638=CARTESIAN_POINT ( 'NONE',  ( 1.726321361862525858E-17, 0.1048611110352444808, -0.2819296736111110979 ) ) ;
#4640=LINE ( 'NONE', #15860, #4687 ) ;
#4641=FACE_OUTER_BOUND ( 'NONE', #159, .T. ) ;
#4644=CARTESIAN_POINT ( 'NONE',  ( -1.853979398150703436E-06, 4.543833384706993606, -0.3119999999944916280 ) ) ;
#4645=CARTESIAN_POINT ( 'NONE',  ( -0.2819296736111110979, 0.3965277777019111660, -3.452642723725051716E-17 ) ) ;
#4646=CARTESIAN_POINT ( 'NONE',  ( 0.1167790944451423257, 0.5458333332574666352, -0.2819296736111110424 ) ) ;
#4647=CARTESIAN_POINT ( 'NONE',  ( -0.2819296736111110424, 4.085500000075865223, -0.1167790944451423119 ) ) ;
#4649=CARTESIAN_POINT ( 'NONE',  ( 0.1167790944451424368, 4.661888888964754507, 0.2819296736111110424 ) ) ;
#4651=CARTESIAN_POINT ( 'NONE',  ( 0.2896569607109293898, 5.081861310233479756, -0.1164848292807667690 ) ) ;
#4654=CARTESIAN_POINT ( 'NONE',  ( -0.2206173157302028232, 3.773000000151732092, -0.2206173157302028232 ) ) ;
#4657=VECTOR ( 'NONE', #19383, 39.37007874015748143 ) ;
#4659=CARTESIAN_POINT ( 'NONE',  ( 0.2610103255563372415, 0.03242967361111056407, 0.1075682626660545288 ) ) ;
#4664=CARTESIAN_POINT ( 'NONE',  ( -0.01780398822517776855, 4.571142336066150946, 0.3116242173092940715 ) ) ;
#4666=CARTESIAN_POINT ( 'NONE',  ( -0.2819296736111110979, 0.1326388888130222710, -3.452642723725051716E-17 ) ) ;
#4668=CARTESIAN_POINT ( 'NONE',  ( 0.2819296736111110979, -0.006250000075866630166, 0.000000000000000000 ) ) ;
#4669=CARTESIAN_POINT ( 'NONE',  ( -0.1761266028516242366, 4.732970605661459551, 0.2598151860325674800 ) ) ;
#4672=CARTESIAN_POINT ( 'NONE',  ( -0.02115692209977381583, 5.070961635096757014, 0.3120000024408280948 ) ) ;
#4675=VECTOR ( 'NONE', #16181, 39.37007874015748143 ) ;
#4676=CARTESIAN_POINT ( 'NONE',  ( -0.2890877230579003143, 4.665425013968962809, -0.1173655244367800971 ) ) ;
#4677=CARTESIAN_POINT ( 'NONE',  ( -0.1993543840281266910, 5.248694444520310753, -0.1993543840281266910 ) ) ;
#4678=CARTESIAN_POINT ( 'NONE',  ( -0.1292346314604056190, 0.08402777762604483891, -0.3119999999999999996 ) ) ;
#4679=CARTESIAN_POINT ( 'NONE',  ( -0.2631359636943425562, 5.174404950919535118, -0.1348571213356563603 ) ) ;
#4680=CARTESIAN_POINT ( 'NONE',  ( -0.3102357779240257352, 4.778494202458470674, -0.05181659030984726161 ) ) ;
#4681=CARTESIAN_POINT ( 'NONE',  ( -0.3119999999999998885, 4.616750000151732536, 0.1292346314604058410 ) ) ;
#4682=CARTESIAN_POINT ( 'NONE',  ( 5.178964085587577574E-17, 4.658416666742532186, 0.2819296736111110979 ) ) ;
#4683=ORIENTED_EDGE ( 'NONE', *, *, #7642, .F. ) ;
#4684=CARTESIAN_POINT ( 'NONE',  ( 0.1993543840281266633, 3.998694444520309865, -0.1993543840281266910 ) ) ;
#4687=VECTOR ( 'NONE', #6468, 39.37007874015748143 ) ;
#4689=EDGE_CURVE ( 'NONE', #6065, #1879, #23621, .T. ) ;
#4692=CARTESIAN_POINT ( 'NONE',  ( 0.1292346314604056745, 0.07708333318160039138, -0.3119999999999999996 ) ) ;
#4694=CARTESIAN_POINT ( 'NONE',  ( 0.1292346314604056745, 0.1881944442927115102, -0.3119999999999999996 ) ) ;
#4698=CARTESIAN_POINT ( 'NONE',  ( 0.2819296736111110979, 0.1465277777019111383, 0.000000000000000000 ) ) ;
#4701=CARTESIAN_POINT ( 'NONE',  ( 0.2819296736111110979, 4.547305555631421470, -3.452642723725051716E-17 ) ) ;
#4705=CARTESIAN_POINT ( 'NONE',  ( 0.2206173157302028232, 0.4624999998482670627, -0.2206173157302028232 ) ) ;
#4706=CARTESIAN_POINT ( 'NONE',  ( -0.3119999999999998885, 4.387583333333331836, 0.1292346314604058410 ) ) ;
#4708=CARTESIAN_POINT ( 'NONE',  ( -0.2206173157302027676, 5.175777777929509327, 0.2206173157302028787 ) ) ;
#4709=CARTESIAN_POINT ( 'NONE',  ( 5.731347020009612645E-17, 4.675777777777777366, 0.3119999999999999996 ) ) ;
#4717=CARTESIAN_POINT ( 'NONE',  ( 0.3119999807920359469, 3.806624880628000085, 0.04084226214478610395 ) ) ;
#4719=CARTESIAN_POINT ( 'NONE',  ( 0.2819296736111110424, 0.04583333325746670461, 0.1167790944451424923 ) ) ;
#4726=CARTESIAN_POINT ( 'NONE',  ( -0.1736506380193462984, 4.271243467713559561, -0.2598347738710399257 ) ) ;
#4728=CARTESIAN_POINT ( 'NONE',  ( -0.1292346314604058410, 0.3895833333333328929, 0.3119999999999998885 ) ) ;
#4729=CARTESIAN_POINT ( 'NONE',  ( 0.3119999999999999996, 5.022999999999999687, -3.820898013339742174E-17 ) ) ;
#4730=CARTESIAN_POINT ( 'NONE',  ( -0.2819296736111110979, 4.186194444520309865, 0.000000000000000000 ) ) ;
#4731=CARTESIAN_POINT ( 'NONE',  ( 0.2819296736111110424, 4.009111111186976828, -0.1167790944451423396 ) ) ;
#4735=ORIENTED_EDGE ( 'NONE', *, *, #9191, .T. ) ;
#4737=CARTESIAN_POINT ( 'NONE',  ( -0.1993543840281266355, 4.415361111186976828, 0.1993543840281267465 ) ) ;
#4738=CARTESIAN_POINT ( 'NONE',  ( -0.1987419572019689940, 5.161870250129094728, 0.2237073997642387846 ) ) ;
#4744=CARTESIAN_POINT ( 'NONE',  ( 0.2819296736111110979, 4.175777777853643791, -0.1167790944451423396 ) ) ;
#4745=CARTESIAN_POINT ( 'NONE',  ( -0.3125412538830298903, 4.835929051231298459, 0.01504738431389416112 ) ) ;
#4749=CARTESIAN_POINT ( 'NONE',  ( 0.1167790944451423535, 0.1361111110352444808, 0.2819296736111110424 ) ) ;
#4755=CARTESIAN_POINT ( 'NONE',  ( 0.2206173157302028787, 3.960499999999999243, 0.2206173157302027954 ) ) ;
#4758=CARTESIAN_POINT ( 'NONE',  ( 0.2819296736111110979, 0.4798611110352444808, 0.000000000000000000 ) ) ;
#4759=CARTESIAN_POINT ( 'NONE',  ( -0.1993543840281266355, 4.151472222298088433, 0.1993543840281267465 ) ) ;
#4763=CARTESIAN_POINT ( 'NONE',  ( 0.2819296736111110424, 4.620222222298088433, -0.1167790944451423396 ) ) ;
#4764=CARTESIAN_POINT ( 'NONE',  ( 0.2439254949411622519, 5.136159674610036419, -0.1850816115523053751 ) ) ;
#4765=CARTESIAN_POINT ( 'NONE',  ( -5.731347020009612645E-17, 0.3861111109593781676, 0.3119999999999999996 ) ) ;
#4768=CARTESIAN_POINT ( 'NONE',  ( 0.2206173157302027954, 3.814666666818399055, -0.2206173157302028232 ) ) ;
#4771=( BOUNDED_CURVE ( )  B_SPLINE_CURVE ( 2, ( #754, #23055, #13810, #8788, #23769, #9036, #9274, #1358, #21835 ),
 .UNSPECIFIED., .F., .F. ) 
 B_SPLINE_CURVE_WITH_KNOTS ( ( 3, 2, 2, 2, 3 ),
 ( 0.1875000000000000000, 0.1979166666666666574, 0.2083333333333333426, 0.2187500000000000000, 0.2291666666666666574 ),
 .UNSPECIFIED. ) 
 CURVE ( )  GEOMETRIC_REPRESENTATION_ITEM ( )  RATIONAL_B_SPLINE_CURVE ( ( 1.000000000000000000, 0.9238795325112867385, 1.000000000000000000, 0.9238795325112867385, 1.000000000000000000, 0.9238795325112867385, 1.000000000000000000, 0.9238795325112867385, 1.000000000000000000 ) ) 
 REPRESENTATION_ITEM ( '' )  );
#4774=CARTESIAN_POINT ( 'NONE',  ( 5.178964085587577574E-17, 4.811194444520309865, 0.2819296736111110979 ) ) ;
#4778=CARTESIAN_POINT ( 'NONE',  ( -0.3072307265066616666, 5.116075199176159494, 0.03881433307613120498 ) ) ;
#4779=CARTESIAN_POINT ( 'NONE',  ( 0.3119999999999999996, 0.2402777777777774515, 0.000000000000000000 ) ) ;
#4781=CARTESIAN_POINT ( 'NONE',  ( 0.1167790944451423535, 0.3722222221463555858, 0.2819296736111110424 ) ) ;
#4782=CARTESIAN_POINT ( 'NONE',  ( 0.1167790944451423257, 0.1152777777019111521, -0.2819296736111110424 ) ) ;
#4784=CARTESIAN_POINT ( 'NONE',  ( 0.1971363941232131822, 4.093330204894787272, -0.2454781584649298742 ) ) ;
#4789=CARTESIAN_POINT ( 'NONE',  ( -0.2884725026384663549, 4.665377838955494738, -0.1188664842351418310 ) ) ;
#4790=CARTESIAN_POINT ( 'NONE',  ( -1.726321361862525858E-17, 3.838972222298087544, -0.2819296736111110979 ) ) ;
#4794=CARTESIAN_POINT ( 'NONE',  ( 0.1839153728783990138, 0.05322839143466908535, 0.2408560696376421950 ) ) ;
#4796=CARTESIAN_POINT ( 'NONE',  ( -0.3119999999999999996, 4.613277777929510215, 0.000000000000000000 ) ) ;
#4799=CARTESIAN_POINT ( 'NONE',  ( 0.2819296736111110979, 4.731333333409200925, -0.1167790944451423396 ) ) ;
#4800=CARTESIAN_POINT ( 'NONE',  ( 0.2819296736111110979, 4.154944444520309865, 0.1167790944451422425 ) ) ;
#4807=CARTESIAN_POINT ( 'NONE',  ( 0.3119999999999999996, 0.07013888873715595773, -0.1292346314604056468 ) ) ;
#4812=ORIENTED_EDGE ( 'NONE', *, *, #8726, .F. ) ;
#4816=CARTESIAN_POINT ( 'NONE',  ( -1.726321361862525858E-17, 4.394527777853643791, -0.2819296736111110979 ) ) ;
#4817=DIRECTION ( 'NONE',  ( 0.000000000000000000, 0.000000000000000000, -1.000000000000000000 ) ) ;
#4820=CARTESIAN_POINT ( 'NONE',  ( 0.1292346314604056745, 0.4659722220704892726, -0.3119999999999999996 ) ) ;
#4821=CARTESIAN_POINT ( 'NONE',  ( -0.2206173157302028232, 4.099388888888888083, -0.2206173157302028232 ) ) ;
#4822=CARTESIAN_POINT ( 'NONE',  ( -1.910449006669871087E-17, 5.210500000151731648, -0.3119999999999999996 ) ) ;
#4824=CARTESIAN_POINT ( 'NONE',  ( 0.06147612581608680876, 4.962219778033143847, 0.3058837411390394889 ) ) ;
#4825=VERTEX_POINT ( 'NONE', #18029 ) ;
#4835=CARTESIAN_POINT ( 'NONE',  ( 1.679791495769851560E-14, 3.793833333485275183, 0.3119999999999999996 ) ) ;
#4837=EDGE_CURVE ( 'NONE', #13879, #17157, #9512, .T. ) ;
#4842=CARTESIAN_POINT ( 'NONE',  ( -0.1167790944451423257, 5.245222222298087544, -0.2819296736111110424 ) ) ;
#4844=ORIENTED_EDGE ( 'NONE', *, *, #10204, .T. ) ;
#4848=CARTESIAN_POINT ( 'NONE',  ( 1.910449006669871087E-17, 0.4208333333333330040, -0.3119999999999999996 ) ) ;
#4849=CARTESIAN_POINT ( 'NONE',  ( -0.3119999999999999996, 4.995222222222221120, 0.000000000000000000 ) ) ;
#4850=CARTESIAN_POINT ( 'NONE',  ( -0.2819296736111110979, 4.130638888964754507, 0.000000000000000000 ) ) ;
#4851=CARTESIAN_POINT ( 'NONE',  ( 5.178964085587577574E-17, 3.991750000075865223, 0.2819296736111110979 ) ) ;
#4852=EDGE_CURVE ( 'NONE', #3183, #21365, #11015, .T. ) ;
#4858=CARTESIAN_POINT ( 'NONE',  ( 0.2782497666485165277, 0.06249891821425377497, 0.1411420113220940853 ) ) ;
#4859=CARTESIAN_POINT ( 'NONE',  ( 0.1167790944451424368, 4.425777777853643791, 0.2819296736111110424 ) ) ;
#4862=VECTOR ( 'NONE', #6885, 39.37007874015748143 ) ;
#4863=MECHANICAL_CONTEXT ( 'NONE', #6704, 'mechanical' ) ;
#4864=DIRECTION ( 'NONE',  ( -0.000000000000000000, -1.000000000000000000, -0.000000000000000000 ) ) ;
#4866=CARTESIAN_POINT ( 'NONE',  ( -0.1993543840281266355, 4.095916666742533074, 0.1993543840281267465 ) ) ;
#4868=CARTESIAN_POINT ( 'NONE',  ( -0.02489526420108369512, 4.822334970157831968, -0.3110451136060463639 ) ) ;
#4873=CARTESIAN_POINT ( 'NONE',  ( 0.2819296736111110424, -0.01666666674253329886, -0.1167790944451423119 ) ) ;
#4881=CYLINDRICAL_SURFACE ( 'NONE', #6766, 0.3119999999999999996 ) ;
#4882=CARTESIAN_POINT ( 'NONE',  ( -0.1571243772177107201, 3.826150417953878780, -0.2726240822627857274 ) ) ;
#4883=CARTESIAN_POINT ( 'NONE',  ( -0.2819296736111110424, 0.4486111110352445364, -0.1167790944451423396 ) ) ;
#4884=CARTESIAN_POINT ( 'NONE',  ( 0.1993543840281267465, 3.998694444520310753, 0.1993543840281266633 ) ) ;
#4887=AXIS2_PLACEMENT_3D ( 'NONE', #10325, #12282, #12403 ) ;
#4888=ORIENTED_EDGE ( 'NONE', *, *, #6476, .F. ) ;
#4889=CARTESIAN_POINT ( 'NONE',  ( -0.1993543840281266910, 4.637583333409199149, -0.1993543840281266910 ) ) ;
#4891=CARTESIAN_POINT ( 'NONE',  ( 0.3041335845296361806, 5.131942972423729543, -0.03838084752963767665 ) ) ;
#4892=CARTESIAN_POINT ( 'NONE',  ( 0.1120921421618772951, 5.088976381486351563, -0.2921505626564902536 ) ) ;
#4893=VERTEX_POINT ( 'NONE', #22886 ) ;
#4894=CARTESIAN_POINT ( 'NONE',  ( -0.2819296736111110424, 5.078555555631420582, 0.1167790944451424923 ) ) ;
#4896=CARTESIAN_POINT ( 'NONE',  ( 0.2769513040667488379, 4.192351017494014620, 0.1439006775907332447 ) ) ;
#4899=CARTESIAN_POINT ( 'NONE',  ( 0.2819296736111111534, 4.932722222298088433, 0.1167790944451422563 ) ) ;
#4903=CARTESIAN_POINT ( 'NONE',  ( -0.04028049885296762500, 5.101242447252128720, -0.3082635314558828665 ) ) ;
#4904=CARTESIAN_POINT ( 'NONE',  ( -0.1019862276394089551, 4.568705723659588713, 0.2955327530433858318 ) ) ;
#4906=CARTESIAN_POINT ( 'NONE',  ( -0.1993543840281266633, 0.4034722221463555858, -0.1993543840281266910 ) ) ;
#4908=CARTESIAN_POINT ( 'NONE',  ( 0.1993543840281266355, 0.04236111103524448085, 0.1993543840281267465 ) ) ;
#4912=CARTESIAN_POINT ( 'NONE',  ( -0.2294867466249408405, 5.064319674093950674, 0.2113761149445206045 ) ) ;
#4916=CARTESIAN_POINT ( 'NONE',  ( -0.1993543840281266910, 4.693138888964754507, -0.1993543840281266910 ) ) ;
#4917=CYLINDRICAL_SURFACE ( 'NONE', #11719, 0.3119999999999999996 ) ;
#4918=CARTESIAN_POINT ( 'NONE',  ( 0.2819296736111110979, 3.880638888964754063, -3.452642723725051716E-17 ) ) ;
#4920=CARTESIAN_POINT ( 'NONE',  ( 0.1902774475453257452, 5.021827821991241336, 0.2506361051183713107 ) ) ;
#4923=CARTESIAN_POINT ( 'NONE',  ( 0.3119999999999999996, 4.196611111262843252, -3.820898013339742174E-17 ) ) ;
#4924=CARTESIAN_POINT ( 'NONE',  ( 0.1167790944451422702, 4.738277777853642903, -0.2819296736111110979 ) ) ;
#4925=( BOUNDED_CURVE ( )  B_SPLINE_CURVE ( 2, ( #1841, #24029, #14543, #21965, #12969, #14903, #22088, #20146, #7339 ),
 .UNSPECIFIED., .F., .F. ) 
 B_SPLINE_CURVE_WITH_KNOTS ( ( 3, 2, 2, 2, 3 ),
 ( 0.6041666666666666297, 0.6145833333333333703, 0.6250000000000000000, 0.6354166666666666297, 0.6458333333333333703 ),
 .UNSPECIFIED. ) 
 CURVE ( )  GEOMETRIC_REPRESENTATION_ITEM ( )  RATIONAL_B_SPLINE_CURVE ( ( 1.000000000000000000, 0.9238795325112867385, 1.000000000000000000, 0.9238795325112867385, 1.000000000000000000, 0.9238795325112867385, 1.000000000000000000, 0.9238795325112867385, 1.000000000000000000 ) ) 
 REPRESENTATION_ITEM ( '' )  );
#4926=CARTESIAN_POINT ( 'NONE',  ( 0.1167790944451422702, 4.168833333409199149, -0.2819296736111110424 ) ) ;
#4927=ADVANCED_FACE ( 'NONE', ( #19112 ), #5821, .T. ) ;
#4931=ORIENTED_EDGE ( 'NONE', *, *, #2306, .T. ) ;
#4932=CARTESIAN_POINT ( 'NONE',  ( -0.2206173157302027954, 0.3652777776260448528, -0.2206173157302028232 ) ) ;
#4937=EDGE_CURVE ( 'NONE', #12807, #7226, #10378, .T. ) ;
#4939=FACE_OUTER_BOUND ( 'NONE', #908, .T. ) ;
#4942=CARTESIAN_POINT ( 'NONE',  ( 0.1993543840281266633, 4.387583333409199149, -0.1993543840281266910 ) ) ;
#4947=CARTESIAN_POINT ( 'NONE',  ( 0.2206173157302028787, 4.071611111111110404, 0.2206173157302027954 ) ) ;
#4948=CARTESIAN_POINT ( 'NONE',  ( 0.2206173157302028787, 4.911888889040620931, 0.2206173157302027954 ) ) ;
#4950=CARTESIAN_POINT ( 'NONE',  ( -1.062695237341364068E-12, 5.118312382271687611, 0.3086920601714014945 ) ) ;
#4952=CARTESIAN_POINT ( 'NONE',  ( -0.3119535588213346866, 4.892301757544008645, 0.04116472303791206266 ) ) ;
#4953=B_SPLINE_CURVE_WITH_KNOTS ( 'NONE', 3,
 ( #13841, #13726, #15783, #663, #15427, #11773, #7977, #4202, #12021, #782, #15308, #22737, #19435, #8212, #22855, #21148, #4436, #6144, #15661, #6025, #11655, #21026, #23080, #4318, #11903, #23201, #6512, #4679, #13493, #20908, #10063, #6389, #19193, #19321, #2503, #19079, #2620, #8090, #2386, #13611, #6268, #17257, #15544, #17610, #2735, #541 ),
 .UNSPECIFIED., .F., .F.,
 ( 4, 2, 2, 2, 2, 2, 2, 2, 2, 2, 2, 2, 2, 2, 2, 2, 2, 2, 2, 2, 2, 2, 4 ),
 ( 0.005337107837582267221, 0.006801130698153545241, 0.008265153558724824129, 0.008997164989010464006, 0.009729176419296105618, 0.01119319927986738884, 0.01192521071015302872, 0.01265722214043866686, 0.01412124500100994315, 0.01558526786158121596, 0.01631727929186685411, 0.01704929072215248878, 0.01851331358272376854, 0.01997733644329504829, 0.02144135930386632805, 0.02217337073415196619, 0.02290538216443760780, 0.02363739359472324594, 0.02436940502500888409, 0.02583342788558016037, 0.02656543931586579851, 0.02729745074615143666, 0.02876147360672271294 ),
 .UNSPECIFIED. ) ;
#4959=CARTESIAN_POINT ( 'NONE',  ( -0.2819296736111110979, 0.1326388888130222710, -3.452642723725051716E-17 ) ) ;
#4962=CARTESIAN_POINT ( 'NONE',  ( 0.1993543840281267465, 5.220916666742532186, 0.1993543840281266633 ) ) ;
#4964=DIRECTION ( 'NONE',  ( -0.000000000000000000, -1.000000000000000000, -0.000000000000000000 ) ) ;
#4965=CARTESIAN_POINT ( 'NONE',  ( -0.1593056001970055702, 4.270767213191519751, -0.2687184019925401568 ) ) ;
#4967=CARTESIAN_POINT ( 'NONE',  ( -0.1292346314604056190, 0.5354166666666662078, -0.3119999999999999996 ) ) ;
#4968=CARTESIAN_POINT ( 'NONE',  ( -1.910449006669871087E-17, 4.814666666666665762, -0.3119999999999999996 ) ) ;
#4969=CARTESIAN_POINT ( 'NONE',  ( -0.1993543840281266910, 4.290361111186976828, -0.1993543840281266910 ) ) ;
#4972=CARTESIAN_POINT ( 'NONE',  ( 0.1292346314604082835, 4.401472222222221120, 0.3119999999999974460 ) ) ;
#4973=FACE_OUTER_BOUND ( 'NONE', #1688, .T. ) ;
#4974=CARTESIAN_POINT ( 'NONE',  ( -0.1993543840281266355, 4.526472222298087544, 0.1993543840281267465 ) ) ;
#4976=EDGE_CURVE ( 'NONE', #1526, #848, #8904, .T. ) ;
#4979=EDGE_CURVE ( 'NONE', #6926, #5016, #13521, .T. ) ;
#4980=VECTOR ( 'NONE', #21329, 39.37007874015748143 ) ;
#4984=CARTESIAN_POINT ( 'NONE',  ( 0.1993543840281266633, 4.179250000075865223, -0.1993543840281266910 ) ) ;
#4985=CARTESIAN_POINT ( 'NONE',  ( 1.312321497832610059E-07, 4.821611112096344520, -0.3119999999999724105 ) ) ;
#4990=CARTESIAN_POINT ( 'NONE',  ( 0.1993543840281266355, 0.5979166665908000056, 0.1993543840281267465 ) ) ;
#4996=ORIENTED_EDGE ( 'NONE', *, *, #6639, .T. ) ;
#4999=CARTESIAN_POINT ( 'NONE',  ( -0.3119999807755027277, 3.834402680349659143, -0.04084143460943073095 ) ) ;
#5000=CARTESIAN_POINT ( 'NONE',  ( -0.2819296736111110979, 0.4520833332574666907, -3.452642723725051716E-17 ) ) ;
#5001=CARTESIAN_POINT ( 'NONE',  ( 0.2819296736111110424, 3.898000000075866112, -0.1167790944451423396 ) ) ;
#5005=CARTESIAN_POINT ( 'NONE',  ( -0.1993543840281266910, 4.748694444520309865, -0.1993543840281266910 ) ) ;
#5007=CARTESIAN_POINT ( 'NONE',  ( 5.731347020009612645E-17, 3.897999999999999243, 0.3119999999999999996 ) ) ;
#5008=EDGE_LOOP ( 'NONE', ( #22575, #4516, #9952, #13940 ) ) ;
#5009=B_SPLINE_CURVE_WITH_KNOTS ( 'NONE', 3,
 ( #23957, #23588, #19951, #10814, #8972, #21895, #5184, #16295, #5062, #12532, #16538, #3241, #12655, #5312, #8849, #10933, #9089, #3362, #18361, #1654, #14719, #11051, #7271, #9218, #16420, #23829, #22133, #7387, #10575, #5434, #18480, #14839, #3599, #5552, #12899, #20315, #19829, #18005, #3124, #8722 ),
 .UNSPECIFIED., .F., .F.,
 ( 4, 2, 1, 2, 2, 1, 2, 2, 2, 2, 2, 2, 1, 1, 2, 2, 2, 2, 2, 2, 2, 4 ),
 ( 0.6487731362554981507, 0.6493439294636441650, 0.6494866277656805575, 0.6495579769166988093, 0.6495936514922079352, 0.6496293260677170611, 0.6499147226717900683, 0.6510563090880819859, 0.6521978955043739035, 0.6533394819206658211, 0.6556226547532496562, 0.6567642411695416849, 0.6569069394715780774, 0.6569782886225963292, 0.6570139631981054551, 0.6570496377736145810, 0.6573350343776875881, 0.6579058275858336025, 0.6601890004184174376, 0.6624721732510013839, 0.6647553460835852190, 0.6670385189161691653 ),
 .UNSPECIFIED. ) ;
#5011=CARTESIAN_POINT ( 'NONE',  ( 0.2819296736111110979, 5.210500000075865223, 0.1167790944451422425 ) ) ;
#5014=CARTESIAN_POINT ( 'NONE',  ( -0.1167790944451423535, 4.974388888964754507, 0.2819296736111110979 ) ) ;
#5016=VERTEX_POINT ( 'NONE', #9932 ) ;
#5017=ADVANCED_FACE ( 'NONE', ( #11643 ), #11521, .T. ) ;
#5018=CARTESIAN_POINT ( 'NONE',  ( -0.3051426028078303987, 5.113331766849443127, -0.05202755180939230145 ) ) ;
#5019=CARTESIAN_POINT ( 'NONE',  ( -0.2802025597200765161, 4.561924260886437210, 0.1428905893484782030 ) ) ;
#5021=CARTESIAN_POINT ( 'NONE',  ( -0.1993543840281267465, 0.1951388888130222710, 0.1993543840281266633 ) ) ;
#5022=ORIENTED_EDGE ( 'NONE', *, *, #7369, .T. ) ;
#5024=CARTESIAN_POINT ( 'NONE',  ( -0.2499688240500823333, 4.730080733492335376, 0.1894356414185249249 ) ) ;
#5025=CARTESIAN_POINT ( 'NONE',  ( -0.2748157666139303124, 5.203214401271618605, 0.07108222885202038210 ) ) ;
#5027=CARTESIAN_POINT ( 'NONE',  ( -0.3009011790701222600, 5.060279419410155022, 0.08637144214764777561 ) ) ;
#5029=CARTESIAN_POINT ( 'NONE',  ( -0.2564683202935754691, 3.885663880049097241, -0.1776738855868679468 ) ) ;
#5031=CARTESIAN_POINT ( 'NONE',  ( -0.1993543840281266910, 4.748694444520309865, -0.1993543840281266910 ) ) ;
#5032=CARTESIAN_POINT ( 'NONE',  ( 0.07186756554182434364, 4.518106518300164964, 0.3043097197694309974 ) ) ;
#5033=CARTESIAN_POINT ( 'NONE',  ( -0.2819296736111110424, 3.738277777853643347, -0.1167790944451423119 ) ) ;
#5034=CARTESIAN_POINT ( 'NONE',  ( -0.2274437723577396042, 0.04798558205255324532, -0.1920016971050759469 ) ) ;
#5035=CARTESIAN_POINT ( 'NONE',  ( 0.2859772800003606563, 5.033587069339882092, -0.1247896800457511945 ) ) ;
#5036=CARTESIAN_POINT ( 'NONE',  ( 0.2782497666485165277, 0.06249891821425377497, 0.1411420113220940853 ) ) ;
#5039=CARTESIAN_POINT ( 'NONE',  ( -0.2206173157302027676, 4.342444444596176290, 0.2206173157302028787 ) ) ;
#5040=CARTESIAN_POINT ( 'NONE',  ( -0.2819296736111110424, 4.703555555631421470, 0.1167790944451424923 ) ) ;
#5041=CARTESIAN_POINT ( 'NONE',  ( 0.1993543840281267465, 3.818138888964754507, 0.1993543840281266633 ) ) ;
#5046=CARTESIAN_POINT ( 'NONE',  ( -0.3120659000946393036, 4.945554085942006850, -0.04037676907161258377 ) ) ;
#5049=CARTESIAN_POINT ( 'NONE',  ( 0.3119999999999998885, 0.1743055554038226151, 0.1292346314604058410 ) ) ;
#5051=CARTESIAN_POINT ( 'NONE',  ( -0.2267756154094652810, 4.384351444865524527, -0.2142830584042328124 ) ) ;
#5053=CARTESIAN_POINT ( 'NONE',  ( 0.000000000000000000, 5.384999999999999787, 0.000000000000000000 ) ) ;
#5057=CARTESIAN_POINT ( 'NONE',  ( 0.2819296736111110979, 0.3687499999241333759, 0.000000000000000000 ) ) ;
#5059=VERTEX_POINT ( 'NONE', #2123 ) ;
#5060=CARTESIAN_POINT ( 'NONE',  ( -0.1993543840281266355, 4.359805555631421470, 0.1993543840281267465 ) ) ;
#5062=CARTESIAN_POINT ( 'NONE',  ( -0.04459125003299137247, 4.237043471246520809, 0.3087979979381368922 ) ) ;
#5063=CARTESIAN_POINT ( 'NONE',  ( 0.2206173157302028787, 4.127166666666665762, 0.2206173157302027954 ) ) ;
#5064=CARTESIAN_POINT ( 'NONE',  ( 0.1292346314604056190, 5.040361111262842364, -0.3119999999999999996 ) ) ;
#5069=ORIENTED_EDGE ( 'NONE', *, *, #8493, .F. ) ;
#5070=CARTESIAN_POINT ( 'NONE',  ( -0.1913865654062817945, 4.883039109442649739, -0.2464053351942348535 ) ) ;
#5074=( BOUNDED_CURVE ( )  B_SPLINE_CURVE ( 2, ( #15746, #23399, #14151, #21708, #11984, #21580, #19397, #10147, #23157 ),
 .UNSPECIFIED., .F., .T. ) 
 B_SPLINE_CURVE_WITH_KNOTS ( ( 3, 2, 2, 2, 3 ),
 ( 0.1875000000000000000, 0.1979166666666666574, 0.2083333333333333426, 0.2187500000000000000, 0.2291666666666666574 ),
 .UNSPECIFIED. ) 
 CURVE ( )  GEOMETRIC_REPRESENTATION_ITEM ( )  RATIONAL_B_SPLINE_CURVE ( ( 1.000000000000000000, 0.9238795325112867385, 1.000000000000000000, 0.9238795325112867385, 1.000000000000000000, 0.9238795325112867385, 1.000000000000000000, 0.9238795325112867385, 1.000000000000000000 ) ) 
 REPRESENTATION_ITEM ( '' )  );
#5078=CARTESIAN_POINT ( 'NONE',  ( -0.2819296736111110979, 0.2958333332574666907, -0.1167790944451423396 ) ) ;
#5080=CARTESIAN_POINT ( 'NONE',  ( -0.2819296736111110424, 5.141055555631421470, -0.1167790944451423119 ) ) ;
#5081=CARTESIAN_POINT ( 'NONE',  ( 0.2135326563692477309, 4.481723286349742708, -0.2284020054868782235 ) ) ;
#5083=CARTESIAN_POINT ( 'NONE',  ( -0.008779695402981809935, 4.599642847705920801, -0.3118941039586931585 ) ) ;
#5087=CARTESIAN_POINT ( 'NONE',  ( -0.1292346314604057023, 4.783416666666665762, 0.3119999999999998885 ) ) ;
#5089=CARTESIAN_POINT ( 'NONE',  ( -0.2819296736111110424, 3.911888888964754507, 0.1167790944451424923 ) ) ;
#5090=CARTESIAN_POINT ( 'NONE',  ( -0.1167790944451423257, 3.800777777853643347, -0.2819296736111110424 ) ) ;
#5092=CARTESIAN_POINT ( 'NONE',  ( 0.3119999999999999996, 0.5111111109593782231, 0.000000000000000000 ) ) ;
#5094=CYLINDRICAL_SURFACE ( 'NONE', #8150, 0.3119999999999999996 ) ;
#5095=CARTESIAN_POINT ( 'NONE',  ( -0.1167790944451423535, 4.585500000075865223, 0.2819296736111110424 ) ) ;
#5096=EDGE_CURVE ( 'NONE', #12983, #1519, #17361, .T. ) ;
#5097=CARTESIAN_POINT ( 'NONE',  ( -0.3034432599227261940, 4.504371932559179115, 0.07687943905626030972 ) ) ;
#5099=B_SPLINE_CURVE_WITH_KNOTS ( 'NONE', 3,
 ( #20567, #20805, #319, #2278, #9715, #7872, #22752, #18860, #441, #2400, #15202, #4217, #9839, #7992, #555, #5806, #15322, #4093, #6043, #13510, #17271, #3865, #15445, #22870, #6160, #8105, #13270, #15560, #18737, #7759, #13626, #21043, #17388, #15089, #11785, #682, #19210, #16905, #2517, #22982, #3977, #13153, #200 ),
 .UNSPECIFIED., .F., .F.,
 ( 4, 2, 2, 2, 2, 1, 1, 2, 2, 2, 2, 2, 2, 2, 2, 2, 2, 2, 2, 2, 1, 2, 4 ),
 ( 0.5208383355989948393, 0.5219801074602197222, 0.5225509933908321081, 0.5228364363561384121, 0.5228721167268016723, 0.5229077970974649325, 0.5229791578387914530, 0.5231218793214446050, 0.5254054230438944817, 0.5276889667663443584, 0.5299725104887942351, 0.5322560542112441118, 0.5333978260724689946, 0.5345395979336938774, 0.5356813697949188713, 0.5368231416561437541, 0.5373940275867562510, 0.5376794705520624440, 0.5377508312933890755, 0.5377865116640523357, 0.5378221920347155960, 0.5379649135173687480, 0.5391066853785936308 ),
 .UNSPECIFIED. ) ;
#5103=CARTESIAN_POINT ( 'NONE',  ( 0.1993543840281267465, 4.109805555631421470, 0.1993543840281266633 ) ) ;
#5104=CARTESIAN_POINT ( 'NONE',  ( 0.000000000000000000, 5.072999999999999510, 0.000000000000000000 ) ) ;
#5105=CARTESIAN_POINT ( 'NONE',  ( 1.337745543335387199E-07, 4.460505239618372642, 0.3119999999999396589 ) ) ;
#5108=CARTESIAN_POINT ( 'NONE',  ( 1.726321361862525858E-17, -0.006250000075866632768, -0.2819296736111110979 ) ) ;
#5110=CARTESIAN_POINT ( 'NONE',  ( 0.1292346314604057300, 0.5631944444444441089, 0.3119999999999998885 ) ) ;
#5117=CARTESIAN_POINT ( 'NONE',  ( -0.2726212559319319273, 3.830960530932576269, -0.1571292937601793949 ) ) ;
#5118=CARTESIAN_POINT ( 'NONE',  ( 0.1167790944451423257, 0.3791666665908000611, -0.2819296736111110424 ) ) ;
#5120=CARTESIAN_POINT ( 'NONE',  ( -1.726321361862525858E-17, 3.741750000075865668, -0.2819296736111110979 ) ) ;
#5123=CARTESIAN_POINT ( 'NONE',  ( 5.178964085587577574E-17, 4.325083333409199149, 0.2819296736111110979 ) ) ;
#5128=CARTESIAN_POINT ( 'NONE',  ( 0.2819296736111110979, 5.158416666742532186, -3.452642723725051716E-17 ) ) ;
#5129=EDGE_CURVE ( 'NONE', #9589, #23206, #22612, .T. ) ;
#5130=( BOUNDED_CURVE ( )  B_SPLINE_CURVE ( 2, ( #16605, #16367, #9405, #5621, #12843, #11118, #12724, #13085, #9281 ),
 .UNSPECIFIED., .F., .F. ) 
 B_SPLINE_CURVE_WITH_KNOTS ( ( 3, 2, 2, 2, 3 ),
 ( 0.1696428571428572063, 0.1741071428571428215, 0.1785714285714284644, 0.1830357142857140795, 0.1874999999999997224 ),
 .UNSPECIFIED. ) 
 CURVE ( )  GEOMETRIC_REPRESENTATION_ITEM ( )  RATIONAL_B_SPLINE_CURVE ( ( 0.9999999999999990008, 0.9238795325112877377, 1.000000000000000000, 0.9238795325112867385, 1.000000000000000000, 0.9238795325112867385, 1.000000000000000000, 0.9238795325112915124, 0.9999999999999952260 ) ) 
 REPRESENTATION_ITEM ( '' )  );
#5131=CARTESIAN_POINT ( 'NONE',  ( -1.960390272410463459E-06, 4.210500054279665783, -0.3119999999938410928 ) ) ;
#5134=CARTESIAN_POINT ( 'NONE',  ( 0.1167790944451422702, 4.946611111186975940, -0.2819296736111110979 ) ) ;
#5138=CARTESIAN_POINT ( 'NONE',  ( -0.06344784419188649605, 4.569835828710965941, 0.3056428810798353934 ) ) ;
#5140=CARTESIAN_POINT ( 'NONE',  ( -0.2819296736111110979, 0.2472222221463555580, 0.1167790944451422425 ) ) ;
#5142=CARTESIAN_POINT ( 'NONE',  ( 0.1993543840281266355, 0.09791666659080004720, 0.1993543840281267465 ) ) ;
#5151=EDGE_CURVE ( 'NONE', #14891, #14020, #11948, .T. ) ;
#5152=CARTESIAN_POINT ( 'NONE',  ( -0.1993543840281266910, 4.415361111186976828, -0.1993543840281266910 ) ) ;
#5154=CARTESIAN_POINT ( 'NONE',  ( -0.2206173157302028787, 0.2680555554038226429, 0.2206173157302027954 ) ) ;
#5155=CARTESIAN_POINT ( 'NONE',  ( 0.2819296736111110979, 5.116750000075866112, -3.452642723725051716E-17 ) ) ;
#5157=CARTESIAN_POINT ( 'NONE',  ( 0.2727877922144690270, 4.923470271033195012, -0.1568345301858280472 ) ) ;
#5158=CARTESIAN_POINT ( 'NONE',  ( 0.2530624153226711526, 5.072996518863750026, 0.1824922298374807572 ) ) ;
#5160=CARTESIAN_POINT ( 'NONE',  ( -0.1206821249410769403, 4.790362928687555311, 0.2884035782607159981 ) ) ;
#5161=CARTESIAN_POINT ( 'NONE',  ( 5.731347020009612645E-17, 4.293833333485065573, 0.3119999999999999996 ) ) ;
#5163=CARTESIAN_POINT ( 'NONE',  ( -1.726321361862525858E-17, 4.463972222298087544, -0.2819296736111110979 ) ) ;
#5164=CARTESIAN_POINT ( 'NONE',  ( 0.2819296736111110979, 3.825083333409198705, -3.452642723725051716E-17 ) ) ;
#5167=ORIENTED_EDGE ( 'NONE', *, *, #4185, .T. ) ;
#5170=CARTESIAN_POINT ( 'NONE',  ( 0.000000000000000000, 5.384999999999999787, 0.000000000000000000 ) ) ;
#5172=CARTESIAN_POINT ( 'NONE',  ( 0.1292346314604057023, 0.2229166665149337201, 0.3119999999999998885 ) ) ;
#5174=CARTESIAN_POINT ( 'NONE',  ( -8.964115882027956832E-07, 3.710500024236165206, -0.3119999999987121964 ) ) ;
#5177=VERTEX_POINT ( 'NONE', #10198 ) ;
#5178=ORIENTED_EDGE ( 'NONE', *, *, #7113, .T. ) ;
#5181=CARTESIAN_POINT ( 'NONE',  ( 0.1993543840281266633, 4.443138888964754507, -0.1993543840281266910 ) ) ;
#5182=CARTESIAN_POINT ( 'NONE',  ( 0.3119999999999998885, 0.1812499999999996614, 0.1292346314604058410 ) ) ;
#5184=CARTESIAN_POINT ( 'NONE',  ( -0.04251946191606173486, 4.237103564431733638, 0.3090897937739507939 ) ) ;
#5185=CARTESIAN_POINT ( 'NONE',  ( -0.1292346314604056745, 4.040361111111110404, -0.3119999999999999996 ) ) ;
#5187=CARTESIAN_POINT ( 'NONE',  ( -0.3119999999999998885, 5.061194444596176290, 0.1292346314604058410 ) ) ;
#5191=CARTESIAN_POINT ( 'NONE',  ( -0.2724990365483070387, 4.895781167980035598, 0.1573335068080851940 ) ) ;
#5197=CARTESIAN_POINT ( 'NONE',  ( 0.2819296736111110979, 0.3861111110352444808, -0.1167790944451422980 ) ) ;
#5199=CARTESIAN_POINT ( 'NONE',  ( 0.2819296736111110424, 5.231333333409200037, -0.1167790944451423396 ) ) ;
#5200=CARTESIAN_POINT ( 'NONE',  ( 0.3021604925011200926, 4.472183788454629827, 0.07803024449590109657 ) ) ;
#5201=ORIENTED_EDGE ( 'NONE', *, *, #16064, .F. ) ;
#5202=CARTESIAN_POINT ( 'NONE',  ( -0.08088021546148146945, 3.768287267155998599, -0.3020254087663621356 ) ) ;
#5203=CARTESIAN_POINT ( 'NONE',  ( -0.1959092998191455937, 4.605422749898409940, -0.2428318580714328434 ) ) ;
#5205=CARTESIAN_POINT ( 'NONE',  ( 0.03656842479768742521, 4.876171843660301874, -0.3099543190786830937 ) ) ;
#5207=CARTESIAN_POINT ( 'NONE',  ( -1.910449006669871087E-17, 4.925777777777777366, -0.3119999999999999996 ) ) ;
#5208=CARTESIAN_POINT ( 'NONE',  ( -0.2206173157302028232, 4.821611111111110404, -0.2206173157302028232 ) ) ;
#5209=CARTESIAN_POINT ( 'NONE',  ( -0.1993543840281266910, 3.901472222298087544, -0.1993543840281266910 ) ) ;
#5210=CARTESIAN_POINT ( 'NONE',  ( -0.1993543840281266355, 3.818138888964754507, 0.1993543840281267465 ) ) ;
#5212=CARTESIAN_POINT ( 'NONE',  ( 0.2206173157302028787, 4.404944444444443441, 0.2206173157302027954 ) ) ;
#5214=CARTESIAN_POINT ( 'NONE',  ( 0.000000000000000000, 5.384999999999999787, 0.000000000000000000 ) ) ;
#5215=CARTESIAN_POINT ( 'NONE',  ( 0.1167790944451422702, 4.446611111186975940, -0.2819296736111110424 ) ) ;
#5217=CARTESIAN_POINT ( 'NONE',  ( -0.2423184047408910302, 4.508223239054410136, 0.1965347448998619739 ) ) ;
#5218=CARTESIAN_POINT ( 'NONE',  ( 0.000000000000000000, 5.384999999999999787, 0.000000000000000000 ) ) ;
#5221=CARTESIAN_POINT ( 'NONE',  ( -0.1993543840281266910, 3.804250000075865668, -0.1993543840281266910 ) ) ;
#5222=ADVANCED_FACE ( 'NONE', ( #13853 ), #11548, .T. ) ;
#5225=CARTESIAN_POINT ( 'NONE',  ( -0.3120018507703757882, 4.445532957081515413, -0.04082774198810235067 ) ) ;
#5226=CARTESIAN_POINT ( 'NONE',  ( 0.2206173157302028232, 0.07361111095937818150, -0.2206173157302028232 ) ) ;
#5228=CARTESIAN_POINT ( 'NONE',  ( 0.1167790944451423257, 0.2124999999241334314, -0.2819296736111110424 ) ) ;
#5238=CARTESIAN_POINT ( 'NONE',  ( -0.1917383918645655105, 3.827338037112651747, -0.2494961988085758198 ) ) ;
#5240=CARTESIAN_POINT ( 'NONE',  ( -0.3119999999999999996, 0.04583333333333299009, -3.820898013339742174E-17 ) ) ;
#5241=CARTESIAN_POINT ( 'NONE',  ( 0.1993543840281267465, 3.887583333409199149, 0.1993543840281266633 ) ) ;
#5244=CARTESIAN_POINT ( 'NONE',  ( -0.2819296736111110979, 4.533416666742532186, 0.000000000000000000 ) ) ;
#5248=CARTESIAN_POINT ( 'NONE',  ( 3.820898013339742174E-17, 5.384999999999999787, 0.3119999999999999996 ) ) ;
#5249=CARTESIAN_POINT ( 'NONE',  ( 0.1751654852437733445, 4.371938874197769387, -0.2588781644951254624 ) ) ;
#5250=CARTESIAN_POINT ( 'NONE',  ( -0.2819296736111110424, 5.134111111186975940, 0.1167790944451424923 ) ) ;
#5252=CARTESIAN_POINT ( 'NONE',  ( 7.773700634137156501E-05, 4.210497796003888737, -0.3120000004945939764 ) ) ;
#5254=CARTESIAN_POINT ( 'NONE',  ( 0.000000000000000000, 5.384999999999999787, 0.000000000000000000 ) ) ;
#5256=CARTESIAN_POINT ( 'NONE',  ( -0.1993543840281266910, 4.901472222298087544, -0.1993543840281266910 ) ) ;
#5258=CARTESIAN_POINT ( 'NONE',  ( -0.1670630085336562987, 4.066582461025795681, 0.2635491965915186530 ) ) ;
#5259=CARTESIAN_POINT ( 'NONE',  ( 5.731347020009612645E-17, 4.897999999999998799, 0.3119999999999999996 ) ) ;
#5261=CARTESIAN_POINT ( 'NONE',  ( -0.1167790944451422702, 0.2888888888130222710, -0.2819296736111110424 ) ) ;
#5263=CARTESIAN_POINT ( 'NONE',  ( 0.1167790944451423257, 0.3374999999241333204, -0.2819296736111110424 ) ) ;
#5264=CARTESIAN_POINT ( 'NONE',  ( -0.2206173157302028232, 4.321611111111110404, -0.2206173157302028232 ) ) ;
#5265=CARTESIAN_POINT ( 'NONE',  ( -0.1780582496145807492, 5.195124778163895840, -0.2256393913368613391 ) ) ;
#5270=CARTESIAN_POINT ( 'NONE',  ( 0.3119999999999999996, 4.189666666666665762, -3.820898013339742174E-17 ) ) ;
#5272=CARTESIAN_POINT ( 'NONE',  ( 0.1167790944451423257, -0.009722222298088854797, -0.2819296736111110424 ) ) ;
#5273=CARTESIAN_POINT ( 'NONE',  ( 0.1167790944451424368, 4.550777777853644679, 0.2819296736111110424 ) ) ;
#5275=CARTESIAN_POINT ( 'NONE',  ( 0.3124347497111735206, 4.530475913665126697, -0.01942892286152598721 ) ) ;
#5276=CARTESIAN_POINT ( 'NONE',  ( -0.1167790944451423535, 4.988277777853642903, 0.2819296736111110424 ) ) ;
#5278=CARTESIAN_POINT ( 'NONE',  ( -0.2992534993645844521, 0.05134832323153658978, -0.03248684396581635186 ) ) ;
#5279=CARTESIAN_POINT ( 'NONE',  ( 0.1736779060279114995, 3.760883958121103987, -0.2600042684560003314 ) ) ;
#5281=CARTESIAN_POINT ( 'NONE',  ( -5.308788303787306404E-17, 0.03949697488198145034, 0.2889969748819818385 ) ) ;
#5283=CARTESIAN_POINT ( 'NONE',  ( 4.282505654011733572E-07, 3.932722210548942776, -0.3119999999997061790 ) ) ;
#5284=CARTESIAN_POINT ( 'NONE',  ( 0.3119999999999999996, 4.248694444596176290, 0.1292346314604056190 ) ) ;
#5285=CARTESIAN_POINT ( 'NONE',  ( 0.1167790944451424506, 4.606333333409200037, 0.2819296736111110424 ) ) ;
#5286=CARTESIAN_POINT ( 'NONE',  ( -0.1993543840281266910, 3.845916666742532186, -0.1993543840281266910 ) ) ;
#5287=AXIS2_PLACEMENT_3D ( 'NONE', #22082, #3187, #16246 ) ;
#5289=ORIENTED_EDGE ( 'NONE', *, *, #14382, .F. ) ;
#5299=ORIENTED_EDGE ( 'NONE', *, *, #20209, .T. ) ;
#5300=CARTESIAN_POINT ( 'NONE',  ( 0.1292346314604057023, 0.2784722220704892726, 0.3119999999999998885 ) ) ;
#5301=CARTESIAN_POINT ( 'NONE',  ( -0.2289623471110959485, 4.384444726759149091, -0.2119507152515421600 ) ) ;
#5302=CARTESIAN_POINT ( 'NONE',  ( -0.1548258371540442990, 5.125004085625619155, 0.2666117704252644605 ) ) ;
#5303=FACE_OUTER_BOUND ( 'NONE', #7127, .T. ) ;
#5307=CARTESIAN_POINT ( 'NONE',  ( 0.1251933906032628718, 5.075263835759200148, 0.2864240098224283271 ) ) ;
#5309=CARTESIAN_POINT ( 'NONE',  ( -0.2819296736111110979, 4.297305555631420582, 0.000000000000000000 ) ) ;
#5310=CARTESIAN_POINT ( 'NONE',  ( -1.726321361862525858E-17, 5.005638888964754507, -0.2819296736111110979 ) ) ;
#5312=CARTESIAN_POINT ( 'NONE',  ( -0.1515187123326594831, 4.233801538027739397, 0.2736959603349944370 ) ) ;
#5313=CARTESIAN_POINT ( 'NONE',  ( -1.910449006669871087E-17, 3.981333333333332725, -0.3119999999999999996 ) ) ;
#5314=CARTESIAN_POINT ( 'NONE',  ( -0.3119999999999999996, 5.057722222373953969, 0.000000000000000000 ) ) ;
#5315=CARTESIAN_POINT ( 'NONE',  ( -1.726321361862525858E-17, 5.075083333409198261, -0.2819296736111110979 ) ) ;
#5320=CARTESIAN_POINT ( 'NONE',  ( -0.1751221285957142437, 0.05731332189368815860, 0.2521211663704562289 ) ) ;
#5321=EDGE_LOOP ( 'NONE', ( #466, #4406, #14176, #9810 ) ) ;
#5323=CARTESIAN_POINT ( 'NONE',  ( 0.1993543840281267465, 5.040361111186975940, 0.1993543840281266633 ) ) ;
#5327=CARTESIAN_POINT ( 'NONE',  ( -0.2819296736111110979, 0.1881944443685777957, -3.452642723725051716E-17 ) ) ;
#5329=CARTESIAN_POINT ( 'NONE',  ( 0.2819296736111110979, 5.227861111186977716, -3.452642723725051716E-17 ) ) ;
#5330=CARTESIAN_POINT ( 'NONE',  ( 0.2961024193012317118, 4.477398186232928623, -0.1021605605434409425 ) ) ;
#5332=CARTESIAN_POINT ( 'NONE',  ( 0.2819296736111110979, 4.936194444520309865, -3.452642723725051716E-17 ) ) ;
#5333=CARTESIAN_POINT ( 'NONE',  ( -0.3039371850020707311, 4.171187110652304852, 0.08147708232397948835 ) ) ;
#5335=CARTESIAN_POINT ( 'NONE',  ( 5.731347020009612645E-17, 4.064666666666665762, 0.3119999999999999996 ) ) ;
#5336=CARTESIAN_POINT ( 'NONE',  ( 0.3119999999999999996, 0.5666666665149336923, 0.000000000000000000 ) ) ;
#5337=CARTESIAN_POINT ( 'NONE',  ( 0.3119999999999999996, 4.689666666666665762, -3.820898013339742174E-17 ) ) ;
#5339=CARTESIAN_POINT ( 'NONE',  ( -0.2819296736111110979, 3.963972222298087544, 0.000000000000000000 ) ) ;
#5340=CARTESIAN_POINT ( 'NONE',  ( 5.178964085587577574E-17, 3.825083333409199149, 0.2819296736111110979 ) ) ;
#5341=CARTESIAN_POINT ( 'NONE',  ( 0.3017741391662112638, 4.032218511630571989, -0.07998161405697697124 ) ) ;
#5344=CARTESIAN_POINT ( 'NONE',  ( 0.3119999999999999996, 3.911888888888888083, -3.820898013339742174E-17 ) ) ;
#5345=VERTEX_POINT ( 'NONE', #14208 ) ;
#5346=CARTESIAN_POINT ( 'NONE',  ( 0.1993543840281267465, 4.207027777853643791, 0.1993543840281266633 ) ) ;
#5347=CARTESIAN_POINT ( 'NONE',  ( 1.241811370555571286E-09, 4.488277777895108400, -0.3119999999999999996 ) ) ;
#5350=CARTESIAN_POINT ( 'NONE',  ( -0.1917386117188931705, 3.954711899498488670, 0.2494960294160712411 ) ) ;
#5351=CARTESIAN_POINT ( 'NONE',  ( -0.3038827018704687855, 4.444373711942660066, -0.08165392154346443054 ) ) ;
#5355=CARTESIAN_POINT ( 'NONE',  ( -0.2819296736111110979, 0.1743055554796889284, -3.452642723725051716E-17 ) ) ;
#5356=CARTESIAN_POINT ( 'NONE',  ( 0.1571283209375275436, 3.853928337557731787, 0.2726217664897950255 ) ) ;
#5357=CARTESIAN_POINT ( 'NONE',  ( 0.000000000000000000, 0.06249999999999967387, 0.000000000000000000 ) ) ;
#5362=CARTESIAN_POINT ( 'NONE',  ( -0.02041513420581141103, 5.092642365365469104, -0.3108785821030984886 ) ) ;
#5365=CARTESIAN_POINT ( 'NONE',  ( 0.2819296736111110424, 0.5874999999241333759, 0.1167790944451424923 ) ) ;
#5366=CARTESIAN_POINT ( 'NONE',  ( -0.1167790944451423535, 3.766055555631421470, 0.2819296736111110424 ) ) ;
#5368=CARTESIAN_POINT ( 'NONE',  ( 5.178964085587577574E-17, 4.380638888964754507, 0.2819296736111110979 ) ) ;
#5369=CARTESIAN_POINT ( 'NONE',  ( 5.731347020009612645E-17, 4.953555555555554157, 0.3119999999999999996 ) ) ;
#5370=CARTESIAN_POINT ( 'NONE',  ( -0.3119999999999999996, 4.602861111111110404, -0.1292346314604056468 ) ) ;
#5373=CARTESIAN_POINT ( 'NONE',  ( 0.1919135583096156505, 4.371358422006517586, -0.2469761307552826579 ) ) ;
#5374=CARTESIAN_POINT ( 'NONE',  ( 0.2819296736111110979, 4.877166666742533963, 0.1167790944451422425 ) ) ;
#5375=CARTESIAN_POINT ( 'NONE',  ( 0.0005648866775877964307, 4.210483983432520283, -0.3119995209647230539 ) ) ;
#5376=LENGTH_MEASURE_WITH_UNIT ( LENGTH_MEASURE( 0.02539999999999999897 ), #14660 );
#5379=CARTESIAN_POINT ( 'NONE',  ( -0.2819296736111110979, 4.571611111186975940, -0.1167790944451422980 ) ) ;
#5383=CARTESIAN_POINT ( 'NONE',  ( -2.918002456435568987E-09, 4.127166543308980806, 0.3119999999999999996 ) ) ;
#5384=CARTESIAN_POINT ( 'NONE',  ( 1.726321361862525858E-17, 0.6187499999241333759, -0.2819296736111110979 ) ) ;
#5385=AXIS2_PLACEMENT_3D ( 'NONE', #21041, #4332, #11783 ) ;
#5387=ORIENTED_EDGE ( 'NONE', *, *, #19903, .F. ) ;
#5388=CARTESIAN_POINT ( 'NONE',  ( -0.1993543840281266633, 0.1812499999241333482, -0.1993543840281266910 ) ) ;
#5395=CARTESIAN_POINT ( 'NONE',  ( -0.1993543840281266633, 0.1118055554796889145, -0.1993543840281266910 ) ) ;
#5396=CARTESIAN_POINT ( 'NONE',  ( -0.1167790944451423535, 4.488277777853644679, 0.2819296736111110424 ) ) ;
#5398=CARTESIAN_POINT ( 'NONE',  ( 0.01388514559274585045, 4.516459957181072404, 0.3120000003946662992 ) ) ;
#5399=CARTESIAN_POINT ( 'NONE',  ( -0.1993543840281266355, 5.040361111186977716, 0.1993543840281267465 ) ) ;
#5400=CARTESIAN_POINT ( 'NONE',  ( 0.1993543840281267465, 4.540361111186976828, 0.1993543840281266633 ) ) ;
#5402=CARTESIAN_POINT ( 'NONE',  ( 0.3120328546110059387, 4.920023481417521438, -0.04056780845644687716 ) ) ;
#5404=CARTESIAN_POINT ( 'NONE',  ( 0.2191938207175568309, 3.911764414538948742, 0.2249900973144438876 ) ) ;
#5405=CARTESIAN_POINT ( 'NONE',  ( -1.910449006669871087E-17, 4.210500000151732536, -0.3119999999999999996 ) ) ;
#5406=CARTESIAN_POINT ( 'NONE',  ( -0.2819296736111110979, 4.477861111186976828, 0.000000000000000000 ) ) ;
#5407=CARTESIAN_POINT ( 'NONE',  ( -0.2819296736111110424, 3.800777777853643347, 0.1167790944451424923 ) ) ;
#5409=VERTEX_POINT ( 'NONE', #3345 ) ;
#5412=ORIENTED_EDGE ( 'NONE', *, *, #4689, .F. ) ;
#5415=CARTESIAN_POINT ( 'NONE',  ( -1.910449006669871087E-17, 4.259111111111110404, -0.3119999999999999996 ) ) ;
#5418=CARTESIAN_POINT ( 'NONE',  ( 0.2206173157302028232, 0.2958333331816003775, -0.2206173157302028232 ) ) ;
#5421=CARTESIAN_POINT ( 'NONE',  ( -0.3119999999999999996, 0.2645833333333330040, -0.1292346314604056745 ) ) ;
#5424=ORIENTED_EDGE ( 'NONE', *, *, #16191, .T. ) ;
#5428=CARTESIAN_POINT ( 'NONE',  ( 0.2858709629710828315, 5.081892701901892018, 0.1261477422632426293 ) ) ;
#5430=CARTESIAN_POINT ( 'NONE',  ( 0.1993543840281266633, 4.276472222298087544, -0.1993543840281266910 ) ) ;
#5431=CARTESIAN_POINT ( 'NONE',  ( 0.1993543840281266633, 5.165361111186976828, -0.1993543840281266910 ) ) ;
#5434=CARTESIAN_POINT ( 'NONE',  ( -0.3115519018914106875, 4.224912875663728862, 0.01957843891848925696 ) ) ;
#5435=CARTESIAN_POINT ( 'NONE',  ( 0.3119999999999999996, 3.908416666666665762, 0.1292346314604056190 ) ) ;
#5436=CARTESIAN_POINT ( 'NONE',  ( -1.910449006669871087E-17, 4.877166666818398610, -0.3119999999999999996 ) ) ;
#5437=CARTESIAN_POINT ( 'NONE',  ( 0.1167790944451422702, 5.182722222298087544, -0.2819296736111110979 ) ) ;
#5441=CARTESIAN_POINT ( 'NONE',  ( 0.01137974820294853848, 0.04292188706665825415, -0.2924218870666587256 ) ) ;
#5445=CARTESIAN_POINT ( 'NONE',  ( -0.2819296736111110424, 5.071611111186976828, -0.1167790944451423119 ) ) ;
#5449=CARTESIAN_POINT ( 'NONE',  ( -0.1167790944451424506, 0.3652777777019109995, 0.2819296736111110424 ) ) ;
#5451=CARTESIAN_POINT ( 'NONE',  ( -0.1167790944451423257, 4.911888888964755395, -0.2819296736111110424 ) ) ;
#5452=CARTESIAN_POINT ( 'NONE',  ( 0.05348210925957119777, 4.486790443027524944, -0.3073820394974481340 ) ) ;
#5454=CARTESIAN_POINT ( 'NONE',  ( 0.1167790944451424368, 4.870222222298087544, 0.2819296736111110424 ) ) ;
#5459=LINE ( 'NONE', #1562, #11794 ) ;
#5461=CARTESIAN_POINT ( 'NONE',  ( -0.3119999999999998885, 4.832027777777777366, 0.1292346314604058410 ) ) ;
#5464=CARTESIAN_POINT ( 'NONE',  ( 0.2819296736111110979, 4.050777777853642903, -0.1167790944451423396 ) ) ;
#5465=CARTESIAN_POINT ( 'NONE',  ( -0.2819296736111110979, 3.811194444520310309, 0.000000000000000000 ) ) ;
#5466=CARTESIAN_POINT ( 'NONE',  ( 0.2223180997122823910, 4.023079565851294781, 0.2197360156277292920 ) ) ;
#5467=CARTESIAN_POINT ( 'NONE',  ( 0.3119999999999999996, 4.411888888888888083, -3.820898013339742174E-17 ) ) ;
#5468=VERTEX_POINT ( 'NONE', #1524 ) ;
#5471=CARTESIAN_POINT ( 'NONE',  ( -0.1413598573426078087, 4.122983608843597381, 0.2782734964209417350 ) ) ;
#5477=CARTESIAN_POINT ( 'NONE',  ( -0.3119981485887119987, 4.447848256106272657, 0.04085602375663895808 ) ) ;
#5478=CARTESIAN_POINT ( 'NONE',  ( 4.589747744727345336E-07, 4.571629220806286753, 0.3119999999992840722 ) ) ;
#5480=CARTESIAN_POINT ( 'NONE',  ( 0.1993543840281266910, 0.1534722221463555858, -0.1993543840281266910 ) ) ;
#5481=CARTESIAN_POINT ( 'NONE',  ( 0.01786091403636311248, 3.876684976164884056, -0.3115615677906792280 ) ) ;
#5482=CARTESIAN_POINT ( 'NONE',  ( 3.820898013339742174E-17, 5.384999999999999787, 0.3119999999999999996 ) ) ;
#5483=CARTESIAN_POINT ( 'NONE',  ( 0.000000000000000000, 5.384999999999999787, -0.3119999999999999996 ) ) ;
#5487=CARTESIAN_POINT ( 'NONE',  ( -0.2829274046655448904, 5.108874275092736283, 0.1269306334051448215 ) ) ;
#5488=CARTESIAN_POINT ( 'NONE',  ( 0.3119999999999998885, 0.01458333333333300050, 0.1292346314604058410 ) ) ;
#5489=CARTESIAN_POINT ( 'NONE',  ( 0.1993543840281266633, 3.845916666742533074, -0.1993543840281266910 ) ) ;
#5491=CARTESIAN_POINT ( 'NONE',  ( -0.2819296736111110424, 4.370222222298088433, 0.1167790944451424923 ) ) ;
#5496=CARTESIAN_POINT ( 'NONE',  ( 0.2602573258582523419, 4.358078633539736124, 0.1720769237772511173 ) ) ;
#5498=CARTESIAN_POINT ( 'NONE',  ( -0.1167790944451423535, 4.974388888964754507, 0.2819296736111110424 ) ) ;
#5499=ADVANCED_FACE ( 'NONE', ( #14457 ), #13971, .T. ) ;
#5500=CARTESIAN_POINT ( 'NONE',  ( -0.2698011859901125464, 5.151896377161309992, -0.1357330994666928470 ) ) ;
#5503=CARTESIAN_POINT ( 'NONE',  ( 0.1167790944451422702, 4.668833333409200037, -0.2819296736111110979 ) ) ;
#5507=CARTESIAN_POINT ( 'NONE',  ( 0.2819296736111110979, 0.5493055554796889561, 0.000000000000000000 ) ) ;
#5510=CARTESIAN_POINT ( 'NONE',  ( 0.1993543840281266355, 0.2645833332574666907, 0.1993543840281267465 ) ) ;
#5517=CARTESIAN_POINT ( 'NONE',  ( -0.1167790944451424506, 0.2402777777019111383, 0.2819296736111110424 ) ) ;
#5518=CARTESIAN_POINT ( 'NONE',  ( -0.1993543840281266633, 0.0006944443685778107491, -0.1993543840281266910 ) ) ;
#5519=CARTESIAN_POINT ( 'NONE',  ( 5.178964085587577574E-17, 4.436194444520310753, 0.2819296736111110979 ) ) ;
#5521=CARTESIAN_POINT ( 'NONE',  ( 1.995346317926969793E-07, 4.516063323326865664, 0.3119999999998666063 ) ) ;
#5522=CARTESIAN_POINT ( 'NONE',  ( -0.2819296736111110424, 5.148000000075865223, 0.1167790944451424923 ) ) ;
#5524=CARTESIAN_POINT ( 'NONE',  ( 0.2819296736111110979, 4.491750000075865223, -3.452642723725051716E-17 ) ) ;
#5525=CYLINDRICAL_SURFACE ( 'NONE', #19984, 0.3119999999999999996 ) ;
#5527=CARTESIAN_POINT ( 'NONE',  ( 0.1195234880381787768, 3.929255801878827725, -0.2891772058695498138 ) ) ;
#5528=CARTESIAN_POINT ( 'NONE',  ( -0.1292346314604057023, 4.012583333485065573, 0.3119999999999998885 ) ) ;
#5529=CARTESIAN_POINT ( 'NONE',  ( 0.1167790944451424506, 4.439666666742532186, 0.2819296736111110424 ) ) ;
#5530=CARTESIAN_POINT ( 'NONE',  ( -0.1993543840281266910, 3.790361111186976828, -0.1993543840281266910 ) ) ;
#5534=DIRECTION ( 'NONE',  ( 0.000000000000000000, 0.000000000000000000, -1.000000000000000000 ) ) ;
#5535=CARTESIAN_POINT ( 'NONE',  ( -0.03162305771917223868, 0.03242967361111057795, 0.2806037246084505110 ) ) ;
#5537=EDGE_CURVE ( 'NONE', #11539, #19405, #3667, .T. ) ;
#5539=CARTESIAN_POINT ( 'NONE',  ( -5.731347020009612645E-17, 0.4416666665149336923, 0.3119999999999999996 ) ) ;
#5541=CARTESIAN_POINT ( 'NONE',  ( 0.000000000000000000, 5.384999999999999787, 0.000000000000000000 ) ) ;
#5543=CARTESIAN_POINT ( 'NONE',  ( 8.375559671162349491E-15, 3.988277777929486678, -0.3119999999999999996 ) ) ;
#5546=CARTESIAN_POINT ( 'NONE',  ( 0.2950997105373021068, 5.088614608052525412, -0.1005531120067661155 ) ) ;
#5548=ADVANCED_FACE ( 'NONE', ( #14935 ), #9319, .T. ) ;
#5549=CARTESIAN_POINT ( 'NONE',  ( -0.1993543840281266355, 4.193138888964754507, 0.1993543840281267465 ) ) ;
#5550=CARTESIAN_POINT ( 'NONE',  ( -0.2819296736111110979, 5.075083333409198261, 0.000000000000000000 ) ) ;
#5551=CARTESIAN_POINT ( 'NONE',  ( -1.910449006669871087E-17, 4.536888888888888083, -0.3119999999999999996 ) ) ;
#5552=CARTESIAN_POINT ( 'NONE',  ( -0.2723413855784990734, 4.219733285630191233, -0.1575963679250307614 ) ) ;
#5553=CARTESIAN_POINT ( 'NONE',  ( -0.3119999999999999996, 3.825083333333333169, -0.1292346314604056468 ) ) ;
#5554=CARTESIAN_POINT ( 'NONE',  ( -0.3119999999999999996, 4.779944444596176290, 0.000000000000000000 ) ) ;
#5556=CARTESIAN_POINT ( 'NONE',  ( -0.1167790944451423119, 5.189666666742533074, -0.2819296736111110979 ) ) ;
#5564=CARTESIAN_POINT ( 'NONE',  ( 0.2819296736111110979, 5.043833333409199149, 0.1167790944451422425 ) ) ;
#5565=( BOUNDED_CURVE ( )  B_SPLINE_CURVE ( 2, ( #21610, #18072, #2958, #17714, #4779, #10291, #6497, #6858, #10526 ),
 .UNSPECIFIED., .F., .F. ) 
 B_SPLINE_CURVE_WITH_KNOTS ( ( 3, 2, 2, 2, 3 ),
 ( 0.3958333333333333148, 0.4062500000000000000, 0.4166666666666666852, 0.4270833333333333148, 0.4375000000000000000 ),
 .UNSPECIFIED. ) 
 CURVE ( )  GEOMETRIC_REPRESENTATION_ITEM ( )  RATIONAL_B_SPLINE_CURVE ( ( 1.000000000000000000, 0.9238795325112867385, 1.000000000000000000, 0.9238795325112867385, 1.000000000000000000, 0.9238795325112867385, 1.000000000000000000, 0.9238795325112867385, 1.000000000000000000 ) ) 
 REPRESENTATION_ITEM ( '' )  );
#5569=CARTESIAN_POINT ( 'NONE',  ( 0.2819296736111110979, 0.3826388888130222710, 0.000000000000000000 ) ) ;
#5571=CARTESIAN_POINT ( 'NONE',  ( -0.1993543840281266910, 5.026472222298088433, -0.1993543840281266910 ) ) ;
#5572=CARTESIAN_POINT ( 'NONE',  ( 0.05322288965628670793, 4.486797450736038861, -0.3074269533229316287 ) ) ;
#5574=CARTESIAN_POINT ( 'NONE',  ( -0.2819296736111110424, 4.856333333409198261, 0.1167790944451424923 ) ) ;
#5578=CARTESIAN_POINT ( 'NONE',  ( 0.3119999999999999996, 4.582027777777777366, -0.1292346314604056745 ) ) ;
#5579=CARTESIAN_POINT ( 'NONE',  ( 0.1993543840281266633, 3.943138888964754507, -0.1993543840281266910 ) ) ;
#5581=CARTESIAN_POINT ( 'NONE',  ( 0.3122779440621588076, 4.030240700459768455, -0.01080743124828337232 ) ) ;
#5582=DIRECTION ( 'NONE',  ( 0.000000000000000000, 0.000000000000000000, -1.000000000000000000 ) ) ;
#5583=CARTESIAN_POINT ( 'NONE',  ( 0.3120000000000000551, 3.908416666666665762, 0.1292346314604056190 ) ) ;
#5585=AXIS2_PLACEMENT_3D ( 'NONE', #17069, #20849, #15247 ) ;
#5586=CARTESIAN_POINT ( 'NONE',  ( -0.1022736100768033840, 4.124198058143811352, 0.2951942865389927673 ) ) ;
#5588=CARTESIAN_POINT ( 'NONE',  ( 0.03058133199899486232, 4.654066622478140403, -0.3105566612530609172 ) ) ;
#5591=EDGE_CURVE ( 'NONE', #18582, #16287, #13238, .T. ) ;
#5592=CARTESIAN_POINT ( 'NONE',  ( -5.731347020009612645E-17, 0.3930555555555551583, 0.3119999999999999996 ) ) ;
#5595=CARTESIAN_POINT ( 'NONE',  ( 0.1993543840281266910, 0.2090277777019111383, -0.1993543840281266910 ) ) ;
#5596=CARTESIAN_POINT ( 'NONE',  ( 0.04074227727064787252, 3.876059980711638264, -0.3094968829426333334 ) ) ;
#5600=VECTOR ( 'NONE', #11738, 39.37007874015748143 ) ;
#5605=CARTESIAN_POINT ( 'NONE',  ( 0.3119999999999998885, 0.07013888888888854256, 0.1292346314604058410 ) ) ;
#5606=CARTESIAN_POINT ( 'NONE',  ( 0.3119999999999999996, 5.078555555555555046, -3.820898013339742174E-17 ) ) ;
#5608=ORIENTED_EDGE ( 'NONE', *, *, #4410, .T. ) ;
#5609=CARTESIAN_POINT ( 'NONE',  ( -0.1167790944451423257, 4.411888888964754507, -0.2819296736111110424 ) ) ;
#5613=CARTESIAN_POINT ( 'NONE',  ( 0.2593853092514534775, 4.358033725289752525, 0.1733876775689600358 ) ) ;
#5614=CARTESIAN_POINT ( 'NONE',  ( 5.178964085587577574E-17, 4.866750000075865223, 0.2819296736111110979 ) ) ;
#5615=ADVANCED_FACE ( 'NONE', ( #7371 ), #12812, .T. ) ;
#5617=CARTESIAN_POINT ( 'NONE',  ( -0.2706342702141287804, 5.158918473216393075, 0.1307827034094938834 ) ) ;
#5621=CARTESIAN_POINT ( 'NONE',  ( -0.3119999999999998885, 4.998694444444444329, 0.1292346314604058410 ) ) ;
#5622=CARTESIAN_POINT ( 'NONE',  ( 0.1167790944451424506, 4.592444444520309865, 0.2819296736111110424 ) ) ;
#5626=CARTESIAN_POINT ( 'NONE',  ( 0.2819296736111110424, 0.4416666665908000611, -0.1167790944451423119 ) ) ;
#5629=CARTESIAN_POINT ( 'NONE',  ( -0.2819296736111110979, 0.1881944443685777957, -3.452642723725051716E-17 ) ) ;
#5637=CARTESIAN_POINT ( 'NONE',  ( 5.731347020009612645E-17, 4.731333333333332725, 0.3119999999999999996 ) ) ;
#5638=CARTESIAN_POINT ( 'NONE',  ( -0.1993543840281267465, 0.2923611110352445364, 0.1993543840281266633 ) ) ;
#5639=CARTESIAN_POINT ( 'NONE',  ( 0.2819296736111110424, 0.03194444436857781650, 0.1167790944451424923 ) ) ;
#5640=CARTESIAN_POINT ( 'NONE',  ( 5.178964085587577574E-17, 4.547305555631421470, 0.2819296736111110979 ) ) ;
#5643=CARTESIAN_POINT ( 'NONE',  ( -0.2819296736111110424, 5.092444444520309865, 0.1167790944451424923 ) ) ;
#5644=CARTESIAN_POINT ( 'NONE',  ( 0.2819296736111111534, 4.488277777853643791, 0.1167790944451422563 ) ) ;
#5645=CARTESIAN_POINT ( 'NONE',  ( 0.3119669420168502683, 4.917723305947723667, 0.04107160245604204313 ) ) ;
#5647=CARTESIAN_POINT ( 'NONE',  ( 0.3119999999999999996, 3.974388889040620931, -3.820898013339742174E-17 ) ) ;
#5655=CARTESIAN_POINT ( 'NONE',  ( -1.910449006669871087E-17, 4.259111111111110404, -0.3119999999999999996 ) ) ;
#5657=CARTESIAN_POINT ( 'NONE',  ( -0.1341874927019925390, 4.845446088247941319, 0.2816776366694470068 ) ) ;
#5659=ORIENTED_EDGE ( 'NONE', *, *, #9519, .T. ) ;
#5660=CARTESIAN_POINT ( 'NONE',  ( -0.2206173157302028787, 0.4902777776260447973, 0.2206173157302027954 ) ) ;
#5663=CARTESIAN_POINT ( 'NONE',  ( 0.2136809747524369418, 4.759464567214101827, -0.2316255526684406485 ) ) ;
#5665=CARTESIAN_POINT ( 'NONE',  ( 0.1570236185076638036, 3.965114079239589362, 0.2726776789891453556 ) ) ;
#5666=ORIENTED_EDGE ( 'NONE', *, *, #19549, .T. ) ;
#5669=CARTESIAN_POINT ( 'NONE',  ( 0.1311029671040783717, 5.096026576386377904, -0.2823468851309067773 ) ) ;
#5670=CARTESIAN_POINT ( 'NONE',  ( -0.2969103764849149174, 4.671736745946869718, 0.09797322420413220878 ) ) ;
#5671=CARTESIAN_POINT ( 'NONE',  ( 0.1993543840281267465, 4.151472222298087544, 0.1993543840281266633 ) ) ;
#5672=CARTESIAN_POINT ( 'NONE',  ( -0.2819296736111110979, 5.130638888964754507, 0.000000000000000000 ) ) ;
#5675=CARTESIAN_POINT ( 'NONE',  ( 0.3119999999999999996, 3.911888888888888083, -3.820898013339742174E-17 ) ) ;
#5676=CARTESIAN_POINT ( 'NONE',  ( -0.3119999999999999996, 4.835500000151732536, 0.000000000000000000 ) ) ;
#5677=CARTESIAN_POINT ( 'NONE',  ( 0.3104765647686094643, 4.806875790144055749, 0.03085341637652804989 ) ) ;
#5679=CARTESIAN_POINT ( 'NONE',  ( 0.3119999999999998885, 0.4034722222222218435, 0.1292346314604058410 ) ) ;
#5683=CARTESIAN_POINT ( 'NONE',  ( 0.2568083155295264319, 0.03694455021989599686, -0.1289653288417937083 ) ) ;
#5684=ORIENTED_EDGE ( 'NONE', *, *, #17942, .F. ) ;
#5688=CARTESIAN_POINT ( 'NONE',  ( 0.1993543840281267465, 5.207027777853642903, 0.1993543840281266633 ) ) ;
#5689=CARTESIAN_POINT ( 'NONE',  ( -0.1167790944451423119, 3.911888888964754507, -0.2819296736111110979 ) ) ;
#5694=CARTESIAN_POINT ( 'NONE',  ( -0.1993543840281267465, 0.5840277777019110550, 0.1993543840281266633 ) ) ;
#5696=CARTESIAN_POINT ( 'NONE',  ( -0.2819296736111110424, 4.981333333409199149, 0.1167790944451424923 ) ) ;
#5697=CARTESIAN_POINT ( 'NONE',  ( -0.1292346314604081170, 3.929249999999999687, -0.3119999999999975016 ) ) ;
#5698=CARTESIAN_POINT ( 'NONE',  ( -0.1993543840281266910, 4.845916666742532186, -0.1993543840281266910 ) ) ;
#5700=CARTESIAN_POINT ( 'NONE',  ( -1.858121103377620624E-07, 4.877166671810766019, -0.3119999999999446549 ) ) ;
#5704=CARTESIAN_POINT ( 'NONE',  ( 0.1292346314604058410, 4.568138888888888971, 0.3119999999999998885 ) ) ;
#5705=CARTESIAN_POINT ( 'NONE',  ( 0.1993543840281266633, 3.887583333409198705, -0.1993543840281266910 ) ) ;
#5707=CARTESIAN_POINT ( 'NONE',  ( 0.1951823636048612975, 4.022064155229219118, 0.2434209937556025827 ) ) ;
#5708=CARTESIAN_POINT ( 'NONE',  ( -0.09974310894697509255, 3.735413644336969430, 0.2956453992739275227 ) ) ;
#5710=CARTESIAN_POINT ( 'NONE',  ( 0.1540770959472501922, 4.594794592340397443, -0.2743014874479684506 ) ) ;
#5713=( BOUNDED_CURVE ( )  B_SPLINE_CURVE ( 2, ( #9716, #5925, #2161, #2519, #6163, #802, #5807, #9961, #21046 ),
 .UNSPECIFIED., .F., .T. ) 
 B_SPLINE_CURVE_WITH_KNOTS ( ( 3, 2, 2, 2, 3 ),
 ( 0.2053571428571429325, 0.2098214285714285754, 0.2142857142857141906, 0.2187499999999998335, 0.2232142857142854764 ),
 .UNSPECIFIED. ) 
 CURVE ( )  GEOMETRIC_REPRESENTATION_ITEM ( )  RATIONAL_B_SPLINE_CURVE ( ( 0.9999999999999985567, 0.9238795325112881818, 1.000000000000000000, 0.9238795325112867385, 1.000000000000000000, 0.9238795325112867385, 1.000000000000000000, 0.9238795325112909573, 0.9999999999999957812 ) ) 
 REPRESENTATION_ITEM ( '' )  );
#5717=CARTESIAN_POINT ( 'NONE',  ( 0.1303732590071332853, 4.151117928182491035, -0.2856235017375695628 ) ) ;
#5719=CARTESIAN_POINT ( 'NONE',  ( 0.1900105704308386045, 5.206640035683666845, 0.2082794372640154323 ) ) ;
#5720=CARTESIAN_POINT ( 'NONE',  ( 0.3008229147836520290, 5.144663873052548908, 0.04257211586236403500 ) ) ;
#5724=CARTESIAN_POINT ( 'NONE',  ( -0.1993543840281266633, 0.1673611110352444808, -0.1993543840281266910 ) ) ;
#5727=CARTESIAN_POINT ( 'NONE',  ( 0.000000000000000000, 5.384999999999999787, 0.000000000000000000 ) ) ;
#5729=CARTESIAN_POINT ( 'NONE',  ( -0.01015435915181665469, 5.092370350171590232, -0.3113982329504829671 ) ) ;
#5731=CARTESIAN_POINT ( 'NONE',  ( 0.2206173157302028232, 0.3027777777777774237, -0.2206173157302028232 ) ) ;
#5732=CARTESIAN_POINT ( 'NONE',  ( -0.1292346314604057023, 5.227861111111110404, 0.3119999999999998885 ) ) ;
#5734=CARTESIAN_POINT ( 'NONE',  ( 0.1993543840281267465, 4.276472222298088433, 0.1993543840281266633 ) ) ;
#5738=ORIENTED_EDGE ( 'NONE', *, *, #23208, .T. ) ;
#5739=EDGE_CURVE ( 'NONE', #6274, #1526, #6265, .T. ) ;
#5740=CARTESIAN_POINT ( 'NONE',  ( -0.2819296736111110424, 4.960500000075865223, -0.1167790944451423119 ) ) ;
#5746=CARTESIAN_POINT ( 'NONE',  ( -0.2819296736111110424, 4.745222222298088433, 0.1167790944451424923 ) ) ;
#5748=CARTESIAN_POINT ( 'NONE',  ( -0.1530498720672202884, 4.067052562292516882, 0.2718834723444233381 ) ) ;
#5750=CARTESIAN_POINT ( 'NONE',  ( 0.1993543840281266355, 0.5423611110352445364, 0.1993543840281267465 ) ) ;
#5752=VERTEX_POINT ( 'NONE', #2247 ) ;
#5753=CARTESIAN_POINT ( 'NONE',  ( 0.2819296736111110979, 0.2159722221463555858, 0.000000000000000000 ) ) ;
#5760=CARTESIAN_POINT ( 'NONE',  ( -0.2819296736111110979, 0.3409722221463556413, -3.452642723725051716E-17 ) ) ;
#5762=CARTESIAN_POINT ( 'NONE',  ( 0.1993543840281266633, 4.179250000075865223, -0.1993543840281266910 ) ) ;
#5765=CARTESIAN_POINT ( 'NONE',  ( 0.1167790944451424368, 4.773000000075866112, 0.2819296736111110424 ) ) ;
#5766=CARTESIAN_POINT ( 'NONE',  ( 5.178964085587577574E-17, 4.366750000075866112, 0.2819296736111110979 ) ) ;
#5768=CARTESIAN_POINT ( 'NONE',  ( 0.3135651898165193185, 3.919649592934535853, -0.02960734467547308443 ) ) ;
#5769=CARTESIAN_POINT ( 'NONE',  ( -0.3119999999999999996, 4.168833333485065573, 0.000000000000000000 ) ) ;
#5778=CARTESIAN_POINT ( 'NONE',  ( 1.910449006669871087E-17, 0.4694444442927115380, -0.3119999999999999996 ) ) ;
#5780=FACE_OUTER_BOUND ( 'NONE', #19468, .T. ) ;
#5788=CARTESIAN_POINT ( 'NONE',  ( -0.1167790944451423257, 3.953555555631421914, -0.2819296736111110424 ) ) ;
#5789=CARTESIAN_POINT ( 'NONE',  ( 0.01388454463234072185, 5.043460286985110841, -0.3120000000000000551 ) ) ;
#5791=CARTESIAN_POINT ( 'NONE',  ( 0.2206173157302028787, 3.849388888888888083, 0.2206173157302027954 ) ) ;
#5793=CARTESIAN_POINT ( 'NONE',  ( -0.3119999999999998885, 4.672305555707288782, 0.1292346314604058410 ) ) ;
#5794=CARTESIAN_POINT ( 'NONE',  ( -0.1993543840281266355, 5.151472222298088433, 0.1993543840281267465 ) ) ;
#5795=CARTESIAN_POINT ( 'NONE',  ( -0.1167790944451423257, 4.175777777853643791, -0.2819296736111110424 ) ) ;
#5796=CARTESIAN_POINT ( 'NONE',  ( -0.06721871850921422309, 3.903017741005486485, 0.3063181425897485433 ) ) ;
#5798=EDGE_CURVE ( 'NONE', #14944, #3503, #19737, .T. ) ;
#5803=CARTESIAN_POINT ( 'NONE',  ( 0.2819296736111110424, 5.161888888964753619, -0.1167790944451423396 ) ) ;
#5804=CARTESIAN_POINT ( 'NONE',  ( 0.1167790944451422702, 3.793833333409199149, -0.2819296736111110979 ) ) ;
#5805=VECTOR ( 'NONE', #19436, 39.37007874015748143 ) ;
#5806=CARTESIAN_POINT ( 'NONE',  ( 0.2211792888862010864, 4.425861817871897586, -0.2225068856345374380 ) ) ;
#5807=CARTESIAN_POINT ( 'NONE',  ( -0.2206173157302028232, 4.932722222222221120, -0.2206173157302028232 ) ) ;
#5809=CARTESIAN_POINT ( 'NONE',  ( -0.1993543840281267465, 0.5284722221463555858, 0.1993543840281266633 ) ) ;
#5811=CARTESIAN_POINT ( 'NONE',  ( -0.2819296736111110424, 4.863277777853643791, -0.1167790944451423119 ) ) ;
#5812=CARTESIAN_POINT ( 'NONE',  ( 0.2727366458256587634, 4.469775673605889565, 0.1569361545628811805 ) ) ;
#5813=CARTESIAN_POINT ( 'NONE',  ( 0.1993543840281267465, 4.818138888964754507, 0.1993543840281266633 ) ) ;
#5816=CARTESIAN_POINT ( 'NONE',  ( 0.3120000000000000551, 4.075083333333332725, 0.1292346314604056190 ) ) ;
#5818=CARTESIAN_POINT ( 'NONE',  ( 0.2206173157302027954, 4.418833333333332725, -0.2206173157302028232 ) ) ;
#5821=CYLINDRICAL_SURFACE ( 'NONE', #18618, 0.3119999999999999996 ) ;
#5825=CARTESIAN_POINT ( 'NONE',  ( -1.910449006669871087E-17, 4.536888888888888083, -0.3119999999999999996 ) ) ;
#5826=B_SPLINE_CURVE_WITH_KNOTS ( 'NONE', 3,
 ( #20475, #21815, #3280, #16338, #23750, #12696, #21930, #3405, #10855, #13297, #15559, #2633, #6405, #18889, #11456, #2750, #12038, #11333, #5831, #10321, #18762, #22543, #20711, #21162, #2189, #5720, #14997, #17054, #9621, #6284, #13739, #10082, #17503, #4007, #19337, #21287, #4453, #13180, #347, #17746, #7786, #15797, #22980, #15677, #11917, #23217 ),
 .UNSPECIFIED., .F., .F.,
 ( 4, 2, 2, 2, 2, 2, 2, 2, 2, 2, 2, 2, 2, 2, 2, 2, 2, 2, 2, 2, 2, 2, 4 ),
 ( 0.02876147360672271294, 0.02951887419360549672, 0.03027627478048828050, 0.03179107595425384458, 0.03330587712801941214, 0.03406327771490218898, 0.03482067830178496581, 0.03633547947555052643, 0.03785028064931608704, 0.03936508182308164072, 0.04012248240996442450, 0.04087988299684719440, 0.04163728358372997818, 0.04239468417061275501, 0.04390948534437830869, 0.04542428651814386931, 0.04693908769190942298, 0.04769648827879220676, 0.04845388886567497666, 0.04996869003944054421, 0.05148349121320609789, 0.05224089180008888167, 0.05299829238697165851 ),
 .UNSPECIFIED. ) ;
#5827=VERTEX_POINT ( 'NONE', #23425 ) ;
#5828=CARTESIAN_POINT ( 'NONE',  ( -0.1656294416274741443, 4.122187037343969074, 0.2644585830901644008 ) ) ;
#5830=CARTESIAN_POINT ( 'NONE',  ( 0.04084089659891350366, 4.320441687794666308, -0.3120000000710619892 ) ) ;
#5831=CARTESIAN_POINT ( 'NONE',  ( 0.2937600628871613329, 5.148624849934147818, -0.07568332425666259022 ) ) ;
#5837=CARTESIAN_POINT ( 'NONE',  ( 0.1993543840281266355, 0.5284722221463555858, 0.1993543840281267465 ) ) ;
#5844=CARTESIAN_POINT ( 'NONE',  ( -0.2206173157302027954, 0.3166666666666663188, -0.2206173157302028232 ) ) ;
#5845=CARTESIAN_POINT ( 'NONE',  ( -0.1292346314604056745, 5.262583333333332725, -0.3119999999999999996 ) ) ;
#5846=EDGE_CURVE ( 'NONE', #21247, #10793, #5565, .T. ) ;
#5847=CARTESIAN_POINT ( 'NONE',  ( -1.726321361862525858E-17, 4.186194444520309865, -0.2819296736111110979 ) ) ;
#5850=ORIENTED_EDGE ( 'NONE', *, *, #13080, .F. ) ;
#5852=CARTESIAN_POINT ( 'NONE',  ( 0.1292346314604056745, 0.3618055555555552694, -0.3119999999999999996 ) ) ;
#5853=CARTESIAN_POINT ( 'NONE',  ( -1.726321361862525858E-17, 4.894527777853642903, -0.2819296736111110979 ) ) ;
#5855=CARTESIAN_POINT ( 'NONE',  ( -0.09684493161512809645, 5.145868290167153525, -0.2881700814494116969 ) ) ;
#5859=CARTESIAN_POINT ( 'NONE',  ( 0.1167790944451424506, 4.759111111186976828, 0.2819296736111110424 ) ) ;
#5860=CARTESIAN_POINT ( 'NONE',  ( 5.731347020009612645E-17, 4.286888888888888083, 0.3119999999999999996 ) ) ;
#5862=CARTESIAN_POINT ( 'NONE',  ( 0.2819296736111110424, 0.6013888888130223265, 0.1167790944451424923 ) ) ;
#5864=CARTESIAN_POINT ( 'NONE',  ( 0.1993543840281266355, 0.4312499999241333759, 0.1993543840281267465 ) ) ;
#5869=CARTESIAN_POINT ( 'NONE',  ( -0.2819296736111110979, 0.2263888888130222710, -0.1167790944451423396 ) ) ;
#5870=CARTESIAN_POINT ( 'NONE',  ( 1.726321361862525858E-17, 0.2159722221463555858, -0.2819296736111110979 ) ) ;
#5873=CARTESIAN_POINT ( 'NONE',  ( 5.178964085587577574E-17, 4.380638888964754507, 0.2819296736111110979 ) ) ;
#5875=EDGE_CURVE ( 'NONE', #6276, #10051, #17325, .T. ) ;
#5876=CARTESIAN_POINT ( 'NONE',  ( -0.2819296736111110424, 4.918833333409199149, -0.1167790944451423119 ) ) ;
#5877=CARTESIAN_POINT ( 'NONE',  ( 0.2819296736111110979, 4.436194444520309865, -3.452642723725051716E-17 ) ) ;
#5878=CARTESIAN_POINT ( 'NONE',  ( 7.484242640931070629E-07, 4.016084960865516251, 0.3119999999981048489 ) ) ;
#5880=CARTESIAN_POINT ( 'NONE',  ( -0.3119999999999999996, 4.165361111262843252, -0.1292346314604056468 ) ) ;
#5881=LINE ( 'NONE', #2241, #6789 ) ;
#5882=DIRECTION ( 'NONE',  ( -0.000000000000000000, -1.000000000000000000, -0.000000000000000000 ) ) ;
#5888=LINE ( 'NONE', #20649, #586 ) ;
#5892=CARTESIAN_POINT ( 'NONE',  ( 0.2206173157302028232, 0.5736111109593782231, -0.2206173157302028232 ) ) ;
#5900=CARTESIAN_POINT ( 'NONE',  ( -0.1292346314604056190, 0.4798611111111107941, -0.3119999999999999996 ) ) ;
#5904=CARTESIAN_POINT ( 'NONE',  ( 1.910449006669871087E-17, 0.2472222220704892726, -0.3119999999999999996 ) ) ;
#5907=CARTESIAN_POINT ( 'NONE',  ( -0.1993543840281266355, 4.082027777853643791, 0.1993543840281267465 ) ) ;
#5909=CARTESIAN_POINT ( 'NONE',  ( -0.2206173157302027676, 4.835499999999999687, 0.2206173157302028787 ) ) ;
#5910=CARTESIAN_POINT ( 'NONE',  ( -0.1292346314604056745, 3.762583333333332725, -0.3119999999999999996 ) ) ;
#5911=CARTESIAN_POINT ( 'NONE',  ( 0.1292346314604058410, 4.797305555707287894, 0.3119999999999998885 ) ) ;
#5912=CARTESIAN_POINT ( 'NONE',  ( 0.2819296736111111534, 4.946611111186976828, 0.1167790944451422563 ) ) ;
#5914=CARTESIAN_POINT ( 'NONE',  ( 5.178964085587577574E-17, 4.366750000075866112, 0.2819296736111110979 ) ) ;
#5918=B_SPLINE_CURVE_WITH_KNOTS ( 'NONE', 3,
 ( #6697, #12555, #7175, #8748, #10715, #8878, #14494, #12416, #6788, #11476, #1959, #8980 ),
 .UNSPECIFIED., .F., .F.,
 ( 4, 2, 2, 2, 2, 4 ),
 ( 0.000000000000000000, 0.001334276959395565938, 0.002668553918791131876, 0.004002830878186698464, 0.004669969357884482843, 0.005337107837582267221 ),
 .UNSPECIFIED. ) ;
#5922=CARTESIAN_POINT ( 'NONE',  ( 0.2819296736111110979, 3.898000000075866112, -0.1167790944451423396 ) ) ;
#5925=CARTESIAN_POINT ( 'NONE',  ( -0.1292346314604075619, 4.950083333333332725, 0.3119999999999980567 ) ) ;
#5927=CARTESIAN_POINT ( 'NONE',  ( 0.1993543840281266355, 0.4868055554796889561, 0.1993543840281267465 ) ) ;
#5929=EDGE_CURVE ( 'NONE', #3340, #16124, #22371, .T. ) ;
#5930=CARTESIAN_POINT ( 'NONE',  ( 0.1167790944451422702, 4.960500000075865223, -0.2819296736111110424 ) ) ;
#5932=AXIS2_PLACEMENT_3D ( 'NONE', #13752, #19222, #11800 ) ;
#5934=CARTESIAN_POINT ( 'NONE',  ( 0.1167790944451422702, 4.557722222298087544, -0.2819296736111110424 ) ) ;
#5935=CARTESIAN_POINT ( 'NONE',  ( 4.589422455927707524E-07, 4.793851445074613693, 0.3119999999992840167 ) ) ;
#5936=CARTESIAN_POINT ( 'NONE',  ( 0.2122804003021576125, 4.856019927748675968, 0.2286534880123932689 ) ) ;
#5939=CARTESIAN_POINT ( 'NONE',  ( -0.3119999999999999996, 4.436194444444444329, -0.1292346314604056468 ) ) ;
#5940=CARTESIAN_POINT ( 'NONE',  ( 0.2819296736111111534, 3.877166666742532186, 0.1167790944451422563 ) ) ;
#5942=CARTESIAN_POINT ( 'NONE',  ( -0.2206173157302027676, 4.002166666666665762, 0.2206173157302028787 ) ) ;
#5944=CARTESIAN_POINT ( 'NONE',  ( 0.3117100783463861990, 4.585130279527236397, 0.01372980001063455260 ) ) ;
#5946=CARTESIAN_POINT ( 'NONE',  ( -0.2348293880619035656, 4.119665766202905033, 0.2088470014844988898 ) ) ;
#5953=CARTESIAN_POINT ( 'NONE',  ( -0.1167790944451424368, 0.4624999999241333759, 0.2819296736111110424 ) ) ;
#5954=DIRECTION ( 'NONE',  ( -0.000000000000000000, -1.000000000000000000, -0.000000000000000000 ) ) ;
#5958=CARTESIAN_POINT ( 'NONE',  ( -0.3078280617541462316, 4.614801766752763434, 0.05510150218785365983 ) ) ;
#5960=CARTESIAN_POINT ( 'NONE',  ( 0.3119999999999999996, 0.2958333333333329485, 0.000000000000000000 ) ) ;
#5961=CARTESIAN_POINT ( 'NONE',  ( -0.3119999999999998885, 5.220916666666665762, 0.1292346314604058410 ) ) ;
#5963=CARTESIAN_POINT ( 'NONE',  ( -0.1167790944451423257, 4.245222222298088433, -0.2819296736111110424 ) ) ;
#5968=CARTESIAN_POINT ( 'NONE',  ( 0.3119999999999999996, 0.3513888888888885287, 0.000000000000000000 ) ) ;
#5969=CARTESIAN_POINT ( 'NONE',  ( 0.1993543840281267465, 4.762583333409199149, 0.1993543840281266633 ) ) ;
#5971=EDGE_CURVE ( 'NONE', #13964, #7602, #4925, .T. ) ;
#5972=CARTESIAN_POINT ( 'NONE',  ( -0.2387229431459631235, 5.150382089001773522, -0.1856462434723448740 ) ) ;
#5974=CARTESIAN_POINT ( 'NONE',  ( 0.04478946178605012346, 3.709278574126537276, -0.3088990676013957937 ) ) ;
#5976=CARTESIAN_POINT ( 'NONE',  ( -1.726321361862525858E-17, 4.408416666742533074, -0.2819296736111110979 ) ) ;
#5979=CARTESIAN_POINT ( 'NONE',  ( -0.02226417865471658208, 4.044440256128997824, -0.3112113514703778727 ) ) ;
#5982=ORIENTED_EDGE ( 'NONE', *, *, #7369, .F. ) ;
#5983=CARTESIAN_POINT ( 'NONE',  ( -0.2819296736111110424, 0.4624999999241333759, -0.1167790944451423396 ) ) ;
#5984=FACE_OUTER_BOUND ( 'NONE', #6690, .T. ) ;
#5990=CARTESIAN_POINT ( 'NONE',  ( 0.2819296736111110424, 0.4763888888130222710, 0.1167790944451424923 ) ) ;
#5991=CARTESIAN_POINT ( 'NONE',  ( 0.2819296736111110424, 0.2611111110352444808, -0.1167790944451423119 ) ) ;
#5992=CARTESIAN_POINT ( 'NONE',  ( -0.1993543840281266355, 4.262583333409199149, 0.1993543840281267465 ) ) ;
#5994=CARTESIAN_POINT ( 'NONE',  ( -0.2819296736111110979, 4.866750000075866112, 0.000000000000000000 ) ) ;
#5995=CARTESIAN_POINT ( 'NONE',  ( -0.2819296736111110979, 4.182722222298087544, -0.1167790944451422980 ) ) ;
#5999=CARTESIAN_POINT ( 'NONE',  ( -1.910449006669871087E-17, 3.988277777929510215, -0.3119999999999999996 ) ) ;
#6004=ADVANCED_FACE ( 'NONE', ( #15025 ), #9284, .T. ) ;
#6006=( BOUNDED_CURVE ( )  B_SPLINE_CURVE ( 2, ( #15364, #13779, #21207, #4499, #11964, #246, #19135, #15130, #20967 ),
 .UNSPECIFIED., .F., .F. ) 
 B_SPLINE_CURVE_WITH_KNOTS ( ( 3, 2, 2, 2, 3 ),
 ( 0.9196428571428570953, 0.9241071428571429047, 0.9285714285714286031, 0.9330357142857144126, 0.9375000000000001110 ),
 .UNSPECIFIED. ) 
 CURVE ( )  GEOMETRIC_REPRESENTATION_ITEM ( )  RATIONAL_B_SPLINE_CURVE ( ( 1.000000000000000000, 0.9238795325112867385, 1.000000000000000000, 0.9238795325112867385, 1.000000000000000000, 0.9238795325112867385, 1.000000000000000000, 0.9238795325112848511, 1.000000000000001998 ) ) 
 REPRESENTATION_ITEM ( '' )  );
#6008=CARTESIAN_POINT ( 'NONE',  ( -0.2447671590917250006, 5.008122686144473867, 0.1936521771237534884 ) ) ;
#6010=CARTESIAN_POINT ( 'NONE',  ( 0.2206173157302028232, 0.4069444442927114824, -0.2206173157302028232 ) ) ;
#6011=ORIENTED_EDGE ( 'NONE', *, *, #21933, .F. ) ;
#6014=CARTESIAN_POINT ( 'NONE',  ( -0.2206173157302028787, 0.5527777777777773682, 0.2206173157302027954 ) ) ;
#6017=ORIENTED_EDGE ( 'NONE', *, *, #11879, .T. ) ;
#6020=CARTESIAN_POINT ( 'NONE',  ( -8.252060436089559755E-07, 4.682689096385127314, 0.3119999999976427185 ) ) ;
#6021=CARTESIAN_POINT ( 'NONE',  ( -0.1167790944451423535, 3.918833333409198705, 0.2819296736111110424 ) ) ;
#6023=CARTESIAN_POINT ( 'NONE',  ( 0.07921175570129510013, 5.120394104548939396, 0.2987029092252261320 ) ) ;
#6025=CARTESIAN_POINT ( 'NONE',  ( -0.2896199013420221458, 5.181292007268502253, 0.04275989185916429652 ) ) ;
#6026=CARTESIAN_POINT ( 'NONE',  ( 0.3119999999999999996, 4.637583333485064685, 0.1292346314604056190 ) ) ;
#6027=CARTESIAN_POINT ( 'NONE',  ( 0.2819296736111110979, 4.953555555631421470, -0.1167790944451423396 ) ) ;
#6031=CARTESIAN_POINT ( 'NONE',  ( -0.2819296736111110424, 4.238277777853642903, -0.1167790944451423119 ) ) ;
#6042=CARTESIAN_POINT ( 'NONE',  ( 5.178964085587577574E-17, 3.880638888964754951, 0.2819296736111110979 ) ) ;
#6043=CARTESIAN_POINT ( 'NONE',  ( 0.2988699043018692714, 4.421723770119410979, -0.09822243194017121759 ) ) ;
#6044=CARTESIAN_POINT ( 'NONE',  ( 0.1292346314604045920, 4.623694444444444329, 0.3120000000000012208 ) ) ;
#6047=CARTESIAN_POINT ( 'NONE',  ( 0.1167790944451423119, 0.5041666665908001166, -0.2819296736111110979 ) ) ;
#6049=VERTEX_POINT ( 'NONE', #12848 ) ;
#6050=CARTESIAN_POINT ( 'NONE',  ( -0.1167790944451423535, 4.654944444520310753, 0.2819296736111110424 ) ) ;
#6051=CARTESIAN_POINT ( 'NONE',  ( 1.337745543335387199E-07, 4.460505239618372642, 0.3119999999999396589 ) ) ;
#6053=CARTESIAN_POINT ( 'NONE',  ( -0.1167790944451423535, 4.641055555631422358, 0.2819296736111110424 ) ) ;
#6054=LINE ( 'NONE', #19104, #16527 ) ;
#6055=CARTESIAN_POINT ( 'NONE',  ( 0.000000000000000000, 5.384999999999999787, 0.000000000000000000 ) ) ;
#6058=CARTESIAN_POINT ( 'NONE',  ( 0.1292346314604056190, 4.422305555555555934, -0.3119999999999999996 ) ) ;
#6059=CARTESIAN_POINT ( 'NONE',  ( 0.1993543840281267465, 3.873694444520310309, 0.1993543840281266633 ) ) ;
#6061=CARTESIAN_POINT ( 'NONE',  ( -0.3120000000000000551, 0.5423611109593781121, 0.1292346314604056190 ) ) ;
#6065=VERTEX_POINT ( 'NONE', #5383 ) ;
#6068=CARTESIAN_POINT ( 'NONE',  ( 3.820898013339742174E-17, 5.384999999999999787, 0.3119999999999999996 ) ) ;
#6072=ORIENTED_EDGE ( 'NONE', *, *, #16045, .F. ) ;
#6075=CARTESIAN_POINT ( 'NONE',  ( 0.2819296736111110979, 0.4243055554796889006, 0.000000000000000000 ) ) ;
#6080=CARTESIAN_POINT ( 'NONE',  ( -0.2743877791054161186, 4.617644326071688177, 0.1497255358440195416 ) ) ;
#6083=CARTESIAN_POINT ( 'NONE',  ( -0.3119999999999999996, 0.2090277777777773960, -0.1292346314604056745 ) ) ;
#6084=CARTESIAN_POINT ( 'NONE',  ( -0.2206173157302028232, 5.099388888888888083, -0.2206173157302028232 ) ) ;
#6086=CARTESIAN_POINT ( 'NONE',  ( -0.1993543840281266910, 4.193138888964754507, -0.1993543840281266910 ) ) ;
#6091=CARTESIAN_POINT ( 'NONE',  ( -0.2819296736111110424, 4.738277777853642903, -0.1167790944451423119 ) ) ;
#6093=CARTESIAN_POINT ( 'NONE',  ( -0.02658772628240861288, 4.515328577936132959, 0.3108651180470201614 ) ) ;
#6095=CARTESIAN_POINT ( 'NONE',  ( 0.0009813424927043168638, 3.710473627540171293, -0.3119986777745635265 ) ) ;
#6096=CARTESIAN_POINT ( 'NONE',  ( 0.2206173157302027676, 0.6152777776260449638, 0.2206173157302028787 ) ) ;
#6098=CARTESIAN_POINT ( 'NONE',  ( -0.2819296736111110424, 4.314666666742533074, 0.1167790944451424923 ) ) ;
#6100=CARTESIAN_POINT ( 'NONE',  ( -0.2115167397750339906, 4.050456258765779971, -0.2294101962960885810 ) ) ;
#6103=CARTESIAN_POINT ( 'NONE',  ( 0.1167790944451423535, 0.4277777777019110550, 0.2819296736111110424 ) ) ;
#6104=CARTESIAN_POINT ( 'NONE',  ( 3.820898013339742174E-17, 5.384999999999999787, 0.3119999999999999996 ) ) ;
#6108=CARTESIAN_POINT ( 'NONE',  ( 5.731347020009612645E-17, 3.953555555555555046, 0.3119999999999999996 ) ) ;
#6110=CARTESIAN_POINT ( 'NONE',  ( -0.1167790944451424506, 0.4069444443685778512, 0.2819296736111110424 ) ) ;
#6111=CARTESIAN_POINT ( 'NONE',  ( -0.1167790944451424368, 0.1291666665908000611, 0.2819296736111110424 ) ) ;
#6112=ORIENTED_EDGE ( 'NONE', *, *, #18697, .T. ) ;
#6113=CARTESIAN_POINT ( 'NONE',  ( 0.1993543840281266633, 4.290361111186976828, -0.1993543840281266910 ) ) ;
#6115=CARTESIAN_POINT ( 'NONE',  ( -0.2819296736111110424, 4.974388888964754507, -0.1167790944451423119 ) ) ;
#6116=CARTESIAN_POINT ( 'NONE',  ( -0.1167790944451423535, 4.307722222298088433, 0.2819296736111110979 ) ) ;
#6119=VERTEX_POINT ( 'NONE', #11244 ) ;
#6120=CARTESIAN_POINT ( 'NONE',  ( 0.3119999999999999996, 4.522999999999999687, -3.820898013339742174E-17 ) ) ;
#6121=CARTESIAN_POINT ( 'NONE',  ( -0.3119999999999999996, 3.943138889040620931, -0.1292346314604056468 ) ) ;
#6127=CARTESIAN_POINT ( 'NONE',  ( -0.3104543573706212145, 5.003321778821203658, 0.03789056874165915023 ) ) ;
#6129=CARTESIAN_POINT ( 'NONE',  ( 0.1993543840281266355, 0.1534722221463556135, 0.1993543840281267465 ) ) ;
#6132=CARTESIAN_POINT ( 'NONE',  ( 0.03688365757930828215, 4.265052467647925560, -0.3099171647324295287 ) ) ;
#6134=CARTESIAN_POINT ( 'NONE',  ( 0.3121991201319634923, 4.753296228494991560, -0.04110499377590303566 ) ) ;
#6136=CARTESIAN_POINT ( 'NONE',  ( 0.2838754445270939009, 5.176981630833639159, 0.07949240647762143008 ) ) ;
#6137=ORIENTED_EDGE ( 'NONE', *, *, #17286, .F. ) ;
#6140=CARTESIAN_POINT ( 'NONE',  ( -1.910449006669871087E-17, 3.870222222222221564, -0.3119999999999999996 ) ) ;
#6142=CARTESIAN_POINT ( 'NONE',  ( -0.1167790944451423257, 3.898000000075865668, -0.2819296736111110424 ) ) ;
#6144=CARTESIAN_POINT ( 'NONE',  ( -0.2786158314465964625, 5.183151893613593408, 0.08921164663449078491 ) ) ;
#6145=CARTESIAN_POINT ( 'NONE',  ( -0.3119999999999998885, 4.450083333485065573, 0.1292346314604058410 ) ) ;
#6147=CARTESIAN_POINT ( 'NONE',  ( 5.178964085587577574E-17, 4.880638888964754507, 0.2819296736111110979 ) ) ;
#6148=ORIENTED_EDGE ( 'NONE', *, *, #8461, .F. ) ;
#6149=CARTESIAN_POINT ( 'NONE',  ( 0.2819296736111110979, 4.269527777853643791, -3.452642723725051716E-17 ) ) ;
#6153=ORIENTED_EDGE ( 'NONE', *, *, #1453, .T. ) ;
#6158=CARTESIAN_POINT ( 'NONE',  ( 0.1292346314604056745, 0.3062499999999995781, -0.3119999999999999996 ) ) ;
#6159=CARTESIAN_POINT ( 'NONE',  ( -1.726321361862525858E-17, 3.741750000075865668, -0.2819296736111110979 ) ) ;
#6160=CARTESIAN_POINT ( 'NONE',  ( 0.2614991890488166937, 4.413735171690442272, 0.1718472760850429104 ) ) ;
#6163=CARTESIAN_POINT ( 'NONE',  ( -0.3119999999999999996, 4.939666666666665762, 0.000000000000000000 ) ) ;
#6167=CARTESIAN_POINT ( 'NONE',  ( -0.1167790944451424506, 0.4763888888130222155, 0.2819296736111110424 ) ) ;
#6169=ORIENTED_EDGE ( 'NONE', *, *, #17076, .F. ) ;
#6170=CARTESIAN_POINT ( 'NONE',  ( 0.1993543840281267465, 4.720916666742533074, 0.1993543840281266633 ) ) ;
#6172=CARTESIAN_POINT ( 'NONE',  ( -0.1993543840281266355, 4.637583333409198261, 0.1993543840281267465 ) ) ;
#6173=CARTESIAN_POINT ( 'NONE',  ( 0.2206173157302027676, 0.2819444442927114824, 0.2206173157302028787 ) ) ;
#6177=CARTESIAN_POINT ( 'NONE',  ( -0.1292346314604056745, 4.207027777777777366, -0.3119999999999999996 ) ) ;
#6179=CARTESIAN_POINT ( 'NONE',  ( -1.726321361862525858E-17, 3.727861111186976384, -0.2819296736111110979 ) ) ;
#6185=CARTESIAN_POINT ( 'NONE',  ( 0.2792411303351374219, 4.700719259618558965, -0.1393336886063105129 ) ) ;
#6187=CARTESIAN_POINT ( 'NONE',  ( 0.1907726824043486646, 4.133016981313245353, 0.2468801249805909759 ) ) ;
#6189=CARTESIAN_POINT ( 'NONE',  ( -0.0003188451214018954817, 3.932731264085634670, -0.3119998472765105890 ) ) ;
#6193=CARTESIAN_POINT ( 'NONE',  ( 0.1993543840281266910, 0.5423611110352445364, -0.1993543840281266910 ) ) ;
#6196=CARTESIAN_POINT ( 'NONE',  ( -5.731347020009612645E-17, 0.5041666666666663188, 0.3119999999999999996 ) ) ;
#6198=ORIENTED_EDGE ( 'NONE', *, *, #2331, .F. ) ;
#6200=CARTESIAN_POINT ( 'NONE',  ( -0.2048285092061691848, 5.112368305460988971, 0.2322580485435521980 ) ) ;
#6203=CARTESIAN_POINT ( 'NONE',  ( 1.910449006669871087E-17, 0.1430555555555552139, -0.3119999999999999996 ) ) ;
#6204=CARTESIAN_POINT ( 'NONE',  ( 0.3119999999999999996, 4.852861111111110404, 0.1292346314604056190 ) ) ;
#6206=CARTESIAN_POINT ( 'NONE',  ( 0.2819296736111110979, 3.894527777853643347, -3.452642723725051716E-17 ) ) ;
#6208=CARTESIAN_POINT ( 'NONE',  ( -0.2726800006319771708, 4.330919655780821387, -0.1570310010236034837 ) ) ;
#6213=CARTESIAN_POINT ( 'NONE',  ( -1.726321361862525858E-17, 4.727861111186976828, -0.2819296736111110979 ) ) ;
#6220=VECTOR ( 'NONE', #17576, 39.37007874015748143 ) ;
#6221=CARTESIAN_POINT ( 'NONE',  ( -0.1993543840281266355, 4.373694444520309865, 0.1993543840281267465 ) ) ;
#6225=CARTESIAN_POINT ( 'NONE',  ( -0.1993543840281266633, 0.4590277777019112215, -0.1993543840281266910 ) ) ;
#6228=CARTESIAN_POINT ( 'NONE',  ( 3.820898013339742174E-17, 5.384999999999999787, 0.3119999999999999996 ) ) ;
#6231=CARTESIAN_POINT ( 'NONE',  ( 1.519200945994765378E-06, 3.766055514889470324, -0.3119999999963013471 ) ) ;
#6232=CARTESIAN_POINT ( 'NONE',  ( 0.2819296736111110424, 0.4208333332574666907, 0.1167790944451424923 ) ) ;
#6233=CARTESIAN_POINT ( 'NONE',  ( -5.178964085587577574E-17, 0.1326388888130222710, 0.2819296736111110979 ) ) ;
#6234=CARTESIAN_POINT ( 'NONE',  ( -0.2819296736111110424, 4.092444444520309865, 0.1167790944451424923 ) ) ;
#6237=CARTESIAN_POINT ( 'NONE',  ( -1.726321361862525858E-17, 4.963972222298088433, -0.2819296736111110979 ) ) ;
#6241=ORIENTED_EDGE ( 'NONE', *, *, #4244, .F. ) ;
#6243=CARTESIAN_POINT ( 'NONE',  ( 0.3119999999999999996, 3.804250000151731648, 0.1292346314604056190 ) ) ;
#6247=ORIENTED_EDGE ( 'NONE', *, *, #15293, .F. ) ;
#6252=CARTESIAN_POINT ( 'NONE',  ( -0.1908996484622546286, 5.010266985262351369, 0.2504379711342784032 ) ) ;
#6254=CARTESIAN_POINT ( 'NONE',  ( 0.1993543840281266910, 0.1118055554796889145, -0.1993543840281266910 ) ) ;
#6256=CARTESIAN_POINT ( 'NONE',  ( 0.2860402380377710108, 4.255804247949799723, -0.1246337105255282962 ) ) ;
#6258=CARTESIAN_POINT ( 'NONE',  ( 0.1161582368758659611, 4.075052052462464047, 0.2903959765898691536 ) ) ;
#6265=B_SPLINE_CURVE_WITH_KNOTS ( 'NONE', 3,
 ( #15528, #4422, #11638, #7959, #6252, #13595, #7842, #17239, #10050, #11887, #648, #17356, #766, #21008, #6008, #19180, #19302, #522, #4184, #9681, #2489, #6127, #4301, #13823, #15289, #15647, #23067, #22606, #6375, #21257, #4545, #12008, #22718, #2117, #19063, #7725, #284, #15171, #20772, #4061 ),
 .UNSPECIFIED., .F., .F.,
 ( 4, 2, 2, 1, 2, 2, 1, 1, 2, 2, 2, 2, 2, 2, 2, 2, 1, 2, 2, 2, 2, 4 ),
 ( 0.1370976352218340188, 0.1393776508289605309, 0.1416576664360870708, 0.1418001674115324795, 0.1418714178992551700, 0.1418892305211858496, 0.1419070431431165291, 0.1419426683869778882, 0.1422276703378687057, 0.1427976742396503407, 0.1439376820432136383, 0.1450776898467769360, 0.1462176976503402059, 0.1473577054539035036, 0.1479277093556851386, 0.1482127113065759560, 0.1483552122820213925, 0.1484264627697440830, 0.1484977132574668013, 0.1507777288645933411, 0.1530577444717199087, 0.1553377600788464485 ),
 .UNSPECIFIED. ) ;
#6266=CARTESIAN_POINT ( 'NONE',  ( -0.2819296736111110424, 3.960500000075865668, -0.1167790944451423119 ) ) ;
#6268=CARTESIAN_POINT ( 'NONE',  ( -0.09411960903131520728, 5.165948514229523170, -0.2827352314489141594 ) ) ;
#6269=CARTESIAN_POINT ( 'NONE',  ( 0.3119999999999999996, 4.415361111262844140, 0.1292346314604056190 ) ) ;
#6270=CARTESIAN_POINT ( 'NONE',  ( 0.1993543840281266633, 4.845916666742532186, -0.1993543840281266910 ) ) ;
#6273=CARTESIAN_POINT ( 'NONE',  ( 0.1167790944451424368, 3.981333333409199593, 0.2819296736111110424 ) ) ;
#6274=VERTEX_POINT ( 'NONE', #9134 ) ;
#6276=VERTEX_POINT ( 'NONE', #5478 ) ;
#6283=CARTESIAN_POINT ( 'NONE',  ( -0.3119999999999999996, 0.04236111095937818150, 0.1292346314604056190 ) ) ;
#6284=CARTESIAN_POINT ( 'NONE',  ( 0.2724733894366830889, 5.141277903277533312, 0.1372292302282890064 ) ) ;
#6291=CARTESIAN_POINT ( 'NONE',  ( -0.1993543840281266633, 0.1118055554796889145, -0.1993543840281266910 ) ) ;
#6294=CARTESIAN_POINT ( 'NONE',  ( -0.1993543840281266355, 4.762583333409199149, 0.1993543840281267465 ) ) ;
#6296=CARTESIAN_POINT ( 'NONE',  ( 0.1993543840281266633, 4.720916666742532186, -0.1993543840281266910 ) ) ;
#6298=CARTESIAN_POINT ( 'NONE',  ( 0.2347259105283345526, 4.856899042655335563, 0.2057643236453879643 ) ) ;
#6301=CARTESIAN_POINT ( 'NONE',  ( -0.3119999999999998885, 4.332027777777778255, 0.1292346314604058410 ) ) ;
#6302=CARTESIAN_POINT ( 'NONE',  ( 5.731347020009612645E-17, 5.182722222373954857, 0.3119999999999999996 ) ) ;
#6307=CARTESIAN_POINT ( 'NONE',  ( 0.0007589115252507630483, 4.710479605489643617, -0.3119992096284730509 ) ) ;
#6310=CARTESIAN_POINT ( 'NONE',  ( 0.1049994648621434823, 4.130212265090358770, 0.2947840903239055677 ) ) ;
#6312=CARTESIAN_POINT ( 'NONE',  ( 0.2727449834095620473, 4.312289586052585832, -0.1569221876317137276 ) ) ;
#6315=CARTESIAN_POINT ( 'NONE',  ( 0.1167790944451423535, 0.4694444443685777957, 0.2819296736111110424 ) ) ;
#6324=CARTESIAN_POINT ( 'NONE',  ( -0.3119999999999999996, 0.3791666666666663188, -3.820898013339742174E-17 ) ) ;
#6325=CARTESIAN_POINT ( 'NONE',  ( -0.2206173157302028232, 4.877166666666665762, -0.2206173157302028232 ) ) ;
#6326=CARTESIAN_POINT ( 'NONE',  ( 0.1993543840281267465, 3.998694444520310753, 0.1993543840281266633 ) ) ;
#6331=LINE ( 'NONE', #13786, #4657 ) ;
#6332=CARTESIAN_POINT ( 'NONE',  ( 0.2819296736111110979, 4.825083333409199149, -3.452642723725051716E-17 ) ) ;
#6333=AXIS2_PLACEMENT_3D ( 'NONE', #13896, #21325, #17546 ) ;
#6335=EDGE_CURVE ( 'NONE', #8700, #9142, #11344, .T. ) ;
#6341=CARTESIAN_POINT ( 'NONE',  ( -1.726321361862525858E-17, 4.241750000075866112, -0.2819296736111110979 ) ) ;
#6343=CARTESIAN_POINT ( 'NONE',  ( -0.01686310874185860051, 4.044291452137212417, -0.3115464117857045800 ) ) ;
#6346=( BOUNDED_CURVE ( )  B_SPLINE_CURVE ( 2, ( #7567, #9640, #11474, #22678, #5968, #19030, #9763, #5852, #11598 ),
 .UNSPECIFIED., .F., .F. ) 
 B_SPLINE_CURVE_WITH_KNOTS ( ( 3, 2, 2, 2, 3 ),
 ( 0.5625000000000000000, 0.5729166666666666297, 0.5833333333333333703, 0.5937500000000000000, 0.6041666666666666297 ),
 .UNSPECIFIED. ) 
 CURVE ( )  GEOMETRIC_REPRESENTATION_ITEM ( )  RATIONAL_B_SPLINE_CURVE ( ( 1.000000000000000000, 0.9238795325112867385, 1.000000000000000000, 0.9238795325112867385, 1.000000000000000000, 0.9238795325112867385, 1.000000000000000000, 0.9238795325112867385, 1.000000000000000000 ) ) 
 REPRESENTATION_ITEM ( '' )  );
#6348=CARTESIAN_POINT ( 'NONE',  ( -0.1167790944451422702, 0.3999999999241334869, -0.2819296736111110424 ) ) ;
#6349=CARTESIAN_POINT ( 'NONE',  ( -0.3119999999999999996, 0.4312499999999996891, -0.1292346314604056745 ) ) ;
#6350=CARTESIAN_POINT ( 'NONE',  ( 0.3119999999999999996, 4.470916666666665762, -0.1292346314604056745 ) ) ;
#6354=VERTEX_POINT ( 'NONE', #7993 ) ;
#6356=CARTESIAN_POINT ( 'NONE',  ( -0.008920037193760966057, 3.766295647218201648, -0.3118907412506480847 ) ) ;
#6357=CARTESIAN_POINT ( 'NONE',  ( 0.2819296736111110979, 0.4798611110352444808, 0.000000000000000000 ) ) ;
#6358=CARTESIAN_POINT ( 'NONE',  ( -0.1167790944451424368, 0.2402777777019111660, 0.2819296736111110424 ) ) ;
#6359=CARTESIAN_POINT ( 'NONE',  ( 0.1167790944451424368, 4.106333333409199149, 0.2819296736111110424 ) ) ;
#6362=CARTESIAN_POINT ( 'NONE',  ( -1.726321361862525858E-17, 4.630638888964754507, -0.2819296736111110979 ) ) ;
#6363=CARTESIAN_POINT ( 'NONE',  ( 0.3119999999999999996, 0.3999999998482670627, 0.000000000000000000 ) ) ;
#6367=CARTESIAN_POINT ( 'NONE',  ( 0.2206173157302028787, 3.911888889040621375, 0.2206173157302027954 ) ) ;
#6370=ORIENTED_EDGE ( 'NONE', *, *, #7809, .T. ) ;
#6375=CARTESIAN_POINT ( 'NONE',  ( -0.2934963008899025283, 4.999115531676239677, -0.1058924737439701086 ) ) ;
#6377=CARTESIAN_POINT ( 'NONE',  ( 0.1167790944451423535, 0.09444444436857780956, 0.2819296736111110424 ) ) ;
#6378=VERTEX_POINT ( 'NONE', #21165 ) ;
#6379=CARTESIAN_POINT ( 'NONE',  ( 0.2200028038784669626, 4.259231549017496121, -0.2224089350982841329 ) ) ;
#6387=CARTESIAN_POINT ( 'NONE',  ( 5.178964085587577574E-17, 5.213972222298088433, 0.2819296736111110979 ) ) ;
#6389=CARTESIAN_POINT ( 'NONE',  ( -0.2200173413850973203, 5.171548481154046861, -0.1982843659929367508 ) ) ;
#6391=CARTESIAN_POINT ( 'NONE',  ( 0.3119999999999999996, 4.588972222373954857, -0.1292346314604056745 ) ) ;
#6392=CARTESIAN_POINT ( 'NONE',  ( -0.2819296736111110424, 4.870222222298087544, 0.1167790944451424923 ) ) ;
#6393=ORIENTED_EDGE ( 'NONE', *, *, #828, .T. ) ;
#6394=CARTESIAN_POINT ( 'NONE',  ( 5.178964085587577574E-17, 4.088972222298087544, 0.2819296736111110979 ) ) ;
#6405=CARTESIAN_POINT ( 'NONE',  ( 0.2077910874648161710, 5.154453376781931162, -0.2182455333876957004 ) ) ;
#6409=CARTESIAN_POINT ( 'NONE',  ( -5.731347020009612645E-17, 0.2194444442927115380, 0.3119999999999999996 ) ) ;
#6410=CARTESIAN_POINT ( 'NONE',  ( 0.1993543840281266910, 0.09791666659080001944, -0.1993543840281266910 ) ) ;
#6413=CARTESIAN_POINT ( 'NONE',  ( -0.2819296736111110979, 4.630638888964754507, 0.000000000000000000 ) ) ;
#6416=DIRECTION ( 'NONE',  ( -0.7705154201994630636, 1.803387422376048611E-06, -0.6374213576839050654 ) ) ;
#6418=CARTESIAN_POINT ( 'NONE',  ( 0.3119999999999999996, 4.297305555555554157, 0.1292346314604056190 ) ) ;
#6421=CARTESIAN_POINT ( 'NONE',  ( 0.02036188714951491646, 4.961035658764420653, 0.3119999977765351429 ) ) ;
#6423=VERTEX_POINT ( 'NONE', #10203 ) ;
#6427=CARTESIAN_POINT ( 'NONE',  ( 0.05605008125374450617, 4.684288922465986715, 0.3069347663937170845 ) ) ;
#6431=CARTESIAN_POINT ( 'NONE',  ( -1.910449006669871087E-17, 4.425777777777777366, -0.3119999999999999996 ) ) ;
#6434=CARTESIAN_POINT ( 'NONE',  ( 1.726321361862525858E-17, 0.06319444436857780956, -0.2819296736111110979 ) ) ;
#6437=CARTESIAN_POINT ( 'NONE',  ( 0.2206173157302027676, 0.5111111111111107386, 0.2206173157302028787 ) ) ;
#6438=FACE_OUTER_BOUND ( 'NONE', #17793, .T. ) ;
#6440=CARTESIAN_POINT ( 'NONE',  ( -1.062695237341364068E-12, 5.118312382271687611, 0.3086920601714014945 ) ) ;
#6441=EDGE_CURVE ( 'NONE', #2791, #23806, #13975, .T. ) ;
#6442=CARTESIAN_POINT ( 'NONE',  ( -0.3105867304364036685, 4.281119371102881210, 0.04220986312590439132 ) ) ;
#6444=FACE_OUTER_BOUND ( 'NONE', #15190, .T. ) ;
#6445=CARTESIAN_POINT ( 'NONE',  ( 0.3119999999999999996, 0.5736111111111107386, 0.000000000000000000 ) ) ;
#6446=CARTESIAN_POINT ( 'NONE',  ( 0.3119999999999999996, 4.915361111111109516, -0.1292346314604056745 ) ) ;
#6447=CARTESIAN_POINT ( 'NONE',  ( 0.1167790944451422702, 4.016055555631422358, -0.2819296736111110424 ) ) ;
#6448=CARTESIAN_POINT ( 'NONE',  ( -0.1292346314604056190, 0.5840277776260448528, -0.3119999999999999996 ) ) ;
#6454=CARTESIAN_POINT ( 'NONE',  ( 0.1167790944451422702, 4.668833333409200037, -0.2819296736111110424 ) ) ;
#6461=CARTESIAN_POINT ( 'NONE',  ( 0.2819296736111110979, 4.286888888964754507, -0.1167790944451423396 ) ) ;
#6462=CARTESIAN_POINT ( 'NONE',  ( -0.2993258702403846505, 4.832972278583333114, -0.09025194431095438785 ) ) ;
#6466=CARTESIAN_POINT ( 'NONE',  ( 1.726321361862525858E-17, 0.6187499999241333759, -0.2819296736111110979 ) ) ;
#6468=DIRECTION ( 'NONE',  ( -0.000000000000000000, -1.000000000000000000, -0.000000000000000000 ) ) ;
#6472=EDGE_CURVE ( 'NONE', #5016, #4599, #3999, .T. ) ;
#6474=CARTESIAN_POINT ( 'NONE',  ( -0.1993543840281266633, 0.3895833332574667462, -0.1993543840281266910 ) ) ;
#6475=CARTESIAN_POINT ( 'NONE',  ( -5.178964085587577574E-17, 0.4104166665908000056, 0.2819296736111110979 ) ) ;
#6476=EDGE_CURVE ( 'NONE', #787, #5016, #11671, .T. ) ;
#6478=CARTESIAN_POINT ( 'NONE',  ( 0.1167790944451422702, 4.127166666742532186, -0.2819296736111110424 ) ) ;
#6480=CARTESIAN_POINT ( 'NONE',  ( -0.2819296736111110424, 4.759111111186978604, 0.1167790944451424923 ) ) ;
#6481=CARTESIAN_POINT ( 'NONE',  ( 0.2754369701929059167, 5.127252903595911349, 0.1376149775922576313 ) ) ;
#6482=CARTESIAN_POINT ( 'NONE',  ( 0.2206173157302028232, 0.4069444442927114824, -0.2206173157302028232 ) ) ;
#6486=CARTESIAN_POINT ( 'NONE',  ( 0.2206173157302027954, 4.696611111111110404, -0.2206173157302028232 ) ) ;
#6487=CARTESIAN_POINT ( 'NONE',  ( 0.1292346314604056190, 3.929250000151732536, -0.3119999999999999996 ) ) ;
#6494=ORIENTED_EDGE ( 'NONE', *, *, #4412, .T. ) ;
#6497=CARTESIAN_POINT ( 'NONE',  ( 0.2206173157302028232, 0.2472222222222218435, -0.2206173157302028232 ) ) ;
#6498=ORIENTED_EDGE ( 'NONE', *, *, #17202, .F. ) ;
#6499=CARTESIAN_POINT ( 'NONE',  ( 0.1167790944451423257, 0.1152777777019111521, -0.2819296736111110424 ) ) ;
#6500=CARTESIAN_POINT ( 'NONE',  ( 0.2821852889849572610, 4.256074823217026015, -0.1331099846749929372 ) ) ;
#6501=CARTESIAN_POINT ( 'NONE',  ( -0.2206173157302028787, 0.3305555555555552139, 0.2206173157302027954 ) ) ;
#6502=CARTESIAN_POINT ( 'NONE',  ( 0.3018349262019693890, 4.083264140120535401, 0.07899231521169805537 ) ) ;
#6508=CARTESIAN_POINT ( 'NONE',  ( -0.1912962694986284351, 4.660659591632862586, -0.2498291629754902654 ) ) ;
#6510=CARTESIAN_POINT ( 'NONE',  ( 0.1167790944451424368, 3.870222222298087988, 0.2819296736111110424 ) ) ;
#6511=CARTESIAN_POINT ( 'NONE',  ( -8.251178249108312710E-07, 5.016022433328296337, 0.3119999999976432181 ) ) ;
#6512=CARTESIAN_POINT ( 'NONE',  ( -0.2778680883334028184, 5.175875489270271856, -0.09957862134326772585 ) ) ;
#6513=CARTESIAN_POINT ( 'NONE',  ( -0.2594798065058602776, 4.785276866862929523, 0.1777679019147691830 ) ) ;
#6514=CARTESIAN_POINT ( 'NONE',  ( -0.1292346314604057023, 4.457027777929509327, 0.3119999999999998885 ) ) ;
#6515=CARTESIAN_POINT ( 'NONE',  ( -0.1993543840281266355, 4.762583333409199149, 0.1993543840281267465 ) ) ;
#6516=ORIENTED_EDGE ( 'NONE', *, *, #22890, .F. ) ;
#6517=CARTESIAN_POINT ( 'NONE',  ( 0.1993543840281266633, 4.165361111186975940, -0.1993543840281266910 ) ) ;
#6522=CARTESIAN_POINT ( 'NONE',  ( 0.2206173157302027676, 0.4555555555555552139, 0.2206173157302028787 ) ) ;
#6524=B_SPLINE_CURVE_WITH_KNOTS ( 'NONE', 3,
 ( #10410, #4659, #23295, #1003, #17470, #6608, #14173, #23536, #17590, #21604, #12360, #21253, #19778, #3076, #17952, #12003, #881, #3548 ),
 .UNSPECIFIED., .F., .F.,
 ( 4, 2, 2, 2, 2, 2, 2, 2, 4 ),
 ( 1.514782153580211930E-17, 0.001110697466041064363, 0.002221394932082113548, 0.003332092398123162515, 0.004442789864164211483, 0.005553487330205260884, 0.006664184796246309418, 0.007774882262287358820, 0.008885579728328409088 ),
 .UNSPECIFIED. ) ;
#6529=CARTESIAN_POINT ( 'NONE',  ( 0.2819296736111110979, 0.09097222214635558579, 0.000000000000000000 ) ) ;
#6532=CARTESIAN_POINT ( 'NONE',  ( -0.1167790944451423535, 4.418833333409198261, 0.2819296736111110424 ) ) ;
#6533=CARTESIAN_POINT ( 'NONE',  ( 0.1092791156175890038, 5.203332556872312331, 0.2819296736111110424 ) ) ;
#6536=DIRECTION ( 'NONE',  ( -0.000000000000000000, -1.000000000000000000, -0.000000000000000000 ) ) ;
#6537=CARTESIAN_POINT ( 'NONE',  ( 0.2206173157302028787, 4.182722222222221120, 0.2206173157302027954 ) ) ;
#6539=CARTESIAN_POINT ( 'NONE',  ( -0.3119999999999998885, 5.172305555707287006, 0.1292346314604058410 ) ) ;
#6541=CARTESIAN_POINT ( 'NONE',  ( 0.1041572415211016039, 4.963483492082001902, 0.2942352266619563395 ) ) ;
#6543=VERTEX_POINT ( 'NONE', #23458 ) ;
#6544=CARTESIAN_POINT ( 'NONE',  ( -0.1660923693448534966, 4.882155643265540412, -0.2642717717335951177 ) ) ;
#6548=DIRECTION ( 'NONE',  ( -0.000000000000000000, -1.000000000000000000, -0.000000000000000000 ) ) ;
#6551=CARTESIAN_POINT ( 'NONE',  ( -0.1167790944451424506, 0.08749999992413336203, 0.2819296736111110424 ) ) ;
#6556=ORIENTED_EDGE ( 'NONE', *, *, #21909, .F. ) ;
#6557=DIRECTION ( 'NONE',  ( 0.000000000000000000, 0.000000000000000000, -1.000000000000000000 ) ) ;
#6560=FACE_OUTER_BOUND ( 'NONE', #1347, .T. ) ;
#6561=CARTESIAN_POINT ( 'NONE',  ( -0.2206173157302027954, 0.4833333333333329485, -0.2206173157302028232 ) ) ;
#6562=CARTESIAN_POINT ( 'NONE',  ( -0.2206173157302028232, 4.932722222222221120, -0.2206173157302028232 ) ) ;
#6563=CARTESIAN_POINT ( 'NONE',  ( -0.1993543840281266910, 4.179250000075865223, -0.1993543840281266910 ) ) ;
#6565=CARTESIAN_POINT ( 'NONE',  ( 0.1993543840281266633, 3.957027777853643791, -0.1993543840281266910 ) ) ;
#6569=ORIENTED_EDGE ( 'NONE', *, *, #11833, .F. ) ;
#6573=CARTESIAN_POINT ( 'NONE',  ( -0.2819296736111110424, 4.523000000075865223, 0.1167790944451424923 ) ) ;
#6575=CARTESIAN_POINT ( 'NONE',  ( -0.3119999999999999996, 4.106333333333332725, 0.000000000000000000 ) ) ;
#6577=LINE ( 'NONE', #8162, #21649 ) ;
#6580=CARTESIAN_POINT ( 'NONE',  ( -0.2819296736111110979, 4.085500000075865223, -0.1167790944451422980 ) ) ;
#6582=SPHERICAL_SURFACE ( 'NONE', #21617, 0.3119999999999999996 ) ;
#6586=CARTESIAN_POINT ( 'NONE',  ( -0.1167790944451422702, 0.1083333332574667046, -0.2819296736111110424 ) ) ;
#6588=CARTESIAN_POINT ( 'NONE',  ( -0.1292346314604058410, 0.4451388888888885287, 0.3119999999999998885 ) ) ;
#6592=EDGE_CURVE ( 'NONE', #19405, #70, #14904, .T. ) ;
#6593=CARTESIAN_POINT ( 'NONE',  ( 0.3120000000000000551, 3.963972222222221564, 0.1292346314604056190 ) ) ;
#6594=CARTESIAN_POINT ( 'NONE',  ( -0.3120015917345935752, 3.781041443398025059, 0.04082955656978376480 ) ) ;
#6595=CARTESIAN_POINT ( 'NONE',  ( -0.2494961085522761357, 3.841226936246323831, 0.1917385093088717907 ) ) ;
#6596=CARTESIAN_POINT ( 'NONE',  ( 1.726321361862525858E-17, 0.3826388888130222710, -0.2819296736111110979 ) ) ;
#6597=CARTESIAN_POINT ( 'NONE',  ( 0.1993543840281266633, 4.123694444520309865, -0.1993543840281266910 ) ) ;
#6600=CARTESIAN_POINT ( 'NONE',  ( -0.1167790944451423257, 4.745222222298088433, -0.2819296736111110424 ) ) ;
#6601=CARTESIAN_POINT ( 'NONE',  ( 0.2303917398207527556, 5.125144739340170119, 0.2040722439002406741 ) ) ;
#6603=ORIENTED_EDGE ( 'NONE', *, *, #9517, .T. ) ;
#6605=CARTESIAN_POINT ( 'NONE',  ( -0.3119999999999998885, 3.838972222373954857, 0.1292346314604058410 ) ) ;
#6608=CARTESIAN_POINT ( 'NONE',  ( 0.2161795966814163694, 0.03242967361111068897, 0.1815435138465212317 ) ) ;
#6609=CARTESIAN_POINT ( 'NONE',  ( -0.2819296736111110979, 4.793833333409199149, -0.1167790944451422980 ) ) ;
#6611=VERTEX_POINT ( 'NONE', #11282 ) ;
#6612=CARTESIAN_POINT ( 'NONE',  ( -0.05041081173230543833, 5.101548709612324650, -0.3067424804290312945 ) ) ;
#6614=CARTESIAN_POINT ( 'NONE',  ( 0.3119999999999999996, 0.6256944442927115935, -0.1292346314604056468 ) ) ;
#6616=CARTESIAN_POINT ( 'NONE',  ( -0.3119999999999999996, 0.3201388888888885287, -0.1292346314604056745 ) ) ;
#6617=CARTESIAN_POINT ( 'NONE',  ( 0.3011242999017837985, 4.083187727495992903, 0.08166723430258095162 ) ) ;
#6619=CARTESIAN_POINT ( 'NONE',  ( -0.2620971190287328390, 5.062880408242417474, 0.1705199924471070549 ) ) ;
#6624=CARTESIAN_POINT ( 'NONE',  ( -3.990790521751304672E-07, 4.654944455680286808, -0.3119999999997447038 ) ) ;
#6625=CARTESIAN_POINT ( 'NONE',  ( -0.1167790944451423257, 3.786888888964754063, -0.2819296736111110424 ) ) ;
#6628=CARTESIAN_POINT ( 'NONE',  ( -0.1535721704690733991, 4.770579318579037498, -0.2744936891675854862 ) ) ;
#6629=CARTESIAN_POINT ( 'NONE',  ( -0.2206173157302027676, 4.509111111262843252, 0.2206173157302028787 ) ) ;
#6630=CARTESIAN_POINT ( 'NONE',  ( 5.178964085587577574E-17, 4.769527777853643791, 0.2819296736111110979 ) ) ;
#6633=CARTESIAN_POINT ( 'NONE',  ( -0.2819296736111110979, 4.130638888964754507, 0.000000000000000000 ) ) ;
#6639=EDGE_CURVE ( 'NONE', #15989, #9981, #15113, .T. ) ;
#6643=CARTESIAN_POINT ( 'NONE',  ( 1.910449006669871087E-17, 0.02499999984826707308, -0.3119999999999999996 ) ) ;
#6644=CARTESIAN_POINT ( 'NONE',  ( -0.1825813392756855669, 4.382625187681782108, -0.2540029803607526948 ) ) ;
#6651=CARTESIAN_POINT ( 'NONE',  ( 0.1167790944451423119, 0.04583333325746669767, -0.2819296736111110979 ) ) ;
#6653=CARTESIAN_POINT ( 'NONE',  ( -0.1167790944451423257, 4.453555555631420582, -0.2819296736111110424 ) ) ;
#6654=CARTESIAN_POINT ( 'NONE',  ( -0.1993543840281266355, 5.193138888964753619, 0.1993543840281267465 ) ) ;
#6658=CARTESIAN_POINT ( 'NONE',  ( -0.3119999999999999996, 4.050777777777777366, 0.000000000000000000 ) ) ;
#6660=CARTESIAN_POINT ( 'NONE',  ( -0.3119999999999999996, 5.224388889040620931, 0.000000000000000000 ) ) ;
#6662=CARTESIAN_POINT ( 'NONE',  ( 0.1149486178008431447, 4.984919243813402900, -0.2909162232891184252 ) ) ;
#6663=CARTESIAN_POINT ( 'NONE',  ( 3.820898013339742174E-17, 5.384999999999999787, 0.3119999999999999996 ) ) ;
#6666=CARTESIAN_POINT ( 'NONE',  ( -0.1839906024682744501, 4.882774787087751811, -0.2519870536740796974 ) ) ;
#6667=CARTESIAN_POINT ( 'NONE',  ( 0.1658549492420689775, 4.132149360891332890, 0.2644516142144350268 ) ) ;
#6670=EDGE_CURVE ( 'NONE', #15989, #21365, #13245, .T. ) ;
#6674=CARTESIAN_POINT ( 'NONE',  ( 0.1167790944451423257, 0.6013888888130223265, -0.2819296736111110424 ) ) ;
#6677=CARTESIAN_POINT ( 'NONE',  ( -0.2819296736111110979, 5.088972222298087544, 0.000000000000000000 ) ) ;
#6680=FACE_OUTER_BOUND ( 'NONE', #11036, .T. ) ;
#6683=CARTESIAN_POINT ( 'NONE',  ( 0.1292346314604056745, 0.4173611111111108496, -0.3119999999999999996 ) ) ;
#6684=CARTESIAN_POINT ( 'NONE',  ( 0.3119999999999999996, 4.970916666666665762, -0.1292346314604056745 ) ) ;
#6685=CARTESIAN_POINT ( 'NONE',  ( -0.2819296736111110979, 4.297305555631420582, 0.000000000000000000 ) ) ;
#6686=CARTESIAN_POINT ( 'NONE',  ( -0.2819296736111110424, 3.925777777853644235, 0.1167790944451424923 ) ) ;
#6689=CARTESIAN_POINT ( 'NONE',  ( 0.3108838931427311825, 4.807001385996093390, 0.02636691118709539108 ) ) ;
#6690=EDGE_LOOP ( 'NONE', ( #14400, #12884, #14374, #16085 ) ) ;
#6691=CARTESIAN_POINT ( 'NONE',  ( 0.2819296736111110979, 4.491750000075865223, -3.452642723725051716E-17 ) ) ;
#6693=CARTESIAN_POINT ( 'NONE',  ( -0.2427454876524849925, 4.508203593491248107, 0.1960069984806188936 ) ) ;
#6697=CARTESIAN_POINT ( 'NONE',  ( 0.1900105704308386045, 5.206640035683666845, 0.2082794372640154323 ) ) ;
#6698=CARTESIAN_POINT ( 'NONE',  ( -0.2819296736111110979, 4.144527777853643791, 0.000000000000000000 ) ) ;
#6700=CARTESIAN_POINT ( 'NONE',  ( -0.3117958023240662846, 4.835187445956109720, -0.01167036106402472885 ) ) ;
#6704=APPLICATION_CONTEXT ( 'configuration controlled 3d designs of mechanical parts and assemblies' ) ;
#6705=CARTESIAN_POINT ( 'NONE',  ( 0.1167790944451423257, 0.6152777777019110550, -0.2819296736111110424 ) ) ;
#6713=CARTESIAN_POINT ( 'NONE',  ( -0.0005457459119219430560, 3.766070220202782703, -0.3119995940632557252 ) ) ;
#6715=CARTESIAN_POINT ( 'NONE',  ( -0.1993543840281267465, 0.3479166665908000611, 0.1993543840281266633 ) ) ;
#6716=CARTESIAN_POINT ( 'NONE',  ( 0.1993543840281267465, 4.165361111186976828, 0.1993543840281266633 ) ) ;
#6720=CARTESIAN_POINT ( 'NONE',  ( -0.1167790944451423535, 4.710500000075865223, 0.2819296736111110424 ) ) ;
#6721=CARTESIAN_POINT ( 'NONE',  ( 0.1620925312155838405, 5.138945716096764649, -0.2584997478798148340 ) ) ;
#6723=CARTESIAN_POINT ( 'NONE',  ( 0.1292346314604057300, 0.3895833331816003775, 0.3119999999999998885 ) ) ;
#6725=CARTESIAN_POINT ( 'NONE',  ( 0.000000000000000000, 5.384999999999999787, 0.000000000000000000 ) ) ;
#6727=CARTESIAN_POINT ( 'NONE',  ( -0.1993543840281266355, 5.082027777853643791, 0.1993543840281267465 ) ) ;
#6728=CARTESIAN_POINT ( 'NONE',  ( 0.1466396438660773627, 4.206187273484634837, -0.2762320324114326819 ) ) ;
#6731=CARTESIAN_POINT ( 'NONE',  ( 0.1167790944451422702, 4.891055555631421470, -0.2819296736111110979 ) ) ;
#6734=CARTESIAN_POINT ( 'NONE',  ( -0.2513697473550708938, 5.108907442184293934, -0.1815747212199412541 ) ) ;
#6735=CARTESIAN_POINT ( 'NONE',  ( -0.2206173157302028787, 0.2124999998482670627, 0.2206173157302027954 ) ) ;
#6737=CARTESIAN_POINT ( 'NONE',  ( 1.726321361862525858E-17, 0.3965277777019111105, -0.2819296736111110979 ) ) ;
#6739=CARTESIAN_POINT ( 'NONE',  ( 0.1618212287091538581, 4.094532934258117152, -0.2700669807813751433 ) ) ;
#6741=CARTESIAN_POINT ( 'NONE',  ( -0.07784249766847600727, 5.069340931627631441, 0.3027131100711323852 ) ) ;
#6744=CARTESIAN_POINT ( 'NONE',  ( -0.2819296736111110424, 4.814666666742533074, 0.1167790944451424923 ) ) ;
#6745=ORIENTED_EDGE ( 'NONE', *, *, #9740, .T. ) ;
#6747=CARTESIAN_POINT ( 'NONE',  ( -0.2819296736111110424, 3.793833333409199149, -0.1167790944451423119 ) ) ;
#6748=CARTESIAN_POINT ( 'NONE',  ( -0.2714878203009086777, 0.04947802436987754071, -0.1267951674310540955 ) ) ;
#6749=CARTESIAN_POINT ( 'NONE',  ( 0.3118802040654409802, 5.028715422347283415, 0.04186130555678244797 ) ) ;
#6750=CARTESIAN_POINT ( 'NONE',  ( -5.731347020009612645E-17, 0.4486111111111107386, 0.3119999999999999996 ) ) ;
#6752=CARTESIAN_POINT ( 'NONE',  ( 5.731347020009612645E-17, 4.404944444596177178, 0.3119999999999999996 ) ) ;
#6754=CARTESIAN_POINT ( 'NONE',  ( -0.1167790944451423535, 4.654944444520310753, 0.2819296736111110979 ) ) ;
#6756=CARTESIAN_POINT ( 'NONE',  ( 0.1993543840281267465, 4.095916666742532186, 0.1993543840281266633 ) ) ;
#6758=ORIENTED_EDGE ( 'NONE', *, *, #23915, .T. ) ;
#6764=CARTESIAN_POINT ( 'NONE',  ( 1.910449006669871087E-17, 0.3583333331816003775, -0.3119999999999999996 ) ) ;
#6765=CARTESIAN_POINT ( 'NONE',  ( -0.3120492848101305006, 4.389992572532343651, -0.04054563350898530288 ) ) ;
#6766=AXIS2_PLACEMENT_3D ( 'NONE', #21945, #14646, #14402 ) ;
#6769=ORIENTED_EDGE ( 'NONE', *, *, #10189, .T. ) ;
#6770=ORIENTED_EDGE ( 'NONE', *, *, #12728, .F. ) ;
#6772=CARTESIAN_POINT ( 'NONE',  ( 0.1993543840281266910, 0.6118055554796889561, -0.1993543840281266910 ) ) ;
#6774=CARTESIAN_POINT ( 'NONE',  ( -0.2819296736111110424, 4.523000000075865223, 0.1167790944451424923 ) ) ;
#6776=EDGE_CURVE ( 'NONE', #8220, #15596, #23502, .T. ) ;
#6781=CARTESIAN_POINT ( 'NONE',  ( -0.1292346314604057023, 3.950083333333332281, 0.3119999999999998885 ) ) ;
#6784=CARTESIAN_POINT ( 'NONE',  ( 0.3108730060166250975, 4.973664493242656803, 0.02649485966508354287 ) ) ;
#6788=CARTESIAN_POINT ( 'NONE',  ( 0.03482881598886129748, 5.199150166515222438, 0.2833619536528675931 ) ) ;
#6789=VECTOR ( 'NONE', #11384, 39.37007874015748143 ) ;
#6794=AXIS2_PLACEMENT_3D ( 'NONE', #5254, #3795, #130 ) ;
#6801=CARTESIAN_POINT ( 'NONE',  ( 0.1993543840281266633, 5.068138888964754507, -0.1993543840281266910 ) ) ;
#6804=CARTESIAN_POINT ( 'NONE',  ( -0.1876531964494600191, 4.605128802226668761, -0.2492760297041929085 ) ) ;
#6805=CARTESIAN_POINT ( 'NONE',  ( -0.2854188144692234586, 4.283709271031463039, 0.1301228050348401111 ) ) ;
#6807=CARTESIAN_POINT ( 'NONE',  ( 1.910449006669871087E-17, 0.5319444444444439979, -0.3119999999999999996 ) ) ;
#6808=CARTESIAN_POINT ( 'NONE',  ( -1.910449006669871087E-17, 4.759111111111110404, -0.3119999999999999996 ) ) ;
#6809=CARTESIAN_POINT ( 'NONE',  ( 0.2819296736111111534, 4.266055555631421470, 0.1167790944451422563 ) ) ;
#6810=CARTESIAN_POINT ( 'NONE',  ( 0.2819296736111110424, 3.786888888964754507, -0.1167790944451423396 ) ) ;
#6812=CARTESIAN_POINT ( 'NONE',  ( -0.3119999999999999996, 3.880638888888887639, -0.1292346314604056468 ) ) ;
#6815=CARTESIAN_POINT ( 'NONE',  ( 0.1167790944451422702, 4.557722222298087544, -0.2819296736111110424 ) ) ;
#6823=CARTESIAN_POINT ( 'NONE',  ( -0.1167790944451423119, 4.023000000075866112, -0.2819296736111110979 ) ) ;
#6824=CARTESIAN_POINT ( 'NONE',  ( -0.1536748323684310469, 4.826214147890177664, -0.2744405328660507459 ) ) ;
#6829=CARTESIAN_POINT ( 'NONE',  ( -5.178964085587577574E-17, 0.02152777770191114173, 0.2819296736111110979 ) ) ;
#6838=CARTESIAN_POINT ( 'NONE',  ( -0.2726209726102415964, 3.840039493605415633, 0.1571297853222173302 ) ) ;
#6839=CARTESIAN_POINT ( 'NONE',  ( 0.2819296736111110424, 0.3652777777019111105, 0.1167790944451424923 ) ) ;
#6840=CARTESIAN_POINT ( 'NONE',  ( -0.1993543840281266355, 3.873694444520310309, 0.1993543840281267465 ) ) ;
#6843=ORIENTED_EDGE ( 'NONE', *, *, #22259, .F. ) ;
#6844=CARTESIAN_POINT ( 'NONE',  ( 0.2819296736111110424, 4.675777777853643791, -0.1167790944451423396 ) ) ;
#6845=CARTESIAN_POINT ( 'NONE',  ( 0.1783598947430071191, 5.123355972270982051, 0.2511911702540504665 ) ) ;
#6849=CARTESIAN_POINT ( 'NONE',  ( -0.1993543840281266910, 5.068138888964754507, -0.1993543840281266910 ) ) ;
#6851=CARTESIAN_POINT ( 'NONE',  ( 0.2639807749865303310, 4.191608379692064013, 0.1663089970397409745 ) ) ;
#6854=CARTESIAN_POINT ( 'NONE',  ( 5.178964085587577574E-17, 4.866750000075865223, 0.2819296736111110979 ) ) ;
#6857=CARTESIAN_POINT ( 'NONE',  ( -1.903245722532910002E-17, 5.100068075568266579, -0.3108236144263021861 ) ) ;
#6858=CARTESIAN_POINT ( 'NONE',  ( 0.1292346314604056745, 0.2506944444444441089, -0.3119999999999999996 ) ) ;
#6860=CARTESIAN_POINT ( 'NONE',  ( -5.178964085587577574E-17, 0.2576388888130222155, 0.2819296736111110979 ) ) ;
#6861=CARTESIAN_POINT ( 'NONE',  ( 0.2819296736111110424, 0.05277777770191114520, -0.1167790944451423119 ) ) ;
#6865=CARTESIAN_POINT ( 'NONE',  ( -0.09469529337756199538, 5.068847041801435083, 0.2977286714186166972 ) ) ;
#6866=CARTESIAN_POINT ( 'NONE',  ( 0.2206173157302027954, 4.196611111111110404, -0.2206173157302028232 ) ) ;
#6868=CARTESIAN_POINT ( 'NONE',  ( -0.2819296736111110979, 4.755638888964754507, 0.000000000000000000 ) ) ;
#6870=CARTESIAN_POINT ( 'NONE',  ( 0.2275323619091996763, 4.536638745974315157, -0.2154182091710123426 ) ) ;
#6871=CARTESIAN_POINT ( 'NONE',  ( -0.2819296736111110979, 5.255638888964754507, 0.000000000000000000 ) ) ;
#6877=CARTESIAN_POINT ( 'NONE',  ( -0.04622087296078272040, 4.792553729289763531, 0.3085726088726347127 ) ) ;
#6878=CARTESIAN_POINT ( 'NONE',  ( -0.2206173157302027676, 4.231333333485065573, 0.2206173157302028787 ) ) ;
#6879=B_SPLINE_CURVE_WITH_KNOTS ( 'NONE', 3,
 ( #4138, #13426, #2206, #17067, #13672, #361, #2321, #22911, #4376, #9757, #22793, #6208, #4262, #15245, #481, #17430, #21086, #15485 ),
 .UNSPECIFIED., .F., .F.,
 ( 4, 2, 2, 2, 2, 2, 2, 2, 4 ),
 ( 0.5756575327745111492, 0.5779426686689235204, 0.5802278045633358916, 0.5825129404577482628, 0.5847980763521607450, 0.5870832122465731162, 0.5893683481409854874, 0.5916534840353978586, 0.5939386199298102298 ),
 .UNSPECIFIED. ) ;
#6880=CARTESIAN_POINT ( 'NONE',  ( 0.2819296736111110979, 4.786888888964754507, -0.1167790944451423396 ) ) ;
#6881=EDGE_LOOP ( 'NONE', ( #4210, #678, #16413, #459 ) ) ;
#6882=CARTESIAN_POINT ( 'NONE',  ( 0.2819296736111110424, 3.884111111186976384, -0.1167790944451423396 ) ) ;
#6885=DIRECTION ( 'NONE',  ( -0.000000000000000000, -1.000000000000000000, -0.000000000000000000 ) ) ;
#6889=CARTESIAN_POINT ( 'NONE',  ( 0.3119999999999998885, 0.2854166665149337478, 0.1292346314604058410 ) ) ;
#6892=CARTESIAN_POINT ( 'NONE',  ( -0.2015352175386056210, 4.383312114150648142, -0.2394718385862008581 ) ) ;
#6893=EDGE_CURVE ( 'NONE', #17266, #19560, #3744, .T. ) ;
#6895=CARTESIAN_POINT ( 'NONE',  ( 0.000000000000000000, 5.384999999999999787, -0.3119999999999999996 ) ) ;
#6897=EDGE_LOOP ( 'NONE', ( #21623, #11677, #22304, #23414, #11938, #10743, #2395, #14729, #6603, #11908, #1591, #6908, #12249, #4423, #20661, #18370, #3856, #19805, #17653, #4541, #8708, #17477, #8789, #3611, #23879, #15109, #13632, #6153, #13886, #6393, #21152, #15059, #9121, #5659, #8754, #18354, #5424, #23530, #1302, #9, #17553, #5178, #3803, #6017, #10567, #23463, #2406, #19246, #8219, #12207, #20850, #12632, #2510, #11648, #12144, #13430, #6137 ) ) ;
#6899=CARTESIAN_POINT ( 'NONE',  ( -0.1993543840281266633, 0.3340277777019111660, -0.1993543840281266910 ) ) ;
#6902=CARTESIAN_POINT ( 'NONE',  ( 0.2819296736111110979, 4.380638888964754507, -3.452642723725051716E-17 ) ) ;
#6906=CARTESIAN_POINT ( 'NONE',  ( -0.3119999999999999996, 3.991749999999999243, -0.1292346314604056468 ) ) ;
#6907=CARTESIAN_POINT ( 'NONE',  ( 0.3119999999999999996, 4.866750000151731648, -0.1292346314604056745 ) ) ;
#6908=ORIENTED_EDGE ( 'NONE', *, *, #12477, .T. ) ;
#6913=EDGE_CURVE ( 'NONE', #12181, #5059, #19881, .T. ) ;
#6917=ORIENTED_EDGE ( 'NONE', *, *, #2055, .F. ) ;
#6918=CARTESIAN_POINT ( 'NONE',  ( -0.3119999999999998885, 4.443138888888888083, 0.1292346314604058410 ) ) ;
#6921=CARTESIAN_POINT ( 'NONE',  ( 0.2819296736111110424, 0.1569444443685777679, 0.1167790944451424923 ) ) ;
#6923=CARTESIAN_POINT ( 'NONE',  ( -0.2819296736111110979, 5.255638888964754507, 0.000000000000000000 ) ) ;
#6924=CARTESIAN_POINT ( 'NONE',  ( 0.06854178015534857782, 4.486376190189668378, -0.3045296682676547073 ) ) ;
#6926=VERTEX_POINT ( 'NONE', #1619 ) ;
#6927=FACE_OUTER_BOUND ( 'NONE', #5321, .T. ) ;
#6930=CARTESIAN_POINT ( 'NONE',  ( 0.2782497666485165277, 0.06249891821425377497, 0.1411420113220940853 ) ) ;
#6931=CARTESIAN_POINT ( 'NONE',  ( 0.3119999999999999996, 4.797305555555554157, 0.1292346314604056190 ) ) ;
#6932=CARTESIAN_POINT ( 'NONE',  ( 0.1167790944451424506, 3.925777777853643347, 0.2819296736111110424 ) ) ;
#6933=CARTESIAN_POINT ( 'NONE',  ( 0.1797087373818229139, 3.735609845915246474, -0.2172305470487487511 ) ) ;
#6935=CARTESIAN_POINT ( 'NONE',  ( 0.2206173157302027954, 4.418833333333332725, -0.2206173157302028232 ) ) ;
#6937=CARTESIAN_POINT ( 'NONE',  ( -0.2206173157302027676, 4.557722222222221120, 0.2206173157302028787 ) ) ;
#6938=CARTESIAN_POINT ( 'NONE',  ( 0.1993543840281266633, 4.498694444520309865, -0.1993543840281266910 ) ) ;
#6939=B_SPLINE_CURVE_WITH_KNOTS ( 'NONE', 3,
 ( #16437, #14740, #12920, #16676, #7409, #23725, #20091, #23847, #5572, #5452, #9107, #9359, #7050, #6924, #20453, #14860, #22034, #21792, #3749, #8871, #5081, #3256, #11193, #14362, #5330, #11070, #10833, #20331, #7167, #12549, #16556, #23978, #7289, #19969, #18142, #21911, #5200, #22155, #20934, #11435, #5812, #13391, #20813, #82, #20574, #7767, #6051 ),
 .UNSPECIFIED., .F., .F.,
 ( 4, 2, 1, 2, 2, 1, 1, 2, 2, 2, 2, 2, 2, 2, 2, 2, 1, 1, 2, 2, 1, 1, 2, 2, 2, 2, 4 ),
 ( 0.4842883486437473683, 0.4848597289547300071, 0.4851454191102213542, 0.4852882641879670556, 0.4853061198226852335, 0.4853239754574034670, 0.4853596867268398785, 0.4854311092657127014, 0.4865738698876779234, 0.4877166305096431453, 0.4888593911316083673, 0.4900021517535736448, 0.4911449123755388668, 0.4922876729975040888, 0.4934304336194693108, 0.4945731942414345328, 0.4946446167803074112, 0.4946624724150255892, 0.4946714002323847059, 0.4946803280497438227, 0.4947160393191802341, 0.4948588843969258799, 0.4951445745524171160, 0.4957159548633996993, 0.4980014761073300322, 0.5002869973512602542, 0.5025725185951905871 ),
 .UNSPECIFIED. ) ;
#6940=CARTESIAN_POINT ( 'NONE',  ( -0.2806174154849702118, 4.506217266555575307, 0.1379780153053364600 ) ) ;
#6943=CARTESIAN_POINT ( 'NONE',  ( -1.296004783052830448E-07, 4.710500003633881327, -0.3119999999999730766 ) ) ;
#6944=( BOUNDED_CURVE ( )  B_SPLINE_CURVE ( 2, ( #18506, #19975, #23730, #22041, #5336, #18267, #8999, #20098, #7055 ),
 .UNSPECIFIED., .F., .F. ) 
 B_SPLINE_CURVE_WITH_KNOTS ( ( 3, 2, 2, 2, 3 ),
 ( 0.8125000000000000000, 0.8229166666666666297, 0.8333333333333333703, 0.8437500000000000000, 0.8541666666666666297 ),
 .UNSPECIFIED. ) 
 CURVE ( )  GEOMETRIC_REPRESENTATION_ITEM ( )  RATIONAL_B_SPLINE_CURVE ( ( 1.000000000000000000, 0.9238795325112867385, 1.000000000000000000, 0.9238795325112867385, 1.000000000000000000, 0.9238795325112867385, 1.000000000000000000, 0.9238795325112867385, 1.000000000000000000 ) ) 
 REPRESENTATION_ITEM ( '' )  );
#6948=CARTESIAN_POINT ( 'NONE',  ( -1.726321361862525858E-17, 4.075083333409199149, -0.2819296736111110979 ) ) ;
#6949=CARTESIAN_POINT ( 'NONE',  ( -0.3079124582538622645, 4.834082022064681183, -0.05131535407519589864 ) ) ;
#6953=CARTESIAN_POINT ( 'NONE',  ( -0.1993543840281266633, 0.0006944443685778107491, -0.1993543840281266910 ) ) ;
#6963=CARTESIAN_POINT ( 'NONE',  ( -5.178964085587577574E-17, 0.5215277777019111660, 0.2819296736111110979 ) ) ;
#6964=CARTESIAN_POINT ( 'NONE',  ( 0.2819296736111110979, 3.783416666742532186, -3.452642723725051716E-17 ) ) ;
#6967=CARTESIAN_POINT ( 'NONE',  ( -1.726321361862525858E-17, 4.463972222298087544, -0.2819296736111110979 ) ) ;
#6968=CARTESIAN_POINT ( 'NONE',  ( 0.03989520295803244965, 5.142369579426448567, -0.3022423214455481899 ) ) ;
#6971=CARTESIAN_POINT ( 'NONE',  ( 0.3021975922303085649, 4.365644181327585471, -0.08256521648007630887 ) ) ;
#6972=CARTESIAN_POINT ( 'NONE',  ( -0.2819296736111110424, 5.127166666742532186, -0.1167790944451423119 ) ) ;
#6976=CARTESIAN_POINT ( 'NONE',  ( 0.1167790944451422702, 4.835500000075865223, -0.2819296736111110979 ) ) ;
#6980=CARTESIAN_POINT ( 'NONE',  ( -0.03984146987716615657, 4.544964378884258416, -0.3119997632626998474 ) ) ;
#6982=CARTESIAN_POINT ( 'NONE',  ( -0.1993543840281267465, 0.3618055554796889006, 0.1993543840281266633 ) ) ;
#6984=CARTESIAN_POINT ( 'NONE',  ( -0.1993543840281267465, 0.08402777770191115214, 0.1993543840281266633 ) ) ;
#6986=DIRECTION ( 'NONE',  ( 6.123233995736811642E-17, 0.000000000000000000, -1.000000000000000000 ) ) ;
#6989=CARTESIAN_POINT ( 'NONE',  ( -0.09802781027409257497, 5.046564986788329321, -0.2971681987422591931 ) ) ;
#6993=CARTESIAN_POINT ( 'NONE',  ( 0.1993543840281267465, 4.443138888964754507, 0.1993543840281266633 ) ) ;
#6995=CARTESIAN_POINT ( 'NONE',  ( 0.2251296462303276347, 4.523151383338628762, 0.2168217435695329043 ) ) ;
#6996=CARTESIAN_POINT ( 'NONE',  ( 0.2819296736111110979, 5.057722222298088433, 0.1167790944451422425 ) ) ;
#6997=CARTESIAN_POINT ( 'NONE',  ( 1.791833110003796271E-17, 0.04312855400452411669, -0.2926285540045244216 ) ) ;
#6998=CARTESIAN_POINT ( 'NONE',  ( 0.2674007968890174669, 3.757045421648967487, -0.1629501482939255674 ) ) ;
#7002=CARTESIAN_POINT ( 'NONE',  ( -0.1019843081256275041, 4.790927999518966196, 0.2955334162662792141 ) ) ;
#7003=CARTESIAN_POINT ( 'NONE',  ( 0.1292346314604058410, 4.297305555707287894, 0.3119999999999998885 ) ) ;
#7004=CARTESIAN_POINT ( 'NONE',  ( 0.1993543840281266633, 4.734805555631421470, -0.1993543840281266910 ) ) ;
#7005=CARTESIAN_POINT ( 'NONE',  ( -1.726321361862525858E-17, 3.950083333409199149, -0.2819296736111110979 ) ) ;
#7015=CARTESIAN_POINT ( 'NONE',  ( -5.731347020009612645E-17, 0.3305555554038226429, 0.3119999999999999996 ) ) ;
#7017=CARTESIAN_POINT ( 'NONE',  ( 1.364852645245658621E-07, 4.377166663151471404, -0.3119999999999701346 ) ) ;
#7020=DIRECTION ( 'NONE',  ( -0.000000000000000000, -1.000000000000000000, -0.000000000000000000 ) ) ;
#7023=CARTESIAN_POINT ( 'NONE',  ( 1.726321361862525858E-17, 0.1604166665908000333, -0.2819296736111110979 ) ) ;
#7025=VERTEX_POINT ( 'NONE', #11955 ) ;
#7026=CARTESIAN_POINT ( 'NONE',  ( 0.2819296736111110979, 4.432722222298088433, 0.1167790944451422425 ) ) ;
#7027=CARTESIAN_POINT ( 'NONE',  ( 1.910449006669871087E-17, 0.1986111111111107386, -0.3119999999999999996 ) ) ;
#7030=ADVANCED_FACE ( 'NONE', ( #6438 ), #13892, .T. ) ;
#7031=CARTESIAN_POINT ( 'NONE',  ( 0.3119999999999999996, 4.022999999999998799, -3.820898013339742174E-17 ) ) ;
#7032=CARTESIAN_POINT ( 'NONE',  ( 0.1292346314604056190, 4.984805555707287006, -0.3119999999999999996 ) ) ;
#7035=CARTESIAN_POINT ( 'NONE',  ( 0.3120000000000000551, 4.852861111111110404, 0.1292346314604056190 ) ) ;
#7036=EDGE_CURVE ( 'NONE', #23454, #7806, #13977, .T. ) ;
#7037=CARTESIAN_POINT ( 'NONE',  ( -8.252060436089559755E-07, 4.682689096385127314, 0.3119999999976427185 ) ) ;
#7039=EDGE_CURVE ( 'NONE', #6611, #14348, #18622, .T. ) ;
#7047=CARTESIAN_POINT ( 'NONE',  ( 1.726321361862525858E-17, 0.2854166665908000056, -0.2819296736111110979 ) ) ;
#7049=CARTESIAN_POINT ( 'NONE',  ( -0.2819296736111110424, 5.085500000075866112, -0.1167790944451423119 ) ) ;
#7050=CARTESIAN_POINT ( 'NONE',  ( 0.06089257667514946099, 4.486588928204580107, -0.3060585940131039240 ) ) ;
#7052=CYLINDRICAL_SURFACE ( 'NONE', #9521, 0.3119999999999999996 ) ;
#7053=CARTESIAN_POINT ( 'NONE',  ( 0.003006042110193701388, 4.877085829448629895, -0.3119876125383257426 ) ) ;
#7055=CARTESIAN_POINT ( 'NONE',  ( 1.910449006669871087E-17, 0.5805555554038225319, -0.3119999999999999996 ) ) ;
#7056=CARTESIAN_POINT ( 'NONE',  ( 0.2206173157302027954, 4.807722222222221120, -0.2206173157302028232 ) ) ;
#7057=CARTESIAN_POINT ( 'NONE',  ( 0.2819296736111110979, 3.995222222298087544, -0.1167790944451423396 ) ) ;
#7058=CARTESIAN_POINT ( 'NONE',  ( 0.1167790944451424368, 3.828555555631421470, 0.2819296736111110424 ) ) ;
#7059=CARTESIAN_POINT ( 'NONE',  ( 0.1744173410699168814, 4.038682005623637217, -0.2596828359170899048 ) ) ;
#7061=EDGE_LOOP ( 'NONE', ( #22630, #202, #12960, #11826 ) ) ;
#7064=CARTESIAN_POINT ( 'NONE',  ( 5.178964085587577574E-17, 4.533416666742532186, 0.2819296736111110979 ) ) ;
#7065=CARTESIAN_POINT ( 'NONE',  ( -0.2965624338261537152, 4.505027248459144928, 0.09917050682623472502 ) ) ;
#7071=CARTESIAN_POINT ( 'NONE',  ( 0.2819296736111110979, 3.950083333409199149, -3.452642723725051716E-17 ) ) ;
#7076=CARTESIAN_POINT ( 'NONE',  ( 0.2819296736111110979, 0.1465277777019111383, 0.000000000000000000 ) ) ;
#7085=CARTESIAN_POINT ( 'NONE',  ( 0.2206173157302027676, 0.1222222222222218990, 0.2206173157302028787 ) ) ;
#7086=CARTESIAN_POINT ( 'NONE',  ( -0.1993543840281266355, 3.762583333409198705, 0.1993543840281267465 ) ) ;
#7088=CARTESIAN_POINT ( 'NONE',  ( -0.2819296736111110424, 4.529944444520310753, -0.1167790944451423119 ) ) ;
#7094=EDGE_CURVE ( 'NONE', #3584, #13967, #6939, .T. ) ;
#7096=CARTESIAN_POINT ( 'NONE',  ( -0.1993543840281266355, 5.193138888964753619, 0.1993543840281267465 ) ) ;
#7100=CARTESIAN_POINT ( 'NONE',  ( -0.3119999999999999996, 0.2090277777777774237, -0.1292346314604056745 ) ) ;
#7101=CARTESIAN_POINT ( 'NONE',  ( 5.178964085587577574E-17, 4.922305555631420582, 0.2819296736111110979 ) ) ;
#7103=CARTESIAN_POINT ( 'NONE',  ( -0.1562568192738307826, 4.066946061297420201, 0.2700551682292786082 ) ) ;
#7106=CARTESIAN_POINT ( 'NONE',  ( -0.2819296736111110424, 0.2958333332574666907, -0.1167790944451423396 ) ) ;
#7107=CARTESIAN_POINT ( 'NONE',  ( 0.1167790944451423257, 0.05972222214635558579, -0.2819296736111110424 ) ) ;
#7112=CIRCLE ( 'NONE', #2448, 0.3119999999999999996 ) ;
#7113=EDGE_CURVE ( 'NONE', #22483, #10834, #16609, .T. ) ;
#7117=CARTESIAN_POINT ( 'NONE',  ( -0.2819296736111110979, 4.588972222298088433, 0.000000000000000000 ) ) ;
#7119=CARTESIAN_POINT ( 'NONE',  ( -0.1167790944451423535, 5.043833333409199149, 0.2819296736111110424 ) ) ;
#7121=CARTESIAN_POINT ( 'NONE',  ( 0.03947139886607073378, 3.764953234593765519, -0.3096039074880256314 ) ) ;
#7122=CARTESIAN_POINT ( 'NONE',  ( 0.1720740510253924160, 0.05226575782620486443, 0.2482834776946442890 ) ) ;
#7124=CARTESIAN_POINT ( 'NONE',  ( 0.3119999999999999996, 4.252166666818399499, -3.820898013339742174E-17 ) ) ;
#7125=CARTESIAN_POINT ( 'NONE',  ( -0.1167790944451423119, 4.523000000075866112, -0.2819296736111110979 ) ) ;
#7126=CARTESIAN_POINT ( 'NONE',  ( -0.2819296736111110979, 3.852861111186976828, 0.000000000000000000 ) ) ;
#7127=EDGE_LOOP ( 'NONE', ( #12755, #17092, #16007, #6770 ) ) ;
#7134=CARTESIAN_POINT ( 'NONE',  ( -0.2496812655993395358, 4.940926318456405397, -0.1915063317200945969 ) ) ;
#7137=CARTESIAN_POINT ( 'NONE',  ( 0.3119999999999998885, 0.2298611109593782231, 0.1292346314604058410 ) ) ;
#7139=CARTESIAN_POINT ( 'NONE',  ( -0.2684960426425861968, 5.119940279400660543, 0.1531817516059036377 ) ) ;
#7144=( BOUNDED_CURVE ( )  B_SPLINE_CURVE ( 2, ( #16371, #14790, #22206, #1840, #6, #15024, #22449, #16492, #12847 ),
 .UNSPECIFIED., .F., .F. ) 
 B_SPLINE_CURVE_WITH_KNOTS ( ( 3, 2, 2, 2, 3 ),
 ( 0.3124999999999999445, 0.3169642857142856429, 0.3214285714285713969, 0.3258928571428570953, 0.3303571428571427937 ),
 .UNSPECIFIED. ) 
 CURVE ( )  GEOMETRIC_REPRESENTATION_ITEM ( )  RATIONAL_B_SPLINE_CURVE ( ( 1.000000000000000888, 0.9238795325112857393, 1.000000000000000000, 0.9238795325112867385, 1.000000000000000000, 0.9238795325112867385, 1.000000000000000000, 0.9238795325112877377, 0.9999999999999990008 ) ) 
 REPRESENTATION_ITEM ( '' )  );
#7148=CARTESIAN_POINT ( 'NONE',  ( -0.1167790944451423257, 4.120222222298087544, -0.2819296736111110424 ) ) ;
#7149=CARTESIAN_POINT ( 'NONE',  ( -0.2819296736111110979, 5.127166666742532186, -0.1167790944451422980 ) ) ;
#7152=CARTESIAN_POINT ( 'NONE',  ( -0.2206173157302028232, 4.043833333333332725, -0.2206173157302028232 ) ) ;
#7153=CARTESIAN_POINT ( 'NONE',  ( 5.731347020009612645E-17, 4.960500000151731648, 0.3119999999999999996 ) ) ;
#7154=CARTESIAN_POINT ( 'NONE',  ( 0.3102322028195323989, 4.806806770341049528, 0.03330294158711297886 ) ) ;
#7155=CARTESIAN_POINT ( 'NONE',  ( -0.3119999999999998885, 4.165361111111110404, 0.1292346314604058410 ) ) ;
#7157=CARTESIAN_POINT ( 'NONE',  ( -0.09675901534512296176, 0.05896212819178082293, 0.2930612987570491157 ) ) ;
#7159=CIRCLE ( 'NONE', #21186, 0.3119999999999999996 ) ;
#7164=CARTESIAN_POINT ( 'NONE',  ( 0.1993543840281266910, 0.2784722221463555858, -0.1993543840281266910 ) ) ;
#7166=CARTESIAN_POINT ( 'NONE',  ( 0.1993543840281267465, 5.109805555631420582, 0.1993543840281266633 ) ) ;
#7167=CARTESIAN_POINT ( 'NONE',  ( 0.3064354089977339157, 4.472750180103851392, 0.05870368663529628578 ) ) ;
#7169=CARTESIAN_POINT ( 'NONE',  ( 0.1167790944451422702, 4.779944444520309865, -0.2819296736111110424 ) ) ;
#7170=CARTESIAN_POINT ( 'NONE',  ( 0.000000000000000000, 5.384999999999999787, 0.000000000000000000 ) ) ;
#7171=CARTESIAN_POINT ( 'NONE',  ( -2.750539236387841874E-07, 4.266055563097283176, -0.3119999999998787632 ) ) ;
#7172=CARTESIAN_POINT ( 'NONE',  ( 0.1292346314604009005, 4.068138888888888083, 0.3120000000000048845 ) ) ;
#7174=CARTESIAN_POINT ( 'NONE',  ( -0.2206173157302028232, 4.710499999999999687, -0.2206173157302028232 ) ) ;
#7175=CARTESIAN_POINT ( 'NONE',  ( 0.1634417798997719051, 5.205158050261544211, 0.2312413009345976878 ) ) ;
#7176=CARTESIAN_POINT ( 'NONE',  ( -0.2819296736111110979, 4.071611111186976828, -0.1167790944451422980 ) ) ;
#7178=CARTESIAN_POINT ( 'NONE',  ( -0.2819296736111110424, 3.759111111186976828, 0.1167790944451424923 ) ) ;
#7179=CARTESIAN_POINT ( 'NONE',  ( 0.1028766551507927507, 4.040942783538628902, -0.2950564953585517736 ) ) ;
#7185=CARTESIAN_POINT ( 'NONE',  ( -1.726321361862525858E-17, 4.227861111186976828, -0.2819296736111110979 ) ) ;
#7186=CARTESIAN_POINT ( 'NONE',  ( -0.01087916929289088099, 4.488590625638971154, -0.3118577123740120527 ) ) ;
#7190=CARTESIAN_POINT ( 'NONE',  ( -2.266361716303445225E-16, 4.432722222374099630, -0.3119999999999999996 ) ) ;
#7193=CARTESIAN_POINT ( 'NONE',  ( -0.1167790944451424368, 0.1847222221463556413, 0.2819296736111110424 ) ) ;
#7194=CARTESIAN_POINT ( 'NONE',  ( 0.008932132220340730649, 3.876926249342690145, -0.3118903982160737831 ) ) ;
#7195=DIRECTION ( 'NONE',  ( -0.000000000000000000, -1.000000000000000000, -0.000000000000000000 ) ) ;
#7200=CARTESIAN_POINT ( 'NONE',  ( 0.1988757138996042617, 3.752970977545328157, -0.2404006040361021113 ) ) ;
#7202=CARTESIAN_POINT ( 'NONE',  ( 1.910449006669871087E-17, -0.02361111111111144356, -0.3119999999999999996 ) ) ;
#7203=CARTESIAN_POINT ( 'NONE',  ( -0.2819296736111110979, 3.922305555631421914, 0.000000000000000000 ) ) ;
#7207=CARTESIAN_POINT ( 'NONE',  ( 0.1993543840281267465, 4.387583333409199149, 0.1993543840281266633 ) ) ;
#7209=CARTESIAN_POINT ( 'NONE',  ( -0.3119999999999999996, 4.380638888888888083, -0.1292346314604056468 ) ) ;
#7210=CARTESIAN_POINT ( 'NONE',  ( 0.01962962522499191176, 4.376629226301396614, -0.3119684076890694158 ) ) ;
#7211=CARTESIAN_POINT ( 'NONE',  ( -0.1167790944451423257, 5.231333333409198261, -0.2819296736111110424 ) ) ;
#7213=CARTESIAN_POINT ( 'NONE',  ( 0.2875779526214432003, 4.193046792779527188, 0.1220845629366733021 ) ) ;
#7215=CYLINDRICAL_SURFACE ( 'NONE', #5287, 0.3119999999999999996 ) ;
#7218=CARTESIAN_POINT ( 'NONE',  ( -0.1167790944451423119, 4.620222222298087544, -0.2819296736111110979 ) ) ;
#7220=CARTESIAN_POINT ( 'NONE',  ( -0.1545212632259251595, 4.067003750745931789, 0.2710483404691284015 ) ) ;
#7223=CARTESIAN_POINT ( 'NONE',  ( -0.1167790944451422702, 0.3444444443685777402, -0.2819296736111110424 ) ) ;
#7224=ADVANCED_FACE ( 'NONE', ( #14557 ), #23340, .T. ) ;
#7226=VERTEX_POINT ( 'NONE', #8353 ) ;
#7227=CARTESIAN_POINT ( 'NONE',  ( -0.1167790944451422702, 0.2333333332574666907, -0.2819296736111110424 ) ) ;
#7228=CARTESIAN_POINT ( 'NONE',  ( -0.3119999999999999996, 4.325083333333332725, -0.1292346314604056468 ) ) ;
#7234=CARTESIAN_POINT ( 'NONE',  ( -0.2565705662273032872, 3.885668986695542060, -0.1775261799423144271 ) ) ;
#7235=CARTESIAN_POINT ( 'NONE',  ( -0.1167790944451422702, 0.1083333332574667046, -0.2819296736111110424 ) ) ;
#7236=CARTESIAN_POINT ( 'NONE',  ( 0.1993543840281267465, 4.554250000075866112, 0.1993543840281266633 ) ) ;
#7238=CARTESIAN_POINT ( 'NONE',  ( 0.03118581108655819195, 4.516944820282859929, 0.3111218374044668611 ) ) ;
#7240=CARTESIAN_POINT ( 'NONE',  ( 0.1167790944451424368, 5.050777777853643791, 0.2819296736111110424 ) ) ;
#7241=CARTESIAN_POINT ( 'NONE',  ( -0.2865907421542747691, 0.05024142792322828371, -0.09003034002162962901 ) ) ;
#7242=CARTESIAN_POINT ( 'NONE',  ( 0.2959576967297150585, 3.749313823154953873, 0.1001818723666523803 ) ) ;
#7245=CARTESIAN_POINT ( 'NONE',  ( 0.09681669869989185939, 3.929937981323567087, -0.2975949584254778957 ) ) ;
#7246=CARTESIAN_POINT ( 'NONE',  ( -0.3119999999999999996, 4.335500000151731648, 0.000000000000000000 ) ) ;
#7247=CARTESIAN_POINT ( 'NONE',  ( 0.1993543840281267465, 4.498694444520309865, 0.1993543840281266633 ) ) ;
#7248=CARTESIAN_POINT ( 'NONE',  ( 0.1167790944451424368, 3.870222222298087988, 0.2819296736111110424 ) ) ;
#7250=ORIENTED_EDGE ( 'NONE', *, *, #20260, .T. ) ;
#7253=CARTESIAN_POINT ( 'NONE',  ( -0.1292346314604057300, 4.283416666666665762, 0.3119999999999998885 ) ) ;
#7254=CARTESIAN_POINT ( 'NONE',  ( -0.3037294952134644288, 4.948996506944134843, 0.08224234445281884687 ) ) ;
#7257=ORIENTED_EDGE ( 'NONE', *, *, #12814, .F. ) ;
#7258=CARTESIAN_POINT ( 'NONE',  ( 0.3119999999999999996, 0.1812499998482670904, -0.1292346314604056468 ) ) ;
#7260=CARTESIAN_POINT ( 'NONE',  ( -0.1930140748054549049, 3.716415235292884311, -0.2451613398821450296 ) ) ;
#7266=CARTESIAN_POINT ( 'NONE',  ( 0.3042850080729309070, 5.083614731684491517, 0.07087365376649608362 ) ) ;
#7268=CARTESIAN_POINT ( 'NONE',  ( 5.178964085587577574E-17, 4.311194444520309865, 0.2819296736111110979 ) ) ;
#7269=CARTESIAN_POINT ( 'NONE',  ( 0.2819296736111111534, 5.099388888964754507, 0.1167790944451422563 ) ) ;
#7271=CARTESIAN_POINT ( 'NONE',  ( -0.3076274917712982782, 4.225837578920637050, 0.05212383236253055607 ) ) ;
#7272=CARTESIAN_POINT ( 'NONE',  ( 0.1292346314604056190, 3.811194444444443441, -0.3119999999999999996 ) ) ;
#7273=CARTESIAN_POINT ( 'NONE',  ( -1.910449006669871087E-17, 4.932722222373954857, -0.3119999999999999996 ) ) ;
#7274=CARTESIAN_POINT ( 'NONE',  ( 0.2916638615397387779, 4.804523324935893847, 0.1117996548601188078 ) ) ;
#7275=CARTESIAN_POINT ( 'NONE',  ( 0.000000000000000000, 5.384999999999999787, -0.3119999999999999996 ) ) ;
#7277=CARTESIAN_POINT ( 'NONE',  ( 0.1112748779815979916, 0.04093257519601814498, -0.2692499194552509523 ) ) ;
#7280=( BOUNDED_CURVE ( )  B_SPLINE_CURVE ( 2, ( #12110, #17336, #2813, #629, #23279, #6593, #4755, #15390, #6108 ),
 .UNSPECIFIED., .F., .T. ) 
 B_SPLINE_CURVE_WITH_KNOTS ( ( 3, 2, 2, 2, 3 ),
 ( 0.8303571428571426827, 0.8348214285714283811, 0.8392857142857141906, 0.8437500000000000000, 0.8482142857142856984 ),
 .UNSPECIFIED. ) 
 CURVE ( )  GEOMETRIC_REPRESENTATION_ITEM ( )  RATIONAL_B_SPLINE_CURVE ( ( 1.000000000000003775, 0.9238795325112829637, 1.000000000000000000, 0.9238795325112867385, 1.000000000000000000, 0.9238795325112867385, 1.000000000000000000, 0.9238795325112867385, 1.000000000000000000 ) ) 
 REPRESENTATION_ITEM ( '' )  );
#7282=CARTESIAN_POINT ( 'NONE',  ( -0.1993543840281266910, 5.012583333409199149, -0.1993543840281266910 ) ) ;
#7283=( BOUNDED_CURVE ( )  B_SPLINE_CURVE ( 2, ( #23738, #14873, #6937, #21806, #14501, #18155, #9735, #18881, #5825 ),
 .UNSPECIFIED., .F., .F. ) 
 B_SPLINE_CURVE_WITH_KNOTS ( ( 3, 2, 2, 2, 3 ),
 ( 0.4553571428571429602, 0.4598214285714286587, 0.4642857142857144126, 0.4687500000000001110, 0.4732142857142858094 ),
 .UNSPECIFIED. ) 
 CURVE ( )  GEOMETRIC_REPRESENTATION_ITEM ( )  RATIONAL_B_SPLINE_CURVE ( ( 0.9999999999999981126, 0.9238795325112886259, 1.000000000000000000, 0.9238795325112867385, 1.000000000000000000, 0.9238795325112867385, 1.000000000000000000, 0.9238795325112848511, 1.000000000000001998 ) ) 
 REPRESENTATION_ITEM ( '' )  );
#7285=CARTESIAN_POINT ( 'NONE',  ( 0.1993543840281266355, 0.3756944443685777957, 0.1993543840281267465 ) ) ;
#7288=CARTESIAN_POINT ( 'NONE',  ( -0.1993543840281266355, 5.040361111186977716, 0.1993543840281267465 ) ) ;
#7289=CARTESIAN_POINT ( 'NONE',  ( 0.3050023557400097785, 4.472545578696121460, 0.06570874416663827211 ) ) ;
#7292=CARTESIAN_POINT ( 'NONE',  ( 0.1167790944451422702, 4.835500000075865223, -0.2819296736111110424 ) ) ;
#7294=CARTESIAN_POINT ( 'NONE',  ( -1.910449006669871087E-17, 5.036888888888888971, -0.3119999999999999996 ) ) ;
#7297=CARTESIAN_POINT ( 'NONE',  ( 0.2206173157302028787, 4.627166666666665762, 0.2206173157302027954 ) ) ;
#7299=CARTESIAN_POINT ( 'NONE',  ( -0.1993543840281266355, 4.082027777853643791, 0.1993543840281267465 ) ) ;
#7300=LINE ( 'NONE', #14749, #20227 ) ;
#7301=CARTESIAN_POINT ( 'NONE',  ( 0.1565020774999655861, 4.020729645363375404, 0.2706823387111469414 ) ) ;
#7302=CARTESIAN_POINT ( 'NONE',  ( 0.3120000000000000551, 4.408416666666666650, 0.1292346314604056190 ) ) ;
#7305=CARTESIAN_POINT ( 'NONE',  ( -0.1730627168398009008, 4.121933759322424784, 0.2596022278612341583 ) ) ;
#7306=CARTESIAN_POINT ( 'NONE',  ( 0.3119999999999999996, 0.07708333333333300397, -0.1292346314604056468 ) ) ;
#7314=CARTESIAN_POINT ( 'NONE',  ( 0.1993543840281266910, 0.2645833332574666907, -0.1993543840281266910 ) ) ;
#7315=CARTESIAN_POINT ( 'NONE',  ( 0.002232267356213628925, 3.877106664906796230, -0.3119931564268053625 ) ) ;
#7316=CARTESIAN_POINT ( 'NONE',  ( 3.820898013339742174E-17, 5.384999999999999787, 0.3119999999999999996 ) ) ;
#7321=CARTESIAN_POINT ( 'NONE',  ( -0.2338243153676845543, 5.099281701770390640, -0.2058997526750516449 ) ) ;
#7323=CARTESIAN_POINT ( 'NONE',  ( 0.2819296736111110979, 0.5909722221463555858, 0.000000000000000000 ) ) ;
#7324=CARTESIAN_POINT ( 'NONE',  ( 0.1797082215028593943, 3.735609866510083865, -0.2172309738199109941 ) ) ;
#7326=CARTESIAN_POINT ( 'NONE',  ( 0.2819296736111110979, 4.450083333409199149, -3.452642723725051716E-17 ) ) ;
#7327=CARTESIAN_POINT ( 'NONE',  ( 0.2206173157302028787, 4.960499999999998799, 0.2206173157302027954 ) ) ;
#7329=ORIENTED_EDGE ( 'NONE', *, *, #4837, .F. ) ;
#7330=VECTOR ( 'NONE', #414, 39.37007874015748143 ) ;
#7331=CARTESIAN_POINT ( 'NONE',  ( 0.04079027354135526806, 4.350485889367855741, 0.3119999945730878022 ) ) ;
#7332=CARTESIAN_POINT ( 'NONE',  ( 0.1167790944451424368, 4.925777777853642903, 0.2819296736111110424 ) ) ;
#7336=CARTESIAN_POINT ( 'NONE',  ( 0.2819296736111110979, 4.769527777853642903, -3.452642723725051716E-17 ) ) ;
#7339=CARTESIAN_POINT ( 'NONE',  ( -5.731347020009612645E-17, 0.4416666665149336923, 0.3119999999999999996 ) ) ;
#7340=CARTESIAN_POINT ( 'NONE',  ( 1.726321361862525858E-17, 0.5631944443685776847, -0.2819296736111110979 ) ) ;
#7343=CARTESIAN_POINT ( 'NONE',  ( 0.1167790944451423257, 0.2263888888130222710, -0.2819296736111110424 ) ) ;
#7344=CARTESIAN_POINT ( 'NONE',  ( -0.1292346314604081170, 4.318138888888888083, -0.3119999999999975016 ) ) ;
#7345=CARTESIAN_POINT ( 'NONE',  ( -0.2805147388977641820, 5.200218985593472176, -0.05155921707341403620 ) ) ;
#7349=CARTESIAN_POINT ( 'NONE',  ( -0.3125022104525487232, 3.890849970558711401, -0.006219195744223885054 ) ) ;
#7350=B_SPLINE_CURVE_WITH_KNOTS ( 'NONE', 3,
 ( #13534, #822, #23235, #15582, #20828, #6307, #23006, #19472, #11813, #15466, #4477, #13760, #2768, #20948, #17645, #4120, #933, #17530, #19003, #17177, #11941, #19116, #22891, #15345, #6185, #19358, #11578, #7893, #4239, #8251, #15702, #13648, #2302, #8364, #9738, #462, #583, #2421, #23117, #19233, #21066, #2539, #9862, #6427, #13880, #21310, #17291, #20079, #1545, #2882, #21902, #7037 ),
 .UNSPECIFIED., .F., .F.,
 ( 4, 2, 1, 1, 1, 1, 1, 1, 2, 2, 2, 2, 2, 2, 2, 2, 2, 2, 1, 1, 2, 2, 2, 2, 2, 2, 2, 2, 2, 4 ),
 ( 0.3380880081932458592, 0.3380924783650609000, 0.3380969485368759408, 0.3381058888805060225, 0.3381237695677661859, 0.3381595309422865125, 0.3382310536913272214, 0.3383740991894085282, 0.3386601901855712526, 0.3392323721778965906, 0.3403767361625473220, 0.3415211001471980534, 0.3426654641318487848, 0.3438098281164995162, 0.3443820101088249097, 0.3446681011049875787, 0.3446859817922477420, 0.3447038624795079054, 0.3447396238540282321, 0.3448111466030689409, 0.3449541921011502477, 0.3472429200704517105, 0.3495316480397531178, 0.3518203760090545251, 0.3541091039783559324, 0.3552534679630066083, 0.3553965134610879706, 0.3555395589591693328, 0.3558256499553320018, 0.3563978319476573398 ),
 .UNSPECIFIED. ) ;
#7351=CARTESIAN_POINT ( 'NONE',  ( 1.726321361862525858E-17, -0.006250000075866632768, -0.2819296736111110979 ) ) ;
#7352=CARTESIAN_POINT ( 'NONE',  ( 0.2819296736111110979, 4.446611111186976828, 0.1167790944451422425 ) ) ;
#7354=B_SPLINE_CURVE_WITH_KNOTS ( 'NONE', 3,
 ( #23615, #13042, #9242, #20220, #3508, #6930 ),
 .UNSPECIFIED., .F., .F.,
 ( 4, 2, 4 ),
 ( 0.05028785581520123227, 0.1127878554948266582, 0.1752878551744520841 ),
 .UNSPECIFIED. ) ;
#7355=CARTESIAN_POINT ( 'NONE',  ( 0.01477765123391010932, 4.543413721529206306, -0.3116996714995854401 ) ) ;
#7356=CARTESIAN_POINT ( 'NONE',  ( 0.1167790944451424368, 5.106333333409198261, 0.2819296736111110424 ) ) ;
#7357=CARTESIAN_POINT ( 'NONE',  ( 0.1167790944451422702, 4.446611111186976828, -0.2819296736111110979 ) ) ;
#7358=CARTESIAN_POINT ( 'NONE',  ( 0.2531481986011811514, 3.757757936612477145, -0.1838958115507471347 ) ) ;
#7360=CARTESIAN_POINT ( 'NONE',  ( 0.1297984762942410164, 3.908702258813368857, 0.2857640727182840790 ) ) ;
#7361=CARTESIAN_POINT ( 'NONE',  ( -1.910449006669871087E-17, 4.099388889040620931, -0.3119999999999999996 ) ) ;
#7362=CARTESIAN_POINT ( 'NONE',  ( 5.178964085587577574E-17, 4.436194444520310753, 0.2819296736111110979 ) ) ;
#7363=CARTESIAN_POINT ( 'NONE',  ( 0.2819296736111110424, 3.828555555631421026, -0.1167790944451423396 ) ) ;
#7369=EDGE_CURVE ( 'NONE', #11100, #7025, #2281, .T. ) ;
#7370=CARTESIAN_POINT ( 'NONE',  ( -0.08174960291637467513, 4.935080742073520099, -0.3038624884746509713 ) ) ;
#7371=FACE_OUTER_BOUND ( 'NONE', #3653, .T. ) ;
#7373=CARTESIAN_POINT ( 'NONE',  ( -5.731347020009612645E-17, 0.5527777776260448528, 0.3119999999999999996 ) ) ;
#7375=CARTESIAN_POINT ( 'NONE',  ( -0.1997712965817471376, 3.716669753339185700, -0.2396573947470825861 ) ) ;
#7380=VECTOR ( 'NONE', #14894, 39.37007874015748143 ) ;
#7382=CARTESIAN_POINT ( 'NONE',  ( 0.1969676853939942296, 5.093707226201246385, -0.2418488411147588502 ) ) ;
#7384=CARTESIAN_POINT ( 'NONE',  ( -0.2819296736111110424, 4.238277777853642903, -0.1167790944451423119 ) ) ;
#7385=CARTESIAN_POINT ( 'NONE',  ( 0.1993543840281267465, 5.095916666742532186, 0.1993543840281266633 ) ) ;
#7387=CARTESIAN_POINT ( 'NONE',  ( -0.3094852631870094739, 4.225487789190556676, 0.03986035098601010268 ) ) ;
#7388=CARTESIAN_POINT ( 'NONE',  ( -1.910449006669871087E-17, 3.759111111111109960, -0.3119999999999999996 ) ) ;
#7389=CARTESIAN_POINT ( 'NONE',  ( 0.2206173157302028787, 5.023000000151731648, 0.2206173157302027954 ) ) ;
#7390=CARTESIAN_POINT ( 'NONE',  ( 0.1167790944451422702, 5.127166666742532186, -0.2819296736111110979 ) ) ;
#7395=ORIENTED_EDGE ( 'NONE', *, *, #18460, .F. ) ;
#7397=CARTESIAN_POINT ( 'NONE',  ( 0.2793135105113299654, 0.03335568393651896363, 0.05007282442598128686 ) ) ;
#7402=CARTESIAN_POINT ( 'NONE',  ( 0.2819296736111110424, 5.106333333409198261, -0.1167790944451423396 ) ) ;
#7406=CARTESIAN_POINT ( 'NONE',  ( -0.2819296736111111534, 0.3027777777019111660, 0.1167790944451422563 ) ) ;
#7408=CARTESIAN_POINT ( 'NONE',  ( 5.178964085587577574E-17, 4.880638888964754507, 0.2819296736111110979 ) ) ;
#7409=CARTESIAN_POINT ( 'NONE',  ( 0.04280166039970490638, 4.487079570219966840, -0.3091224059445770722 ) ) ;
#7410=CARTESIAN_POINT ( 'NONE',  ( 0.2819296736111110979, 4.877166666742533963, 0.1167790944451422425 ) ) ;
#7413=CARTESIAN_POINT ( 'NONE',  ( -0.002403927698694708574, 4.266120144334736963, -0.3119999978808592478 ) ) ;
#7416=CARTESIAN_POINT ( 'NONE',  ( -0.1292346314604056745, 4.595916666666665762, -0.3119999999999999996 ) ) ;
#7418=CARTESIAN_POINT ( 'NONE',  ( -0.1993543840281266355, 3.970916666742532186, 0.1993543840281267465 ) ) ;
#7419=CARTESIAN_POINT ( 'NONE',  ( 0.04820796449995154442, 5.072973651020436847, 0.3082531300064171864 ) ) ;
#7420=CARTESIAN_POINT ( 'NONE',  ( 0.1561509399989899904, 4.039288193619596790, -0.2708485047170307025 ) ) ;
#7421=DIRECTION ( 'NONE',  ( -0.000000000000000000, -1.000000000000000000, -0.000000000000000000 ) ) ;
#7422=CARTESIAN_POINT ( 'NONE',  ( 0.2206173157302027954, 3.918833333333332281, -0.2206173157302028232 ) ) ;
#7423=ORIENTED_EDGE ( 'NONE', *, *, #17379, .F. ) ;
#7424=( BOUNDED_CURVE ( )  B_SPLINE_CURVE ( 2, ( #1427, #8855, #16299, #7155, #10938, #12658, #23711, #21780, #23834 ),
 .UNSPECIFIED., .F., .F. ) 
 B_SPLINE_CURVE_WITH_KNOTS ( ( 3, 2, 2, 2, 3 ),
 ( 0.7053571428571429047, 0.7098214285714286031, 0.7142857142857144126, 0.7187500000000001110, 0.7232142857142858094 ),
 .UNSPECIFIED. ) 
 CURVE ( )  GEOMETRIC_REPRESENTATION_ITEM ( )  RATIONAL_B_SPLINE_CURVE ( ( 1.000000000000000000, 0.9238795325112867385, 1.000000000000000000, 0.9238795325112867385, 1.000000000000000000, 0.9238795325112867385, 1.000000000000000000, 0.9238795325112848511, 1.000000000000001998 ) ) 
 REPRESENTATION_ITEM ( '' )  );
#7428=CARTESIAN_POINT ( 'NONE',  ( 0.3107331597152522829, 4.640251624014341658, 0.02937061414036503879 ) ) ;
#7434=CARTESIAN_POINT ( 'NONE',  ( 0.2819296736111110424, 0.2541666665908000056, 0.1167790944451424923 ) ) ;
#7436=DIRECTION ( 'NONE',  ( -0.000000000000000000, -1.000000000000000000, -0.000000000000000000 ) ) ;
#7439=CARTESIAN_POINT ( 'NONE',  ( -0.2789096574489232094, 5.101491767903201691, -0.1383920302399104796 ) ) ;
#7441=CARTESIAN_POINT ( 'NONE',  ( 0.2819296736111110424, 0.5944444443685777957, -0.1167790944451423119 ) ) ;
#7442=CARTESIAN_POINT ( 'NONE',  ( -0.3119999999999999996, 5.158416666666665762, -0.1292346314604056468 ) ) ;
#7444=CARTESIAN_POINT ( 'NONE',  ( -0.2819296736111110979, 4.422305555631421470, 0.000000000000000000 ) ) ;
#7448=DIRECTION ( 'NONE',  ( 1.224646799147353207E-16, 0.000000000000000000, -1.000000000000000000 ) ) ;
#7449=CARTESIAN_POINT ( 'NONE',  ( 5.178964085587577574E-17, 5.033416666742532186, 0.2819296736111110979 ) ) ;
#7450=CARTESIAN_POINT ( 'NONE',  ( -0.2909262194017099845, 5.157387803290264472, 0.07538336336425460749 ) ) ;
#7451=CARTESIAN_POINT ( 'NONE',  ( -0.3119999999999999996, 0.2124999999999996336, -3.820898013339742174E-17 ) ) ;
#7452=CARTESIAN_POINT ( 'NONE',  ( 5.178964085587577574E-17, 4.755638888964754507, 0.2819296736111110979 ) ) ;
#7454=CARTESIAN_POINT ( 'NONE',  ( -0.09554088032208432613, 4.068872337771485270, 0.2980384827267206216 ) ) ;
#7455=CARTESIAN_POINT ( 'NONE',  ( 0.2206173157302028787, 4.904944444444443441, 0.2206173157302027954 ) ) ;
#7456=CARTESIAN_POINT ( 'NONE',  ( -0.1993543840281267465, 0.4729166665907999501, 0.1993543840281266633 ) ) ;
#7459=CARTESIAN_POINT ( 'NONE',  ( -0.1993543840281267465, 0.1395833332574666907, 0.1993543840281266633 ) ) ;
#7466=CARTESIAN_POINT ( 'NONE',  ( -0.2565929520051963841, 3.885670105107792427, -0.1774938258202259367 ) ) ;
#7467=CARTESIAN_POINT ( 'NONE',  ( 0.1993543840281266355, 0.2506944443685777957, 0.1993543840281267465 ) ) ;
#7469=CARTESIAN_POINT ( 'NONE',  ( -0.2819296736111110424, 4.536888888964754507, 0.1167790944451424923 ) ) ;
#7473=CARTESIAN_POINT ( 'NONE',  ( 0.1167790944451422702, 5.182722222298088433, -0.2819296736111110424 ) ) ;
#7474=CARTESIAN_POINT ( 'NONE',  ( -0.1993543840281266910, 4.457027777853642903, -0.1993543840281266910 ) ) ;
#7475=CARTESIAN_POINT ( 'NONE',  ( 0.004295427132208190675, 3.765940144888689556, -0.3119999790882598822 ) ) ;
#7478=CARTESIAN_POINT ( 'NONE',  ( -0.3119999999999998885, 4.116750000151731648, 0.1292346314604058410 ) ) ;
#7480=CARTESIAN_POINT ( 'NONE',  ( -0.2819296736111110979, 4.588972222298088433, 0.000000000000000000 ) ) ;
#7481=CARTESIAN_POINT ( 'NONE',  ( 0.1015006192750689817, 3.724843167714382286, -0.2819296736111111534 ) ) ;
#7490=CARTESIAN_POINT ( 'NONE',  ( -0.2206173157302028787, 0.4347222220704892726, 0.2206173157302027954 ) ) ;
#7493=CARTESIAN_POINT ( 'NONE',  ( -0.2711786023059446493, 3.719745625394835109, -0.1610394760142928317 ) ) ;
#7495=CARTESIAN_POINT ( 'NONE',  ( 0.1572698204966380964, 3.983617205690540786, -0.2725461618487980409 ) ) ;
#7497=ADVANCED_FACE ( 'NONE', ( #10465 ), #17894, .T. ) ;
#7499=CARTESIAN_POINT ( 'NONE',  ( 0.1675087228796504069, 5.076665303775934390, 0.2633721787117046520 ) ) ;
#7502=CARTESIAN_POINT ( 'NONE',  ( 0.1993543840281266633, 4.332027777853642903, -0.1993543840281266910 ) ) ;
#7503=CARTESIAN_POINT ( 'NONE',  ( -0.2819296736111110424, 5.134111111186975940, 0.1167790944451424923 ) ) ;
#7506=CARTESIAN_POINT ( 'NONE',  ( -0.3119999999999999996, 3.884111111111110404, 0.000000000000000000 ) ) ;
#7507=CARTESIAN_POINT ( 'NONE',  ( -0.2206173157302027676, 4.786888889040620931, 0.2206173157302028787 ) ) ;
#7510=CARTESIAN_POINT ( 'NONE',  ( -0.2819296736111110424, 5.203332556872311443, 0.1092791156175831058 ) ) ;
#7516=CARTESIAN_POINT ( 'NONE',  ( -0.1167790944451423257, 5.064666666742533074, -0.2819296736111110424 ) ) ;
#7517=CARTESIAN_POINT ( 'NONE',  ( 0.1167790944451424506, 3.939666666742532186, 0.2819296736111110424 ) ) ;
#7518=VECTOR ( 'NONE', #13586, 39.37007874015748143 ) ;
#7521=ADVANCED_FACE ( 'NONE', ( #12187 ), #16471, .T. ) ;
#7524=CARTESIAN_POINT ( 'NONE',  ( -0.2819296736111110979, 0.1847222221463555858, -0.1167790944451423396 ) ) ;
#7526=CARTESIAN_POINT ( 'NONE',  ( -0.1167790944451423535, 4.877166666742533963, 0.2819296736111110424 ) ) ;
#7527=CARTESIAN_POINT ( 'NONE',  ( -0.1993543840281266910, 4.957027777853642903, -0.1993543840281266910 ) ) ;
#7530=CARTESIAN_POINT ( 'NONE',  ( -1.910449006669871087E-17, 4.592444444444443441, -0.3119999999999999996 ) ) ;
#7531=CARTESIAN_POINT ( 'NONE',  ( 0.000000000000000000, 5.384999999999999787, 0.000000000000000000 ) ) ;
#7532=CARTESIAN_POINT ( 'NONE',  ( 0.1292346314604056190, 4.588972222222221120, -0.3119999999999999996 ) ) ;
#7533=CARTESIAN_POINT ( 'NONE',  ( 0.2819296736111110979, 3.769527777853642903, -3.452642723725051716E-17 ) ) ;
#7536=CARTESIAN_POINT ( 'NONE',  ( 7.484242640931070629E-07, 4.016084960865516251, 0.3119999999981048489 ) ) ;
#7541=CARTESIAN_POINT ( 'NONE',  ( -0.03772805809618737238, 4.100482206091769832, -0.3120000000000012208 ) ) ;
#7542=DIRECTION ( 'NONE',  ( -0.000000000000000000, -1.000000000000000000, -0.000000000000000000 ) ) ;
#7544=CARTESIAN_POINT ( 'NONE',  ( 3.820898013339742174E-17, 5.384999999999999787, 0.3119999999999999996 ) ) ;
#7545=CARTESIAN_POINT ( 'NONE',  ( 3.820898013339742174E-17, 5.384999999999999787, 0.3119999999999999996 ) ) ;
#7548=CARTESIAN_POINT ( 'NONE',  ( 0.1167790944451423535, 0.3027777777019111105, 0.2819296736111110424 ) ) ;
#7549=CARTESIAN_POINT ( 'NONE',  ( 1.910449006669871087E-17, 0.1916666665149337478, -0.3119999999999999996 ) ) ;
#7551=FACE_OUTER_BOUND ( 'NONE', #11421, .T. ) ;
#7557=CARTESIAN_POINT ( 'NONE',  ( 0.3119999999999999996, -0.03402777777777810791, -0.1292346314604056468 ) ) ;
#7558=CARTESIAN_POINT ( 'NONE',  ( -0.3119999999999999996, 5.269527777777777366, -0.1292346314604056468 ) ) ;
#7560=VERTEX_POINT ( 'NONE', #23988 ) ;
#7561=CARTESIAN_POINT ( 'NONE',  ( -0.2819296736111110424, 4.203555555631421470, 0.1167790944451424923 ) ) ;
#7562=EDGE_CURVE ( 'NONE', #18493, #13675, #7300, .T. ) ;
#7567=CARTESIAN_POINT ( 'NONE',  ( -5.731347020009612645E-17, 0.3374999999999996336, 0.3119999999999999996 ) ) ;
#7568=CARTESIAN_POINT ( 'NONE',  ( 0.1993543840281266633, 4.998694444520309865, -0.1993543840281266910 ) ) ;
#7574=CARTESIAN_POINT ( 'NONE',  ( 0.1993543840281266633, 4.720916666742532186, -0.1993543840281266910 ) ) ;
#7578=CARTESIAN_POINT ( 'NONE',  ( 0.2819296736111110424, 0.4347222221463555858, 0.1167790944451424923 ) ) ;
#7580=CARTESIAN_POINT ( 'NONE',  ( -5.178964085587577574E-17, 0.3131944443685777957, 0.2819296736111110979 ) ) ;
#7586=LINE ( 'NONE', #15037, #15969 ) ;
#7587=CARTESIAN_POINT ( 'NONE',  ( 0.1993543840281266355, 0.1951388888130222155, 0.1993543840281267465 ) ) ;
#7588=CARTESIAN_POINT ( 'NONE',  ( -0.1167790944451422702, 0.05277777770191114520, -0.2819296736111110424 ) ) ;
#7589=CARTESIAN_POINT ( 'NONE',  ( -0.1993543840281266910, 4.248694444520310753, -0.1993543840281266910 ) ) ;
#7592=CARTESIAN_POINT ( 'NONE',  ( -0.1993543840281266355, 4.762583333409199149, 0.1993543840281267465 ) ) ;
#7594=CARTESIAN_POINT ( 'NONE',  ( -0.2819296736111110979, 4.516055555631421470, -0.1167790944451422980 ) ) ;
#7595=CARTESIAN_POINT ( 'NONE',  ( 0.000000000000000000, 5.384999999999999787, -0.3119999999999999996 ) ) ;
#7596=CARTESIAN_POINT ( 'NONE',  ( 0.2748323731540602832, 3.923346161548030953, -0.1544819192003367703 ) ) ;
#7597=CARTESIAN_POINT ( 'NONE',  ( 0.2206173157302028787, 4.134111111262843252, 0.2206173157302027954 ) ) ;
#7598=PRODUCT_DEFINITION_FORMATION_WITH_SPECIFIED_SOURCE ( 'ANY', '', #19646, .NOT_KNOWN. ) ;
#7602=VERTEX_POINT ( 'NONE', #10599 ) ;
#7605=CARTESIAN_POINT ( 'NONE',  ( -0.2471927412204658892, 4.841317424427891147, 0.1938822679348655431 ) ) ;
#7607=EDGE_LOOP ( 'NONE', ( #17840, #2972, #5167, #7864 ) ) ;
#7608=CARTESIAN_POINT ( 'NONE',  ( -5.731347020009612645E-17, 0.4972222220704892726, 0.3119999999999999996 ) ) ;
#7611=CARTESIAN_POINT ( 'NONE',  ( 0.06860513764972499262, 4.740183546148049487, 0.3064380078074160352 ) ) ;
#7619=CARTESIAN_POINT ( 'NONE',  ( -0.3032940676781117340, 4.666745353835117349, -0.07416804978120151992 ) ) ;
#7620=CARTESIAN_POINT ( 'NONE',  ( 5.178964085587577574E-17, 4.200083333409199149, 0.2819296736111110979 ) ) ;
#7623=CARTESIAN_POINT ( 'NONE',  ( -0.2206173157302027676, 3.835499999999998799, 0.2206173157302028787 ) ) ;
#7624=CARTESIAN_POINT ( 'NONE',  ( -0.3119999999999998885, 4.727861111262843252, 0.1292346314604058410 ) ) ;
#7626=CARTESIAN_POINT ( 'NONE',  ( -0.1167790944451423535, 5.154944444520309865, 0.2819296736111110979 ) ) ;
#7627=CARTESIAN_POINT ( 'NONE',  ( -0.1993543840281266355, 4.193138888964754507, 0.1993543840281267465 ) ) ;
#7628=CARTESIAN_POINT ( 'NONE',  ( -0.03429112345822225155, 3.903953541745516453, 0.3120000015083762568 ) ) ;
#7633=CARTESIAN_POINT ( 'NONE',  ( -0.06818719739654979795, 0.05951326967753017838, 0.3015576727156116243 ) ) ;
#7634=VERTEX_POINT ( 'NONE', #1325 ) ;
#7638=CARTESIAN_POINT ( 'NONE',  ( -0.1993543840281266355, 5.082027777853643791, 0.1993543840281267465 ) ) ;
#7639=CARTESIAN_POINT ( 'NONE',  ( -0.2819296736111110979, 3.977861111186976828, 0.000000000000000000 ) ) ;
#7642=EDGE_CURVE ( 'NONE', #6378, #1715, #726, .T. ) ;
#7645=CARTESIAN_POINT ( 'NONE',  ( 0.1167790944451423535, 0.4277777777019111660, 0.2819296736111110979 ) ) ;
#7647=CARTESIAN_POINT ( 'NONE',  ( -0.2819296736111110424, 4.870222222298087544, 0.1167790944451424923 ) ) ;
#7649=CARTESIAN_POINT ( 'NONE',  ( 0.2819296736111110424, 4.884111111186975940, -0.1167790944451423396 ) ) ;
#7651=CARTESIAN_POINT ( 'NONE',  ( 0.2199754637977810179, 4.856310113992576838, 0.2213457067253412347 ) ) ;
#7652=CARTESIAN_POINT ( 'NONE',  ( 0.3119999999999999996, 4.078555555555555046, -3.820898013339742174E-17 ) ) ;
#7654=CARTESIAN_POINT ( 'NONE',  ( -0.3119999999999999996, 4.547305555555555934, -0.1292346314604056468 ) ) ;
#7655=CARTESIAN_POINT ( 'NONE',  ( -0.1167790944451423535, 3.752166666742532186, 0.2819296736111110979 ) ) ;
#7656=CARTESIAN_POINT ( 'NONE',  ( 0.02997679058488651391, 4.987417349384497101, -0.3106133072238613235 ) ) ;
#7657=CARTESIAN_POINT ( 'NONE',  ( -0.1052608686101951518, 3.735246098045301721, 0.2937075919364244281 ) ) ;
#7658=CARTESIAN_POINT ( 'NONE',  ( 0.2916724325548126773, 4.582301768384474450, 0.1117771105708152413 ) ) ;
#7660=CARTESIAN_POINT ( 'NONE',  ( -0.1791194818499489971, 4.104818640075733605, -0.2582428417481592020 ) ) ;
#7661=EDGE_CURVE ( 'NONE', #21247, #3503, #11323, .T. ) ;
#7662=CARTESIAN_POINT ( 'NONE',  ( 0.2856515860211834013, 4.644828526069876951, -0.1311504800872141663 ) ) ;
#7665=EDGE_CURVE ( 'NONE', #10917, #1519, #16325, .T. ) ;
#7667=VERTEX_POINT ( 'NONE', #24108 ) ;
#7669=CIRCLE ( 'NONE', #16245, 0.2495000000000007212 ) ;
#7670=CARTESIAN_POINT ( 'NONE',  ( 0.2819296736111110979, 0.4798611110352444808, 0.000000000000000000 ) ) ;
#7675=CARTESIAN_POINT ( 'NONE',  ( -0.3062927780948892509, 5.103999883774990920, -0.05168569905423461147 ) ) ;
#7677=CARTESIAN_POINT ( 'NONE',  ( -0.1292346314604058410, 0.3340277777777773682, 0.3119999999999998885 ) ) ;
#7678=CARTESIAN_POINT ( 'NONE',  ( -0.3119999999999999996, 5.161888888888888083, 0.000000000000000000 ) ) ;
#7679=CARTESIAN_POINT ( 'NONE',  ( -0.2819296736111110979, 4.255638888964754507, 0.000000000000000000 ) ) ;
#7685=CARTESIAN_POINT ( 'NONE',  ( -0.1993543840281266355, 4.915361111186976828, 0.1993543840281267465 ) ) ;
#7687=CARTESIAN_POINT ( 'NONE',  ( -0.1833914370424524765, 5.148434169276817407, -0.2416754135350870913 ) ) ;
#7692=CARTESIAN_POINT ( 'NONE',  ( -1.910449006669871087E-17, 3.981333333333332725, -0.3119999999999999996 ) ) ;
#7694=CARTESIAN_POINT ( 'NONE',  ( 5.178964085587577574E-17, 4.588972222298087544, 0.2819296736111110979 ) ) ;
#7696=CARTESIAN_POINT ( 'NONE',  ( -0.008323108056630971682, 4.044058012889800935, -0.3119051118721674065 ) ) ;
#7698=CARTESIAN_POINT ( 'NONE',  ( 0.1993543840281266355, 0.5979166665908001166, 0.1993543840281267465 ) ) ;
#7700=CARTESIAN_POINT ( 'NONE',  ( 0.1167790944451423535, 0.2611111110352444808, 0.2819296736111110424 ) ) ;
#7707=CARTESIAN_POINT ( 'NONE',  ( 0.1167790944451423119, 0.2124999999241334037, -0.2819296736111110979 ) ) ;
#7708=CARTESIAN_POINT ( 'NONE',  ( 0.1993543840281266355, 0.3062499999241333759, 0.1993543840281267465 ) ) ;
#7709=CARTESIAN_POINT ( 'NONE',  ( -0.1167790944451423257, 4.300777777853642903, -0.2819296736111110424 ) ) ;
#7712=CARTESIAN_POINT ( 'NONE',  ( -0.2819296736111110424, 4.981333333409199149, 0.1167790944451424923 ) ) ;
#7713=CARTESIAN_POINT ( 'NONE',  ( -0.1167790944451423119, 4.342444444520310753, -0.2819296736111110979 ) ) ;
#7714=CARTESIAN_POINT ( 'NONE',  ( 0.2530624153226711526, 5.072996518863750026, 0.1824922298374807572 ) ) ;
#7715=CARTESIAN_POINT ( 'NONE',  ( 0.3119999999999999996, 4.526472222222221120, -0.1292346314604056745 ) ) ;
#7716=CARTESIAN_POINT ( 'NONE',  ( 0.2206173157302027954, 4.036888889040620931, -0.2206173157302028232 ) ) ;
#7717=CARTESIAN_POINT ( 'NONE',  ( 0.1292346314604056745, 0.1395833333333330317, -0.3119999999999999996 ) ) ;
#7719=ORIENTED_EDGE ( 'NONE', *, *, #19953, .F. ) ;
#7723=CARTESIAN_POINT ( 'NONE',  ( 0.1797085267211815662, 3.721720965436318362, -0.2172307213220433242 ) ) ;
#7725=CARTESIAN_POINT ( 'NONE',  ( -0.1912963777039489444, 4.993992924180794546, -0.2498290115581893456 ) ) ;
#7727=CARTESIAN_POINT ( 'NONE',  ( -0.3119999999999999996, 0.5944444442927114824, -3.820898013339742174E-17 ) ) ;
#7728=ORIENTED_EDGE ( 'NONE', *, *, #1230, .F. ) ;
#7731=CARTESIAN_POINT ( 'NONE',  ( 0.02974333840505747131, 4.765210078712510899, -0.3106355410811253437 ) ) ;
#7740=CARTESIAN_POINT ( 'NONE',  ( 0.2819296736111110979, 3.932722222298087544, 0.1167790944451422425 ) ) ;
#7743=CARTESIAN_POINT ( 'NONE',  ( -0.3119999999999999996, 3.772999999999999243, 0.000000000000000000 ) ) ;
#7745=CARTESIAN_POINT ( 'NONE',  ( 0.3119999999999999996, 4.752166666818398610, -3.820898013339742174E-17 ) ) ;
#7746=CARTESIAN_POINT ( 'NONE',  ( 0.1993543840281267465, 4.887583333409199149, 0.1993543840281266633 ) ) ;
#7748=CARTESIAN_POINT ( 'NONE',  ( -0.2819296736111110979, 4.297305555631420582, 0.000000000000000000 ) ) ;
#7751=ORIENTED_EDGE ( 'NONE', *, *, #11438, .F. ) ;
#7754=B_SPLINE_CURVE_WITH_KNOTS ( 'NONE', 3,
 ( #772, #19790, #15533, #6739, #4784, #21138, #2612, #2838, #21380, #15774, #21495, #17480, #6502, #17966, #1256, #13952, #2725, #6617, #10179, #10297, #14183, #17602, #10056, #22956, #8204, #2965, #23072, #15653, #10421, #6258, #17720, #13718, #8445, #12139 ),
 .UNSPECIFIED., .F., .F.,
 ( 4, 2, 2, 2, 2, 2, 2, 2, 1, 1, 1, 1, 2, 2, 2, 2, 2, 2, 4 ),
 ( 0.7401386592960095268, 0.7424993613057664366, 0.7448600633155233464, 0.7472207653252802562, 0.7495814673350371660, 0.7507618183399156209, 0.7507802613243668155, 0.7507894828165924128, 0.7507987043088180101, 0.7508355902777205104, 0.7509093622155254000, 0.7510569060911351791, 0.7513519938423547373, 0.7519421693447939647, 0.7543028713545505415, 0.7554832223594288854, 0.7566635733643072292, 0.7578439243691855731, 0.7590242753740639170 ),
 .UNSPECIFIED. ) ;
#7756=CARTESIAN_POINT ( 'NONE',  ( 0.2819296736111110979, 5.213972222298088433, -3.452642723725051716E-17 ) ) ;
#7757=CARTESIAN_POINT ( 'NONE',  ( -1.726321361862525858E-17, 3.963972222298087988, -0.2819296736111110979 ) ) ;
#7759=CARTESIAN_POINT ( 'NONE',  ( 0.1202474488300702554, 4.408426576200284330, 0.2881835540050379785 ) ) ;
#7761=CARTESIAN_POINT ( 'NONE',  ( 1.312321497832610059E-07, 4.821611112096344520, -0.3119999999999724105 ) ) ;
#7763=CARTESIAN_POINT ( 'NONE',  ( -0.1167790944451424506, 0.4208333332574666352, 0.2819296736111110424 ) ) ;
#7765=B_SPLINE_CURVE_WITH_KNOTS ( 'NONE', 3,
 ( #21147, #3963, #19192, #2502, #9941, #17371 ),
 .UNSPECIFIED., .F., .F.,
 ( 4, 2, 4 ),
 ( 0.000000000000000000, 0.001232805887355176112, 0.002465611774710352224 ),
 .UNSPECIFIED. ) ;
#7766=CARTESIAN_POINT ( 'NONE',  ( 0.2819296736111110424, 5.064666666742533074, -0.1167790944451423396 ) ) ;
#7767=CARTESIAN_POINT ( 'NONE',  ( 0.04086849681330569084, 4.461661661955456104, 0.3120000008906269051 ) ) ;
#7768=CARTESIAN_POINT ( 'NONE',  ( -0.1993543840281266910, 4.568138888964754507, -0.1993543840281266910 ) ) ;
#7769=CARTESIAN_POINT ( 'NONE',  ( 0.1292346314604056745, 0.2993055554038226429, -0.3119999999999999996 ) ) ;
#7770=CARTESIAN_POINT ( 'NONE',  ( 0.2387770904324161558, 4.869557469296990959, -0.2024777428408112145 ) ) ;
#7772=CYLINDRICAL_SURFACE ( 'NONE', #12780, 0.3119999999999999996 ) ;
#7773=CARTESIAN_POINT ( 'NONE',  ( -0.1292346314604057023, 4.561194444444443441, 0.3119999999999998885 ) ) ;
#7774=CARTESIAN_POINT ( 'NONE',  ( 0.1167790944451424506, 3.759111111186976828, 0.2819296736111110424 ) ) ;
#7776=( BOUNDED_CURVE ( )  B_SPLINE_CURVE ( 2, ( #2661, #19716, #3019, #6918, #4604, #1310, #21787, #8735, #6431 ),
 .UNSPECIFIED., .F., .F. ) 
 B_SPLINE_CURVE_WITH_KNOTS ( ( 3, 2, 2, 2, 3 ),
 ( 0.5267857142857140795, 0.5312499999999997780, 0.5357142857142855874, 0.5401785714285712858, 0.5446428571428569843 ),
 .UNSPECIFIED. ) 
 CURVE ( )  GEOMETRIC_REPRESENTATION_ITEM ( )  RATIONAL_B_SPLINE_CURVE ( ( 1.000000000000003775, 0.9238795325112829637, 1.000000000000000000, 0.9238795325112867385, 1.000000000000000000, 0.9238795325112867385, 1.000000000000000000, 0.9238795325112886259, 0.9999999999999981126 ) ) 
 REPRESENTATION_ITEM ( '' )  );
#7777=CARTESIAN_POINT ( 'NONE',  ( -0.3119999999999998885, 3.998694444444443885, 0.1292346314604058410 ) ) ;
#7783=CARTESIAN_POINT ( 'NONE',  ( -0.05621373772049894496, 4.125565998086674568, 0.3085550974868493390 ) ) ;
#7785=CARTESIAN_POINT ( 'NONE',  ( 0.2723844339573918694, 4.303051290467792889, 0.1575471963731641112 ) ) ;
#7786=CARTESIAN_POINT ( 'NONE',  ( 0.07856389089914374291, 5.132760641740106600, 0.2966322975708292065 ) ) ;
#7787=ORIENTED_EDGE ( 'NONE', *, *, #22172, .T. ) ;
#7791=CARTESIAN_POINT ( 'NONE',  ( 0.2819296736111110424, 0.5874999999241333759, 0.1167790944451424923 ) ) ;
#7792=CARTESIAN_POINT ( 'NONE',  ( 0.000000000000000000, 5.072999999999999510, 0.000000000000000000 ) ) ;
#7796=CARTESIAN_POINT ( 'NONE',  ( 1.910449006669871087E-17, 0.4763888888888885287, -0.3119999999999999996 ) ) ;
#7798=CARTESIAN_POINT ( 'NONE',  ( -0.1292346314604056190, 0.2020833333333329485, -0.3119999999999999996 ) ) ;
#7799=CARTESIAN_POINT ( 'NONE',  ( -0.3119999999999999996, 5.272999999999998799, 0.000000000000000000 ) ) ;
#7801=CARTESIAN_POINT ( 'NONE',  ( -0.2819296736111110979, 4.144527777853643791, 0.000000000000000000 ) ) ;
#7806=VERTEX_POINT ( 'NONE', #7419 ) ;
#7808=CARTESIAN_POINT ( 'NONE',  ( 0.1167790944451422702, 4.946611111186975940, -0.2819296736111110424 ) ) ;
#7809=EDGE_CURVE ( 'NONE', #15412, #2004, #4563, .T. ) ;
#7815=CARTESIAN_POINT ( 'NONE',  ( 0.2819296736111111534, 4.224388888964755395, 0.1167790944451422563 ) ) ;
#7820=CARTESIAN_POINT ( 'NONE',  ( 0.1993543840281266910, 0.3895833332574666352, -0.1993543840281266910 ) ) ;
#7825=CARTESIAN_POINT ( 'NONE',  ( 0.1292346314603988466, 5.033416666666665762, -0.3120000000000067164 ) ) ;
#7826=CARTESIAN_POINT ( 'NONE',  ( -0.2819296736111110979, 0.3930555554796889561, -0.1167790944451423396 ) ) ;
#7827=CARTESIAN_POINT ( 'NONE',  ( -0.1993543840281267465, 0.1812499999241333759, 0.1993543840281266633 ) ) ;
#7829=CARTESIAN_POINT ( 'NONE',  ( -0.1167790944451423257, 4.356333333409199149, -0.2819296736111110424 ) ) ;
#7831=CARTESIAN_POINT ( 'NONE',  ( -0.1993543840281266355, 4.929250000075866112, 0.1993543840281267465 ) ) ;
#7832=CARTESIAN_POINT ( 'NONE',  ( -1.726321361862525858E-17, 4.227861111186976828, -0.2819296736111110979 ) ) ;
#7835=CARTESIAN_POINT ( 'NONE',  ( -0.1292346314604056745, 3.991750000151732980, -0.3119999999999999996 ) ) ;
#7841=LINE ( 'NONE', #15288, #17342 ) ;
#7842=CARTESIAN_POINT ( 'NONE',  ( -0.2256660336270156497, 5.008917305905795203, 0.2154793158332795333 ) ) ;
#7844=CARTESIAN_POINT ( 'NONE',  ( 0.3119999999999998885, 0.5076388887371560132, 0.1292346314604058410 ) ) ;
#7846=DIRECTION ( 'NONE',  ( -0.000000000000000000, -1.000000000000000000, -0.000000000000000000 ) ) ;
#7848=CARTESIAN_POINT ( 'NONE',  ( -0.1292346314604056190, 0.5354166666666663188, -0.3119999999999999996 ) ) ;
#7850=CARTESIAN_POINT ( 'NONE',  ( 0.2335907231169286336, 5.183691625336232178, -0.1757699240049868106 ) ) ;
#7854=CARTESIAN_POINT ( 'NONE',  ( 3.887228417612631703E-07, 4.154944433789834690, -0.3119999999997578044 ) ) ;
#7855=CARTESIAN_POINT ( 'NONE',  ( -0.2307680606616751562, 4.675378956632738614, 0.2099770340440785255 ) ) ;
#7856=CARTESIAN_POINT ( 'NONE',  ( 0.2819296736111110979, 3.991750000075865223, -3.452642723725051716E-17 ) ) ;
#7860=CARTESIAN_POINT ( 'NONE',  ( 0.2206173157302027954, 4.648000000151731648, -0.2206173157302028232 ) ) ;
#7861=CARTESIAN_POINT ( 'NONE',  ( -0.1167790944451423119, 4.856333333409199149, -0.2819296736111110979 ) ) ;
#7863=CARTESIAN_POINT ( 'NONE',  ( -0.2819296736111110979, 4.241750000075865223, 0.000000000000000000 ) ) ;
#7864=ORIENTED_EDGE ( 'NONE', *, *, #12330, .T. ) ;
#7871=CARTESIAN_POINT ( 'NONE',  ( 0.2819296736111110979, 3.953555555631421470, -0.1167790944451423396 ) ) ;
#7872=CARTESIAN_POINT ( 'NONE',  ( 0.09525661631228125870, 4.429985109478741023, -0.2971466434106878607 ) ) ;
#7873=CARTESIAN_POINT ( 'NONE',  ( 0.3119999999999999996, 4.637583333333332725, -0.1292346314604056745 ) ) ;
#7876=CARTESIAN_POINT ( 'NONE',  ( 0.1167790944451423119, 0.5597222221463556968, -0.2819296736111110979 ) ) ;
#7879=CARTESIAN_POINT ( 'NONE',  ( 0.2819296736111110979, 4.672305555631421470, -3.452642723725051716E-17 ) ) ;
#7881=CARTESIAN_POINT ( 'NONE',  ( 0.2819296736111110979, 4.658416666742532186, -3.452642723725051716E-17 ) ) ;
#7884=FACE_OUTER_BOUND ( 'NONE', #8547, .T. ) ;
#7886=CARTESIAN_POINT ( 'NONE',  ( -0.3119999999999998885, 4.443138888888888083, 0.1292346314604058410 ) ) ;
#7889=CARTESIAN_POINT ( 'NONE',  ( -0.2206173157302028232, 3.988277777777776922, -0.2206173157302028232 ) ) ;
#7893=CARTESIAN_POINT ( 'NONE',  ( 0.2828379296212147898, 4.700474317598876794, -0.1317075689354028911 ) ) ;
#7895=CARTESIAN_POINT ( 'NONE',  ( 0.001541891433799943327, 4.654900223093500600, -0.3119964281628413993 ) ) ;
#7897=CARTESIAN_POINT ( 'NONE',  ( 0.1918605058169607913, 4.315775238200347808, -0.2494071876536460841 ) ) ;
#7898=ORIENTED_EDGE ( 'NONE', *, *, #17465, .F. ) ;
#7900=CARTESIAN_POINT ( 'NONE',  ( -5.178964085587577574E-17, 0.5215277777019111660, 0.2819296736111110979 ) ) ;
#7901=DIRECTION ( 'NONE',  ( -0.000000000000000000, -1.000000000000000000, -0.000000000000000000 ) ) ;
#7903=CARTESIAN_POINT ( 'NONE',  ( -5.731347020009612645E-17, 0.1708333333333330040, 0.3119999999999999996 ) ) ;
#7906=CARTESIAN_POINT ( 'NONE',  ( -0.3106743519353148963, 4.612164334677839150, -0.03847270028753647930 ) ) ;
#7909=CARTESIAN_POINT ( 'NONE',  ( -0.3119999999999999996, 0.3236111111111107941, -3.820898013339742174E-17 ) ) ;
#7910=CARTESIAN_POINT ( 'NONE',  ( 0.3119999999999999996, 5.189666666666666650, -3.820898013339742174E-17 ) ) ;
#7912=CARTESIAN_POINT ( 'NONE',  ( -0.2819296736111110424, 4.307722222298088433, -0.1167790944451423119 ) ) ;
#7918=FACE_OUTER_BOUND ( 'NONE', #4535, .T. ) ;
#7919=CARTESIAN_POINT ( 'NONE',  ( -0.1167790944451423535, 4.752166666742533074, 0.2819296736111110424 ) ) ;
#7920=CARTESIAN_POINT ( 'NONE',  ( -0.1334452016168097832, 5.163863756405055128, 0.2677057760511410422 ) ) ;
#7924=CARTESIAN_POINT ( 'NONE',  ( 0.1167790944451424506, 4.328555555631421470, 0.2819296736111110424 ) ) ;
#7927=CARTESIAN_POINT ( 'NONE',  ( 0.2206173157302028787, 4.293833333333332725, 0.2206173157302027954 ) ) ;
#7931=CARTESIAN_POINT ( 'NONE',  ( 0.2819296736111110424, 0.4972222221463556413, -0.1167790944451423119 ) ) ;
#7932=CARTESIAN_POINT ( 'NONE',  ( 5.731347020009612645E-17, 4.120222222222221120, 0.3119999999999999996 ) ) ;
#7933=CARTESIAN_POINT ( 'NONE',  ( 3.820898013339742174E-17, 5.384999999999999787, 0.3119999999999999996 ) ) ;
#7938=CARTESIAN_POINT ( 'NONE',  ( 0.2819296736111110979, 0.5354166665908000056, 0.000000000000000000 ) ) ;
#7939=CARTESIAN_POINT ( 'NONE',  ( 0.1167790944451423535, 0.2472222221463555303, 0.2819296736111110424 ) ) ;
#7940=CARTESIAN_POINT ( 'NONE',  ( 0.1993543840281266633, 4.345916666742532186, -0.1993543840281266910 ) ) ;
#7942=CARTESIAN_POINT ( 'NONE',  ( 0.1993543840281266633, 4.957027777853642903, -0.1993543840281266910 ) ) ;
#7943=CARTESIAN_POINT ( 'NONE',  ( 0.1993543840281267465, 4.151472222298087544, 0.1993543840281266633 ) ) ;
#7948=CARTESIAN_POINT ( 'NONE',  ( -0.1292346314604056745, 3.825083333485065129, -0.3119999999999999996 ) ) ;
#7952=SHAPE_REPRESENTATION ( 'Aloris-BXA-Center-Rod', ( #9127 ), #15765 ) ;
#7954=EDGE_LOOP ( 'NONE', ( #13374, #8460, #18853, #11689 ) ) ;
#7959=CARTESIAN_POINT ( 'NONE',  ( -0.1552057294347528038, 5.011424740845276560, 0.2737342765630598751 ) ) ;
#7961=CARTESIAN_POINT ( 'NONE',  ( -0.2819296736111110424, 0.01805555547968892491, -0.1167790944451423396 ) ) ;
#7965=CARTESIAN_POINT ( 'NONE',  ( 0.1154082656451064642, 4.762710407878993912, -0.2907850784680934830 ) ) ;
#7968=CARTESIAN_POINT ( 'NONE',  ( 0.2214705455607580142, 5.184159519586463816, -0.1905467935019724002 ) ) ;
#7970=ORIENTED_EDGE ( 'NONE', *, *, #21096, .F. ) ;
#7973=CARTESIAN_POINT ( 'NONE',  ( -0.1292346314604081170, 4.040361111111110404, -0.3119999999999975016 ) ) ;
#7974=CARTESIAN_POINT ( 'NONE',  ( -0.1993543840281266355, 4.026472222298087544, 0.1993543840281267465 ) ) ;
#7977=CARTESIAN_POINT ( 'NONE',  ( -0.1298740736329927759, 5.192253054662280043, 0.2575819732643157001 ) ) ;
#7978=CARTESIAN_POINT ( 'NONE',  ( -0.1292346314604056745, 4.713972222373954857, -0.3119999999999999996 ) ) ;
#7979=CARTESIAN_POINT ( 'NONE',  ( 0.1167790944451424506, 4.995222222298087544, 0.2819296736111110424 ) ) ;
#7980=CARTESIAN_POINT ( 'NONE',  ( 0.1993543840281267465, 4.262583333409199149, 0.1993543840281266633 ) ) ;
#7991=CARTESIAN_POINT ( 'NONE',  ( 1.910449006669871087E-17, 0.1361111109593781676, -0.3119999999999999996 ) ) ;
#7992=CARTESIAN_POINT ( 'NONE',  ( 0.1423755856867760516, 4.428580575607206526, -0.2791577753537264894 ) ) ;
#7993=CARTESIAN_POINT ( 'NONE',  ( -1.910449006669871087E-17, 4.425777777777777366, -0.3119999999999999996 ) ) ;
#7995=CARTESIAN_POINT ( 'NONE',  ( 0.03284172987836220248, 0.06131004178175258196, 0.3095030519831387661 ) ) ;
#7997=CARTESIAN_POINT ( 'NONE',  ( -5.178964085587577574E-17, 0.5354166665908000056, 0.2819296736111110979 ) ) ;
#8000=CARTESIAN_POINT ( 'NONE',  ( 0.1167790944451422702, 4.738277777853642903, -0.2819296736111110424 ) ) ;
#8002=CARTESIAN_POINT ( 'NONE',  ( -0.2819296736111110979, 4.741750000075865223, 0.000000000000000000 ) ) ;
#8003=CARTESIAN_POINT ( 'NONE',  ( -0.05067229266822954187, 4.156391035130668321, -0.3080256783650057728 ) ) ;
#8004=CARTESIAN_POINT ( 'NONE',  ( 0.2912189908955998274, 4.866517260218439667, -0.1119643521765174149 ) ) ;
#8006=CARTESIAN_POINT ( 'NONE',  ( 1.791833110003796271E-17, 0.04312855400452411669, -0.2926285540045244216 ) ) ;
#8007=CARTESIAN_POINT ( 'NONE',  ( -0.1292346314604057023, 4.227861111111110404, 0.3119999999999998885 ) ) ;
#8008=CARTESIAN_POINT ( 'NONE',  ( -0.2819296736111110979, 3.852861111186976828, 0.000000000000000000 ) ) ;
#8011=CARTESIAN_POINT ( 'NONE',  ( 0.3133650935564305517, 4.586437319524496736, -0.03335398037977004015 ) ) ;
#8015=CARTESIAN_POINT ( 'NONE',  ( 0.2260310869702762682, 4.147801854619606488, -0.2186894788897151554 ) ) ;
#8022=CARTESIAN_POINT ( 'NONE',  ( 0.1167790944451423535, 0.4138888888130222155, 0.2819296736111110424 ) ) ;
#8028=CARTESIAN_POINT ( 'NONE',  ( -0.2339481197358992404, 5.111336026920037412, 0.2038494990519414962 ) ) ;
#8031=CARTESIAN_POINT ( 'NONE',  ( 0.3119999999999998885, 0.1812499999999996614, 0.1292346314604058410 ) ) ;
#8032=CARTESIAN_POINT ( 'NONE',  ( 0.3119999999999999996, 4.911888888888888083, -3.820898013339742174E-17 ) ) ;
#8034=CARTESIAN_POINT ( 'NONE',  ( 0.1167790944451424368, 4.217444444520310753, 0.2819296736111110424 ) ) ;
#8035=LINE ( 'NONE', #11836, #12791 ) ;
#8040=DIRECTION ( 'NONE',  ( -0.000000000000000000, -1.000000000000000000, -0.000000000000000000 ) ) ;
#8041=CARTESIAN_POINT ( 'NONE',  ( -0.1993543840281266355, 4.804250000075865223, 0.1993543840281267465 ) ) ;
#8046=CARTESIAN_POINT ( 'NONE',  ( 0.1292346314604056745, 0.6326388887371557912, -0.3119999999999999996 ) ) ;
#8047=AXIS2_PLACEMENT_3D ( 'NONE', #21108, #13448, #9655 ) ;
#8048=CARTESIAN_POINT ( 'NONE',  ( 0.1167790944451424506, 4.384111111186976828, 0.2819296736111110424 ) ) ;
#8050=( BOUNDED_CURVE ( )  B_SPLINE_CURVE ( 1, ( #9499, #12641 ),
 .UNSPECIFIED., .F., .F. ) 
 B_SPLINE_CURVE_WITH_KNOTS ( ( 2, 2 ),
 ( 0.000000000000000000, 1.000000000000000000 ),
 .UNSPECIFIED. ) 
 CURVE ( )  GEOMETRIC_REPRESENTATION_ITEM ( )  RATIONAL_B_SPLINE_CURVE ( ( 0.9836825870399050764, 0.9836825870399050764 ) ) 
 REPRESENTATION_ITEM ( '' )  );
#8052=( BOUNDED_CURVE ( )  B_SPLINE_CURVE ( 2, ( #9462, #9342, #3733, #5679, #16895, #16784, #65, #3853, #9583 ),
 .UNSPECIFIED., .F., .T. ) 
 B_SPLINE_CURVE_WITH_KNOTS ( ( 3, 2, 2, 2, 3 ),
 ( 0.6458333333333333703, 0.6562500000000000000, 0.6666666666666666297, 0.6770833333333333703, 0.6875000000000000000 ),
 .UNSPECIFIED. ) 
 CURVE ( )  GEOMETRIC_REPRESENTATION_ITEM ( )  RATIONAL_B_SPLINE_CURVE ( ( 1.000000000000000000, 0.9238795325112867385, 1.000000000000000000, 0.9238795325112867385, 1.000000000000000000, 0.9238795325112867385, 1.000000000000000000, 0.9238795325112867385, 1.000000000000000000 ) ) 
 REPRESENTATION_ITEM ( '' )  );
#8055=CARTESIAN_POINT ( 'NONE',  ( -0.1167790944451422702, 0.4555555554796890116, -0.2819296736111110424 ) ) ;
#8062=CARTESIAN_POINT ( 'NONE',  ( -5.178964085587577574E-17, 0.4659722221463555858, 0.2819296736111110979 ) ) ;
#8063=CARTESIAN_POINT ( 'NONE',  ( 0.1993543840281266910, 0.2090277777019111383, -0.1993543840281266910 ) ) ;
#8064=CARTESIAN_POINT ( 'NONE',  ( -0.2819296736111110424, 4.203555555631421470, 0.1167790944451424923 ) ) ;
#8066=CARTESIAN_POINT ( 'NONE',  ( 0.2819296736111110424, 4.842444444520309865, -0.1167790944451423396 ) ) ;
#8069=CARTESIAN_POINT ( 'NONE',  ( 0.1292346314604058410, 3.963972222373954413, 0.3119999999999998885 ) ) ;
#8077=CARTESIAN_POINT ( 'NONE',  ( 0.2819296736111110424, 0.05277777770191114520, -0.1167790944451423119 ) ) ;
#8080=CARTESIAN_POINT ( 'NONE',  ( 0.006132810802118407977, 4.265890496703536705, -0.3119484895688790504 ) ) ;
#8082=CARTESIAN_POINT ( 'NONE',  ( 0.0007409178576027871874, 4.766034521252337619, -0.3119991761991793844 ) ) ;
#8084=CARTESIAN_POINT ( 'NONE',  ( 4.312521114635084752E-13, 5.190332509204934830, -0.2890970118899086061 ) ) ;
#8087=CARTESIAN_POINT ( 'NONE',  ( -0.2648504260907811325, 4.673840770439461778, 0.1658194286430906550 ) ) ;
#8088=CARTESIAN_POINT ( 'NONE',  ( 0.2819296736111110979, 4.047305555631421470, -3.452642723725051716E-17 ) ) ;
#8090=CARTESIAN_POINT ( 'NONE',  ( -0.1463856370309246369, 5.168083914757449548, -0.2593197864242284822 ) ) ;
#8092=EDGE_CURVE ( 'NONE', #19908, #16571, #17089, .T. ) ;
#8093=CARTESIAN_POINT ( 'NONE',  ( 0.3119999999999999996, 4.418833333485065573, -3.820898013339742174E-17 ) ) ;
#8094=CARTESIAN_POINT ( 'NONE',  ( 0.2819296736111111534, 5.002166666742533074, 0.1167790944451422563 ) ) ;
#8096=CARTESIAN_POINT ( 'NONE',  ( -1.726321361862525858E-17, 4.116750000075865223, -0.2819296736111110979 ) ) ;
#8097=VERTEX_POINT ( 'NONE', #16866 ) ;
#8104=CARTESIAN_POINT ( 'NONE',  ( 1.910449006669871087E-17, 0.08055555540382261515, -0.3119999999999999996 ) ) ;
#8105=CARTESIAN_POINT ( 'NONE',  ( 0.2323269574505744950, 4.412370849970273845, 0.2096127310370168306 ) ) ;
#8110=CARTESIAN_POINT ( 'NONE',  ( 1.726321361862525858E-17, 0.4520833332574667462, -0.2819296736111110979 ) ) ;
#8113=CARTESIAN_POINT ( 'NONE',  ( 0.1167790944451424368, 4.717444444520309865, 0.2819296736111110424 ) ) ;
#8115=CARTESIAN_POINT ( 'NONE',  ( -0.1167790944451423535, 4.752166666742533074, 0.2819296736111110424 ) ) ;
#8116=CARTESIAN_POINT ( 'NONE',  ( -0.04059609524757908788, 4.156104316328405268, -0.3095148733534341390 ) ) ;
#8117=EDGE_CURVE ( 'NONE', #1934, #2014, #22913, .T. ) ;
#8119=CARTESIAN_POINT ( 'NONE',  ( 0.2967211878843482586, 4.860212748769966673, 0.1045282615683273547 ) ) ;
#8120=DIRECTION ( 'NONE',  ( -0.000000000000000000, -1.000000000000000000, -0.000000000000000000 ) ) ;
#8123=CARTESIAN_POINT ( 'NONE',  ( 0.3119999999999999996, 4.352861111111110404, 0.1292346314604056190 ) ) ;
#8126=CARTESIAN_POINT ( 'NONE',  ( -0.1292346314604058410, 0.5493055554038226429, 0.3119999999999998885 ) ) ;
#8127=EDGE_LOOP ( 'NONE', ( #14298, #12029, #2106, #18952 ) ) ;
#8128=CARTESIAN_POINT ( 'NONE',  ( 0.2672908904913715578, 4.580718530736621830, 0.1620962247036812631 ) ) ;
#8133=CARTESIAN_POINT ( 'NONE',  ( 0.3105407428941047709, 4.142119987277710358, -0.03873399703425771390 ) ) ;
#8136=CARTESIAN_POINT ( 'NONE',  ( -0.02550062582863994037, 3.933446043089724231, -0.3109980386088752047 ) ) ;
#8139=CARTESIAN_POINT ( 'NONE',  ( 1.726321361862525858E-17, 0.4381944443685778512, -0.2819296736111110979 ) ) ;
#8140=SPHERICAL_SURFACE ( 'NONE', #12904, 0.3119999999999999996 ) ;
#8148=CARTESIAN_POINT ( 'NONE',  ( -5.731347020009612645E-17, 0.3374999999999996336, 0.3119999999999999996 ) ) ;
#8149=CARTESIAN_POINT ( 'NONE',  ( -0.3119999999999999996, 4.884111111111110404, 0.000000000000000000 ) ) ;
#8150=AXIS2_PLACEMENT_3D ( 'NONE', #5214, #22289, #12935 ) ;
#8151=CARTESIAN_POINT ( 'NONE',  ( -0.2819296736111110979, 3.977861111186976828, 0.000000000000000000 ) ) ;
#8153=CARTESIAN_POINT ( 'NONE',  ( -0.2206173157302027676, 3.891055555555554601, 0.2206173157302028787 ) ) ;
#8156=CARTESIAN_POINT ( 'NONE',  ( -0.3119999973396838655, 4.001073216847850667, -0.04084072313200213383 ) ) ;
#8158=CARTESIAN_POINT ( 'NONE',  ( 0.1167790944451422702, 4.779944444520309865, -0.2819296736111110424 ) ) ;
#8162=CARTESIAN_POINT ( 'NONE',  ( 3.820898013339742174E-17, 5.384999999999999787, 0.3119999999999999996 ) ) ;
#8166=CARTESIAN_POINT ( 'NONE',  ( -0.1993543840281266910, 4.248694444520310753, -0.1993543840281266910 ) ) ;
#8167=CARTESIAN_POINT ( 'NONE',  ( -0.06581070416570369841, 4.045665677644000091, -0.3054227462770962020 ) ) ;
#8169=FACE_OUTER_BOUND ( 'NONE', #8727, .T. ) ;
#8170=CARTESIAN_POINT ( 'NONE',  ( -5.178964085587577574E-17, 0.4243055554796889006, 0.2819296736111110979 ) ) ;
#8176=CARTESIAN_POINT ( 'NONE',  ( -0.1917236326748512631, 3.771781958134273083, -0.2495076210021671681 ) ) ;
#8177=CARTESIAN_POINT ( 'NONE',  ( -0.1993543840281266633, 0.5006944443685777957, -0.1993543840281266910 ) ) ;
#8178=CARTESIAN_POINT ( 'NONE',  ( 0.2819296736111110424, 0.2055555554796889006, -0.1167790944451423119 ) ) ;
#8179=CARTESIAN_POINT ( 'NONE',  ( 0.1993543840281266633, 3.957027777853643791, -0.1993543840281266910 ) ) ;
#8181=CARTESIAN_POINT ( 'NONE',  ( -0.2819296736111110424, 4.696611111186977716, -0.1167790944451423119 ) ) ;
#8183=CARTESIAN_POINT ( 'NONE',  ( 0.3029461644517479901, 5.080632737976908508, -0.07557799413177579417 ) ) ;
#8188=CARTESIAN_POINT ( 'NONE',  ( 0.3119999999999999996, 3.811194444596177622, -0.1292346314604056745 ) ) ;
#8190=( BOUNDED_CURVE ( )  B_SPLINE_CURVE ( 2, ( #12376, #10778, #18204, #14551, #18322, #11016, #8229, #1500, #1620 ),
 .UNSPECIFIED., .F., .T. ) 
 B_SPLINE_CURVE_WITH_KNOTS ( ( 3, 2, 2, 2, 3 ),
 ( 0.9553571428571425717, 0.9598214285714283811, 0.9642857142857141906, 0.9687500000000000000, 0.9732142857142858094 ),
 .UNSPECIFIED. ) 
 CURVE ( )  GEOMETRIC_REPRESENTATION_ITEM ( )  RATIONAL_B_SPLINE_CURVE ( ( 1.000000000000005773, 0.9238795325112810763, 1.000000000000000000, 0.9238795325112867385, 1.000000000000000000, 0.9238795325112867385, 1.000000000000000000, 0.9238795325112848511, 1.000000000000001998 ) ) 
 REPRESENTATION_ITEM ( '' )  );
#8195=ORIENTED_EDGE ( 'NONE', *, *, #23305, .T. ) ;
#8199=ORIENTED_EDGE ( 'NONE', *, *, #17960, .T. ) ;
#8200=CARTESIAN_POINT ( 'NONE',  ( 0.2819296736111110979, 0.1048611110352444808, 0.000000000000000000 ) ) ;
#8202=CARTESIAN_POINT ( 'NONE',  ( 0.003049558294924298047, 4.265973550867800057, -0.3119872481712610002 ) ) ;
#8204=CARTESIAN_POINT ( 'NONE',  ( 0.2576415818302536520, 4.080194459578224020, 0.1799301507806963518 ) ) ;
#8206=CARTESIAN_POINT ( 'NONE',  ( 0.1933203555740233281, 5.172664093799754781, 0.2239000762248374854 ) ) ;
#8207=CARTESIAN_POINT ( 'NONE',  ( -1.910449006669871087E-17, 4.092444444444444329, -0.3119999999999999996 ) ) ;
#8210=CARTESIAN_POINT ( 'NONE',  ( -0.2819296736111110424, 4.078555555631421470, 0.1167790944451424923 ) ) ;
#8211=CARTESIAN_POINT ( 'NONE',  ( -0.1292346314604058410, 0.1048611109593781676, 0.3119999999999998885 ) ) ;
#8212=CARTESIAN_POINT ( 'NONE',  ( -0.2332192335059636024, 5.186968840224980504, 0.1733688601932164841 ) ) ;
#8213=CARTESIAN_POINT ( 'NONE',  ( 3.820898013339742174E-17, 5.384999999999999787, 0.3119999999999999996 ) ) ;
#8214=CARTESIAN_POINT ( 'NONE',  ( 5.731347020009612645E-17, 4.516055555707287894, 0.3119999999999999996 ) ) ;
#8215=CARTESIAN_POINT ( 'NONE',  ( 0.2819296736111110979, 5.009111111186976828, -0.1167790944451423396 ) ) ;
#8217=CARTESIAN_POINT ( 'NONE',  ( -0.2819296736111110424, 4.078555555631421470, 0.1167790944451424923 ) ) ;
#8219=ORIENTED_EDGE ( 'NONE', *, *, #22918, .T. ) ;
#8220=VERTEX_POINT ( 'NONE', #9549 ) ;
#8226=CARTESIAN_POINT ( 'NONE',  ( -1.960390272410463459E-06, 4.210500054279665783, -0.3119999999938410928 ) ) ;
#8227=CARTESIAN_POINT ( 'NONE',  ( 0.3119999999999999996, 0.1812499998482670904, -0.1292346314604056468 ) ) ;
#8229=CARTESIAN_POINT ( 'NONE',  ( -0.2206173157302028232, 3.766055555555554601, -0.2206173157302028232 ) ) ;
#8230=ORIENTED_EDGE ( 'NONE', *, *, #6335, .T. ) ;
#8231=LINE ( 'NONE', #21651, #23185 ) ;
#8235=ADVANCED_FACE ( 'NONE', ( #15401 ), #13705, .T. ) ;
#8236=CARTESIAN_POINT ( 'NONE',  ( 0.1167790944451424368, 4.703555555631420582, 0.2819296736111110424 ) ) ;
#8241=CARTESIAN_POINT ( 'NONE',  ( -0.1292346314604056745, 4.318138888888888083, -0.3119999999999999996 ) ) ;
#8243=FACE_OUTER_BOUND ( 'NONE', #9596, .T. ) ;
#8244=CARTESIAN_POINT ( 'NONE',  ( 0.08226311336655546536, 4.962829471254590175, 0.3009951623300980428 ) ) ;
#8248=B_SPLINE_CURVE_WITH_KNOTS ( 'NONE', 1,
 ( #12129, #8560 ),
 .UNSPECIFIED., .F., .F.,
 ( 2, 2 ),
 ( 0.000000000000000000, 1.000000000000000000 ),
 .UNSPECIFIED. ) ;
#8251=CARTESIAN_POINT ( 'NONE',  ( 0.2833369697430000445, 4.700439859952622257, -0.1306314325063157311 ) ) ;
#8252=CARTESIAN_POINT ( 'NONE',  ( 0.1907739469436010582, 4.133017026477499911, 0.2468791227802183130 ) ) ;
#8254=EDGE_CURVE ( 'NONE', #16767, #12181, #2443, .T. ) ;
#8259=CARTESIAN_POINT ( 'NONE',  ( -0.2819296736111110979, 0.07361111103524446697, -0.1167790944451423396 ) ) ;
#8260=CARTESIAN_POINT ( 'NONE',  ( -0.09561951185436078082, 5.206640035683668621, 0.2653980274966651343 ) ) ;
#8262=CARTESIAN_POINT ( 'NONE',  ( 0.1292346314604057300, 0.5076388888888885287, 0.3119999999999998885 ) ) ;
#8265=VERTEX_POINT ( 'NONE', #20761 ) ;
#8267=CARTESIAN_POINT ( 'NONE',  ( 0.000000000000000000, 5.384999999999999787, -0.3119999999999999996 ) ) ;
#8268=CARTESIAN_POINT ( 'NONE',  ( 0.3119999999999999996, 4.748694444444444329, -0.1292346314604056745 ) ) ;
#8269=CARTESIAN_POINT ( 'NONE',  ( 0.2206173157302027676, 0.5666666666666663188, 0.2206173157302028787 ) ) ;
#8270=CARTESIAN_POINT ( 'NONE',  ( -0.2206173157302027676, 5.057722222222222008, 0.2206173157302028787 ) ) ;
#8271=CARTESIAN_POINT ( 'NONE',  ( 0.1993543840281266633, 4.068138888964754507, -0.1993543840281266910 ) ) ;
#8277=CARTESIAN_POINT ( 'NONE',  ( -0.1917386021594863765, 4.010339725230847030, 0.2494960349349919226 ) ) ;
#8278=CARTESIAN_POINT ( 'NONE',  ( -0.2819296736111110424, 4.682722222298087544, -0.1167790944451423119 ) ) ;
#8285=CARTESIAN_POINT ( 'NONE',  ( 0.1993543840281267465, 4.332027777853642903, 0.1993543840281266633 ) ) ;
#8291=CARTESIAN_POINT ( 'NONE',  ( -0.1167790944451422702, -0.002777777853644409437, -0.2819296736111110424 ) ) ;
#8293=CARTESIAN_POINT ( 'NONE',  ( 0.000000000000000000, 5.384999999999999787, -0.3119999999999999996 ) ) ;
#8300=CARTESIAN_POINT ( 'NONE',  ( -0.1167790944451422702, 0.3861111110352444808, -0.2819296736111110979 ) ) ;
#8301=CARTESIAN_POINT ( 'NONE',  ( 0.2819296736111110424, 0.5388888888130223265, -0.1167790944451423119 ) ) ;
#8302=CARTESIAN_POINT ( 'NONE',  ( 0.2819296736111110424, 4.009111111186976828, -0.1167790944451423396 ) ) ;
#8304=CARTESIAN_POINT ( 'NONE',  ( 5.178964085587577574E-17, 4.658416666742532186, 0.2819296736111110979 ) ) ;
#8306=CARTESIAN_POINT ( 'NONE',  ( 0.3029724772689905699, 5.076302895770250068, 0.07975337583219681281 ) ) ;
#8309=CARTESIAN_POINT ( 'NONE',  ( 0.2206173157302028787, 4.793833333333332725, 0.2206173157302027954 ) ) ;
#8310=CARTESIAN_POINT ( 'NONE',  ( 0.1292346314604056190, 3.873694444596177622, -0.3119999999999999996 ) ) ;
#8317=CARTESIAN_POINT ( 'NONE',  ( -0.05024295495402558709, 4.570215981136505512, 0.3079318380950444300 ) ) ;
#8319=CARTESIAN_POINT ( 'NONE',  ( 0.1292346314604057023, 0.6118055554038226429, 0.3119999999999998885 ) ) ;
#8320=CARTESIAN_POINT ( 'NONE',  ( 0.2828977024960969144, 4.256026029941413213, -0.1315892272411629260 ) ) ;
#8322=CARTESIAN_POINT ( 'NONE',  ( -5.731347020009612645E-17, 0.3374999999999996336, 0.3119999999999999996 ) ) ;
#8325=CARTESIAN_POINT ( 'NONE',  ( 0.04792230210257000106, 5.168523637897857625, 0.2932814512039932375 ) ) ;
#8326=ADVANCED_FACE ( 'NONE', ( #10516 ), #14052, .T. ) ;
#8328=CARTESIAN_POINT ( 'NONE',  ( -0.2902337294436940773, 4.665514674916999560, -0.1145022281107502676 ) ) ;
#8330=CARTESIAN_POINT ( 'NONE',  ( 0.1993543840281267465, 3.818138888964754507, 0.1993543840281266633 ) ) ;
#8331=CARTESIAN_POINT ( 'NONE',  ( 0.05352015321003111142, 5.017547458390650306, 0.3073860041716943714 ) ) ;
#8334=CARTESIAN_POINT ( 'NONE',  ( -0.2206173157302028232, 4.439666666818398610, -0.2206173157302028232 ) ) ;
#8335=CARTESIAN_POINT ( 'NONE',  ( 0.1993543840281267465, 4.832027777853643791, 0.1993543840281266633 ) ) ;
#8336=CARTESIAN_POINT ( 'NONE',  ( -0.2819296736111110979, 4.075083333409199149, 0.000000000000000000 ) ) ;
#8337=ORIENTED_EDGE ( 'NONE', *, *, #10342, .F. ) ;
#8346=CARTESIAN_POINT ( 'NONE',  ( 1.910449006669871087E-17, 0.1916666665149337478, -0.3119999999999999996 ) ) ;
#8348=AXIS2_PLACEMENT_3D ( 'NONE', #18311, #22203, #14787 ) ;
#8349=CARTESIAN_POINT ( 'NONE',  ( -1.910449006669871087E-17, 4.147999999999998799, -0.3119999999999999996 ) ) ;
#8350=DIRECTION ( 'NONE',  ( 0.000000000000000000, 0.000000000000000000, -1.000000000000000000 ) ) ;
#8353=CARTESIAN_POINT ( 'NONE',  ( -5.731347020009612645E-17, 0.5527777776260448528, 0.3119999999999999996 ) ) ;
#8354=CARTESIAN_POINT ( 'NONE',  ( 0.1167790944451422702, 4.502166666742532186, -0.2819296736111110424 ) ) ;
#8355=DIRECTION ( 'NONE',  ( 0.000000000000000000, 0.000000000000000000, -1.000000000000000000 ) ) ;
#8358=CARTESIAN_POINT ( 'NONE',  ( 6.614309848781084774E-13, 0.03242967361111062652, 0.2819296736111109869 ) ) ;
#8359=CARTESIAN_POINT ( 'NONE',  ( -1.910449006669871087E-17, 4.259111111111110404, -0.3119999999999999996 ) ) ;
#8361=CARTESIAN_POINT ( 'NONE',  ( 0.3108823422949931192, 4.973667548811621764, 0.02638502853553916644 ) ) ;
#8364=CARTESIAN_POINT ( 'NONE',  ( 0.3040647624429579921, 4.698881436987698557, -0.08103250758201478721 ) ) ;
#8372=CARTESIAN_POINT ( 'NONE',  ( -0.2819296736111111534, 0.08055555547968892838, 0.1167790944451422563 ) ) ;
#8378=CARTESIAN_POINT ( 'NONE',  ( -0.2150490341232084990, 4.620419474169768392, 0.2274236258241670028 ) ) ;
#8382=CARTESIAN_POINT ( 'NONE',  ( -0.3119999999999999996, 0.3826388888888884732, 0.1292346314604056190 ) ) ;
#8383=CARTESIAN_POINT ( 'NONE',  ( -0.2206173157302027676, 5.002166666666665762, 0.2206173157302028787 ) ) ;
#8384=CARTESIAN_POINT ( 'NONE',  ( 0.1167790944451422702, 4.279944444520309865, -0.2819296736111110979 ) ) ;
#8385=CARTESIAN_POINT ( 'NONE',  ( 0.2819296736111110979, 4.005638888964754507, -3.452642723725051716E-17 ) ) ;
#8387=CARTESIAN_POINT ( 'NONE',  ( 1.910449006669871087E-17, 0.4208333333333330040, -0.3119999999999999996 ) ) ;
#8388=CARTESIAN_POINT ( 'NONE',  ( 0.3112018351208193923, 4.807111871885667576, 0.02239305249707624484 ) ) ;
#8393=CARTESIAN_POINT ( 'NONE',  ( 0.2819296736111110979, 4.821611111186976828, 0.1167790944451422425 ) ) ;
#8394=VECTOR ( 'NONE', #2582, 39.37007874015748143 ) ;
#8395=CARTESIAN_POINT ( 'NONE',  ( -5.488040394358968970E-07, 4.960478275469978549, 0.3119999999989728212 ) ) ;
#8396=CARTESIAN_POINT ( 'NONE',  ( -0.2393751185404155990, 5.160436163643965735, 0.1810856521565251398 ) ) ;
#8402=CARTESIAN_POINT ( 'NONE',  ( 0.2819296736111111534, 4.168833333409199149, 0.1167790944451422563 ) ) ;
#8409=CARTESIAN_POINT ( 'NONE',  ( -0.2819296736111110979, 0.1222222221463555719, 0.1167790944451422425 ) ) ;
#8416=CARTESIAN_POINT ( 'NONE',  ( -0.1571327148983266975, 3.789293766973461430, 0.2726194340734207078 ) ) ;
#8417=CARTESIAN_POINT ( 'NONE',  ( -0.04084075481946490560, 3.822708396179054446, -0.3120000000000004436 ) ) ;
#8418=CARTESIAN_POINT ( 'NONE',  ( -0.1167790944451422702, 0.5527777777019111660, -0.2819296736111110424 ) ) ;
#8419=CARTESIAN_POINT ( 'NONE',  ( -0.1993543840281266355, 4.040361111186976828, 0.1993543840281267465 ) ) ;
#8422=CARTESIAN_POINT ( 'NONE',  ( -0.1993543840281266355, 4.651472222298087544, 0.1993543840281267465 ) ) ;
#8424=CARTESIAN_POINT ( 'NONE',  ( 0.3134329418737113460, 4.363010638796406937, 0.009240974733256862236 ) ) ;
#8426=ORIENTED_EDGE ( 'NONE', *, *, #19915, .F. ) ;
#8429=CARTESIAN_POINT ( 'NONE',  ( 5.731347020009612645E-17, 3.849388889040620931, 0.3119999999999999996 ) ) ;
#8431=VECTOR ( 'NONE', #5954, 39.37007874015748143 ) ;
#8432=EDGE_CURVE ( 'NONE', #13675, #12402, #1367, .T. ) ;
#8435=CARTESIAN_POINT ( 'NONE',  ( 0.1993543840281266633, 4.887583333409199149, -0.1993543840281266910 ) ) ;
#8438=CARTESIAN_POINT ( 'NONE',  ( -0.2777204190475047185, 5.110469173811334365, -0.1386666054842166096 ) ) ;
#8441=CARTESIAN_POINT ( 'NONE',  ( 0.2819296736111110424, 0.04583333325746670461, 0.1167790944451424923 ) ) ;
#8443=CARTESIAN_POINT ( 'NONE',  ( 1.726321361862525858E-17, 0.007638888813022257952, -0.2819296736111110979 ) ) ;
#8444=DIRECTION ( 'NONE',  ( -0.000000000000000000, -1.000000000000000000, -0.000000000000000000 ) ) ;
#8445=CARTESIAN_POINT ( 'NONE',  ( 0.02497667677238979075, 4.072372283987069075, 0.3120000032441070936 ) ) ;
#8447=CARTESIAN_POINT ( 'NONE',  ( -1.910449006669871087E-17, 4.481333333333331836, -0.3119999999999999996 ) ) ;
#8448=EDGE_CURVE ( 'NONE', #10939, #3183, #18814, .T. ) ;
#8452=CARTESIAN_POINT ( 'NONE',  ( 0.2819296736111110979, 3.825083333409198705, -3.452642723725051716E-17 ) ) ;
#8455=CARTESIAN_POINT ( 'NONE',  ( -0.05195898594955755678, 4.792388845571896816, 0.3076436305813794458 ) ) ;
#8456=CARTESIAN_POINT ( 'NONE',  ( 0.1292346314604058410, 4.575083333485065573, 0.3119999999999998885 ) ) ;
#8457=CARTESIAN_POINT ( 'NONE',  ( -0.2819296736111110979, 4.811194444520309865, 0.000000000000000000 ) ) ;
#8459=CARTESIAN_POINT ( 'NONE',  ( -0.1993543840281266910, 4.068138888964754507, -0.1993543840281266910 ) ) ;
#8460=ORIENTED_EDGE ( 'NONE', *, *, #8536, .T. ) ;
#8461=EDGE_CURVE ( 'NONE', #4893, #6926, #18964, .T. ) ;
#8467=CARTESIAN_POINT ( 'NONE',  ( 0.1292346314604056745, 0.4729166666666663743, -0.3119999999999999996 ) ) ;
#8469=CARTESIAN_POINT ( 'NONE',  ( -0.1292346314604056190, 0.02847222207048929338, -0.3119999999999999996 ) ) ;
#8470=CARTESIAN_POINT ( 'NONE',  ( -0.0004270822970283075638, 4.377178143069785143, -0.3119997496178308904 ) ) ;
#8476=DIRECTION ( 'NONE',  ( -0.000000000000000000, -1.000000000000000000, -0.000000000000000000 ) ) ;
#8477=CARTESIAN_POINT ( 'NONE',  ( -0.2819296736111110979, 4.352861111186976828, 0.000000000000000000 ) ) ;
#8478=CARTESIAN_POINT ( 'NONE',  ( -5.731347020009612645E-17, 0.1708333333333330040, 0.3119999999999999996 ) ) ;
#8482=CARTESIAN_POINT ( 'NONE',  ( -0.1292346314604057023, 4.338972222222222008, 0.3119999999999998885 ) ) ;
#8483=AXIS2_PLACEMENT_3D ( 'NONE', #22238, #11035, #16522 ) ;
#8484=CARTESIAN_POINT ( 'NONE',  ( 5.731347020009612645E-17, 5.127166666818398610, 0.3119999999999999996 ) ) ;
#8485=CARTESIAN_POINT ( 'NONE',  ( 0.06745385251108179658, 4.962394104578971898, 0.3046372139198416651 ) ) ;
#8490=CARTESIAN_POINT ( 'NONE',  ( 0.3013181215143252434, 4.138612934927133225, 0.08484923786493389630 ) ) ;
#8492=CARTESIAN_POINT ( 'NONE',  ( -1.726321361862525858E-17, 5.227861111186975940, -0.2819296736111110979 ) ) ;
#8493=EDGE_CURVE ( 'NONE', #6611, #14624, #10105, .T. ) ;
#8494=CARTESIAN_POINT ( 'NONE',  ( 0.1571292521837519829, 3.817071648848574306, -0.2726212835620034358 ) ) ;
#8496=EDGE_CURVE ( 'NONE', #18946, #13418, #10905, .T. ) ;
#8497=B_SPLINE_CURVE_WITH_KNOTS ( 'NONE', 3,
 ( #3855, #11299, #191, #7633, #23836, #7157, #9096, #14600, #20203, #5320, #3488, #12784, #1663, #14728, #22143, #12907, #16266, #16391, #21626, #1267, #8584, #20040, #8693, #14560, #16143, #1508, #3328, #5278, #19673, #14316, #7241, #6748, #10902, #12502, #12258, #5034, #19799, #23558, #12383, #16021, #8943, #10786, #2974, #1145, #8817, #3210, #18213, #6997 ),
 .UNSPECIFIED., .F., .F.,
 ( 4, 2, 2, 2, 2, 2, 2, 2, 2, 2, 2, 2, 2, 2, 2, 2, 2, 2, 2, 2, 2, 2, 2, 4 ),
 ( 0.002493122863401542495, 0.004000377874406220446, 0.004754005379908560723, 0.005507632885410900132, 0.007014887896415579818, 0.007768515401917921830, 0.008522142907420263841, 0.009275770412922604985, 0.01002939791842494613, 0.01153665292942963189, 0.01229028043493197303, 0.01304390794043431417, 0.01455116295143899993, 0.01530479045694134108, 0.01605841796244368222, 0.01756567297344836798, 0.01907292798445305027, 0.01982655548995539141, 0.02058018299545773255, 0.02208743800646241831, 0.02359469301746710060, 0.02510194802847178636, 0.02585557553397412750, 0.02660920303947646864 ),
 .UNSPECIFIED. ) ;
#8499=CARTESIAN_POINT ( 'NONE',  ( -0.2819296736111110979, 0.1291666665908000611, -0.1167790944451423396 ) ) ;
#8507=CARTESIAN_POINT ( 'NONE',  ( 0.000000000000000000, 5.384999999999999787, 0.000000000000000000 ) ) ;
#8508=CARTESIAN_POINT ( 'NONE',  ( 0.2206173157302027676, 0.3999999999999996336, 0.2206173157302028787 ) ) ;
#8509=CARTESIAN_POINT ( 'NONE',  ( -0.1292346314604056745, 4.984805555555555934, -0.3119999999999999996 ) ) ;
#8511=CARTESIAN_POINT ( 'NONE',  ( -0.1993543840281266355, 4.248694444520309865, 0.1993543840281267465 ) ) ;
#8512=CARTESIAN_POINT ( 'NONE',  ( 0.1167790944451424368, 3.939666666742532186, 0.2819296736111110424 ) ) ;
#8514=CARTESIAN_POINT ( 'NONE',  ( -0.3119999999999998885, 3.887583333333332725, 0.1292346314604058410 ) ) ;
#8519=CARTESIAN_POINT ( 'NONE',  ( -0.2726213461307027686, 3.997589792078371396, -0.1571291336435313157 ) ) ;
#8520=CARTESIAN_POINT ( 'NONE',  ( -0.1167790944451423257, 4.564666666742531298, -0.2819296736111110424 ) ) ;
#8522=CARTESIAN_POINT ( 'NONE',  ( -0.1068925302184129816, 4.491398126007289271, -0.2939241610522889125 ) ) ;
#8526=CARTESIAN_POINT ( 'NONE',  ( 0.1993543840281267465, 3.998694444520310753, 0.1993543840281266633 ) ) ;
#8528=CARTESIAN_POINT ( 'NONE',  ( -0.04965346344051063676, 4.823057060546735997, -0.3081848164328563899 ) ) ;
#8533=CARTESIAN_POINT ( 'NONE',  ( 0.1993543840281266910, 0.04236111103524448085, -0.1993543840281266910 ) ) ;
#8536=EDGE_CURVE ( 'NONE', #9670, #12181, #18661, .T. ) ;
#8542=CARTESIAN_POINT ( 'NONE',  ( -0.05083916931420053020, 3.767441789872082669, -0.3079993799698920731 ) ) ;
#8544=CARTESIAN_POINT ( 'NONE',  ( 1.726321361862525858E-17, 0.4381944443685778512, -0.2819296736111110979 ) ) ;
#8545=CARTESIAN_POINT ( 'NONE',  ( 0.1993543840281267465, 4.109805555631421470, 0.1993543840281266633 ) ) ;
#8547=EDGE_LOOP ( 'NONE', ( #13676, #22357, #9069, #3904 ) ) ;
#8548=EDGE_CURVE ( 'NONE', #4825, #5409, #6346, .T. ) ;
#8549=CARTESIAN_POINT ( 'NONE',  ( -0.2819296736111110424, 4.648000000075866112, 0.1167790944451424923 ) ) ;
#8552=CARTESIAN_POINT ( 'NONE',  ( 0.1746784157998219900, 5.086973785772764600, -0.2585344347967651335 ) ) ;
#8555=CARTESIAN_POINT ( 'NONE',  ( -1.726321361862525858E-17, 5.116750000075865223, -0.2819296736111110979 ) ) ;
#8557=AXIS2_PLACEMENT_3D ( 'NONE', #11628, #16984, #276 ) ;
#8559=ORIENTED_EDGE ( 'NONE', *, *, #9740, .F. ) ;
#8560=CARTESIAN_POINT ( 'NONE',  ( 1.726321361862525858E-17, 0.6048611110352445364, -0.2819296736111110979 ) ) ;
#8561=CARTESIAN_POINT ( 'NONE',  ( 0.1993543840281266633, 4.832027777853643791, -0.1993543840281266910 ) ) ;
#8563=CARTESIAN_POINT ( 'NONE',  ( 1.910449006669871087E-17, 0.3027777776260448528, -0.3119999999999999996 ) ) ;
#8565=CARTESIAN_POINT ( 'NONE',  ( -0.07317740563318354818, 4.569553305210725114, 0.3034604867065505696 ) ) ;
#8566=VERTEX_POINT ( 'NONE', #22561 ) ;
#8567=CARTESIAN_POINT ( 'NONE',  ( 0.2819296736111110424, 0.3861111110352444808, -0.1167790944451423119 ) ) ;
#8569=ADVANCED_FACE ( 'NONE', ( #7918 ), #11841, .T. ) ;
#8570=FACE_OUTER_BOUND ( 'NONE', #17703, .T. ) ;
#8571=CARTESIAN_POINT ( 'NONE',  ( -0.1292346314604056190, 0.3131944444444441089, -0.3119999999999999996 ) ) ;
#8574=CARTESIAN_POINT ( 'NONE',  ( -0.2817863736917600725, 5.053780319418576639, -0.1342011136461285226 ) ) ;
#8578=CARTESIAN_POINT ( 'NONE',  ( -0.1167790944451423257, 4.800777777853643791, -0.2819296736111110424 ) ) ;
#8583=CARTESIAN_POINT ( 'NONE',  ( 5.178964085587577574E-17, 3.866750000075865668, 0.2819296736111110979 ) ) ;
#8584=CARTESIAN_POINT ( 'NONE',  ( -0.2851672621379254258, 0.05388838813870399508, 0.1040316926689665855 ) ) ;
#8585=CARTESIAN_POINT ( 'NONE',  ( 0.03417214391962999920, 5.016978872011788937, 0.3101611866967836084 ) ) ;
#8588=CARTESIAN_POINT ( 'NONE',  ( -0.3119999999999998885, 4.227861111262844140, 0.1292346314604058410 ) ) ;
#8589=CARTESIAN_POINT ( 'NONE',  ( -0.2819296736111110424, 4.814666666742533074, 0.1167790944451424923 ) ) ;
#8591=CARTESIAN_POINT ( 'NONE',  ( -0.2819296736111110979, 4.019527777853642903, 0.000000000000000000 ) ) ;
#8593=ORIENTED_EDGE ( 'NONE', *, *, #19915, .T. ) ;
#8602=CARTESIAN_POINT ( 'NONE',  ( 0.2206173157302028232, 0.3513888887371559577, -0.2206173157302028232 ) ) ;
#8603=FACE_OUTER_BOUND ( 'NONE', #23174, .T. ) ;
#8607=CARTESIAN_POINT ( 'NONE',  ( 0.2819296736111110979, 0.09444444436857780956, -0.1167790944451422980 ) ) ;
#8609=CARTESIAN_POINT ( 'NONE',  ( 0.1167790944451424368, 4.425777777853643791, 0.2819296736111110424 ) ) ;
#8614=CARTESIAN_POINT ( 'NONE',  ( 0.2206173157302028787, 4.016055555555555046, 0.2206173157302027954 ) ) ;
#8616=CARTESIAN_POINT ( 'NONE',  ( -0.1292346314604057023, 5.123694444596177178, 0.3119999999999998885 ) ) ;
#8617=CARTESIAN_POINT ( 'NONE',  ( 0.2101503697800941040, 4.967001120964043004, 0.2322385514659185413 ) ) ;
#8619=ORIENTED_EDGE ( 'NONE', *, *, #18218, .F. ) ;
#8622=CARTESIAN_POINT ( 'NONE',  ( 0.000000000000000000, 5.384999999999999787, 0.000000000000000000 ) ) ;
#8623=CARTESIAN_POINT ( 'NONE',  ( 0.3038794415728064968, 3.805497571066078777, 0.08166545862924670662 ) ) ;
#8625=CARTESIAN_POINT ( 'NONE',  ( 0.2819296736111110424, 0.1013888888130222571, 0.1167790944451424923 ) ) ;
#8628=CARTESIAN_POINT ( 'NONE',  ( -0.1993543840281266355, 5.151472222298088433, 0.1993543840281267465 ) ) ;
#8630=ADVANCED_FACE ( 'NONE', ( #9887 ), #10011, .T. ) ;
#8631=CARTESIAN_POINT ( 'NONE',  ( 0.000000000000000000, 5.384999999999999787, 0.000000000000000000 ) ) ;
#8633=LINE ( 'NONE', #16078, #18398 ) ;
#8634=CARTESIAN_POINT ( 'NONE',  ( -0.2206173157302028787, 0.4972222222222218435, 0.2206173157302027954 ) ) ;
#8635=CARTESIAN_POINT ( 'NONE',  ( -0.3119999999999998885, 4.720916666666666650, 0.1292346314604058410 ) ) ;
#8636=CARTESIAN_POINT ( 'NONE',  ( 0.1993543840281267465, 4.207027777853643791, 0.1993543840281266633 ) ) ;
#8637=CARTESIAN_POINT ( 'NONE',  ( 0.1167790944451424368, 3.995222222298087988, 0.2819296736111110424 ) ) ;
#8640=CARTESIAN_POINT ( 'NONE',  ( 7.484242640931070629E-07, 4.016084960865516251, 0.3119999999981048489 ) ) ;
#8641=CARTESIAN_POINT ( 'NONE',  ( -0.1993543840281266910, 4.457027777853642903, -0.1993543840281266910 ) ) ;
#8642=CARTESIAN_POINT ( 'NONE',  ( -0.2401696643338466775, 4.508321440767591781, 0.1991626441011656312 ) ) ;
#8646=CARTESIAN_POINT ( 'NONE',  ( 0.1167790944451424506, 4.106333333409199149, 0.2819296736111110424 ) ) ;
#8647=CARTESIAN_POINT ( 'NONE',  ( -0.01743693570811869625, 4.822118045354796045, -0.3115821376521073494 ) ) ;
#8650=CARTESIAN_POINT ( 'NONE',  ( -0.1993543840281266633, 0.05624999992413336897, -0.1993543840281266910 ) ) ;
#8653=DIRECTION ( 'NONE',  ( 0.000000000000000000, 0.000000000000000000, -1.000000000000000000 ) ) ;
#8659=CARTESIAN_POINT ( 'NONE',  ( 1.059513921322799533E-10, 3.821611107313654720, -0.3119999999999999996 ) ) ;
#8660=CARTESIAN_POINT ( 'NONE',  ( 1.726321361862525858E-17, 0.4937499999241333759, -0.2819296736111110979 ) ) ;
#8661=CARTESIAN_POINT ( 'NONE',  ( -0.1993543840281266910, 3.970916666742532186, -0.1993543840281266910 ) ) ;
#8664=CARTESIAN_POINT ( 'NONE',  ( -1.726321361862525858E-17, 4.575083333409199149, -0.2819296736111110979 ) ) ;
#8666=CARTESIAN_POINT ( 'NONE',  ( 0.3121506383504715210, 5.078286358898017383, 0.009141518313334958193 ) ) ;
#8668=CARTESIAN_POINT ( 'NONE',  ( 0.1292346314604058410, 3.741750000151732536, 0.3119999999999998885 ) ) ;
#8669=CARTESIAN_POINT ( 'NONE',  ( 0.2677787189661461897, 4.191816329952293252, 0.1601340282671347148 ) ) ;
#8672=CARTESIAN_POINT ( 'NONE',  ( 0.03458881943681251653, 5.206640035683668621, 0.2803355776336168281 ) ) ;
#8673=CARTESIAN_POINT ( 'NONE',  ( 0.1167790944451424506, 4.981333333409198261, 0.2819296736111110424 ) ) ;
#8675=ORIENTED_EDGE ( 'NONE', *, *, #342, .F. ) ;
#8676=AXIS2_PLACEMENT_3D ( 'NONE', #12148, #21750, #23079 ) ;
#8678=CARTESIAN_POINT ( 'NONE',  ( -0.2933685965344436375, 5.111756720891555084, -0.1009642549206684198 ) ) ;
#8679=CARTESIAN_POINT ( 'NONE',  ( -0.008838905694748024067, 4.571396606871324764, 0.3119999992378313380 ) ) ;
#8681=CARTESIAN_POINT ( 'NONE',  ( -0.2819296736111110979, 0.1881944443685777957, -3.452642723725051716E-17 ) ) ;
#8683=CARTESIAN_POINT ( 'NONE',  ( -0.2819296736111110979, 0.08055555547968892838, 0.1167790944451422425 ) ) ;
#8685=CARTESIAN_POINT ( 'NONE',  ( -0.2826589919575409060, 5.202197775706403071, 0.03072956325641070657 ) ) ;
#8687=CARTESIAN_POINT ( 'NONE',  ( -0.2015210671123849329, 5.065410029797029701, 0.2392828963600910630 ) ) ;
#8690=CARTESIAN_POINT ( 'NONE',  ( 0.2819296736111110979, 4.783416666742532186, -3.452642723725051716E-17 ) ) ;
#8691=CARTESIAN_POINT ( 'NONE',  ( 1.519200945994765378E-06, 3.766055514889470324, -0.3119999999963013471 ) ) ;
#8692=CARTESIAN_POINT ( 'NONE',  ( 0.1015009281151166981, 3.724843158531562892, -0.2819296736111110979 ) ) ;
#8693=CARTESIAN_POINT ( 'NONE',  ( -0.2934558719060931797, 0.05332506518006699392, 0.07539210639951753057 ) ) ;
#8694=CARTESIAN_POINT ( 'NONE',  ( -5.731347020009612645E-17, 0.1083333331816004053, 0.3119999999999999996 ) ) ;
#8697=CARTESIAN_POINT ( 'NONE',  ( 0.2206173157302027954, 4.370222222373953969, -0.2206173157302028232 ) ) ;
#8699=CARTESIAN_POINT ( 'NONE',  ( -0.2819296736111110979, 4.696611111186977716, -0.1167790944451422980 ) ) ;
#8700=VERTEX_POINT ( 'NONE', #4858 ) ;
#8701=EDGE_CURVE ( 'NONE', #17157, #15989, #21146, .T. ) ;
#8702=CARTESIAN_POINT ( 'NONE',  ( -0.1993543840281266355, 3.804250000075865223, 0.1993543840281267465 ) ) ;
#8705=ADVANCED_FACE ( 'NONE', ( #4973 ), #4623, .T. ) ;
#8708=ORIENTED_EDGE ( 'NONE', *, *, #8254, .T. ) ;
#8709=CARTESIAN_POINT ( 'NONE',  ( -5.731347020009612645E-17, 0.3861111109593781676, 0.3119999999999999996 ) ) ;
#8710=B_SPLINE_CURVE_WITH_KNOTS ( 'NONE', 1,
 ( #9650, #17086 ),
 .UNSPECIFIED., .F., .F.,
 ( 2, 2 ),
 ( 0.000000000000000000, 1.000000000000000000 ),
 .UNSPECIFIED. ) ;
#8715=EDGE_LOOP ( 'NONE', ( #15524, #15842, #11032, #18341 ) ) ;
#8717=CARTESIAN_POINT ( 'NONE',  ( -0.2819296736111110979, 0.2854166665908000611, -3.452642723725051716E-17 ) ) ;
#8719=CARTESIAN_POINT ( 'NONE',  ( 5.178964085587577574E-17, 4.533416666742532186, 0.2819296736111110979 ) ) ;
#8722=CARTESIAN_POINT ( 'NONE',  ( -1.960390272410463459E-06, 4.210500054279665783, -0.3119999999938410928 ) ) ;
#8723=CARTESIAN_POINT ( 'NONE',  ( 0.1292346314604058410, 4.068138888888888083, 0.3119999999999998885 ) ) ;
#8724=CARTESIAN_POINT ( 'NONE',  ( 0.2206173157302027954, 4.870222222373954857, -0.2206173157302028232 ) ) ;
#8726=EDGE_CURVE ( 'NONE', #19405, #22848, #6331, .T. ) ;
#8727=EDGE_LOOP ( 'NONE', ( #4084, #15016, #19028, #18073 ) ) ;
#8728=LINE ( 'NONE', #7275, #4675 ) ;
#8729=CARTESIAN_POINT ( 'NONE',  ( 1.201146141948970407E-06, 4.904991752689871198, 0.3119999999951060254 ) ) ;
#8735=CARTESIAN_POINT ( 'NONE',  ( -0.1292346314604081170, 4.429249999999999687, -0.3119999999999975016 ) ) ;
#8737=CARTESIAN_POINT ( 'NONE',  ( 0.1167790944451423535, 0.1499999999241333759, 0.2819296736111110979 ) ) ;
#8739=CARTESIAN_POINT ( 'NONE',  ( 0.2819296736111110424, 5.175777777853644679, -0.1167790944451423396 ) ) ;
#8743=CARTESIAN_POINT ( 'NONE',  ( -0.1908862062913858626, 4.605243227715043908, -0.2467925334992447373 ) ) ;
#8744=CARTESIAN_POINT ( 'NONE',  ( -0.1178635634473103738, 4.269440902833853357, -0.2905642712132933125 ) ) ;
#8746=CARTESIAN_POINT ( 'NONE',  ( -0.3119999999999999996, 0.5493055555555551583, 0.1292346314604056190 ) ) ;
#8747=CARTESIAN_POINT ( 'NONE',  ( 0.1292346314604056190, 4.811194444444443441, -0.3119999999999999996 ) ) ;
#8748=CARTESIAN_POINT ( 'NONE',  ( 0.1340080504559709729, 5.203643142954044620, 0.2502513067613080788 ) ) ;
#8749=CARTESIAN_POINT ( 'NONE',  ( -0.2819296736111110979, 4.019527777853642903, 0.000000000000000000 ) ) ;
#8752=CARTESIAN_POINT ( 'NONE',  ( 0.3119999999999998885, 0.5076388887371560132, 0.1292346314604058410 ) ) ;
#8754=ORIENTED_EDGE ( 'NONE', *, *, #1780, .T. ) ;
#8755=CARTESIAN_POINT ( 'NONE',  ( 0.1292346314604031765, 3.922305555555555490, -0.3120000000000024420 ) ) ;
#8756=CARTESIAN_POINT ( 'NONE',  ( 0.2819296736111110979, 4.547305555631421470, -3.452642723725051716E-17 ) ) ;
#8757=CARTESIAN_POINT ( 'NONE',  ( -0.3089083532858699077, 4.500952954266654871, -0.04389791046443763944 ) ) ;
#8765=CARTESIAN_POINT ( 'NONE',  ( -0.2819296736111110424, 4.148000000075866112, 0.1167790944451424923 ) ) ;
#8767=CARTESIAN_POINT ( 'NONE',  ( -0.3119999999999998885, 4.887583333333332725, 0.1292346314604058410 ) ) ;
#8771=CARTESIAN_POINT ( 'NONE',  ( 0.2819296736111110424, 0.08749999992413336203, 0.1167790944451424923 ) ) ;
#8773=DIRECTION ( 'NONE',  ( 0.000000000000000000, 0.000000000000000000, 1.000000000000000000 ) ) ;
#8778=ORIENTED_EDGE ( 'NONE', *, *, #13957, .T. ) ;
#8782=CARTESIAN_POINT ( 'NONE',  ( -0.2819296736111110979, 0.5111111110352446474, 0.1167790944451422425 ) ) ;
#8783=CARTESIAN_POINT ( 'NONE',  ( -0.1993543840281266910, 3.915361111186976384, -0.1993543840281266910 ) ) ;
#8785=ORIENTED_EDGE ( 'NONE', *, *, #10668, .T. ) ;
#8786=CARTESIAN_POINT ( 'NONE',  ( 0.2819296736111110424, 4.342444444520311642, -0.1167790944451423396 ) ) ;
#8787=CARTESIAN_POINT ( 'NONE',  ( 0.01997118933809540267, 5.142873989094642440, -0.3040754418437698892 ) ) ;
#8788=CARTESIAN_POINT ( 'NONE',  ( -0.3119999999999999996, 0.1465277776260448528, -0.1292346314604056745 ) ) ;
#8789=ORIENTED_EDGE ( 'NONE', *, *, #10680, .T. ) ;
#8790=CARTESIAN_POINT ( 'NONE',  ( -0.1993543840281266355, 5.137583333409198261, 0.1993543840281267465 ) ) ;
#8794=AXIS2_PLACEMENT_3D ( 'NONE', #5218, #21696, #3274 ) ;
#8795=CARTESIAN_POINT ( 'NONE',  ( -0.2819296736111110979, 4.849388888964755395, -0.1167790944451422980 ) ) ;
#8800=CARTESIAN_POINT ( 'NONE',  ( -0.1876229909954430231, 4.549487878473160052, -0.2524456540483745459 ) ) ;
#8803=CARTESIAN_POINT ( 'NONE',  ( 0.1993543840281266910, 0.2784722221463555858, -0.1993543840281266910 ) ) ;
#8805=CARTESIAN_POINT ( 'NONE',  ( 0.2819296736111110424, 0.04583333325746670461, 0.1167790944451424923 ) ) ;
#8809=CARTESIAN_POINT ( 'NONE',  ( -0.2434908057415208216, 5.063736957178592846, 0.1953540873034801117 ) ) ;
#8810=LINE ( 'NONE', #23671, #12643 ) ;
#8811=CARTESIAN_POINT ( 'NONE',  ( -0.3115168255710737966, 3.890354268893235989, -0.02373096174760461544 ) ) ;
#8814=CARTESIAN_POINT ( 'NONE',  ( 0.1167790944451424368, 4.495222222298088433, 0.2819296736111110424 ) ) ;
#8815=CARTESIAN_POINT ( 'NONE',  ( 0.001849798306578129140, 4.543780820092050199, -0.3119953020238740438 ) ) ;
#8816=CARTESIAN_POINT ( 'NONE',  ( -0.1993543840281266910, 3.790361111186976828, -0.1993543840281266910 ) ) ;
#8817=CARTESIAN_POINT ( 'NONE',  ( -0.03933790649247456001, 0.04385992660403156135, -0.2908781100274356324 ) ) ;
#8818=CARTESIAN_POINT ( 'NONE',  ( 0.3096594984987066645, 3.751112016665212767, 0.03836432376948438472 ) ) ;
#8822=CARTESIAN_POINT ( 'NONE',  ( -0.07317541673116574608, 4.791775583817363682, 0.3034609665091877462 ) ) ;
#8824=CARTESIAN_POINT ( 'NONE',  ( -0.3119999999999999996, 4.391055555707287894, 0.000000000000000000 ) ) ;
#8825=CARTESIAN_POINT ( 'NONE',  ( -0.2819296736111110979, 4.644527777853643791, 0.000000000000000000 ) ) ;
#8826=CARTESIAN_POINT ( 'NONE',  ( -0.2819296736111110424, 3.904944444520309865, -0.1167790944451423119 ) ) ;
#8831=ORIENTED_EDGE ( 'NONE', *, *, #23305, .F. ) ;
#8832=CARTESIAN_POINT ( 'NONE',  ( 0.2206173157302027676, 0.1708333331816004053, 0.2206173157302028787 ) ) ;
#8834=CARTESIAN_POINT ( 'NONE',  ( -0.0008552964370042808167, 4.377189652761055427, -0.3119989957290913996 ) ) ;
#8835=CARTESIAN_POINT ( 'NONE',  ( -0.1964023011945066899, 3.716541689590819431, -0.2424612127253647220 ) ) ;
#8839=ORIENTED_EDGE ( 'NONE', *, *, #967, .T. ) ;
#8841=CARTESIAN_POINT ( 'NONE',  ( 0.2206057284202265489, 5.078575579926999595, 0.2213988795958710953 ) ) ;
#8842=CARTESIAN_POINT ( 'NONE',  ( 0.2819296736111110979, 0.2055555554796889006, -0.1167790944451422980 ) ) ;
#8846=CARTESIAN_POINT ( 'NONE',  ( -0.1167790944451423535, 4.474388888964753619, 0.2819296736111110424 ) ) ;
#8847=CARTESIAN_POINT ( 'NONE',  ( 0.1292346314604056745, 0.1951388888888886119, -0.3119999999999999996 ) ) ;
#8848=FACE_OUTER_BOUND ( 'NONE', #5008, .T. ) ;
#8849=CARTESIAN_POINT ( 'NONE',  ( -0.1706684928076038221, 4.233164261868517464, 0.2620792061749219748 ) ) ;
#8850=CARTESIAN_POINT ( 'NONE',  ( -0.3119999999999998885, 4.109805555555554157, 0.1292346314604058410 ) ) ;
#8852=CARTESIAN_POINT ( 'NONE',  ( 0.2206173157302027954, 5.036888889040620931, -0.2206173157302028232 ) ) ;
#8855=CARTESIAN_POINT ( 'NONE',  ( -0.1292346314604057300, 4.172305555555555046, 0.3119999999999998885 ) ) ;
#8856=ORIENTED_EDGE ( 'NONE', *, *, #18218, .T. ) ;
#8857=CARTESIAN_POINT ( 'NONE',  ( -0.2062328096137425182, 4.883584785677744122, -0.2343418988765107736 ) ) ;
#8860=B_SPLINE_CURVE_WITH_KNOTS ( 'NONE', 3,
 ( #5700, #13163, #14614, #22038, #18265, #20577, #16441, #7053, #3874, #11317, #14490, #21913, #5205, #12678, #12799, #3384, #1561, #11565, #15456, #20937, #7770, #18993, #17281, #22879, #4345, #21056, #2172, #22648, #20817, #693, #8004, #4230, #4465, #9605, #11929, #8119, #2528, #452, #212, #6298, #3988, #7651, #4106, #5936, #9726, #13394, #17164, #11439, #13751, #20698, #13638, #17036, #330, #11799, #19348, #11682 ),
 .UNSPECIFIED., .F., .F.,
 ( 4, 2, 1, 1, 1, 1, 1, 1, 2, 2, 2, 2, 2, 2, 2, 2, 1, 2, 2, 2, 2, 2, 2, 2, 1, 2, 2, 2, 2, 2, 2, 4 ),
 ( 0.2284379164993652067, 0.2284424888044066237, 0.2284470611094480408, 0.2284562057195309026, 0.2284744949396965985, 0.2285110733800279903, 0.2285842302606907739, 0.2287305440220163133, 0.2290231715446674476, 0.2296084265899696608, 0.2307789366805741149, 0.2319494467711785690, 0.2331199568617830231, 0.2342904669523874772, 0.2348757219976896904, 0.2351683495203407970, 0.2353146632816663641, 0.2353878201623291477, 0.2354243986026605395, 0.2354609770429919313, 0.2378019972242008118, 0.2401430174054097200, 0.2413135274960141741, 0.2418987825413164150, 0.2421914100639675216, 0.2423377238252930610, 0.2424108807059558446, 0.2424840375866186282, 0.2436545476772231378, 0.2448250577678276474, 0.2459955678584321292, 0.2471660779490366389 ),
 .UNSPECIFIED. ) ;
#8865=ADVANCED_FACE ( 'NONE', ( #10845 ), #5094, .T. ) ;
#8866=EDGE_CURVE ( 'NONE', #17266, #20417, #1805, .T. ) ;
#8868=CARTESIAN_POINT ( 'NONE',  ( -0.2819296736111111534, 0.3583333332574666907, 0.1167790944451422563 ) ) ;
#8870=CARTESIAN_POINT ( 'NONE',  ( -0.2819296736111110424, 5.092444444520309865, 0.1167790944451424923 ) ) ;
#8871=CARTESIAN_POINT ( 'NONE',  ( 0.1818344428640181754, 4.482884648730991906, -0.2543617637045067492 ) ) ;
#8873=CARTESIAN_POINT ( 'NONE',  ( 0.000000000000000000, 5.384999999999999787, 0.000000000000000000 ) ) ;
#8874=CARTESIAN_POINT ( 'NONE',  ( -8.379073922441706732E-07, 4.293833316950179224, 0.3119999999988748440 ) ) ;
#8877=CARTESIAN_POINT ( 'NONE',  ( 0.3119999999999999996, 4.748694444444444329, -0.1292346314604056745 ) ) ;
#8878=CARTESIAN_POINT ( 'NONE',  ( 0.08598857743947876942, 5.201362809669102027, 0.2716196834644542535 ) ) ;
#8879=CARTESIAN_POINT ( 'NONE',  ( -0.2819296736111110424, 3.967444444520310309, 0.1167790944451424923 ) ) ;
#8880=CARTESIAN_POINT ( 'NONE',  ( 0.2819296736111110979, 3.783416666742532186, -3.452642723725051716E-17 ) ) ;
#8884=DIRECTION ( 'NONE',  ( -0.000000000000000000, -1.000000000000000000, -0.000000000000000000 ) ) ;
#8886=CARTESIAN_POINT ( 'NONE',  ( -0.1167790944451423535, 4.529944444520309865, 0.2819296736111110424 ) ) ;
#8887=CARTESIAN_POINT ( 'NONE',  ( -0.005371487263433293718, 4.488432277541713589, -0.3120000000213787317 ) ) ;
#8891=CARTESIAN_POINT ( 'NONE',  ( 0.1292346314604056745, 0.08402777777777743762, -0.3119999999999999996 ) ) ;
#8893=CARTESIAN_POINT ( 'NONE',  ( -0.2819296736111110979, 4.088972222298088433, 0.000000000000000000 ) ) ;
#8894=CARTESIAN_POINT ( 'NONE',  ( -0.2704625092236399575, 4.840203190926620103, 0.1611498159692242860 ) ) ;
#8895=CARTESIAN_POINT ( 'NONE',  ( -0.08164014826675215775, 4.458214446043974100, 0.3038864024473010295 ) ) ;
#8898=CARTESIAN_POINT ( 'NONE',  ( -0.2819296736111110979, 0.3409722221463556413, -3.452642723725051716E-17 ) ) ;
#8900=FACE_OUTER_BOUND ( 'NONE', #9684, .T. ) ;
#8904=B_SPLINE_CURVE_WITH_KNOTS ( 'NONE', 3,
 ( #21062, #22768, #218, #2050, #3880, #16923, #2296, #2179, #7656, #15106, #9612, #17042, #6662, #19467, #2765, #10218, #21181, #16057, #17522, #17642, #23472, #4596, #930, #12054, #8361, #818, #6784, #10100, #14107, #23111, #15697, #21537, #14227, #12177, #13756, #1057, #19585, #1179, #8617, #15811, #15928, #23231, #6541, #21303, #8244, #12294, #8485, #4471, #21661, #19353, #11936, #4824, #2877, #6421, #13874 ),
 .UNSPECIFIED., .F., .F.,
 ( 4, 2, 1, 1, 1, 1, 2, 2, 2, 2, 2, 2, 1, 1, 2, 2, 1, 1, 1, 2, 2, 2, 2, 2, 2, 2, 2, 1, 1, 2, 2, 1, 1, 4 ),
 ( 0.1553377600788464485, 0.1553555988096145257, 0.1553734375403825752, 0.1554091150019187018, 0.1554804699249909827, 0.1556231797711355169, 0.1559085994634245853, 0.1564794388480027221, 0.1576211176171589956, 0.1599044751554715427, 0.1621878326937841175, 0.1644711902320966646, 0.1647566099243857329, 0.1648993197705302671, 0.1649706746936025481, 0.1649795940589865728, 0.1649885134243705975, 0.1650063521551386470, 0.1650420296166747458, 0.1656128690012524107, 0.1667545477704077406, 0.1678962265395630704, 0.1690379053087184003, 0.1701795840778737301, 0.1713212628470290599, 0.1718921022316067249, 0.1721775219238955712, 0.1723202317700399944, 0.1723915866931121921, 0.1724272641546482909, 0.1724361835200323156, 0.1724451028854163404, 0.1724629416161844175, 0.1736046203853397751 ),
 .UNSPECIFIED. ) ;
#8905=ORIENTED_EDGE ( 'NONE', *, *, #13080, .T. ) ;
#8908=CARTESIAN_POINT ( 'NONE',  ( -0.08166536455864450983, 3.847164242900631859, 0.3038794701439369583 ) ) ;
#8909=CARTESIAN_POINT ( 'NONE',  ( -0.2206173157302028787, 0.1083333333333329901, 0.2206173157302027954 ) ) ;
#8910=CARTESIAN_POINT ( 'NONE',  ( -0.1167790944451423535, 3.821611111186977272, 0.2819296736111110424 ) ) ;
#8914=CARTESIAN_POINT ( 'NONE',  ( -0.1993543840281266355, 4.484805555631421470, 0.1993543840281267465 ) ) ;
#8915=EDGE_CURVE ( 'NONE', #10834, #17381, #3077, .T. ) ;
#8919=CARTESIAN_POINT ( 'NONE',  ( 0.2818991764556534885, 4.359328379276062648, 0.1340068449377857795 ) ) ;
#8920=CARTESIAN_POINT ( 'NONE',  ( -0.2819296736111110979, 5.241750000075865223, 0.000000000000000000 ) ) ;
#8921=CARTESIAN_POINT ( 'NONE',  ( 0.0002807800906013602411, 4.210492038945215398, -0.3119999059963255994 ) ) ;
#8924=CARTESIAN_POINT ( 'NONE',  ( -0.2819296736111110424, 4.911888888964754507, 0.1167790944451424923 ) ) ;
#8928=CARTESIAN_POINT ( 'NONE',  ( 0.1993543840281266355, 0.2645833332574666907, 0.1993543840281267465 ) ) ;
#8930=CARTESIAN_POINT ( 'NONE',  ( -5.178964085587577574E-17, 0.03541666659080003332, 0.2819296736111110979 ) ) ;
#8937=CARTESIAN_POINT ( 'NONE',  ( 0.1993543840281266910, 0.09791666659080001944, -0.1993543840281266910 ) ) ;
#8938=CARTESIAN_POINT ( 'NONE',  ( -0.2819296736111110424, 4.425777777853643791, 0.1167790944451424923 ) ) ;
#8939=DIRECTION ( 'NONE',  ( 0.000000000000000000, 0.000000000000000000, -1.000000000000000000 ) ) ;
#8940=CARTESIAN_POINT ( 'NONE',  ( 0.2982715858037333079, 4.532666993397491240, -0.09547612790609734390 ) ) ;
#8941=CARTESIAN_POINT ( 'NONE',  ( 0.2819296736111110979, 5.005638888964754507, -3.452642723725051716E-17 ) ) ;
#8943=CARTESIAN_POINT ( 'NONE',  ( -0.1338711291748117538, 0.04577227553858571885, -0.2639161900088024537 ) ) ;
#8944=CARTESIAN_POINT ( 'NONE',  ( 0.01475392317844165246, 3.765650153564859437, -0.3120907002652242856 ) ) ;
#8945=CARTESIAN_POINT ( 'NONE',  ( 3.820898013339742174E-17, 5.384999999999999787, 0.3119999999999999996 ) ) ;
#8946=CARTESIAN_POINT ( 'NONE',  ( 0.2938106225197735233, 3.922092824913935072, -0.1134682388069244707 ) ) ;
#8947=CARTESIAN_POINT ( 'NONE',  ( -0.3119999999999999996, 4.387583333485066461, -0.1292346314604056468 ) ) ;
#8948=CARTESIAN_POINT ( 'NONE',  ( -0.1167790944451423119, 4.467444444520309865, -0.2819296736111110979 ) ) ;
#8949=CARTESIAN_POINT ( 'NONE',  ( 0.2819296736111110424, 3.939666666742531742, -0.1167790944451423396 ) ) ;
#8952=VERTEX_POINT ( 'NONE', #23993 ) ;
#8956=CARTESIAN_POINT ( 'NONE',  ( -0.3039946847935154350, 4.944401201872332230, -0.08125663725904756773 ) ) ;
#8959=CARTESIAN_POINT ( 'NONE',  ( -0.1292346314604056190, 0.3618055554038225874, -0.3119999999999999996 ) ) ;
#8961=CARTESIAN_POINT ( 'NONE',  ( -0.2704070349950395968, 4.395731272337639162, 0.1569688776948623132 ) ) ;
#8962=CARTESIAN_POINT ( 'NONE',  ( -0.2515410393475099315, 5.120907854582883445, 0.1785482678038019244 ) ) ;
#8963=DIRECTION ( 'NONE',  ( -0.000000000000000000, -1.000000000000000000, -0.000000000000000000 ) ) ;
#8966=CARTESIAN_POINT ( 'NONE',  ( 0.3057358687413568865, 5.087467270640830819, -0.06349570009324533026 ) ) ;
#8968=CARTESIAN_POINT ( 'NONE',  ( -0.2819296736111110424, 4.127166666742532186, -0.1167790944451423119 ) ) ;
#8969=CARTESIAN_POINT ( 'NONE',  ( 0.2819296736111110979, 5.161888888964753619, -0.1167790944451423396 ) ) ;
#8972=CARTESIAN_POINT ( 'NONE',  ( -0.03683881386148459003, 4.237268085405634821, 0.3098358431719507866 ) ) ;
#8973=CARTESIAN_POINT ( 'NONE',  ( 0.1292346314604056190, 4.144527777777777366, -0.3119999999999999996 ) ) ;
#8974=CARTESIAN_POINT ( 'NONE',  ( 0.1292346314604058410, 4.908416666818398610, 0.3119999999999998885 ) ) ;
#8975=CARTESIAN_POINT ( 'NONE',  ( -0.2819296736111110979, 5.088972222298087544, 0.000000000000000000 ) ) ;
#8977=AXIS2_PLACEMENT_3D ( 'NONE', #21821, #1227, #8653 ) ;
#8978=CARTESIAN_POINT ( 'NONE',  ( 0.2206173157302028787, 4.849388888888888083, 0.2206173157302027954 ) ) ;
#8980=CARTESIAN_POINT ( 'NONE',  ( 5.253288188650943643E-17, 5.197747365142496356, 0.2859756893339090444 ) ) ;
#8981=CARTESIAN_POINT ( 'NONE',  ( -0.1570247121346943220, 4.900413900555340874, 0.2726770930307582663 ) ) ;
#8991=CARTESIAN_POINT ( 'NONE',  ( 0.1993543840281266910, 0.3340277777019111660, -0.1993543840281266910 ) ) ;
#8993=CARTESIAN_POINT ( 'NONE',  ( -0.1993543840281266910, 5.137583333409199149, -0.1993543840281266910 ) ) ;
#8996=CARTESIAN_POINT ( 'NONE',  ( -0.2819296736111110979, 4.797305555631420582, 0.000000000000000000 ) ) ;
#8997=CARTESIAN_POINT ( 'NONE',  ( -0.1003379275823265415, 4.179873057794735836, 0.2961323726520993516 ) ) ;
#8999=CARTESIAN_POINT ( 'NONE',  ( 0.2206173157302028232, 0.5736111109593782231, -0.2206173157302028232 ) ) ;
#9000=CARTESIAN_POINT ( 'NONE',  ( 0.1292346314604058410, 4.790361111111110404, 0.3119999999999998885 ) ) ;
#9001=CARTESIAN_POINT ( 'NONE',  ( 0.1167790944451422702, 4.057722222298087544, -0.2819296736111110979 ) ) ;
#9002=CARTESIAN_POINT ( 'NONE',  ( 5.178964085587577574E-17, 3.769527777853644235, 0.2819296736111110979 ) ) ;
#9003=CARTESIAN_POINT ( 'NONE',  ( 7.459700445346810805E-07, 4.043833313442511290, -0.3119999999991081574 ) ) ;
#9004=CARTESIAN_POINT ( 'NONE',  ( -1.910449006669871087E-17, 4.425777777777777366, -0.3119999999999999996 ) ) ;
#9005=ORIENTED_EDGE ( 'NONE', *, *, #2055, .T. ) ;
#9007=ORIENTED_EDGE ( 'NONE', *, *, #22555, .T. ) ;
#9008=CARTESIAN_POINT ( 'NONE',  ( 0.2819296736111110979, 4.266055555631421470, 0.1167790944451422425 ) ) ;
#9009=CARTESIAN_POINT ( 'NONE',  ( -0.2025260695160075453, 4.494500837587061426, -0.2412900599587802508 ) ) ;
#9010=EDGE_CURVE ( 'NONE', #1106, #16767, #7283, .T. ) ;
#9011=ADVANCED_FACE ( 'NONE', ( #4117 ), #15226, .T. ) ;
#9012=CARTESIAN_POINT ( 'NONE',  ( 1.910449006669871087E-17, 0.08749999999999966138, -0.3119999999999999996 ) ) ;
#9014=CARTESIAN_POINT ( 'NONE',  ( 0.1993543840281267465, 3.776472222298087988, 0.1993543840281266633 ) ) ;
#9015=CARTESIAN_POINT ( 'NONE',  ( -0.04084070934671252956, 3.959337429128877872, 0.3120000006064171938 ) ) ;
#9017=CARTESIAN_POINT ( 'NONE',  ( 1.910449006669871087E-17, 0.5249999998482670627, -0.3119999999999999996 ) ) ;
#9018=CARTESIAN_POINT ( 'NONE',  ( 0.2782497666485165277, 0.06249891821425377497, 0.1411420113220940853 ) ) ;
#9020=CARTESIAN_POINT ( 'NONE',  ( -0.1167790944451424368, 0.3513888888130222155, 0.2819296736111110424 ) ) ;
#9030=CARTESIAN_POINT ( 'NONE',  ( -0.3119999999999999996, 0.04930555555555521385, 0.1292346314604056190 ) ) ;
#9031=CARTESIAN_POINT ( 'NONE',  ( 0.1167790944451422702, 3.849388888964754951, -0.2819296736111110424 ) ) ;
#9034=CARTESIAN_POINT ( 'NONE',  ( -1.726321361862525858E-17, 4.519527777853643791, -0.2819296736111110979 ) ) ;
#9035=CARTESIAN_POINT ( 'NONE',  ( 1.910449006669871087E-17, 0.1361111109593781676, -0.3119999999999999996 ) ) ;
#9036=CARTESIAN_POINT ( 'NONE',  ( -0.3120000000000000551, 0.1534722220704892726, 0.1292346314604056190 ) ) ;
#9039=CARTESIAN_POINT ( 'NONE',  ( -1.726321361862525858E-17, 5.172305555631420582, -0.2819296736111110979 ) ) ;
#9040=CARTESIAN_POINT ( 'NONE',  ( 0.2806972955496128130, 4.200680281449905351, -0.1374172179846145925 ) ) ;
#9043=CARTESIAN_POINT ( 'NONE',  ( 5.178964085587577574E-17, 4.700083333409199149, 0.2819296736111110979 ) ) ;
#9047=CARTESIAN_POINT ( 'NONE',  ( 1.726321361862525858E-17, 0.3409722221463556413, -0.2819296736111110979 ) ) ;
#9049=CARTESIAN_POINT ( 'NONE',  ( 0.1993543840281266355, 0.2090277777019111383, 0.1993543840281267465 ) ) ;
#9050=CARTESIAN_POINT ( 'NONE',  ( -0.2081274754753156542, 4.716903871102764434, -0.2331404442114669018 ) ) ;
#9051=CARTESIAN_POINT ( 'NONE',  ( -0.2485974056653872943, 5.197792025490196366, -0.1419878697022586012 ) ) ;
#9055=CARTESIAN_POINT ( 'NONE',  ( -0.2329574276516829245, 3.884553289494028672, -0.2088804256055948050 ) ) ;
#9056=CARTESIAN_POINT ( 'NONE',  ( 0.1993543840281266910, 0.04236111103524448085, -0.1993543840281266910 ) ) ;
#9057=CARTESIAN_POINT ( 'NONE',  ( -0.2819296736111110424, 4.529944444520310753, -0.1167790944451423119 ) ) ;
#9059=CARTESIAN_POINT ( 'NONE',  ( 0.09528670647744390265, 4.518783353215682475, 0.2983507620828029783 ) ) ;
#9060=CARTESIAN_POINT ( 'NONE',  ( -1.726321361862525858E-17, 5.130638888964754507, -0.2819296736111110979 ) ) ;
#9062=DIRECTION ( 'NONE',  ( -0.000000000000000000, -1.000000000000000000, -0.000000000000000000 ) ) ;
#9065=CARTESIAN_POINT ( 'NONE',  ( 5.731347020009612645E-17, 4.238277777929510215, 0.3119999999999999996 ) ) ;
#9066=CARTESIAN_POINT ( 'NONE',  ( 0.1993543840281266633, 4.568138888964755395, -0.1993543840281266910 ) ) ;
#9067=CARTESIAN_POINT ( 'NONE',  ( -0.1993543840281266355, 3.748694444520309865, 0.1993543840281267465 ) ) ;
#9069=ORIENTED_EDGE ( 'NONE', *, *, #12017, .F. ) ;
#9076=CARTESIAN_POINT ( 'NONE',  ( 1.910449006669871087E-17, 0.1916666665149337478, -0.3119999999999999996 ) ) ;
#9077=DIRECTION ( 'NONE',  ( 0.000000000000000000, 0.000000000000000000, -1.000000000000000000 ) ) ;
#9078=CARTESIAN_POINT ( 'NONE',  ( -0.2779820761605299451, 5.119293720360404087, 0.1354021004295479780 ) ) ;
#9079=CARTESIAN_POINT ( 'NONE',  ( -0.1292346314604056190, 0.2576388888888885287, -0.3119999999999999996 ) ) ;
#9083=CARTESIAN_POINT ( 'NONE',  ( 0.05068837741648516554, 5.073009555618063438, 0.3078549794868774558 ) ) ;
#9086=CARTESIAN_POINT ( 'NONE',  ( -0.1993543840281266355, 4.304250000075865223, 0.1993543840281267465 ) ) ;
#9087=CARTESIAN_POINT ( 'NONE',  ( -0.1167790944451423535, 5.141055555631421470, 0.2819296736111110979 ) ) ;
#9089=CARTESIAN_POINT ( 'NONE',  ( -0.2206810875299578256, 4.231324935242756879, 0.2214992208011696551 ) ) ;
#9090=CARTESIAN_POINT ( 'NONE',  ( 0.3119999999999999996, 4.019527777777777366, 0.1292346314604056190 ) ) ;
#9091=CARTESIAN_POINT ( 'NONE',  ( -0.2206173157302027676, 5.064666666818399499, 0.2206173157302028787 ) ) ;
#9092=CARTESIAN_POINT ( 'NONE',  ( 4.589422455927707524E-07, 4.793851445074613693, 0.3119999999992840167 ) ) ;
#9093=CARTESIAN_POINT ( 'NONE',  ( 0.1292346314604095325, 4.845916666666666650, 0.3119999999999962248 ) ) ;
#9096=CARTESIAN_POINT ( 'NONE',  ( -0.1060100004866296602, 0.05877850679265330530, 0.2896447613046597702 ) ) ;
#9098=VECTOR ( 'NONE', #19763, 39.37007874015748143 ) ;
#9100=CARTESIAN_POINT ( 'NONE',  ( -0.2819296736111110979, 5.075083333409198261, 0.000000000000000000 ) ) ;
#9103=CARTESIAN_POINT ( 'NONE',  ( 0.2819296736111110979, 0.3305555554796889561, -0.1167790944451422980 ) ) ;
#9106=CARTESIAN_POINT ( 'NONE',  ( -0.1167790944451423535, 4.988277777853642903, 0.2819296736111110424 ) ) ;
#9107=CARTESIAN_POINT ( 'NONE',  ( 0.05409597954341190812, 4.486773822218035335, -0.3072748769328391694 ) ) ;
#9109=CARTESIAN_POINT ( 'NONE',  ( -0.2819296736111110424, 4.793833333409199149, -0.1167790944451423119 ) ) ;
#9110=CARTESIAN_POINT ( 'NONE',  ( -0.2492977952293752575, 4.162941096864973822, -0.1919975030541300476 ) ) ;
#9114=CARTESIAN_POINT ( 'NONE',  ( 0.3119999999999999996, 4.630638888888888971, 0.1292346314604056190 ) ) ;
#9116=CARTESIAN_POINT ( 'NONE',  ( 0.1993543840281266633, 4.109805555631420582, -0.1993543840281266910 ) ) ;
#9119=CARTESIAN_POINT ( 'NONE',  ( 0.2962862119097752212, 4.032746098098823673, -0.09776748290151990317 ) ) ;
#9121=ORIENTED_EDGE ( 'NONE', *, *, #18577, .T. ) ;
#9124=CARTESIAN_POINT ( 'NONE',  ( 0.2819296736111110424, 4.273000000075865223, -0.1167790944451423396 ) ) ;
#9127=AXIS2_PLACEMENT_3D ( 'NONE', #15878, #23181, #23294 ) ;
#9128=CARTESIAN_POINT ( 'NONE',  ( -0.3118270672008495725, 4.114353485223650075, 0.03906138359714995262 ) ) ;
#9129=CARTESIAN_POINT ( 'NONE',  ( 0.2206173157302028232, 0.08055555555555521385, -0.2206173157302028232 ) ) ;
#9133=CARTESIAN_POINT ( 'NONE',  ( -0.3038752989638471846, 4.449004309992175443, 0.08168146717636678988 ) ) ;
#9134=CARTESIAN_POINT ( 'NONE',  ( -8.251178249108312710E-07, 5.016022433328296337, 0.3119999999976432181 ) ) ;
#9136=CARTESIAN_POINT ( 'NONE',  ( 0.2819296736111110424, 0.1499999999241333482, -0.1167790944451423119 ) ) ;
#9138=B_SPLINE_CURVE_WITH_KNOTS ( 'NONE', 3,
 ( #10234, #13419, #19247, #21322, #4612, #17662, #948, #22905, #13773, #4255, #19019, #17304, #11706, #13666, #596, #10000, #17188, #8378, #474, #2669, #6080, #15715, #23129, #5958, #22669, #15479, #7906, #2314, #15358, #13547, #23372, #1318, #16198, #5203, #10836, #17781, #21681, #8743, #18144, #6804, #16315, #14245, #19971, #12312, #14364, #1199, #21439, #23488, #19844, #23612, #5083, #12677, #20094, #14125, #19725 ),
 .UNSPECIFIED., .F., .F.,
 ( 4, 2, 2, 1, 2, 2, 1, 1, 1, 2, 2, 2, 2, 2, 2, 2, 2, 2, 2, 1, 2, 2, 1, 1, 2, 2, 2, 2, 1, 1, 2, 4 ),
 ( 0.3932770965733057844, 0.3955159922397885608, 0.3957958541980989287, 0.3958133455704933024, 0.3958220912566904892, 0.3958308369428876761, 0.3958658196876764790, 0.3959357851772540293, 0.3960757161564091855, 0.3966354400730296992, 0.3977548879062707821, 0.3999937835727528923, 0.4011132314059939197, 0.4022326792392350026, 0.4033521270724760299, 0.4044715749057171128, 0.4055910227389581402, 0.4067104705721992230, 0.4072701944888197367, 0.4073401599783972871, 0.4073576513507917163, 0.4073751427231860900, 0.4074101254679748929, 0.4075500564471299936, 0.4078299184054402504, 0.4089493662386812778, 0.4100688140719223052, 0.4106285379885428188, 0.4109083999468530757, 0.4110483309260082319, 0.4111182964155857822, 0.4111882619051633325 ),
 .UNSPECIFIED. ) ;
#9142=VERTEX_POINT ( 'NONE', #11447 ) ;
#9144=CARTESIAN_POINT ( 'NONE',  ( -0.2045975126714155434, 5.098224757089310444, -0.2344162392893719138 ) ) ;
#9148=CARTESIAN_POINT ( 'NONE',  ( 0.3119999999999999996, -0.03750000000000033168, 0.000000000000000000 ) ) ;
#9149=CARTESIAN_POINT ( 'NONE',  ( -0.1993543840281266910, 3.748694444520310309, -0.1993543840281266910 ) ) ;
#9151=CARTESIAN_POINT ( 'NONE',  ( 0.2819296736111110979, 4.338972222298087544, -3.452642723725051716E-17 ) ) ;
#9152=CARTESIAN_POINT ( 'NONE',  ( 0.2206173157302028232, 0.1291666665149337201, -0.2206173157302028232 ) ) ;
#9155=CARTESIAN_POINT ( 'NONE',  ( 0.2597711826752152064, 4.358053561029723078, 0.1728091967789982530 ) ) ;
#9156=CARTESIAN_POINT ( 'NONE',  ( -0.2819296736111110424, 4.911888888964754507, 0.1167790944451424923 ) ) ;
#9158=CARTESIAN_POINT ( 'NONE',  ( 0.2947569499035622154, 4.199647669654026139, -0.1038884209671450953 ) ) ;
#9162=CARTESIAN_POINT ( 'NONE',  ( -1.726321361862525858E-17, 4.561194444520309865, -0.2819296736111110979 ) ) ;
#9165=CARTESIAN_POINT ( 'NONE',  ( 0.2206173157302027954, 4.918833333333332725, -0.2206173157302028232 ) ) ;
#9166=CARTESIAN_POINT ( 'NONE',  ( 0.1993543840281266910, 0.5562499999241333759, -0.1993543840281266910 ) ) ;
#9169=CARTESIAN_POINT ( 'NONE',  ( 0.2819296736111110424, 0.1569444443685778234, 0.1167790944451424923 ) ) ;
#9171=CARTESIAN_POINT ( 'NONE',  ( -0.2659313529060423065, 5.198830554906272994, -0.1047787905467276182 ) ) ;
#9180=CARTESIAN_POINT ( 'NONE',  ( -0.2819296736111110424, 4.481333333409199149, 0.1167790944451424923 ) ) ;
#9182=CARTESIAN_POINT ( 'NONE',  ( 0.0005263094765449479037, 4.543818392271642637, -0.3119995841748594567 ) ) ;
#9183=CARTESIAN_POINT ( 'NONE',  ( -0.1167790944451423257, 5.189666666742533074, -0.2819296736111110424 ) ) ;
#9184=CARTESIAN_POINT ( 'NONE',  ( -0.1167790944451423119, 4.398000000075866112, -0.2819296736111110979 ) ) ;
#9185=CARTESIAN_POINT ( 'NONE',  ( 0.2530760179677841171, 3.746625009379008109, 0.1847156476164619199 ) ) ;
#9187=LINE ( 'NONE', #16630, #21456 ) ;
#9188=ORIENTED_EDGE ( 'NONE', *, *, #20646, .F. ) ;
#9190=CARTESIAN_POINT ( 'NONE',  ( -1.910449006669871087E-17, 4.043833333485065573, -0.3119999999999999996 ) ) ;
#9191=EDGE_CURVE ( 'NONE', #5827, #6276, #16184, .T. ) ;
#9192=CARTESIAN_POINT ( 'NONE',  ( -0.1993543840281266355, 4.595916666742532186, 0.1993543840281267465 ) ) ;
#9193=CARTESIAN_POINT ( 'NONE',  ( -0.2819296736111110424, 3.849388888964754063, -0.1167790944451423119 ) ) ;
#9199=CARTESIAN_POINT ( 'NONE',  ( 5.731347020009612645E-17, 4.231333333333332725, 0.3119999999999999996 ) ) ;
#9200=DIRECTION ( 'NONE',  ( 1.000000000000000000, 0.000000000000000000, 0.000000000000000000 ) ) ;
#9203=CARTESIAN_POINT ( 'NONE',  ( -0.2206173157302027954, 0.4208333331816004330, -0.2206173157302028232 ) ) ;
#9205=CARTESIAN_POINT ( 'NONE',  ( -0.03246180010856898612, 3.711382886895558286, -0.3109571910464125066 ) ) ;
#9207=CARTESIAN_POINT ( 'NONE',  ( 5.463034709641816805E-17, 5.167344860100310910, 0.2973937581265823082 ) ) ;
#9211=AXIS2_PLACEMENT_3D ( 'NONE', #18462, #20535, #5534 ) ;
#9215=CARTESIAN_POINT ( 'NONE',  ( -0.1167790944451423257, 4.231333333409199149, -0.2819296736111110424 ) ) ;
#9216=CARTESIAN_POINT ( 'NONE',  ( 0.2819296736111111534, 5.154944444520309865, 0.1167790944451422563 ) ) ;
#9218=CARTESIAN_POINT ( 'NONE',  ( -0.3082045718900721654, 4.225735098311363735, 0.04853676656518685073 ) ) ;
#9219=CARTESIAN_POINT ( 'NONE',  ( 0.3119999999999999996, 3.915361111111111292, -0.1292346314604056745 ) ) ;
#9221=CARTESIAN_POINT ( 'NONE',  ( -0.3119999999999999996, 4.887583333485065573, -0.1292346314604056468 ) ) ;
#9222=CARTESIAN_POINT ( 'NONE',  ( 0.3108175396127563217, 4.806979697495309622, 0.02714641660050034003 ) ) ;
#9226=B_SPLINE_CURVE_WITH_KNOTS ( 'NONE', 3,
 ( #19593, #21430, #1065, #8494, #21546, #12303, #15820, #14117, #14234, #4717, #8623, #21671, #12423, #19836, #19477, #23360, #15936, #4835 ),
 .UNSPECIFIED., .F., .F.,
 ( 4, 2, 2, 2, 2, 2, 2, 2, 4 ),
 ( 0.9228889348174078577, 0.9251733130190006316, 0.9274576912205934054, 0.9297420694221861792, 0.9320264476237789530, 0.9343108258253717269, 0.9365952040269645007, 0.9388795822285572745, 0.9411639604301500484 ),
 .UNSPECIFIED. ) ;
#9227=CARTESIAN_POINT ( 'NONE',  ( 0.05682895016479121153, 0.04205235519552708023, -0.2861892567955108269 ) ) ;
#9230=CARTESIAN_POINT ( 'NONE',  ( 0.1167790944451424368, 5.203555555631421470, 0.2819296736111110424 ) ) ;
#9233=CARTESIAN_POINT ( 'NONE',  ( 1.726321361862525858E-17, 0.2298611110352444531, -0.2819296736111110979 ) ) ;
#9235=CARTESIAN_POINT ( 'NONE',  ( 0.1993543840281267465, 4.887583333409199149, 0.1993543840281266633 ) ) ;
#9238=CARTESIAN_POINT ( 'NONE',  ( 0.2819296736111110979, 4.825083333409199149, -3.452642723725051716E-17 ) ) ;
#9239=CARTESIAN_POINT ( 'NONE',  ( -2.307748244742446386E-07, 4.182713274783838919, 0.3119999999998222528 ) ) ;
#9240=CARTESIAN_POINT ( 'NONE',  ( -0.1292346314604057300, 5.061194444444443441, 0.3119999999999998885 ) ) ;
#9242=CARTESIAN_POINT ( 'NONE',  ( 0.1720490635147988168, 0.06249999999999968081, 0.2634598316069546309 ) ) ;
#9243=CARTESIAN_POINT ( 'NONE',  ( 5.731347020009612645E-17, 4.397999999999999687, 0.3119999999999999996 ) ) ;
#9245=CARTESIAN_POINT ( 'NONE',  ( 5.178964085587577574E-17, 3.977861111186976384, 0.2819296736111110979 ) ) ;
#9246=CARTESIAN_POINT ( 'NONE',  ( -0.2819296736111110424, 3.863277777853644235, -0.1167790944451423119 ) ) ;
#9247=CARTESIAN_POINT ( 'NONE',  ( 0.2963184418439536727, 4.032743120851792540, -0.09767001781238864033 ) ) ;
#9248=CARTESIAN_POINT ( 'NONE',  ( 0.1292346314604031765, 4.422305555555555046, -0.3120000000000024420 ) ) ;
#9251=CARTESIAN_POINT ( 'NONE',  ( -0.1733170103021690056, 4.121925038073740666, 0.2594324947820166316 ) ) ;
#9252=CARTESIAN_POINT ( 'NONE',  ( 0.1684295338161674871, 4.632258567753597234, 0.2661145548031557673 ) ) ;
#9255=LINE ( 'NONE', #7544, #9556 ) ;
#9259=CARTESIAN_POINT ( 'NONE',  ( -0.1993543840281267465, 0.2923611110352445364, 0.1993543840281266633 ) ) ;
#9261=CARTESIAN_POINT ( 'NONE',  ( 1.910449006669871087E-17, 0.5874999999999996891, -0.3119999999999999996 ) ) ;
#9265=ORIENTED_EDGE ( 'NONE', *, *, #10204, .F. ) ;
#9269=CARTESIAN_POINT ( 'NONE',  ( -0.2206173157302028787, 0.05277777777777744456, 0.2206173157302027954 ) ) ;
#9270=CARTESIAN_POINT ( 'NONE',  ( 0.2819296736111110424, 3.842444444520310309, -0.1167790944451423396 ) ) ;
#9272=CARTESIAN_POINT ( 'NONE',  ( -0.2819296736111110424, 4.425777777853643791, 0.1167790944451424923 ) ) ;
#9273=DIRECTION ( 'NONE',  ( 0.000000000000000000, 0.000000000000000000, -1.000000000000000000 ) ) ;
#9274=CARTESIAN_POINT ( 'NONE',  ( -0.2206173157302028787, 0.1569444442927115102, 0.2206173157302027954 ) ) ;
#9277=CARTESIAN_POINT ( 'NONE',  ( 0.08374467998906506838, 4.374797057175100257, -0.3008178344637207902 ) ) ;
#9278=CARTESIAN_POINT ( 'NONE',  ( -0.1167790944451423257, 4.842444444520309865, -0.2819296736111110424 ) ) ;
#9281=CARTESIAN_POINT ( 'NONE',  ( -1.910449006669871087E-17, 4.981333333333332725, -0.3119999999999999996 ) ) ;
#9282=CARTESIAN_POINT ( 'NONE',  ( 0.2819296736111111534, 4.710500000075865223, 0.1167790944451422563 ) ) ;
#9284=CYLINDRICAL_SURFACE ( 'NONE', #9699, 0.3119999999999999996 ) ;
#9285=CARTESIAN_POINT ( 'NONE',  ( -0.2819296736111110424, 0.5736111110352444253, -0.1167790944451423396 ) ) ;
#9289=CARTESIAN_POINT ( 'NONE',  ( -0.2819296736111110424, 0.2958333332574666907, -0.1167790944451423396 ) ) ;
#9290=CARTESIAN_POINT ( 'NONE',  ( -1.054647954922321762E-07, 4.988277780858759947, -0.3119999999999820695 ) ) ;
#9296=CARTESIAN_POINT ( 'NONE',  ( -0.1696533514972167755, 3.882199842881781660, -0.2624525851558037748 ) ) ;
#9297=CARTESIAN_POINT ( 'NONE',  ( -5.178964085587577574E-17, 0.2437499999241333204, 0.2819296736111110979 ) ) ;
#9299=CARTESIAN_POINT ( 'NONE',  ( 0.2819296736111110979, 4.616750000075865223, -3.452642723725051716E-17 ) ) ;
#9302=CARTESIAN_POINT ( 'NONE',  ( 0.2819296736111110979, 5.002166666742532186, 0.1167790944451422425 ) ) ;
#9303=CARTESIAN_POINT ( 'NONE',  ( -0.1993543840281266355, 4.415361111186976828, 0.1993543840281267465 ) ) ;
#9304=CARTESIAN_POINT ( 'NONE',  ( 0.06953549797911996733, 3.740285477686101867, 0.3047298766157227612 ) ) ;
#9307=CARTESIAN_POINT ( 'NONE',  ( 0.3119999999999999996, 3.970916666818399055, 0.1292346314604056190 ) ) ;
#9308=CARTESIAN_POINT ( 'NONE',  ( 0.1993543840281266633, 4.457027777853643791, -0.1993543840281266910 ) ) ;
#9309=CARTESIAN_POINT ( 'NONE',  ( 0.3119999999999999996, 0.1291666666666663188, 0.000000000000000000 ) ) ;
#9312=ORIENTED_EDGE ( 'NONE', *, *, #8092, .T. ) ;
#9315=ORIENTED_EDGE ( 'NONE', *, *, #14190, .T. ) ;
#9318=CARTESIAN_POINT ( 'NONE',  ( -0.1099907963434661878, 4.846209151129420079, 0.2920362175865332532 ) ) ;
#9319=SPHERICAL_SURFACE ( 'NONE', #15903, 0.3119999999999999996 ) ;
#9321=CARTESIAN_POINT ( 'NONE',  ( -0.1292346314604056190, 0.5840277776260447418, -0.3119999999999999996 ) ) ;
#9324=CARTESIAN_POINT ( 'NONE',  ( -0.09421363705610538708, 3.713154806801743923, -0.2985087040289488014 ) ) ;
#9326=CARTESIAN_POINT ( 'NONE',  ( -0.1292346314604058410, 0.5006944444444441089, 0.3119999999999998885 ) ) ;
#9334=B_SPLINE_CURVE_WITH_KNOTS ( 'NONE', 3,
 ( #5281, #2976, #12749, #1510, #3331, #1269, #1023, #7122, #4794, #21629, #21987, #12624, #14075, #5036 ),
 .UNSPECIFIED., .F., .F.,
 ( 4, 2, 2, 2, 2, 2, 4 ),
 ( 0.002465611774710352224, 0.003521823575328993962, 0.004578035375947636133, 0.006690458977184919609, 0.007746670777803561780, 0.008802882578422202217, 0.01091530617965948656 ),
 .UNSPECIFIED. ) ;
#9335=CARTESIAN_POINT ( 'NONE',  ( -0.2819296736111110424, 4.293833333409199149, -0.1167790944451423119 ) ) ;
#9336=CARTESIAN_POINT ( 'NONE',  ( 0.1167790944451424506, 5.036888888964754507, 0.2819296736111110424 ) ) ;
#9339=CARTESIAN_POINT ( 'NONE',  ( 0.1292346314604056190, 3.922305555555555046, -0.3119999999999999996 ) ) ;
#9340=CARTESIAN_POINT ( 'NONE',  ( -0.2206173157302027676, 4.842444444596176290, 0.2206173157302028787 ) ) ;
#9341=CARTESIAN_POINT ( 'NONE',  ( 0.2852864521860641323, 4.804037699710621112, 0.1277937968658160450 ) ) ;
#9342=CARTESIAN_POINT ( 'NONE',  ( 0.1292346314604057300, 0.3965277777777774237, 0.3119999999999998885 ) ) ;
#9345=VECTOR ( 'NONE', #7846, 39.37007874015748143 ) ;
#9346=CARTESIAN_POINT ( 'NONE',  ( 0.2838164519978598754, 0.03466679542269811981, -0.01821027516514309857 ) ) ;
#9348=ORIENTED_EDGE ( 'NONE', *, *, #20795, .F. ) ;
#9350=CARTESIAN_POINT ( 'NONE',  ( -0.2819296736111110424, 5.189666666742532186, 0.1167790944451424923 ) ) ;
#9356=CARTESIAN_POINT ( 'NONE',  ( 0.1993543840281266910, 0.2229166665908000333, -0.1993543840281266910 ) ) ;
#9358=CARTESIAN_POINT ( 'NONE',  ( 0.1167790944451424368, 5.050777777853643791, 0.2819296736111110424 ) ) ;
#9359=CARTESIAN_POINT ( 'NONE',  ( 0.05463760851107932887, 4.486759113827675449, -0.3071788916223130439 ) ) ;
#9360=CARTESIAN_POINT ( 'NONE',  ( 0.1167790944451424368, 4.925777777853642903, 0.2819296736111110424 ) ) ;
#9364=CARTESIAN_POINT ( 'NONE',  ( 5.731347020009612645E-17, 4.897999999999998799, 0.3119999999999999996 ) ) ;
#9365=DIRECTION ( 'NONE',  ( 0.000000000000000000, 0.000000000000000000, -1.000000000000000000 ) ) ;
#9366=CARTESIAN_POINT ( 'NONE',  ( 0.3119999999999999996, 4.470916666666665762, -0.1292346314604056745 ) ) ;
#9368=CARTESIAN_POINT ( 'NONE',  ( -0.1993543840281266910, 3.845916666742532186, -0.1993543840281266910 ) ) ;
#9370=CARTESIAN_POINT ( 'NONE',  ( 0.1923084850919542510, 4.021960649823486555, 0.2457072462168881366 ) ) ;
#9374=CARTESIAN_POINT ( 'NONE',  ( -0.2935801054093536977, 4.116470801662853951, 0.1121277540818491902 ) ) ;
#9375=CARTESIAN_POINT ( 'NONE',  ( -3.990790521751304672E-07, 4.654944455680286808, -0.3119999999997447038 ) ) ;
#9383=ORIENTED_EDGE ( 'NONE', *, *, #8117, .F. ) ;
#9385=CARTESIAN_POINT ( 'NONE',  ( -0.2819296736111110979, 0.2888888888130223265, 0.1167790944451422425 ) ) ;
#9386=CARTESIAN_POINT ( 'NONE',  ( 0.2726250823473003182, 3.867817045068989934, -0.1571225677078837979 ) ) ;
#9388=CARTESIAN_POINT ( 'NONE',  ( -0.2206173157302027954, 0.1499999999999996336, -0.2206173157302028232 ) ) ;
#9390=CARTESIAN_POINT ( 'NONE',  ( -0.09984127256979968834, 5.094866437056988495, -0.2954929550594492249 ) ) ;
#9392=CARTESIAN_POINT ( 'NONE',  ( 1.910449006669871087E-17, 0.08749999999999966138, -0.3119999999999999996 ) ) ;
#9393=CARTESIAN_POINT ( 'NONE',  ( 0.1292346314604056190, 5.200083333333331836, -0.3119999999999999996 ) ) ;
#9395=CARTESIAN_POINT ( 'NONE',  ( 0.2819296736111110979, 4.172305555631421470, -3.452642723725051716E-17 ) ) ;
#9400=CARTESIAN_POINT ( 'NONE',  ( 0.1569501933412678629, 4.353958851224170701, 0.2727168492022662427 ) ) ;
#9401=CARTESIAN_POINT ( 'NONE',  ( 0.2819296736111110979, 4.936194444520309865, -3.452642723725051716E-17 ) ) ;
#9402=CARTESIAN_POINT ( 'NONE',  ( -0.2740592345421557496, 5.152155295800852741, -0.1267607899272875649 ) ) ;
#9403=CARTESIAN_POINT ( 'NONE',  ( 0.1711834221389471333, 3.705440968472438534, -0.2633095395294266505 ) ) ;
#9405=CARTESIAN_POINT ( 'NONE',  ( -0.2206173157302027676, 5.002166666666665762, 0.2206173157302028787 ) ) ;
#9406=CARTESIAN_POINT ( 'NONE',  ( 5.178964085587577574E-17, 4.644527777853642903, 0.2819296736111110979 ) ) ;
#9410=CARTESIAN_POINT ( 'NONE',  ( 0.2819296736111110424, 0.4972222221463556413, -0.1167790944451423119 ) ) ;
#9413=CARTESIAN_POINT ( 'NONE',  ( -0.1167790944451424368, 0.3097222221463556968, 0.2819296736111110424 ) ) ;
#9414=CARTESIAN_POINT ( 'NONE',  ( -0.1241992254576447796, 4.714064213952139148, -0.2879476753977870396 ) ) ;
#9420=CARTESIAN_POINT ( 'NONE',  ( 0.1167790944451423535, 0.3583333332574666907, 0.2819296736111110979 ) ) ;
#9422=CARTESIAN_POINT ( 'NONE',  ( -0.1167790944451423257, 4.189666666742533074, -0.2819296736111110424 ) ) ;
#9424=CARTESIAN_POINT ( 'NONE',  ( 0.1993543840281266633, 4.845916666742532186, -0.1993543840281266910 ) ) ;
#9425=CARTESIAN_POINT ( 'NONE',  ( 0.1993543840281266633, 4.498694444520309865, -0.1993543840281266910 ) ) ;
#9428=CARTESIAN_POINT ( 'NONE',  ( 0.2195291445273800934, 3.925916276105013480, -0.2262840060551973564 ) ) ;
#9430=CARTESIAN_POINT ( 'NONE',  ( 5.731347020009612645E-17, 4.127166666818398610, 0.3119999999999999996 ) ) ;
#9439=CARTESIAN_POINT ( 'NONE',  ( -0.1666460382175411203, 4.844395531962456758, 0.2656379378495577481 ) ) ;
#9441=VERTEX_POINT ( 'NONE', #2653 ) ;
#9442=CARTESIAN_POINT ( 'NONE',  ( -0.3119999999999999996, 0.4868055554038225874, 0.1292346314604056190 ) ) ;
#9445=CARTESIAN_POINT ( 'NONE',  ( 0.09335422435517687356, 4.763370768640803554, -0.2986308128854576194 ) ) ;
#9448=ORIENTED_EDGE ( 'NONE', *, *, #16907, .F. ) ;
#9451=LINE ( 'NONE', #22619, #11150 ) ;
#9452=CARTESIAN_POINT ( 'NONE',  ( -0.2740703737067639589, 4.673339054025664296, 0.1502709304893539988 ) ) ;
#9453=CARTESIAN_POINT ( 'NONE',  ( 0.1993543840281266633, 4.220916666742532186, -0.1993543840281266910 ) ) ;
#9454=DIRECTION ( 'NONE',  ( -0.000000000000000000, -1.000000000000000000, -0.000000000000000000 ) ) ;
#9457=CARTESIAN_POINT ( 'NONE',  ( 0.3119999999999999996, 3.800777777777776478, -3.820898013339742174E-17 ) ) ;
#9459=CARTESIAN_POINT ( 'NONE',  ( 0.3119999999999999996, 4.693138889040620931, 0.1292346314604056190 ) ) ;
#9461=CARTESIAN_POINT ( 'NONE',  ( 0.1167790944451424506, 5.106333333409199149, 0.2819296736111110424 ) ) ;
#9462=CARTESIAN_POINT ( 'NONE',  ( -5.731347020009612645E-17, 0.3930555555555551583, 0.3119999999999999996 ) ) ;
#9465=CARTESIAN_POINT ( 'NONE',  ( 1.791833110003796271E-17, 0.04312855400452411669, -0.2926285540045244216 ) ) ;
#9469=CARTESIAN_POINT ( 'NONE',  ( 0.2819296736111110979, 5.154944444520308977, 0.1167790944451422425 ) ) ;
#9470=CARTESIAN_POINT ( 'NONE',  ( -0.2819296736111110424, 3.759111111186976828, 0.1167790944451424923 ) ) ;
#9471=CARTESIAN_POINT ( 'NONE',  ( 0.000000000000000000, 5.384999999999999787, -0.3119999999999999996 ) ) ;
#9476=CARTESIAN_POINT ( 'NONE',  ( -0.1993543840281266633, 0.4034722221463555858, -0.1993543840281266910 ) ) ;
#9478=CARTESIAN_POINT ( 'NONE',  ( -0.1993543840281266355, 4.984805555631421470, 0.1993543840281267465 ) ) ;
#9480=CARTESIAN_POINT ( 'NONE',  ( 0.2819296736111110979, 4.880638888964754507, -3.452642723725051716E-17 ) ) ;
#9486=CARTESIAN_POINT ( 'NONE',  ( -0.3119999999999999996, 4.495222222222221120, 0.000000000000000000 ) ) ;
#9487=CARTESIAN_POINT ( 'NONE',  ( 0.1993543840281266633, 3.832027777853643791, -0.1993543840281266910 ) ) ;
#9490=CARTESIAN_POINT ( 'NONE',  ( -0.07694078045636083829, 3.736091107400131506, 0.3024941216908801911 ) ) ;
#9491=CARTESIAN_POINT ( 'NONE',  ( 0.3039870060688493192, 4.583505726166830385, 0.07103347446430215151 ) ) ;
#9496=CARTESIAN_POINT ( 'NONE',  ( 0.04861964814276396873, 4.653546418008869701, -0.3084262645696678740 ) ) ;
#9498=CARTESIAN_POINT ( 'NONE',  ( -0.001116513862715997783, 3.932753884148758594, -0.3119982877432843082 ) ) ;
#9499=CARTESIAN_POINT ( 'NONE',  ( 0.1797084794423411680, 3.735609856212664948, -0.2172307604343298448 ) ) ;
#9502=CARTESIAN_POINT ( 'NONE',  ( 0.2819296736111110424, 0.4833333332574667462, -0.1167790944451423119 ) ) ;
#9503=CARTESIAN_POINT ( 'NONE',  ( 0.1917372575570133186, 3.855115785418520513, 0.2494970157359910623 ) ) ;
#9509=CARTESIAN_POINT ( 'NONE',  ( 0.3120000000000000551, 4.352861111111110404, 0.1292346314604056190 ) ) ;
#9510=CARTESIAN_POINT ( 'NONE',  ( -0.3119999999999999996, 0.1604166666666663188, 0.1292346314604056190 ) ) ;
#9511=CARTESIAN_POINT ( 'NONE',  ( 0.3119999999999999996, 5.193138888888888083, -0.1292346314604056745 ) ) ;
#9512=B_SPLINE_CURVE_WITH_KNOTS ( 'NONE', 3,
 ( #9003, #92, #10964, #1802, #14498, #7179, #22287, #7420, #7059, #3391, #18389, #1684, #22045, #14621, #23858, #12684, #20102, #24109, #10843, #12805, #9247, #9119, #22165, #12932, #16447, #14750, #16688, #5341, #11081, #14871, #5581, #13047, #18272, #20224, #3514, #1924, #20463, #5466, #22406, #1568, #5707, #9370, #16811, #13170, #16567, #20342, #23989, #1447, #7301, #3630, #18510, #3760, #7536 ),
 .UNSPECIFIED., .F., .F.,
 ( 4, 2, 2, 2, 2, 2, 2, 2, 1, 1, 1, 2, 2, 2, 2, 2, 2, 2, 2, 2, 2, 2, 1, 1, 2, 2, 2, 2, 4 ),
 ( 0.7766889378257704202, 0.7778316968405288856, 0.7789744558552873510, 0.7801172148700458164, 0.7812599738848041708, 0.7824027328995626362, 0.7835454919143211017, 0.7838311816680106903, 0.7839026041064330874, 0.7839383153256442860, 0.7839561709352499408, 0.7839650987400527127, 0.7839740265448555956, 0.7841168714217005009, 0.7846882509290801222, 0.7858310099438394758, 0.7869737689585987184, 0.7881165279733580720, 0.7892592869881173145, 0.7904020460028766681, 0.7909734255102562894, 0.7911162703871011947, 0.7911876928255237029, 0.7912234040447349015, 0.7912412596543405563, 0.7912591152639461001, 0.7915448050176359107, 0.7926875640323953753, 0.7949730820619140825 ),
 .UNSPECIFIED. ) ;
#9513=CARTESIAN_POINT ( 'NONE',  ( 0.1993543840281267465, 4.109805555631421470, 0.1993543840281266633 ) ) ;
#9517=EDGE_CURVE ( 'NONE', #3616, #16166, #2301, .T. ) ;
#9518=CARTESIAN_POINT ( 'NONE',  ( -0.2819296736111110424, 4.904944444520310753, -0.1167790944451423119 ) ) ;
#9519=EDGE_CURVE ( 'NONE', #16287, #23361, #7424, .T. ) ;
#9520=DIRECTION ( 'NONE',  ( 8.659560562354904508E-17, 0.7071067811865497932, -0.7071067811865452413 ) ) ;
#9521=AXIS2_PLACEMENT_3D ( 'NONE', #8873, #4964, #6557 ) ;
#9524=DIRECTION ( 'NONE',  ( -0.000000000000000000, -1.000000000000000000, -0.000000000000000000 ) ) ;
#9526=CARTESIAN_POINT ( 'NONE',  ( -0.1993543840281266910, 4.623694444520309865, -0.1993543840281266910 ) ) ;
#9528=CARTESIAN_POINT ( 'NONE',  ( 0.2206173157302027954, 4.307722222222221120, -0.2206173157302028232 ) ) ;
#9530=CARTESIAN_POINT ( 'NONE',  ( 0.1167790944451423257, 0.4486111110352445364, -0.2819296736111110424 ) ) ;
#9532=CARTESIAN_POINT ( 'NONE',  ( 0.1993543840281266910, 0.3340277777019111660, -0.1993543840281266910 ) ) ;
#9539=CARTESIAN_POINT ( 'NONE',  ( -0.1993543840281266633, 0.1673611110352444808, -0.1993543840281266910 ) ) ;
#9540=CARTESIAN_POINT ( 'NONE',  ( 0.2819296736111110979, 0.2020833332574666907, 0.000000000000000000 ) ) ;
#9541=CARTESIAN_POINT ( 'NONE',  ( 5.178964085587577574E-17, 4.269527777853643791, 0.2819296736111110979 ) ) ;
#9544=CARTESIAN_POINT ( 'NONE',  ( 5.178964085587577574E-17, 4.936194444520309865, 0.2819296736111110979 ) ) ;
#9546=CARTESIAN_POINT ( 'NONE',  ( 0.1993543840281266633, 4.387583333409199149, -0.1993543840281266910 ) ) ;
#9547=CARTESIAN_POINT ( 'NONE',  ( 0.1988756632394131918, 3.704359868413474199, -0.2404006459456452249 ) ) ;
#9548=VERTEX_POINT ( 'NONE', #4950 ) ;
#9549=CARTESIAN_POINT ( 'NONE',  ( 5.463034709641816805E-17, 5.167344860100310910, 0.2973937581265823082 ) ) ;
#9550=CARTESIAN_POINT ( 'NONE',  ( 0.1292346314604058410, 4.186194444596176290, 0.3119999999999998885 ) ) ;
#9552=CARTESIAN_POINT ( 'NONE',  ( -5.731347020009612645E-17, 0.1152777777777774515, 0.3119999999999999996 ) ) ;
#9556=VECTOR ( 'NONE', #11211, 39.37007874015748143 ) ;
#9557=CARTESIAN_POINT ( 'NONE',  ( -0.08048290441869994372, 4.847107040683704682, 0.3016807249711052075 ) ) ;
#9559=EDGE_CURVE ( 'NONE', #3584, #5059, #8728, .T. ) ;
#9561=CARTESIAN_POINT ( 'NONE',  ( -0.3119999999999999996, 0.5354166665149336923, -0.1292346314604056745 ) ) ;
#9562=VERTEX_POINT ( 'NONE', #12537 ) ;
#9567=DIRECTION ( 'NONE',  ( -0.000000000000000000, -1.000000000000000000, -0.000000000000000000 ) ) ;
#9574=CARTESIAN_POINT ( 'NONE',  ( 0.2819296736111110979, 4.043833333409200037, 0.1167790944451422425 ) ) ;
#9577=CARTESIAN_POINT ( 'NONE',  ( -0.1292346314604057023, 3.783416666666665762, 0.3119999999999998885 ) ) ;
#9578=CARTESIAN_POINT ( 'NONE',  ( 0.3119999999999999996, 4.811194444596175401, -0.1292346314604056745 ) ) ;
#9580=CARTESIAN_POINT ( 'NONE',  ( -0.1993543840281266355, 4.984805555631421470, 0.1993543840281267465 ) ) ;
#9582=CARTESIAN_POINT ( 'NONE',  ( -0.1167790944451423257, 4.286888888964754507, -0.2819296736111110424 ) ) ;
#9583=CARTESIAN_POINT ( 'NONE',  ( 1.910449006669871087E-17, 0.4208333333333330040, -0.3119999999999999996 ) ) ;
#9588=SHAPE_DEFINITION_REPRESENTATION ( #15937, #7952 ) ;
#9589=VERTEX_POINT ( 'NONE', #3129 ) ;
#9591=CARTESIAN_POINT ( 'NONE',  ( 0.1993543840281266633, 5.220916666742532186, -0.1993543840281266910 ) ) ;
#9592=CARTESIAN_POINT ( 'NONE',  ( -0.1993543840281266355, 3.873694444520310309, 0.1993543840281267465 ) ) ;
#9593=VECTOR ( 'NONE', #10101, 39.37007874015748143 ) ;
#9596=EDGE_LOOP ( 'NONE', ( #12659, #13850, #22248, #13532, #6169, #14546, #22327, #15904, #716, #14084, #9383, #9704, #16896, #23974, #7329, #2380, #11541, #3434, #15726, #5387, #702, #2299, #484, #5289, #23906, #4118, #5069, #5850, #1156, #7257, #1955, #12012, #259, #19843, #4546, #17453, #4189, #6247, #11044, #12581, #8337, #2911, #5684, #4124, #23299, #94, #1086, #21373, #18501, #14163, #19887, #22712, #3461, #1030, #20215, #3836, #10796, #17295, #7728 ) ) ;
#9598=CARTESIAN_POINT ( 'NONE',  ( 0.2819296736111110424, 0.6013888888130223265, 0.1167790944451424923 ) ) ;
#9600=CARTESIAN_POINT ( 'NONE',  ( 0.1993543840281266633, 4.845916666742532186, -0.1993543840281266910 ) ) ;
#9603=CARTESIAN_POINT ( 'NONE',  ( -0.2819296736111110424, 4.571611111186975940, -0.1167790944451423119 ) ) ;
#9605=CARTESIAN_POINT ( 'NONE',  ( 0.3141651762424315653, 4.863855663901686555, -0.02248318143069297226 ) ) ;
#9609=CARTESIAN_POINT ( 'NONE',  ( -0.3119999999999999996, 4.550777777777777366, 0.000000000000000000 ) ) ;
#9610=CARTESIAN_POINT ( 'NONE',  ( -0.2819296736111110979, 3.849388888964754507, -0.1167790944451422980 ) ) ;
#9612=CARTESIAN_POINT ( 'NONE',  ( 0.05926878199548974574, 4.986570782386274381, -0.3065401363359365750 ) ) ;
#9613=ORIENTED_EDGE ( 'NONE', *, *, #6441, .F. ) ;
#9620=CARTESIAN_POINT ( 'NONE',  ( -0.0001593111292714336792, 3.932726740070024540, -0.3119999695236226889 ) ) ;
#9621=CARTESIAN_POINT ( 'NONE',  ( 0.2876526673451095251, 5.142634612739459321, 0.1007097082411073097 ) ) ;
#9624=CARTESIAN_POINT ( 'NONE',  ( -0.1167790944451424368, 0.5180555554796888451, 0.2819296736111110424 ) ) ;
#9632=( BOUNDED_CURVE ( )  B_SPLINE_CURVE ( 2, ( #9004, #9248, #6935, #24110, #5467, #7302, #5212, #4972, #11082 ),
 .UNSPECIFIED., .F., .T. ) 
 B_SPLINE_CURVE_WITH_KNOTS ( ( 3, 2, 2, 2, 3 ),
 ( 0.5446428571428569843, 0.5491071428571427937, 0.5535714285714284921, 0.5580357142857141906, 0.5624999999999998890 ),
 .UNSPECIFIED. ) 
 CURVE ( )  GEOMETRIC_REPRESENTATION_ITEM ( )  RATIONAL_B_SPLINE_CURVE ( ( 1.000000000000001998, 0.9238795325112848511, 1.000000000000000000, 0.9238795325112867385, 1.000000000000000000, 0.9238795325112867385, 1.000000000000000000, 0.9238795325112886259, 0.9999999999999981126 ) ) 
 REPRESENTATION_ITEM ( '' )  );
#9634=CARTESIAN_POINT ( 'NONE',  ( -0.2206173157302027954, 0.2055555555555551861, -0.2206173157302028232 ) ) ;
#9635=CARTESIAN_POINT ( 'NONE',  ( 0.3119999999999999996, 5.134111111111110404, -3.820898013339742174E-17 ) ) ;
#9636=CARTESIAN_POINT ( 'NONE',  ( 0.2819296736111110424, 4.175777777853643791, -0.1167790944451423396 ) ) ;
#9640=CARTESIAN_POINT ( 'NONE',  ( 0.1292346314604057300, 0.3409722222222218435, 0.3119999999999998885 ) ) ;
#9641=CARTESIAN_POINT ( 'NONE',  ( 0.2819296736111110979, 4.880638888964754507, -3.452642723725051716E-17 ) ) ;
#9643=CARTESIAN_POINT ( 'NONE',  ( -0.2984124910806962849, 5.154444156555171297, -0.04193874527002016545 ) ) ;
#9644=AXIS2_PLACEMENT_3D ( 'NONE', #19223, #9854, #87 ) ;
#9648=CARTESIAN_POINT ( 'NONE',  ( -0.2819296736111110979, 4.255638888964754507, 0.000000000000000000 ) ) ;
#9650=CARTESIAN_POINT ( 'NONE',  ( 1.726321361862525858E-17, 0.6187499999241333759, -0.2819296736111110979 ) ) ;
#9652=CARTESIAN_POINT ( 'NONE',  ( -5.178964085587577574E-17, 0.4243055554796889006, 0.2819296736111110979 ) ) ;
#9653=ORIENTED_EDGE ( 'NONE', *, *, #22778, .F. ) ;
#9654=CARTESIAN_POINT ( 'NONE',  ( 0.2819296736111110979, 0.4381944443685778512, 0.000000000000000000 ) ) ;
#9655=DIRECTION ( 'NONE',  ( 0.000000000000000000, 0.000000000000000000, -1.000000000000000000 ) ) ;
#9656=DIRECTION ( 'NONE',  ( 0.000000000000000000, 0.000000000000000000, -1.000000000000000000 ) ) ;
#9662=CARTESIAN_POINT ( 'NONE',  ( -5.178964085587577574E-17, 0.5770833332574667462, 0.2819296736111110979 ) ) ;
#9663=CARTESIAN_POINT ( 'NONE',  ( 1.726321361862525858E-17, 0.3270833332574666907, -0.2819296736111110979 ) ) ;
#9664=CARTESIAN_POINT ( 'NONE',  ( -0.2819296736111110424, 4.314666666742533074, 0.1167790944451424923 ) ) ;
#9667=CARTESIAN_POINT ( 'NONE',  ( 0.2819296736111110979, 4.891055555631421470, 0.1167790944451422425 ) ) ;
#9668=CARTESIAN_POINT ( 'NONE',  ( -0.2819296736111110424, 4.523000000075865223, 0.1167790944451424923 ) ) ;
#9670=VERTEX_POINT ( 'NONE', #1900 ) ;
#9672=CARTESIAN_POINT ( 'NONE',  ( 5.731347020009612645E-17, 4.016055555707287006, 0.3119999999999999996 ) ) ;
#9681=CARTESIAN_POINT ( 'NONE',  ( -0.2969134259396885023, 5.005069796490948519, 0.09796392844229065422 ) ) ;
#9683=CARTESIAN_POINT ( 'NONE',  ( 0.3119999999999998885, 0.3965277776260449083, 0.1292346314604058410 ) ) ;
#9684=EDGE_LOOP ( 'NONE', ( #11767, #12487, #1603, #14793, #17991 ) ) ;
#9685=CARTESIAN_POINT ( 'NONE',  ( 0.0002138672942954442330, 4.266049809204471188, -0.3119999314205446073 ) ) ;
#9689=CARTESIAN_POINT ( 'NONE',  ( 0.01934007716052928150, 5.189873518840629529, -0.2887964054786675283 ) ) ;
#9694=CARTESIAN_POINT ( 'NONE',  ( -0.2368270405986217797, 4.675129404167337022, 0.2031599927639998471 ) ) ;
#9695=CARTESIAN_POINT ( 'NONE',  ( -0.1993543840281266910, 3.901472222298087544, -0.1993543840281266910 ) ) ;
#9698=CARTESIAN_POINT ( 'NONE',  ( -0.3119999999999998885, 3.887583333333333613, 0.1292346314604058410 ) ) ;
#9699=AXIS2_PLACEMENT_3D ( 'NONE', #14791, #3800, #3553 ) ;
#9700=CARTESIAN_POINT ( 'NONE',  ( -0.2206173157302028232, 4.828555555707287894, -0.2206173157302028232 ) ) ;
#9701=CARTESIAN_POINT ( 'NONE',  ( -0.2819296736111110424, 5.036888888964754507, 0.1167790944451424923 ) ) ;
#9703=CARTESIAN_POINT ( 'NONE',  ( 0.2819296736111110979, 4.321611111186976828, 0.1167790944451422425 ) ) ;
#9704=ORIENTED_EDGE ( 'NONE', *, *, #22341, .F. ) ;
#9710=PRODUCT_DEFINITION ( 'UNKNOWN', '', #7598, #4357 ) ;
#9713=CARTESIAN_POINT ( 'NONE',  ( 0.2819296736111110979, 3.894527777853643347, -3.452642723725051716E-17 ) ) ;
#9715=CARTESIAN_POINT ( 'NONE',  ( 0.08062935572735190071, 4.430412084064282219, -0.3015737216022094658 ) ) ;
#9716=CARTESIAN_POINT ( 'NONE',  ( 5.731347020009612645E-17, 4.953555555555554157, 0.3119999999999999996 ) ) ;
#9719=CARTESIAN_POINT ( 'NONE',  ( 0.2819296736111110424, 0.5458333332574668573, 0.1167790944451424923 ) ) ;
#9721=ORIENTED_EDGE ( 'NONE', *, *, #2323, .T. ) ;
#9722=CARTESIAN_POINT ( 'NONE',  ( 0.1167790944451422702, 4.682722222298088433, -0.2819296736111110424 ) ) ;
#9724=CARTESIAN_POINT ( 'NONE',  ( 0.2819296736111110979, 4.602861111186975940, -3.452642723725051716E-17 ) ) ;
#9726=CARTESIAN_POINT ( 'NONE',  ( 0.2113513854172701378, 4.855985392576767978, 0.2295112932090857261 ) ) ;
#9729=CARTESIAN_POINT ( 'NONE',  ( -1.910449006669871087E-17, 4.592444444444443441, -0.3119999999999999996 ) ) ;
#9730=CARTESIAN_POINT ( 'NONE',  ( -0.1167790944451423119, 3.731333333409198705, -0.2819296736111110979 ) ) ;
#9735=CARTESIAN_POINT ( 'NONE',  ( -0.2206173157302028232, 4.543833333333332725, -0.2206173157302028232 ) ) ;
#9738=CARTESIAN_POINT ( 'NONE',  ( 0.3121158769751342099, 4.697706800928946436, -0.04006652453352290560 ) ) ;
#9740=EDGE_CURVE ( 'NONE', #11982, #11875, #8052, .T. ) ;
#9741=CARTESIAN_POINT ( 'NONE',  ( 0.3088258284620388205, 4.642689360785702490, -0.05851397011192863151 ) ) ;
#9743=CARTESIAN_POINT ( 'NONE',  ( -0.0001528158053696555070, 3.932726555878094388, -0.3120000002100443703 ) ) ;
#9744=ORIENTED_EDGE ( 'NONE', *, *, #13372, .T. ) ;
#9746=CARTESIAN_POINT ( 'NONE',  ( -0.2819296736111110979, 0.5111111110352446474, 0.1167790944451422425 ) ) ;
#9751=CARTESIAN_POINT ( 'NONE',  ( -0.01019282354824687341, 5.118057215992540598, 0.3087295155953159731 ) ) ;
#9754=CARTESIAN_POINT ( 'NONE',  ( -0.1292346314604058410, 0.2784722222222218990, 0.3119999999999998885 ) ) ;
#9755=CARTESIAN_POINT ( 'NONE',  ( -0.3119999999999998885, 5.165361111111110404, 0.1292346314604058410 ) ) ;
#9756=CARTESIAN_POINT ( 'NONE',  ( -1.726321361862525858E-17, 4.130638888964754507, -0.2819296736111110979 ) ) ;
#9757=CARTESIAN_POINT ( 'NONE',  ( -0.3120221670779859680, 4.334383852034481954, -0.04068519730541640678 ) ) ;
#9762=EDGE_CURVE ( 'NONE', #2014, #2791, #12699, .T. ) ;
#9763=CARTESIAN_POINT ( 'NONE',  ( 0.2206173157302028232, 0.3583333333333329485, -0.2206173157302028232 ) ) ;
#9764=CARTESIAN_POINT ( 'NONE',  ( 0.1993543840281266633, 4.832027777853643791, -0.1993543840281266910 ) ) ;
#9767=CARTESIAN_POINT ( 'NONE',  ( -0.02743319922242961131, 4.515305058140716810, 0.3107919259431392578 ) ) ;
#9773=CARTESIAN_POINT ( 'NONE',  ( -0.1993543840281266355, 4.207027777853643791, 0.1993543840281267465 ) ) ;
#9775=CARTESIAN_POINT ( 'NONE',  ( -0.001030184878490023525, 4.043861028467455654, -0.3119985433042023470 ) ) ;
#9778=( BOUNDED_CURVE ( )  B_SPLINE_CURVE ( 1, ( #1382, #10895 ),
 .UNSPECIFIED., .F., .F. ) 
 B_SPLINE_CURVE_WITH_KNOTS ( ( 2, 2 ),
 ( 0.000000000000000000, 1.000000000000000000 ),
 .UNSPECIFIED. ) 
 CURVE ( )  GEOMETRIC_REPRESENTATION_ITEM ( )  RATIONAL_B_SPLINE_CURVE ( ( 0.9836822358325096882, 0.9836822358325096882 ) ) 
 REPRESENTATION_ITEM ( '' )  );
#9781=CARTESIAN_POINT ( 'NONE',  ( 1.726321361862525858E-17, 0.3965277777019111105, -0.2819296736111110979 ) ) ;
#9783=FACE_OUTER_BOUND ( 'NONE', #8715, .T. ) ;
#9786=CARTESIAN_POINT ( 'NONE',  ( 0.000000000000000000, 5.384999999999999787, -0.3119999999999999996 ) ) ;
#9790=CARTESIAN_POINT ( 'NONE',  ( -0.2819296736111111534, 0.5666666665908000056, 0.1167790944451422563 ) ) ;
#9791=CARTESIAN_POINT ( 'NONE',  ( -0.2819296736111110424, 0.1708333332574666907, -0.1167790944451423396 ) ) ;
#9793=CARTESIAN_POINT ( 'NONE',  ( 0.2819296736111110424, 4.398000000075866112, -0.1167790944451423396 ) ) ;
#9795=CARTESIAN_POINT ( 'NONE',  ( -0.1993543840281266910, 4.804250000075865223, -0.1993543840281266910 ) ) ;
#9796=CARTESIAN_POINT ( 'NONE',  ( 0.1167790944451422702, 4.224388888964755395, -0.2819296736111110979 ) ) ;
#9800=CARTESIAN_POINT ( 'NONE',  ( -0.3119999999999998885, 3.783416666818399499, 0.1292346314604058410 ) ) ;
#9804=B_SPLINE_CURVE_WITH_KNOTS ( 'NONE', 3,
 ( #662, #5789, #15543, #22966, #4435, #20670, #18840, #2136, #17008, #13365, #13959, #21269, #17977, #23200, #12503, #17727, #16022, #2734, #15896, #21627, #10431, #23559, #5035, #10543, #10062, #17855, #6749, #10185, #19554, #23439, #4920, #2845, #23318, #14194, #21503, #8331, #1022, #1268, #12384, #8585, #1146, #17609, #6511 ),
 .UNSPECIFIED., .F., .F.,
 ( 4, 2, 2, 2, 2, 2, 2, 2, 2, 2, 1, 1, 1, 2, 2, 2, 2, 2, 2, 2, 2, 2, 4 ),
 ( 0.1187879011222644082, 0.1199322595034874733, 0.1210766178847105384, 0.1222209762659336035, 0.1233653346471566686, 0.1245096930283797476, 0.1250818722189912802, 0.1253679618142970464, 0.1253858424140036620, 0.1253947827138569560, 0.1254037230137102499, 0.1254394842131234811, 0.1255110066119499157, 0.1256540514096028127, 0.1279427681720490539, 0.1302314849344952952, 0.1325202016969415364, 0.1348089184593877776, 0.1359532768406108982, 0.1360963216382637953, 0.1362393664359166645, 0.1365254560312224585, 0.1370976352218340188 ),
 .UNSPECIFIED. ) ;
#9809=CARTESIAN_POINT ( 'NONE',  ( -0.1993543840281266633, 0.01458333325746670114, -0.1993543840281266910 ) ) ;
#9810=ORIENTED_EDGE ( 'NONE', *, *, #828, .F. ) ;
#9811=CARTESIAN_POINT ( 'NONE',  ( 0.02913558044229962174, 4.265265441289421311, -0.3107272591473340118 ) ) ;
#9813=CARTESIAN_POINT ( 'NONE',  ( -0.1292346314604058410, 0.5562499999999995781, 0.3119999999999998885 ) ) ;
#9819=CARTESIAN_POINT ( 'NONE',  ( -0.3119999999999999996, 4.050777777777777366, 0.000000000000000000 ) ) ;
#9820=CARTESIAN_POINT ( 'NONE',  ( -0.2819296736111110979, 4.019527777853642903, 0.000000000000000000 ) ) ;
#9824=CARTESIAN_POINT ( 'NONE',  ( 5.731347020009612645E-17, 4.738277777929510215, 0.3119999999999999996 ) ) ;
#9825=CARTESIAN_POINT ( 'NONE',  ( 0.1167790944451422702, 4.960500000075865223, -0.2819296736111110979 ) ) ;
#9827=CARTESIAN_POINT ( 'NONE',  ( -0.2819296736111110424, 4.293833333409199149, -0.1167790944451423119 ) ) ;
#9829=EDGE_CURVE ( 'NONE', #19258, #10504, #9778, .T. ) ;
#9831=EDGE_CURVE ( 'NONE', #21366, #11205, #10779, .T. ) ;
#9836=CARTESIAN_POINT ( 'NONE',  ( 0.3119999999999999996, 0.2958333333333329485, 0.000000000000000000 ) ) ;
#9838=CARTESIAN_POINT ( 'NONE',  ( -0.2819296736111110979, 3.863277777853644235, -0.1167790944451422980 ) ) ;
#9839=CARTESIAN_POINT ( 'NONE',  ( 0.1134877939392910096, 4.429446129279178912, -0.2906335559990496642 ) ) ;
#9842=VERTEX_POINT ( 'NONE', #21977 ) ;
#9844=CARTESIAN_POINT ( 'NONE',  ( 0.1993543840281266910, 0.5006944443685779067, -0.1993543840281266910 ) ) ;
#9846=ORIENTED_EDGE ( 'NONE', *, *, #10241, .T. ) ;
#9847=CARTESIAN_POINT ( 'NONE',  ( -0.2819296736111110979, 4.700083333409199149, 0.000000000000000000 ) ) ;
#9848=CARTESIAN_POINT ( 'NONE',  ( -0.3119999999999999996, 3.936194444444443885, -0.1292346314604056468 ) ) ;
#9850=CARTESIAN_POINT ( 'NONE',  ( -1.726321361862525858E-17, 4.727861111186976828, -0.2819296736111110979 ) ) ;
#9853=CYLINDRICAL_SURFACE ( 'NONE', #5932, 0.3119999999999999996 ) ;
#9854=DIRECTION ( 'NONE',  ( -0.000000000000000000, -1.000000000000000000, -0.000000000000000000 ) ) ;
#9855=CARTESIAN_POINT ( 'NONE',  ( 0.1292346314604056190, 4.255638888888888083, -0.3119999999999999996 ) ) ;
#9857=CARTESIAN_POINT ( 'NONE',  ( -0.1292346314604056190, 0.5284722220704892726, -0.3119999999999999996 ) ) ;
#9860=CARTESIAN_POINT ( 'NONE',  ( 0.3108174967125439392, 4.584757462357911706, 0.02714687810677645849 ) ) ;
#9862=CARTESIAN_POINT ( 'NONE',  ( 0.07869576298431067707, 4.684959685628617976, 0.3026069602474616982 ) ) ;
#9870=CARTESIAN_POINT ( 'NONE',  ( -0.1993543840281267465, 0.4590277777019111105, 0.1993543840281266633 ) ) ;
#9873=CARTESIAN_POINT ( 'NONE',  ( 1.910449006669871087E-17, 0.5319444444444439979, -0.3119999999999999996 ) ) ;
#9876=CARTESIAN_POINT ( 'NONE',  ( 0.000000000000000000, 5.384999999999999787, -0.3119999999999999996 ) ) ;
#9878=CARTESIAN_POINT ( 'NONE',  ( -0.3119999999999999996, 0.2715277777777774793, 0.1292346314604056190 ) ) ;
#9879=CARTESIAN_POINT ( 'NONE',  ( 0.1292346314604056190, 4.866749999999999687, -0.3119999999999999996 ) ) ;
#9882=CARTESIAN_POINT ( 'NONE',  ( -0.1167790944451423257, 4.189666666742533074, -0.2819296736111110424 ) ) ;
#9887=FACE_OUTER_BOUND ( 'NONE', #17223, .T. ) ;
#9888=CARTESIAN_POINT ( 'NONE',  ( 5.178964085587577574E-17, 4.755638888964754507, 0.2819296736111110979 ) ) ;
#9890=CARTESIAN_POINT ( 'NONE',  ( -0.05588801071484209709, 4.514508298373136164, 0.3071457712218207403 ) ) ;
#9892=FACE_OUTER_BOUND ( 'NONE', #1758, .T. ) ;
#9893=CARTESIAN_POINT ( 'NONE',  ( 0.1167790944451424506, 4.273000000075865223, 0.2819296736111110424 ) ) ;
#9896=CARTESIAN_POINT ( 'NONE',  ( -0.2983136309931767038, 4.055085950308684239, -0.09350340892401856618 ) ) ;
#9899=CARTESIAN_POINT ( 'NONE',  ( -0.2819296736111110979, 0.3548611110352445364, -3.452642723725051716E-17 ) ) ;
#9902=DIRECTION ( 'NONE',  ( -0.000000000000000000, -1.000000000000000000, -0.000000000000000000 ) ) ;
#9905=CARTESIAN_POINT ( 'NONE',  ( 0.3119999999999999996, 5.022999999999999687, -3.820898013339742174E-17 ) ) ;
#9906=CARTESIAN_POINT ( 'NONE',  ( 1.726321361862525858E-17, 0.5493055554796888451, -0.2819296736111110979 ) ) ;
#9907=CARTESIAN_POINT ( 'NONE',  ( 0.1167790944451423535, 0.1916666665908000333, 0.2819296736111110424 ) ) ;
#9908=CARTESIAN_POINT ( 'NONE',  ( 5.178964085587577574E-17, 4.213972222298087544, 0.2819296736111110979 ) ) ;
#9911=CARTESIAN_POINT ( 'NONE',  ( -0.2819296736111110424, 4.870222222298087544, 0.1167790944451424923 ) ) ;
#9914=CARTESIAN_POINT ( 'NONE',  ( 0.1292346314604095325, 4.512583333333333613, 0.3119999999999962248 ) ) ;
#9915=CARTESIAN_POINT ( 'NONE',  ( 0.2206173157302027954, 3.759111111262843696, -0.2206173157302028232 ) ) ;
#9917=CARTESIAN_POINT ( 'NONE',  ( -1.910449006669871087E-17, 4.759111111111110404, -0.3119999999999999996 ) ) ;
#9920=( BOUNDED_CURVE ( )  B_SPLINE_CURVE ( 2, ( #2097, #7825, #20988, #11739, #9905, #3810, #630, #13453, #4165 ),
 .UNSPECIFIED., .F., .T. ) 
 B_SPLINE_CURVE_WITH_KNOTS ( ( 3, 2, 2, 2, 3 ),
 ( 0.1517857142857139685, 0.1562499999999997780, 0.1607142857142855874, 0.1651785714285713969, 0.1696428571428572063 ),
 .UNSPECIFIED. ) 
 CURVE ( )  GEOMETRIC_REPRESENTATION_ITEM ( )  RATIONAL_B_SPLINE_CURVE ( ( 1.000000000000005107, 0.9238795325112815204, 1.000000000000000000, 0.9238795325112867385, 1.000000000000000000, 0.9238795325112867385, 1.000000000000000000, 0.9238795325112857393, 1.000000000000000888 ) ) 
 REPRESENTATION_ITEM ( '' )  );
#9927=CARTESIAN_POINT ( 'NONE',  ( -0.2819296736111110424, 0.1847222221463555858, -0.1167790944451423396 ) ) ;
#9930=VERTEX_POINT ( 'NONE', #5637 ) ;
#9931=CARTESIAN_POINT ( 'NONE',  ( 0.0001053197333313014172, 4.266052725934510903, -0.3119999869445473362 ) ) ;
#9932=CARTESIAN_POINT ( 'NONE',  ( -1.910449006669871087E-17, 4.647999999999998799, -0.3119999999999999996 ) ) ;
#9935=CARTESIAN_POINT ( 'NONE',  ( 0.1304432934080578810, 5.186978988233328813, -0.2602171520964869922 ) ) ;
#9936=ORIENTED_EDGE ( 'NONE', *, *, #2323, .F. ) ;
#9938=CARTESIAN_POINT ( 'NONE',  ( -0.1552113907098449930, 4.678091210889574469, 0.2737309952764502285 ) ) ;
#9940=CARTESIAN_POINT ( 'NONE',  ( -0.2819296736111110424, 4.016055555631421470, -0.1167790944451423119 ) ) ;
#9941=CARTESIAN_POINT ( 'NONE',  ( -0.01607592287031538517, 0.03839369622198421372, 0.2878936962219845741 ) ) ;
#9944=CARTESIAN_POINT ( 'NONE',  ( 0.3119999999999999996, 4.477861111262843252, -0.1292346314604056745 ) ) ;
#9945=CARTESIAN_POINT ( 'NONE',  ( -0.2819296736111110979, 4.866750000075866112, 0.000000000000000000 ) ) ;
#9947=CARTESIAN_POINT ( 'NONE',  ( -0.1993543840281266355, 4.026472222298087544, 0.1993543840281267465 ) ) ;
#9952=ORIENTED_EDGE ( 'NONE', *, *, #11865, .F. ) ;
#9958=CARTESIAN_POINT ( 'NONE',  ( 0.2206173157302028232, 0.1291666665149337201, -0.2206173157302028232 ) ) ;
#9961=CARTESIAN_POINT ( 'NONE',  ( -0.1292346314604112256, 4.929250000000000576, -0.3119999999999945040 ) ) ;
#9963=CARTESIAN_POINT ( 'NONE',  ( -0.2819296736111110979, 0.5770833332574666352, -3.452642723725051716E-17 ) ) ;
#9965=EDGE_CURVE ( 'NONE', #8097, #11233, #9920, .T. ) ;
#9967=CARTESIAN_POINT ( 'NONE',  ( -0.2819296736111110424, 4.807722222298088433, -0.1167790944451423119 ) ) ;
#9969=VECTOR ( 'NONE', #21469, 39.37007874015748143 ) ;
#9971=CARTESIAN_POINT ( 'NONE',  ( 0.2819296736111110979, 4.713972222298087544, -3.452642723725051716E-17 ) ) ;
#9972=CARTESIAN_POINT ( 'NONE',  ( -0.004450248486120969398, 4.155072206286953396, -0.3119727959386125460 ) ) ;
#9976=CARTESIAN_POINT ( 'NONE',  ( 0.2206173157302028787, 4.238277777777777366, 0.2206173157302027954 ) ) ;
#9977=B_SPLINE_CURVE_WITH_KNOTS ( 'NONE', 3,
 ( #5131, #5252, #8921, #5375, #12723, #18426, #20262, #16244, #12596, #14536, #10759, #14291, #1244, #1363, #16121, #6728, #23655, #10635, #21841, #20016, #18189, #20138, #16364, #21728, #3303, #23895, #3428, #10879, #18308, #22079, #1606, #21602, #9040, #9158, #23774, #3547, #14171, #16485, #12841, #10999, #7213, #4896, #1719, #8669, #23417, #12358, #19777, #3073, #23535, #6851, #12475, #19896, #3186, #13315, #20614, #20734, #3912, #4028, #15019 ),
 .UNSPECIFIED., .F., .F.,
 ( 4, 2, 1, 1, 1, 1, 1, 2, 2, 2, 2, 2, 2, 2, 2, 1, 2, 2, 2, 2, 2, 2, 2, 2, 2, 1, 2, 2, 1, 1, 2, 2, 2, 4 ),
 ( 0.6670385189161691653, 0.6670429817324019517, 0.6670474445486348491, 0.6670563701811004220, 0.6670742214460316788, 0.6671099239758941923, 0.6671813290356192194, 0.6673241391550693846, 0.6676097593939694930, 0.6681809998717698207, 0.6693234808273704761, 0.6704659617829711316, 0.6716084427385717870, 0.6718940629774720064, 0.6719654680371970334, 0.6720368730969220605, 0.6721796832163722257, 0.6727509236941725534, 0.6738934046497732089, 0.6750358856053739753, 0.6761783665609747418, 0.6773208475165753972, 0.6784633284721761637, 0.6790345689499764914, 0.6793201891888767108, 0.6793915942486017379, 0.6794094455135329946, 0.6794183711459985675, 0.6794272967784642514, 0.6794629993083267649, 0.6796058094277768191, 0.6807482903833775856, 0.6830332522945791185, 0.6853182142057806514 ),
 .UNSPECIFIED. ) ;
#9978=CARTESIAN_POINT ( 'NONE',  ( -0.3119999999999999996, 5.165361111262843252, -0.1292346314604056468 ) ) ;
#9979=CARTESIAN_POINT ( 'NONE',  ( -1.910449006669871087E-17, 3.981333333333332725, -0.3119999999999999996 ) ) ;
#9981=VERTEX_POINT ( 'NONE', #19047 ) ;
#9985=AXIS2_PLACEMENT_3D ( 'NONE', #10046, #762, #10285 ) ;
#9988=CARTESIAN_POINT ( 'NONE',  ( 0.1978063296366817103, 4.133267444897331444, 0.2413868729338500829 ) ) ;
#9990=CARTESIAN_POINT ( 'NONE',  ( -0.002233241627982304571, 3.932785552190646516, -0.3119931493891720531 ) ) ;
#9993=CARTESIAN_POINT ( 'NONE',  ( 0.1167790944451423257, 0.3791666665908000611, -0.2819296736111110424 ) ) ;
#10000=CARTESIAN_POINT ( 'NONE',  ( -0.1765272216824294027, 4.621815342127092663, 0.2574651026513284924 ) ) ;
#10002=CARTESIAN_POINT ( 'NONE',  ( 5.731347020009612645E-17, 4.731333333333332725, 0.3119999999999999996 ) ) ;
#10003=CARTESIAN_POINT ( 'NONE',  ( 0.3119999999999999996, 0.1847222222222218990, 0.000000000000000000 ) ) ;
#10004=CARTESIAN_POINT ( 'NONE',  ( -0.3119999999999999996, 4.991749999999999687, -0.1292346314604056468 ) ) ;
#10006=CARTESIAN_POINT ( 'NONE',  ( -0.2819296736111110979, 3.922305555631421914, 0.000000000000000000 ) ) ;
#10009=CARTESIAN_POINT ( 'NONE',  ( 0.3117612485122355781, 4.807384657386537086, 0.01257049743255786618 ) ) ;
#10010=ORIENTED_EDGE ( 'NONE', *, *, #34, .F. ) ;
#10011=CYLINDRICAL_SURFACE ( 'NONE', #20239, 0.3119999999999999996 ) ;
#10012=CARTESIAN_POINT ( 'NONE',  ( 0.2819296736111110979, 4.658416666742532186, -3.452642723725051716E-17 ) ) ;
#10015=CARTESIAN_POINT ( 'NONE',  ( -0.1834827640909514057, 5.162357905306088846, 0.2362001855642932580 ) ) ;
#10020=CARTESIAN_POINT ( 'NONE',  ( 0.2819296736111110979, 4.394527777853643791, -3.452642723725051716E-17 ) ) ;
#10023=CARTESIAN_POINT ( 'NONE',  ( -0.2078600217396917860, 4.050312593809051620, -0.2327285559015772332 ) ) ;
#10026=CARTESIAN_POINT ( 'NONE',  ( 0.2819296736111110979, 0.3826388888130222155, 0.000000000000000000 ) ) ;
#10027=CYLINDRICAL_SURFACE ( 'NONE', #8047, 0.3119999999999999996 ) ;
#10028=CARTESIAN_POINT ( 'NONE',  ( 2.570936052289255124E-07, 3.738287934957344127, 0.3119999999997750129 ) ) ;
#10031=ORIENTED_EDGE ( 'NONE', *, *, #21697, .T. ) ;
#10033=LINE ( 'NONE', #17455, #6220 ) ;
#10034=CARTESIAN_POINT ( 'NONE',  ( 0.1993543840281266910, 0.4868055554796889561, -0.1993543840281266910 ) ) ;
#10035=CARTESIAN_POINT ( 'NONE',  ( 0.1993543840281266355, 0.2506944443685777957, 0.1993543840281267465 ) ) ;
#10036=CARTESIAN_POINT ( 'NONE',  ( 5.178964085587577574E-17, 4.047305555631421470, 0.2819296736111110979 ) ) ;
#10038=CARTESIAN_POINT ( 'NONE',  ( 0.2819296736111110979, 4.557722222298087544, 0.1167790944451422425 ) ) ;
#10039=CARTESIAN_POINT ( 'NONE',  ( 0.1381111726236976811, 5.088173287601598815, -0.2808105300433598739 ) ) ;
#10043=CARTESIAN_POINT ( 'NONE',  ( 5.731347020009612645E-17, 3.904944444596176734, 0.3119999999999999996 ) ) ;
#10045=EDGE_CURVE ( 'NONE', #6049, #12796, #7586, .T. ) ;
#10046=CARTESIAN_POINT ( 'NONE',  ( 0.000000000000000000, 5.384999999999999787, 0.000000000000000000 ) ) ;
#10050=CARTESIAN_POINT ( 'NONE',  ( -0.2295375298156325794, 5.008762073107971169, 0.2113211636186998754 ) ) ;
#10051=VERTEX_POINT ( 'NONE', #4644 ) ;
#10052=CARTESIAN_POINT ( 'NONE',  ( -0.2819296736111110979, 0.02499999992413337591, 0.1167790944451422425 ) ) ;
#10054=CARTESIAN_POINT ( 'NONE',  ( 0.2589252677293308325, 4.257452783784655637, -0.1745261803771008813 ) ) ;
#10056=CARTESIAN_POINT ( 'NONE',  ( 0.2906323808137692422, 4.082252095162804295, 0.1137463939449124412 ) ) ;
#10058=CARTESIAN_POINT ( 'NONE',  ( 0.2912207731228424468, 5.179804787033147839, -0.03491938693372079183 ) ) ;
#10061=CARTESIAN_POINT ( 'NONE',  ( -0.2819296736111110424, 3.911888888964754507, 0.1167790944451424923 ) ) ;
#10062=CARTESIAN_POINT ( 'NONE',  ( 0.3040674888080049376, 5.032214460774807385, -0.08102217497193067719 ) ) ;
#10063=CARTESIAN_POINT ( 'NONE',  ( -0.2322136846690653622, 5.172242893738336456, -0.1834769090104111933 ) ) ;
#10065=CARTESIAN_POINT ( 'NONE',  ( 0.2206173157302028787, 4.578555555707287894, 0.2206173157302027954 ) ) ;
#10066=CARTESIAN_POINT ( 'NONE',  ( -0.2819296736111110424, 4.925777777853643791, 0.1167790944451424923 ) ) ;
#10069=CARTESIAN_POINT ( 'NONE',  ( -0.1993543840281266910, 3.957027777853642903, -0.1993543840281266910 ) ) ;
#10075=ORIENTED_EDGE ( 'NONE', *, *, #12544, .T. ) ;
#10081=CARTESIAN_POINT ( 'NONE',  ( -0.1292346314604058410, 0.1604166665149337478, 0.3119999999999998885 ) ) ;
#10082=CARTESIAN_POINT ( 'NONE',  ( 0.2408840922389058614, 5.139268827874871270, 0.1879369982435209474 ) ) ;
#10085=CARTESIAN_POINT ( 'NONE',  ( 0.08123675842391495094, 0.06219723018719916507, 0.3013752234401997354 ) ) ;
#10091=CARTESIAN_POINT ( 'NONE',  ( 0.1167790944451422702, 4.793833333409199149, -0.2819296736111110424 ) ) ;
#10093=CARTESIAN_POINT ( 'NONE',  ( -1.726321361862525858E-17, 4.672305555631421470, -0.2819296736111110979 ) ) ;
#10094=CARTESIAN_POINT ( 'NONE',  ( 0.3119999999999998885, 0.2854166665149337478, 0.1292346314604058410 ) ) ;
#10097=CARTESIAN_POINT ( 'NONE',  ( 1.241811370555571286E-09, 4.488277777895108400, -0.3119999999999999996 ) ) ;
#10098=CARTESIAN_POINT ( 'NONE',  ( -0.2206173157302027676, 4.391055555555555046, 0.2206173157302028787 ) ) ;
#10099=CARTESIAN_POINT ( 'NONE',  ( 0.2206173157302027954, 5.203555555707287894, -0.2206173157302028232 ) ) ;
#10100=CARTESIAN_POINT ( 'NONE',  ( 0.3108595454310983386, 4.973660102971597219, 0.02665253488378086996 ) ) ;
#10101=DIRECTION ( 'NONE',  ( -0.000000000000000000, -1.000000000000000000, -0.000000000000000000 ) ) ;
#10105=B_SPLINE_CURVE_WITH_KNOTS ( 'NONE', 3,
 ( #23892, #12594, #7210, #16839, #14656, #9277, #3545, #22315, #22077, #5249, #5373, #12720, #18186, #16718, #14782, #6971, #20014, #8424, #22197, #20135, #20258, #8919, #12839, #1956, #3789, #10996, #18424, #5496, #9155, #16600, #5613, #20494, #11235, #3301, #9400, #24020, #7331, #12961 ),
 .UNSPECIFIED., .F., .F.,
 ( 4, 2, 2, 2, 2, 2, 2, 2, 2, 2, 2, 2, 1, 1, 1, 2, 2, 1, 2, 2, 4 ),
 ( 0.5573884401815307754, 0.5596720767556532250, 0.5608138950427145053, 0.5619557133297757856, 0.5630975316168369549, 0.5642393499038982352, 0.5653811681909595155, 0.5665229864780206848, 0.5676648047650819651, 0.5688066230521432454, 0.5693775321956737745, 0.5696629867674390946, 0.5698057140533218101, 0.5698770776962630569, 0.5699127595177337913, 0.5699306004284691030, 0.5699395208838368143, 0.5699484413392044146, 0.5710902596262658060, 0.5733738962003884776, 0.5756575327745111492 ),
 .UNSPECIFIED. ) ;
#10109=CARTESIAN_POINT ( 'NONE',  ( 0.1240224521522770712, 4.130797334433546908, 0.2867944741873222347 ) ) ;
#10113=CARTESIAN_POINT ( 'NONE',  ( -0.04827834974809647184, 0.03398119426037959911, 0.2819296736111110979 ) ) ;
#10118=ORIENTED_EDGE ( 'NONE', *, *, #5151, .F. ) ;
#10120=DIRECTION ( 'NONE',  ( -0.000000000000000000, -1.000000000000000000, -0.000000000000000000 ) ) ;
#10122=CARTESIAN_POINT ( 'NONE',  ( -0.1292346314604058410, 0.5006944444444441089, 0.3119999999999998885 ) ) ;
#10123=CARTESIAN_POINT ( 'NONE',  ( -0.3119999999999999996, 4.880638888888888083, -0.1292346314604056468 ) ) ;
#10125=CARTESIAN_POINT ( 'NONE',  ( -0.2819296736111110424, 3.974388888964754507, -0.1167790944451423119 ) ) ;
#10127=CARTESIAN_POINT ( 'NONE',  ( 0.1797085267211815662, 3.721720965436318362, -0.2172307213220433242 ) ) ;
#10128=CARTESIAN_POINT ( 'NONE',  ( 0.2405467123332261370, 4.813840729788613437, -0.2030146156137226099 ) ) ;
#10132=CARTESIAN_POINT ( 'NONE',  ( 0.2819296736111110424, 4.828555555631420582, -0.1167790944451423396 ) ) ;
#10134=CARTESIAN_POINT ( 'NONE',  ( 5.731347020009612645E-17, 4.120222222222221120, 0.3119999999999999996 ) ) ;
#10141=CARTESIAN_POINT ( 'NONE',  ( 0.1993543840281266633, 4.290361111186976828, -0.1993543840281266910 ) ) ;
#10146=CARTESIAN_POINT ( 'NONE',  ( -0.2819296736111110979, 0.4104166665908000056, -3.452642723725051716E-17 ) ) ;
#10147=CARTESIAN_POINT ( 'NONE',  ( -0.1292346314604058410, 0.1118055555555552139, 0.3119999999999998885 ) ) ;
#10148=CARTESIAN_POINT ( 'NONE',  ( 5.731347020009612645E-17, 4.453555555555555046, 0.3119999999999999996 ) ) ;
#10152=CARTESIAN_POINT ( 'NONE',  ( -0.04072772395942860640, 3.767161843808154664, -0.3094987719763222511 ) ) ;
#10153=CARTESIAN_POINT ( 'NONE',  ( -0.1167790944451424506, 0.5736111110352444253, 0.2819296736111110424 ) ) ;
#10154=CARTESIAN_POINT ( 'NONE',  ( -0.1993543840281266633, 0.4451388888130222710, -0.1993543840281266910 ) ) ;
#10155=CARTESIAN_POINT ( 'NONE',  ( 5.178964085587577574E-17, 4.102861111186976828, 0.2819296736111110979 ) ) ;
#10157=CARTESIAN_POINT ( 'NONE',  ( -0.1993543840281266355, 4.595916666742532186, 0.1993543840281267465 ) ) ;
#10163=CARTESIAN_POINT ( 'NONE',  ( -1.910449006669871087E-17, 4.036888888888888083, -0.3119999999999999996 ) ) ;
#10164=CARTESIAN_POINT ( 'NONE',  ( 0.1292346314604058410, 3.797305555707287894, 0.3119999999999998885 ) ) ;
#10174=CARTESIAN_POINT ( 'NONE',  ( 0.1167790944451423535, 0.03888888881302225708, 0.2819296736111110424 ) ) ;
#10177=CARTESIAN_POINT ( 'NONE',  ( 0.2872988799765124335, 4.255711475989661707, -0.1216958920792224202 ) ) ;
#10178=CARTESIAN_POINT ( 'NONE',  ( -0.3069366055884749644, 4.722600365735013739, -0.06133714766361197945 ) ) ;
#10179=CARTESIAN_POINT ( 'NONE',  ( 0.3002986933836771510, 4.083101498185607525, 0.08467756203784890245 ) ) ;
#10181=CARTESIAN_POINT ( 'NONE',  ( 0.2005216093553227330, 5.172899910562626324, 0.2173648676198124963 ) ) ;
#10184=CARTESIAN_POINT ( 'NONE',  ( -0.1167790944451423257, 3.842444444520309865, -0.2819296736111110424 ) ) ;
#10185=CARTESIAN_POINT ( 'NONE',  ( 0.3035936216127623211, 5.027565645647625203, 0.08278009126895921610 ) ) ;
#10188=CARTESIAN_POINT ( 'NONE',  ( 0.3119999999999999996, 4.585500000151731648, -3.820898013339742174E-17 ) ) ;
#10189=EDGE_CURVE ( 'NONE', #19562, #15412, #3393, .T. ) ;
#10190=CARTESIAN_POINT ( 'NONE',  ( -0.1167790944451423119, 4.634111111186976828, -0.2819296736111110979 ) ) ;
#10192=CARTESIAN_POINT ( 'NONE',  ( 0.1167790944451422702, 4.113277777853642903, -0.2819296736111110424 ) ) ;
#10194=VERTEX_POINT ( 'NONE', #4403 ) ;
#10198=CARTESIAN_POINT ( 'NONE',  ( -6.389700406101856968E-07, 4.404919069638722817, 0.3119999999986028949 ) ) ;
#10200=CARTESIAN_POINT ( 'NONE',  ( -0.1292346314604058410, 0.1048611109593781815, 0.3119999999999998885 ) ) ;
#10203=CARTESIAN_POINT ( 'NONE',  ( 5.731347020009612645E-17, 4.453555555555555046, 0.3119999999999999996 ) ) ;
#10204=EDGE_CURVE ( 'NONE', #10793, #23698, #10033, .T. ) ;
#10206=CARTESIAN_POINT ( 'NONE',  ( 0.1993543840281266355, 0.1395833332574667185, 0.1993543840281267465 ) ) ;
#10209=CARTESIAN_POINT ( 'NONE',  ( 0.1167790944451424368, 4.370222222298088433, 0.2819296736111110424 ) ) ;
#10213=CARTESIAN_POINT ( 'NONE',  ( 0.2206173157302027676, 0.4486111109593781676, 0.2206173157302028787 ) ) ;
#10214=CARTESIAN_POINT ( 'NONE',  ( -0.3119999999999999996, 4.213972222222222008, -0.1292346314604056468 ) ) ;
#10216=CARTESIAN_POINT ( 'NONE',  ( 0.1292346314604058410, 5.068138888888888083, 0.3119999999999998885 ) ) ;
#10218=CARTESIAN_POINT ( 'NONE',  ( 0.2635330294133203521, 4.979450665808103693, -0.1720186351255787172 ) ) ;
#10222=CARTESIAN_POINT ( 'NONE',  ( 0.3127913692903316334, 4.140747938380851423, 0.009870907807890409030 ) ) ;
#10234=CARTESIAN_POINT ( 'NONE',  ( 6.388359114324787822E-07, 4.627192232271967853, 0.3119999999985919592 ) ) ;
#10237=CARTESIAN_POINT ( 'NONE',  ( -0.2206173157302027954, 0.3722222222222218990, -0.2206173157302028232 ) ) ;
#10238=CARTESIAN_POINT ( 'NONE',  ( -0.3119999999999999996, 4.936194444444443441, -0.1292346314604056468 ) ) ;
#10239=CARTESIAN_POINT ( 'NONE',  ( 0.1167790944451424506, 4.148000000075866112, 0.2819296736111110424 ) ) ;
#10240=CARTESIAN_POINT ( 'NONE',  ( -0.1993543840281266910, 3.970916666742532186, -0.1993543840281266910 ) ) ;
#10241=EDGE_CURVE ( 'NONE', #5752, #2198, #10566, .T. ) ;
#10244=CARTESIAN_POINT ( 'NONE',  ( 0.3125925260372354741, 4.808137523523458690, -0.01455662600646890834 ) ) ;
#10248=CARTESIAN_POINT ( 'NONE',  ( 0.1167790944451424368, 4.759111111186977716, 0.2819296736111110424 ) ) ;
#10249=VECTOR ( 'NONE', #22195, 39.37007874015748143 ) ;
#10251=CARTESIAN_POINT ( 'NONE',  ( -0.007894445728632182302, 4.515849982952590658, 0.3119999997756114363 ) ) ;
#10255=CARTESIAN_POINT ( 'NONE',  ( 0.2819296736111110979, 4.064666666742532186, -0.1167790944451423396 ) ) ;
#10257=DIRECTION ( 'NONE',  ( 0.000000000000000000, 0.000000000000000000, 1.000000000000000000 ) ) ;
#10258=FACE_OUTER_BOUND ( 'NONE', #18590, .T. ) ;
#10261=CARTESIAN_POINT ( 'NONE',  ( -0.2819296736111110424, 0.1152777777019111521, -0.1167790944451423396 ) ) ;
#10263=CARTESIAN_POINT ( 'NONE',  ( 0.000000000000000000, 5.384999999999999787, -0.3119999999999999996 ) ) ;
#10272=CARTESIAN_POINT ( 'NONE',  ( -0.2819296736111110979, 0.3409722221463556413, -3.452642723725051716E-17 ) ) ;
#10273=CARTESIAN_POINT ( 'NONE',  ( -1.726321361862525858E-17, 4.075083333409199149, -0.2819296736111110979 ) ) ;
#10277=CARTESIAN_POINT ( 'NONE',  ( -0.1993543840281266910, 4.693138888964754507, -0.1993543840281266910 ) ) ;
#10280=CARTESIAN_POINT ( 'NONE',  ( 0.2883059669956098969, 5.075061251213828228, 0.1201015347656402971 ) ) ;
#10283=CARTESIAN_POINT ( 'NONE',  ( -0.3119999999999999996, 3.891055555707287894, 0.000000000000000000 ) ) ;
#10285=DIRECTION ( 'NONE',  ( 0.000000000000000000, 0.000000000000000000, -1.000000000000000000 ) ) ;
#10286=CARTESIAN_POINT ( 'NONE',  ( 0.1629873018068623836, 5.206640035683670398, 0.2306973944900186091 ) ) ;
#10287=CARTESIAN_POINT ( 'NONE',  ( 0.1993543840281266633, 4.998694444520309865, -0.1993543840281266910 ) ) ;
#10290=CARTESIAN_POINT ( 'NONE',  ( -0.3086545942380659047, 5.114261002539869594, -0.02184028893379939135 ) ) ;
#10291=CARTESIAN_POINT ( 'NONE',  ( 0.3119999999999999996, 0.2437499999999996891, -0.1292346314604056468 ) ) ;
#10293=CARTESIAN_POINT ( 'NONE',  ( -5.178964085587577574E-17, 0.03541666659080003332, 0.2819296736111110979 ) ) ;
#10295=CARTESIAN_POINT ( 'NONE',  ( 0.1167790944451423257, 0.004166666590800035055, -0.2819296736111110424 ) ) ;
#10297=CARTESIAN_POINT ( 'NONE',  ( 0.2985525202959439239, 4.082927124627439674, 0.09073774551547199307 ) ) ;
#10299=CARTESIAN_POINT ( 'NONE',  ( -0.2925124024682271284, 5.054586912992379943, -0.1086053545779250423 ) ) ;
#10302=CARTESIAN_POINT ( 'NONE',  ( -0.2722828206202175805, 4.664154358537332179, -0.1577052281583355975 ) ) ;
#10303=AXIS2_PLACEMENT_3D ( 'NONE', #21912, #12551, #18264 ) ;
#10304=CARTESIAN_POINT ( 'NONE',  ( 0.2819296736111110424, 3.773000000075866112, -0.1167790944451423396 ) ) ;
#10305=CARTESIAN_POINT ( 'NONE',  ( 0.05068837741648516554, 5.073009555618063438, 0.3078549794868774558 ) ) ;
#10307=CARTESIAN_POINT ( 'NONE',  ( 0.3119999999999999996, 4.533416666818399499, -0.1292346314604056745 ) ) ;
#10308=CARTESIAN_POINT ( 'NONE',  ( 0.1167790944451424506, 4.828555555631421470, 0.2819296736111110424 ) ) ;
#10312=CARTESIAN_POINT ( 'NONE',  ( -0.2819296736111110424, 4.023000000075866112, 0.1167790944451424923 ) ) ;
#10313=ORIENTED_EDGE ( 'NONE', *, *, #10701, .T. ) ;
#10319=CARTESIAN_POINT ( 'NONE',  ( -0.2206173157302027954, 0.1430555554038226151, -0.2206173157302028232 ) ) ;
#10320=B_SPLINE_CURVE_WITH_KNOTS ( 'NONE', 3,
 ( #9239, #2043, #16914, #20697, #8997, #14743, #16440, #12798, #22037, #5333, #20217, #10957, #18382, #1677, #9110, #16560, #23981, #13750, #11681, #8003, #8116, #13637, #15570, #4229, #9972, #22993, #21174, #4464, #18992, #15334, #13520 ),
 .UNSPECIFIED., .F., .F.,
 ( 4, 2, 2, 2, 2, 2, 2, 2, 2, 2, 2, 1, 1, 1, 1, 1, 2, 4 ),
 ( 0.6853182142057806514, 0.6864601233937474012, 0.6876020325817142620, 0.6898858509576478726, 0.6921696693335813722, 0.6944534877095149827, 0.6967373060854485933, 0.6990211244613822039, 0.7013049428373157035, 0.7024468520252825643, 0.7030178066192659392, 0.7033032839162576266, 0.7034460225647534148, 0.7035173918890014200, 0.7035530765511253115, 0.7035709188821873683, 0.7035798400477183412, 0.7035887612132493141 ),
 .UNSPECIFIED. ) ;
#10321=CARTESIAN_POINT ( 'NONE',  ( 0.2995508976399182122, 5.147601669199691976, -0.04633967184963520836 ) ) ;
#10325=CARTESIAN_POINT ( 'NONE',  ( 0.000000000000000000, 5.384999999999999787, 0.000000000000000000 ) ) ;
#10326=CARTESIAN_POINT ( 'NONE',  ( -0.1167790944451422702, 0.05277777770191114520, -0.2819296736111110979 ) ) ;
#10329=CARTESIAN_POINT ( 'NONE',  ( 0.1993543840281267465, 4.429250000075865223, 0.1993543840281266633 ) ) ;
#10334=CARTESIAN_POINT ( 'NONE',  ( -0.3119999999999999996, 4.380638888888888083, -0.1292346314604056468 ) ) ;
#10335=CARTESIAN_POINT ( 'NONE',  ( 0.3119999999999999996, 5.137583333485064685, 0.1292346314604056190 ) ) ;
#10337=CARTESIAN_POINT ( 'NONE',  ( -0.1292346314604044810, 4.672305555555555934, 0.3120000000000012208 ) ) ;
#10342=EDGE_CURVE ( 'NONE', #16571, #4057, #18214, .T. ) ;
#10347=DIRECTION ( 'NONE',  ( 0.000000000000000000, 0.000000000000000000, -1.000000000000000000 ) ) ;
#10351=CARTESIAN_POINT ( 'NONE',  ( 0.1993543840281266910, 0.1118055554796889145, -0.1993543840281266910 ) ) ;
#10357=FACE_OUTER_BOUND ( 'NONE', #699, .T. ) ;
#10358=CARTESIAN_POINT ( 'NONE',  ( -0.09248661545808961604, 4.268693300206678032, -0.2987603559195510794 ) ) ;
#10361=CARTESIAN_POINT ( 'NONE',  ( 0.3119999999999999996, 0.4069444444444440534, 0.000000000000000000 ) ) ;
#10362=CARTESIAN_POINT ( 'NONE',  ( 0.2206173157302027954, 4.918833333333332725, -0.2206173157302028232 ) ) ;
#10363=CARTESIAN_POINT ( 'NONE',  ( 0.2819296736111110979, 4.158416666742532186, -3.452642723725051716E-17 ) ) ;
#10364=CARTESIAN_POINT ( 'NONE',  ( 0.2819296736111110979, 3.946611111186976384, 0.1167790944451422425 ) ) ;
#10366=CARTESIAN_POINT ( 'NONE',  ( 0.3108998888495465018, 4.807006650212706234, 0.02617762660114440407 ) ) ;
#10368=VERTEX_POINT ( 'NONE', #3089 ) ;
#10370=CARTESIAN_POINT ( 'NONE',  ( -0.2819296736111110424, 4.516055555631421470, -0.1167790944451423119 ) ) ;
#10373=CARTESIAN_POINT ( 'NONE',  ( 0.3119999999999999996, 3.800777777777776478, -3.820898013339742174E-17 ) ) ;
#10374=EDGE_CURVE ( 'NONE', #21824, #14703, #7754, .T. ) ;
#10378=( BOUNDED_CURVE ( )  B_SPLINE_CURVE ( 2, ( #4235, #9857, #11573, #22654, #11445, #6061, #11687, #8126, #15577 ),
 .UNSPECIFIED., .F., .F. ) 
 B_SPLINE_CURVE_WITH_KNOTS ( ( 3, 2, 2, 2, 3 ),
 ( 0.7708333333333333703, 0.7812500000000000000, 0.7916666666666666297, 0.8020833333333333703, 0.8125000000000000000 ),
 .UNSPECIFIED. ) 
 CURVE ( )  GEOMETRIC_REPRESENTATION_ITEM ( )  RATIONAL_B_SPLINE_CURVE ( ( 1.000000000000000000, 0.9238795325112867385, 1.000000000000000000, 0.9238795325112867385, 1.000000000000000000, 0.9238795325112867385, 1.000000000000000000, 0.9238795325112867385, 1.000000000000000000 ) ) 
 REPRESENTATION_ITEM ( '' )  );
#10381=CARTESIAN_POINT ( 'NONE',  ( -0.1993543840281266910, 4.193138888964754507, -0.1993543840281266910 ) ) ;
#10382=CARTESIAN_POINT ( 'NONE',  ( -0.3111057980080598195, 4.834855633700155586, -0.02361667675171789244 ) ) ;
#10387=CARTESIAN_POINT ( 'NONE',  ( 0.2819296736111110979, 0.09097222214635558579, 0.000000000000000000 ) ) ;
#10391=DIRECTION ( 'NONE',  ( -0.000000000000000000, 1.000000000000000000, -0.000000000000000000 ) ) ;
#10397=CARTESIAN_POINT ( 'NONE',  ( -0.2819296736111110979, 0.3444444443685779067, 0.1167790944451422425 ) ) ;
#10398=CARTESIAN_POINT ( 'NONE',  ( -1.726321361862525858E-17, 4.130638888964754507, -0.2819296736111110979 ) ) ;
#10401=CARTESIAN_POINT ( 'NONE',  ( -0.2819296736111110424, 4.592444444520309865, 0.1167790944451424923 ) ) ;
#10402=CARTESIAN_POINT ( 'NONE',  ( 0.2431432128212240862, 5.125660135501770576, 0.1885555529197559810 ) ) ;
#10405=EDGE_LOOP ( 'NONE', ( #13360, #9312, #5608, #959 ) ) ;
#10407=CARTESIAN_POINT ( 'NONE',  ( -0.1993543840281266910, 5.123694444520309865, -0.1993543840281266910 ) ) ;
#10410=CARTESIAN_POINT ( 'NONE',  ( 0.2658661084243346684, 0.03242967361111057795, 0.09380593400082704036 ) ) ;
#10411=CARTESIAN_POINT ( 'NONE',  ( 0.2819296736111110979, 4.939666666742532186, -0.1167790944451423396 ) ) ;
#10418=CARTESIAN_POINT ( 'NONE',  ( 0.2819296736111110424, 0.3791666665908000611, 0.1167790944451424923 ) ) ;
#10421=CARTESIAN_POINT ( 'NONE',  ( 0.1555449433501408241, 4.076298560705016172, 0.2713454068376597861 ) ) ;
#10423=CARTESIAN_POINT ( 'NONE',  ( -0.2736110384480277546, 5.062269768326324026, 0.1517155811448881175 ) ) ;
#10428=CARTESIAN_POINT ( 'NONE',  ( 5.178964085587577574E-17, 3.755638888964754951, 0.2819296736111110979 ) ) ;
#10431=CARTESIAN_POINT ( 'NONE',  ( 0.2832746799703420026, 5.033777524650573376, -0.1307669425342211644 ) ) ;
#10432=CARTESIAN_POINT ( 'NONE',  ( 0.2292520601541578884, 5.072999999999999510, 0.2155101067843893659 ) ) ;
#10433=CARTESIAN_POINT ( 'NONE',  ( -0.03138470014218885940, 4.792977914880279577, 0.3104507266188493153 ) ) ;
#10434=CARTESIAN_POINT ( 'NONE',  ( -0.1292346314604056745, 4.547305555707287894, -0.3119999999999999996 ) ) ;
#10435=CARTESIAN_POINT ( 'NONE',  ( 0.1167790944451424506, 4.717444444520309865, 0.2819296736111110424 ) ) ;
#10437=CARTESIAN_POINT ( 'NONE',  ( 0.2819296736111110979, 4.047305555631421470, -3.452642723725051716E-17 ) ) ;
#10443=ORIENTED_EDGE ( 'NONE', *, *, #4151, .F. ) ;
#10444=CARTESIAN_POINT ( 'NONE',  ( 0.1292346314604056745, 0.1326388887371559577, -0.3119999999999999996 ) ) ;
#10445=CARTESIAN_POINT ( 'NONE',  ( -0.0002437205570828195761, 4.377173215581007248, -0.3119999107914319114 ) ) ;
#10446=CARTESIAN_POINT ( 'NONE',  ( 0.1123264932791831761, 3.756093169699424195, -0.3119999999999978346 ) ) ;
#10450=CARTESIAN_POINT ( 'NONE',  ( 0.2819296736111110979, 0.03888888881302225015, -0.1167790944451422980 ) ) ;
#10452=CARTESIAN_POINT ( 'NONE',  ( 0.2819296736111110979, 4.436194444520309865, -3.452642723725051716E-17 ) ) ;
#10457=CARTESIAN_POINT ( 'NONE',  ( 0.2206173157302027954, 4.141055555555554157, -0.2206173157302028232 ) ) ;
#10459=CARTESIAN_POINT ( 'NONE',  ( -0.1292346314604056745, 5.102861111262844140, -0.3119999999999999996 ) ) ;
#10460=CARTESIAN_POINT ( 'NONE',  ( -0.3119999999999999996, 4.661888888888888083, 0.000000000000000000 ) ) ;
#10465=FACE_OUTER_BOUND ( 'NONE', #18457, .T. ) ;
#10469=CARTESIAN_POINT ( 'NONE',  ( 1.726321361862525858E-17, 0.6048611110352445364, -0.2819296736111110979 ) ) ;
#10472=CARTESIAN_POINT ( 'NONE',  ( 0.2819296736111110979, 5.168833333409199149, 0.1167790944451422425 ) ) ;
#10475=CARTESIAN_POINT ( 'NONE',  ( 0.3119999999999999996, 3.856333333333332281, -3.820898013339742174E-17 ) ) ;
#10478=CARTESIAN_POINT ( 'NONE',  ( -0.2206173157302027954, 0.4277777777777774237, -0.2206173157302028232 ) ) ;
#10479=CARTESIAN_POINT ( 'NONE',  ( 5.731347020009612645E-17, 4.620222222222221120, 0.3119999999999999996 ) ) ;
#10480=CARTESIAN_POINT ( 'NONE',  ( 0.2819296736111110979, 4.269527777853643791, -3.452642723725051716E-17 ) ) ;
#10481=CARTESIAN_POINT ( 'NONE',  ( 0.1993543840281266633, 3.901472222298087988, -0.1993543840281266910 ) ) ;
#10485=CARTESIAN_POINT ( 'NONE',  ( 0.000000000000000000, 5.384999999999999787, 0.000000000000000000 ) ) ;
#10486=CARTESIAN_POINT ( 'NONE',  ( -0.1993543840281266910, 4.512583333409199149, -0.1993543840281266910 ) ) ;
#10493=CARTESIAN_POINT ( 'NONE',  ( -0.1167790944451423535, 4.099388888964754507, 0.2819296736111110979 ) ) ;
#10494=CARTESIAN_POINT ( 'NONE',  ( -0.002180183382288421873, 4.821674524114921923, -0.3119934709836226228 ) ) ;
#10498=CARTESIAN_POINT ( 'NONE',  ( 0.2819296736111110424, 0.6083333332574668573, -0.1167790944451423119 ) ) ;
#10504=VERTEX_POINT ( 'NONE', #16256 ) ;
#10507=CARTESIAN_POINT ( 'NONE',  ( 1.726321361862525858E-17, 0.6048611110352445364, -0.2819296736111110979 ) ) ;
#10508=CARTESIAN_POINT ( 'NONE',  ( 0.1993543840281266355, 0.4173611110352444808, 0.1993543840281267465 ) ) ;
#10510=CARTESIAN_POINT ( 'NONE',  ( -0.2819296736111110424, 3.981333333409199593, 0.1167790944451424923 ) ) ;
#10512=CARTESIAN_POINT ( 'NONE',  ( -0.2819296736111110424, 4.585500000075865223, -0.1167790944451423119 ) ) ;
#10513=CARTESIAN_POINT ( 'NONE',  ( 0.07964491704986943754, 5.141321981404664676, -0.2945216132760368200 ) ) ;
#10516=FACE_OUTER_BOUND ( 'NONE', #3534, .T. ) ;
#10517=CARTESIAN_POINT ( 'NONE',  ( 0.1123265699853363830, 3.707482056679137550, -0.3120000000000000551 ) ) ;
#10522=CARTESIAN_POINT ( 'NONE',  ( -0.1167790944451423119, 4.898000000075865223, -0.2819296736111110979 ) ) ;
#10525=CARTESIAN_POINT ( 'NONE',  ( -0.1292346314604056190, 0.3062499998482671182, -0.3119999999999999996 ) ) ;
#10526=CARTESIAN_POINT ( 'NONE',  ( 1.910449006669871087E-17, 0.2541666666666663188, -0.3119999999999999996 ) ) ;
#10528=CARTESIAN_POINT ( 'NONE',  ( 0.1167790944451423257, 0.2819444443685777957, -0.2819296736111110424 ) ) ;
#10531=CARTESIAN_POINT ( 'NONE',  ( -0.3120000000000000551, 0.3270833333333330040, 0.1292346314604056190 ) ) ;
#10534=CARTESIAN_POINT ( 'NONE',  ( -0.2867585069081046156, 5.054137861884946403, -0.1229525427538243343 ) ) ;
#10539=CARTESIAN_POINT ( 'NONE',  ( -0.1993543840281266910, 4.804250000075865223, -0.1993543840281266910 ) ) ;
#10541=CARTESIAN_POINT ( 'NONE',  ( -1.726321361862525858E-17, 3.727861111186976384, -0.2819296736111110979 ) ) ;
#10543=CARTESIAN_POINT ( 'NONE',  ( 0.2874842063055126351, 5.033475709842507584, -0.1212575126306435908 ) ) ;
#10546=CARTESIAN_POINT ( 'NONE',  ( 0.1292346314604056190, 4.207027777929510215, -0.3119999999999999996 ) ) ;
#10547=EDGE_CURVE ( 'NONE', #15596, #14458, #11454, .T. ) ;
#10548=CARTESIAN_POINT ( 'NONE',  ( -0.1993543840281266910, 4.693138888964754507, -0.1993543840281266910 ) ) ;
#10550=CARTESIAN_POINT ( 'NONE',  ( 0.1993543840281266633, 3.943138888964754507, -0.1993543840281266910 ) ) ;
#10557=CARTESIAN_POINT ( 'NONE',  ( 0.1292346314604056190, 4.255638888888888083, -0.3119999999999999996 ) ) ;
#10560=CARTESIAN_POINT ( 'NONE',  ( -0.2206173157302028787, 0.3791666665149337478, 0.2206173157302027954 ) ) ;
#10561=CARTESIAN_POINT ( 'NONE',  ( -6.389700406101856968E-07, 4.404919069638722817, 0.3119999999986028949 ) ) ;
#10564=( BOUNDED_SURFACE ( )  B_SPLINE_SURFACE ( 1, 2, ( 
 ( #21517, #15443, #4578, #23330, #6643, #8469, #19690, #798, #17625, #6283, #22869, #11916, #13738, #15676, #21161, #23094, #19208, #4807, #2516, #4692, #8104, #17386, #19568, #2993, #2749, #554, #915, #10200, #14090, #15796, #19335, #23215, #2858, #12274, #9958, #10444, #7991, #21042, #10319, #681, #17745, #4452, #2632, #10081, #17501, #21881, #8832, #5049, #20180, #7258, #12885, #14210, #9076, #18347, #16280, #22000, #14331, #16407, #3226, #23455, #1405, #5172, #18230, #7137, #14704, #22120, #16160, #21764, #14577, #12519, #23576, #23692, #12639, #23815, #19938, #10918, #10674, #5300, #12762, #6889, #20300, #21643, #5418, #3585, #1641, #17870, #1527, #3468, #17992, #18108, #16524, #23942, #7015, #14459, #1161, #20058, #3348, #10801, #8602, #16041, #6764, #8959, #4932, #12398, #19815, #3111, #10560, #1284, #8709, #1759, #167, #9683, #17122, #18951, #6010, #11275, #3951, #16761, #9203, #22356, #44, #18707, #7490, #2005, #5539, #15291, #22240, #15173, #18588, #3711, #22608, #13478, #5778, #11037, #11394, #22482, #410, #9442, #5660, #18826, #7608, #2249, #20416, #7844, #18467, #22720, #286, #16644, #14823, #13240, #16877, #9561, #20653, #20893, #16994, #24063, #7373, #3835, #14937, #20539, #13003, #11160, #5892, #1880, #15060, #9321, #13124, #2120, #7727, #13352, #20774, #4063, #11518, #8319, #11760, #21010, #15770, #6614, #23068, #4187, #21259 ),
 ( #19542, #13597, #1011, #11640, #2834, #17598, #9809, #7961, #15649, #10052, #2721, #13825, #10293, #10174, #23304, #8441, #21134, #8077, #13714, #17242, #524, #23189, #17716, #17476, #15413, #17358, #4547, #12010, #15530, #6377, #22951, #14063, #8200, #19304, #6254, #6499, #15886, #19065, #22841, #2372, #4666, #2608, #13946, #650, #888, #4424, #6129, #11889, #19423, #21376, #12134, #4303, #19182, #2491, #768, #9927, #8681, #3086, #5021, #16253, #20025, #16130, #14545, #23545, #1492, #3314, #19785, #23905, #1134, #10887, #16494, #21967, #21492, #5140, #18197, #21612, #6860, #10771, #8928, #14302, #3195, #16374, #8803, #10528, #12486, #5261, #23784, #7106, #12605, #12732, #23663, #3435, #18074, #21736, #19906, #18316, #12248, #10642, #20148, #1613, #9047, #7223, #1374, #14426, #17959, #19662, #6982, #1252, #21851, #4781, #2960, #10418, #17841, #8567, #16008, #23427, #6737, #14179, #4906, #12368, #22208, #135, #15026, #4035, #9652, #16610, #20506, #7578, #16963, #5626, #15144, #9530, #11489, #8, #13210, #24030, #3801, #12850, #7456, #20268, #18793, #14905, #22451, #378, #22326, #9410, #258, #14792, #18553, #1728, #22574, #3678, #17090, #1842, #13092, #11124, #2221, #2088, #5750, #20621, #5507, #12970, #9166, #16728, #7340, #22089, #11245, #9285, #18672, #1972, #16848, #3921, #20386, #11366, #7698, #5862, #13321, #20743, #18921, #14670, #5384 ) ),
 .UNSPECIFIED., .F., .F., .T. ) 
 B_SPLINE_SURFACE_WITH_KNOTS ( ( 2, 2 ),
 ( 3, 2, 2, 2, 2, 2, 2, 2, 2, 2, 2, 2, 2, 2, 2, 2, 2, 2, 2, 2, 2, 2, 2, 2, 2, 2, 2, 2, 2, 2, 2, 2, 2, 2, 2, 2, 2, 2, 2, 2, 2, 2, 2, 2, 2, 2, 2, 2, 2, 2, 2, 2, 2, 2, 2, 2, 2, 2, 2, 2, 2, 2, 2, 2, 2, 2, 2, 2, 2, 2, 2, 2, 2, 2, 2, 2, 2, 2, 2, 2, 2, 2, 2, 2, 2, 2, 2, 2, 2, 2, 3 ),
 ( 0.000000000000000000, 1.000000000000000000 ),
 ( 0.000000000000000000, 0.01041666666666666609, 0.02083333333333333218, 0.03125000000000000000, 0.04166666666666666435, 0.05208333333333333565, 0.06250000000000000000, 0.07291666666666667129, 0.08333333333333332871, 0.09375000000000000000, 0.1041666666666666713, 0.1145833333333333287, 0.1250000000000000000, 0.1354166666666666574, 0.1458333333333333426, 0.1562500000000000000, 0.1666666666666666574, 0.1770833333333333426, 0.1875000000000000000, 0.1979166666666666574, 0.2083333333333333426, 0.2187500000000000000, 0.2291666666666666574, 0.2395833333333333426, 0.2500000000000000000, 0.2604166666666666852, 0.2708333333333333148, 0.2812500000000000000, 0.2916666666666666852, 0.3020833333333333148, 0.3125000000000000000, 0.3229166666666666852, 0.3333333333333333148, 0.3437500000000000000, 0.3541666666666666852, 0.3645833333333333148, 0.3750000000000000000, 0.3854166666666666852, 0.3958333333333333148, 0.4062500000000000000, 0.4166666666666666852, 0.4270833333333333148, 0.4375000000000000000, 0.4479166666666666852, 0.4583333333333333148, 0.4687500000000000000, 0.4791666666666666852, 0.4895833333333333148, 0.5000000000000000000, 0.5104166666666666297, 0.5208333333333333703, 0.5312500000000000000, 0.5416666666666666297, 0.5520833333333333703, 0.5625000000000000000, 0.5729166666666666297, 0.5833333333333333703, 0.5937500000000000000, 0.6041666666666666297, 0.6145833333333333703, 0.6250000000000000000, 0.6354166666666666297, 0.6458333333333333703, 0.6562500000000000000, 0.6666666666666666297, 0.6770833333333333703, 0.6875000000000000000, 0.6979166666666666297, 0.7083333333333333703, 0.7187500000000000000, 0.7291666666666666297, 0.7395833333333333703, 0.7500000000000000000, 0.7604166666666666297, 0.7708333333333333703, 0.7812500000000000000, 0.7916666666666666297, 0.8020833333333333703, 0.8125000000000000000, 0.8229166666666666297, 0.8333333333333333703, 0.8437500000000000000, 0.8541666666666666297, 0.8645833333333333703, 0.8750000000000000000, 0.8854166666666666297, 0.8958333333333333703, 0.9062500000000000000, 0.9166666666666666297, 0.9270833333333333703, 0.9375000000000000000 ),
 .UNSPECIFIED. ) 
 GEOMETRIC_REPRESENTATION_ITEM ( )  RATIONAL_B_SPLINE_SURFACE ( (
 ( 1.000000000000000000, 0.9238795325112867385, 1.000000000000000000, 0.9238795325112867385, 1.000000000000000000, 0.9238795325112867385, 1.000000000000000000, 0.9238795325112867385, 1.000000000000000000, 0.9238795325112867385, 1.000000000000000000, 0.9238795325112867385, 1.000000000000000000, 0.9238795325112867385, 1.000000000000000000, 0.9238795325112867385, 1.000000000000000000, 0.9238795325112867385, 1.000000000000000000, 0.9238795325112867385, 1.000000000000000000, 0.9238795325112867385, 1.000000000000000000, 0.9238795325112867385, 1.000000000000000000, 0.9238795325112867385, 1.000000000000000000, 0.9238795325112867385, 1.000000000000000000, 0.9238795325112867385, 1.000000000000000000, 0.9238795325112867385, 1.000000000000000000, 0.9238795325112867385, 1.000000000000000000, 0.9238795325112867385, 1.000000000000000000, 0.9238795325112867385, 1.000000000000000000, 0.9238795325112867385, 1.000000000000000000, 0.9238795325112867385, 1.000000000000000000, 0.9238795325112867385, 1.000000000000000000, 0.9238795325112867385, 1.000000000000000000, 0.9238795325112867385, 1.000000000000000000, 0.9238795325112867385, 1.000000000000000000, 0.9238795325112867385, 1.000000000000000000, 0.9238795325112867385, 1.000000000000000000, 0.9238795325112867385, 1.000000000000000000, 0.9238795325112867385, 1.000000000000000000, 0.9238795325112867385, 1.000000000000000000, 0.9238795325112867385, 1.000000000000000000, 0.9238795325112867385, 1.000000000000000000, 0.9238795325112867385, 1.000000000000000000, 0.9238795325112867385, 1.000000000000000000, 0.9238795325112867385, 1.000000000000000000, 0.9238795325112867385, 1.000000000000000000, 0.9238795325112867385, 1.000000000000000000, 0.9238795325112867385, 1.000000000000000000, 0.9238795325112867385, 1.000000000000000000, 0.9238795325112867385, 1.000000000000000000, 0.9238795325112867385, 1.000000000000000000, 0.9238795325112867385, 1.000000000000000000, 0.9238795325112867385, 1.000000000000000000, 0.9238795325112867385, 1.000000000000000000, 0.9238795325112867385, 1.000000000000000000, 0.9238795325112867385, 1.000000000000000000, 0.9238795325112867385, 1.000000000000000000, 0.9238795325112867385, 1.000000000000000000, 0.9238795325112867385, 1.000000000000000000, 0.9238795325112867385, 1.000000000000000000, 0.9238795325112867385, 1.000000000000000000, 0.9238795325112867385, 1.000000000000000000, 0.9238795325112867385, 1.000000000000000000, 0.9238795325112867385, 1.000000000000000000, 0.9238795325112867385, 1.000000000000000000, 0.9238795325112867385, 1.000000000000000000, 0.9238795325112867385, 1.000000000000000000, 0.9238795325112867385, 1.000000000000000000, 0.9238795325112867385, 1.000000000000000000, 0.9238795325112867385, 1.000000000000000000, 0.9238795325112867385, 1.000000000000000000, 0.9238795325112867385, 1.000000000000000000, 0.9238795325112867385, 1.000000000000000000, 0.9238795325112867385, 1.000000000000000000, 0.9238795325112867385, 1.000000000000000000, 0.9238795325112867385, 1.000000000000000000, 0.9238795325112867385, 1.000000000000000000, 0.9238795325112867385, 1.000000000000000000, 0.9238795325112867385, 1.000000000000000000, 0.9238795325112867385, 1.000000000000000000, 0.9238795325112867385, 1.000000000000000000, 0.9238795325112867385, 1.000000000000000000, 0.9238795325112867385, 1.000000000000000000, 0.9238795325112867385, 1.000000000000000000, 0.9238795325112867385, 1.000000000000000000, 0.9238795325112867385, 1.000000000000000000, 0.9238795325112867385, 1.000000000000000000, 0.9238795325112867385, 1.000000000000000000, 0.9238795325112867385, 1.000000000000000000, 0.9238795325112867385, 1.000000000000000000, 0.9238795325112867385, 1.000000000000000000, 0.9238795325112867385, 1.000000000000000000, 0.9238795325112867385, 1.000000000000000000, 0.9238795325112867385, 1.000000000000000000, 0.9238795325112867385, 1.000000000000000000, 0.9238795325112867385, 1.000000000000000000, 0.9238795325112867385, 1.000000000000000000, 0.9238795325112867385, 1.000000000000000000, 0.9238795325112867385, 1.000000000000000000, 0.9238795325112867385, 1.000000000000000000),
 ( 1.000000000000000000, 0.9238795325112867385, 1.000000000000000000, 0.9238795325112867385, 1.000000000000000000, 0.9238795325112867385, 1.000000000000000000, 0.9238795325112867385, 1.000000000000000000, 0.9238795325112867385, 1.000000000000000000, 0.9238795325112867385, 1.000000000000000000, 0.9238795325112867385, 1.000000000000000000, 0.9238795325112867385, 1.000000000000000000, 0.9238795325112867385, 1.000000000000000000, 0.9238795325112867385, 1.000000000000000000, 0.9238795325112867385, 1.000000000000000000, 0.9238795325112867385, 1.000000000000000000, 0.9238795325112867385, 1.000000000000000000, 0.9238795325112867385, 1.000000000000000000, 0.9238795325112867385, 1.000000000000000000, 0.9238795325112867385, 1.000000000000000000, 0.9238795325112867385, 1.000000000000000000, 0.9238795325112867385, 1.000000000000000000, 0.9238795325112867385, 1.000000000000000000, 0.9238795325112867385, 1.000000000000000000, 0.9238795325112867385, 1.000000000000000000, 0.9238795325112867385, 1.000000000000000000, 0.9238795325112867385, 1.000000000000000000, 0.9238795325112867385, 1.000000000000000000, 0.9238795325112867385, 1.000000000000000000, 0.9238795325112867385, 1.000000000000000000, 0.9238795325112867385, 1.000000000000000000, 0.9238795325112867385, 1.000000000000000000, 0.9238795325112867385, 1.000000000000000000, 0.9238795325112867385, 1.000000000000000000, 0.9238795325112867385, 1.000000000000000000, 0.9238795325112867385, 1.000000000000000000, 0.9238795325112867385, 1.000000000000000000, 0.9238795325112867385, 1.000000000000000000, 0.9238795325112867385, 1.000000000000000000, 0.9238795325112867385, 1.000000000000000000, 0.9238795325112867385, 1.000000000000000000, 0.9238795325112867385, 1.000000000000000000, 0.9238795325112867385, 1.000000000000000000, 0.9238795325112867385, 1.000000000000000000, 0.9238795325112867385, 1.000000000000000000, 0.9238795325112867385, 1.000000000000000000, 0.9238795325112867385, 1.000000000000000000, 0.9238795325112867385, 1.000000000000000000, 0.9238795325112867385, 1.000000000000000000, 0.9238795325112867385, 1.000000000000000000, 0.9238795325112867385, 1.000000000000000000, 0.9238795325112867385, 1.000000000000000000, 0.9238795325112867385, 1.000000000000000000, 0.9238795325112867385, 1.000000000000000000, 0.9238795325112867385, 1.000000000000000000, 0.9238795325112867385, 1.000000000000000000, 0.9238795325112867385, 1.000000000000000000, 0.9238795325112867385, 1.000000000000000000, 0.9238795325112867385, 1.000000000000000000, 0.9238795325112867385, 1.000000000000000000, 0.9238795325112867385, 1.000000000000000000, 0.9238795325112867385, 1.000000000000000000, 0.9238795325112867385, 1.000000000000000000, 0.9238795325112867385, 1.000000000000000000, 0.9238795325112867385, 1.000000000000000000, 0.9238795325112867385, 1.000000000000000000, 0.9238795325112867385, 1.000000000000000000, 0.9238795325112867385, 1.000000000000000000, 0.9238795325112867385, 1.000000000000000000, 0.9238795325112867385, 1.000000000000000000, 0.9238795325112867385, 1.000000000000000000, 0.9238795325112867385, 1.000000000000000000, 0.9238795325112867385, 1.000000000000000000, 0.9238795325112867385, 1.000000000000000000, 0.9238795325112867385, 1.000000000000000000, 0.9238795325112867385, 1.000000000000000000, 0.9238795325112867385, 1.000000000000000000, 0.9238795325112867385, 1.000000000000000000, 0.9238795325112867385, 1.000000000000000000, 0.9238795325112867385, 1.000000000000000000, 0.9238795325112867385, 1.000000000000000000, 0.9238795325112867385, 1.000000000000000000, 0.9238795325112867385, 1.000000000000000000, 0.9238795325112867385, 1.000000000000000000, 0.9238795325112867385, 1.000000000000000000, 0.9238795325112867385, 1.000000000000000000, 0.9238795325112867385, 1.000000000000000000, 0.9238795325112867385, 1.000000000000000000, 0.9238795325112867385, 1.000000000000000000, 0.9238795325112867385, 1.000000000000000000, 0.9238795325112867385, 1.000000000000000000, 0.9238795325112867385, 1.000000000000000000, 0.9238795325112867385, 1.000000000000000000, 0.9238795325112867385, 1.000000000000000000) ) ) 
 REPRESENTATION_ITEM ( '' )  SURFACE ( )  );
#10566=( BOUNDED_CURVE ( )  B_SPLINE_CURVE ( 2, ( #17126, #7848, #11398, #415, #11644, #291, #6014, #9813, #17246 ),
 .UNSPECIFIED., .F., .T. ) 
 B_SPLINE_CURVE_WITH_KNOTS ( ( 3, 2, 2, 2, 3 ),
 ( 0.8541666666666666297, 0.8645833333333333703, 0.8750000000000000000, 0.8854166666666666297, 0.8958333333333333703 ),
 .UNSPECIFIED. ) 
 CURVE ( )  GEOMETRIC_REPRESENTATION_ITEM ( )  RATIONAL_B_SPLINE_CURVE ( ( 1.000000000000000000, 0.9238795325112867385, 1.000000000000000000, 0.9238795325112867385, 1.000000000000000000, 0.9238795325112867385, 1.000000000000000000, 0.9238795325112867385, 1.000000000000000000 ) ) 
 REPRESENTATION_ITEM ( '' )  );
#10567=ORIENTED_EDGE ( 'NONE', *, *, #19683, .T. ) ;
#10571=CARTESIAN_POINT ( 'NONE',  ( 0.2819296736111110979, 4.491750000075865223, -3.452642723725051716E-17 ) ) ;
#10575=CARTESIAN_POINT ( 'NONE',  ( -0.3100951778434036243, 4.225344069393538682, 0.03479879867075674066 ) ) ;
#10576=CARTESIAN_POINT ( 'NONE',  ( 0.1292346314604058410, 4.012583333333332725, 0.3119999999999998885 ) ) ;
#10579=CARTESIAN_POINT ( 'NONE',  ( -0.1292346314604057023, 5.068138889040620931, 0.3119999999999998885 ) ) ;
#10582=VERTEX_POINT ( 'NONE', #11370 ) ;
#10583=CARTESIAN_POINT ( 'NONE',  ( -1.858121103377620624E-07, 4.877166671810766019, -0.3119999999999446549 ) ) ;
#10590=CARTESIAN_POINT ( 'NONE',  ( -0.1167790944451423535, 5.210500000075866112, 0.2819296736111110424 ) ) ;
#10592=ORIENTED_EDGE ( 'NONE', *, *, #10668, .F. ) ;
#10594=CARTESIAN_POINT ( 'NONE',  ( -0.04876738698855743320, 4.292444203642808098, 0.3083149109922141973 ) ) ;
#10596=CARTESIAN_POINT ( 'NONE',  ( -0.3119999999999999996, 0.4868055555555551583, -0.1292346314604056745 ) ) ;
#10597=CARTESIAN_POINT ( 'NONE',  ( -0.2206173157302027676, 4.779944444444443441, 0.2206173157302028787 ) ) ;
#10598=CARTESIAN_POINT ( 'NONE',  ( -0.1993543840281266910, 4.234805555631421470, -0.1993543840281266910 ) ) ;
#10599=CARTESIAN_POINT ( 'NONE',  ( -5.731347020009612645E-17, 0.4416666665149336923, 0.3119999999999999996 ) ) ;
#10602=EDGE_LOOP ( 'NONE', ( #9936, #14124, #21281, #11111 ) ) ;
#10604=CARTESIAN_POINT ( 'NONE',  ( 0.2819296736111110979, 4.599388888964753619, 0.1167790944451422425 ) ) ;
#10610=CARTESIAN_POINT ( 'NONE',  ( 0.1167790944451424506, 4.161888888964755395, 0.2819296736111110424 ) ) ;
#10615=CARTESIAN_POINT ( 'NONE',  ( -0.2819296736111110424, 0.5736111110352444253, -0.1167790944451423396 ) ) ;
#10617=DIRECTION ( 'NONE',  ( -0.000000000000000000, -1.000000000000000000, -0.000000000000000000 ) ) ;
#10626=CARTESIAN_POINT ( 'NONE',  ( -0.2819296736111110424, 0.3930555554796889561, -0.1167790944451423396 ) ) ;
#10627=CARTESIAN_POINT ( 'NONE',  ( 0.2819296736111110979, 3.894527777853643347, -3.452642723725051716E-17 ) ) ;
#10629=CARTESIAN_POINT ( 'NONE',  ( -0.1167790944451423257, 4.523000000075867000, -0.2819296736111110424 ) ) ;
#10630=CARTESIAN_POINT ( 'NONE',  ( 0.1355903456263229667, 5.139740703596304527, -0.2731414004538880724 ) ) ;
#10631=CARTESIAN_POINT ( 'NONE',  ( -0.2206173157302027676, 4.613277777777776478, 0.2206173157302028787 ) ) ;
#10632=ORIENTED_EDGE ( 'NONE', *, *, #18094, .F. ) ;
#10634=CARTESIAN_POINT ( 'NONE',  ( 0.1993543840281267465, 5.151472222298087544, 0.1993543840281266633 ) ) ;
#10635=CARTESIAN_POINT ( 'NONE',  ( 0.1971119857566866196, 4.204467586177645266, -0.2422589368263572407 ) ) ;
#10636=CARTESIAN_POINT ( 'NONE',  ( 0.2819296736111111534, 4.821611111186976828, 0.1167790944451422563 ) ) ;
#10639=CARTESIAN_POINT ( 'NONE',  ( -5.731347020009612645E-17, 0.3305555554038226429, 0.3119999999999999996 ) ) ;
#10640=CARTESIAN_POINT ( 'NONE',  ( -0.3120000000000000551, 0.2090277776260448528, 0.1292346314604056190 ) ) ;
#10642=CARTESIAN_POINT ( 'NONE',  ( 0.2819296736111110424, 0.3305555554796889561, -0.1167790944451423119 ) ) ;
#10648=CARTESIAN_POINT ( 'NONE',  ( -0.04107592630348370910, 5.070398228275294628, 0.3098506894142968870 ) ) ;
#10649=ADVANCED_FACE ( 'NONE', ( #13216 ), #13325, .T. ) ;
#10651=CARTESIAN_POINT ( 'NONE',  ( -0.08227930641062801420, 3.879488480284497331, -0.3012013832029319382 ) ) ;
#10653=CARTESIAN_POINT ( 'NONE',  ( -0.2819296736111110424, 4.474388888964755395, -0.1167790944451423119 ) ) ;
#10654=CARTESIAN_POINT ( 'NONE',  ( 0.2772880126055080052, 4.534207701474789687, -0.1455781163606088280 ) ) ;
#10655=CARTESIAN_POINT ( 'NONE',  ( 0.1993543840281267465, 5.220916666742532186, 0.1993543840281266633 ) ) ;
#10657=CARTESIAN_POINT ( 'NONE',  ( 1.201146141948970407E-06, 4.904991752689871198, 0.3119999999951060254 ) ) ;
#10659=CARTESIAN_POINT ( 'NONE',  ( -0.05332757804796602052, 4.792349457816412084, 0.3074089561062771647 ) ) ;
#10660=CARTESIAN_POINT ( 'NONE',  ( 0.2206173157302027954, 4.314666666818398610, -0.2206173157302028232 ) ) ;
#10661=VECTOR ( 'NONE', #4157, 39.37007874015748143 ) ;
#10662=CARTESIAN_POINT ( 'NONE',  ( 0.1993543840281266633, 4.790361111186976828, -0.1993543840281266910 ) ) ;
#10663=CARTESIAN_POINT ( 'NONE',  ( -0.1993543840281266910, 3.734805555631421026, -0.1993543840281266910 ) ) ;
#10664=ORIENTED_EDGE ( 'NONE', *, *, #16067, .T. ) ;
#10665=ORIENTED_EDGE ( 'NONE', *, *, #12779, .T. ) ;
#10666=ADVANCED_FACE ( 'NONE', ( #9783 ), #11252, .T. ) ;
#10668=EDGE_CURVE ( 'NONE', #19238, #4599, #22694, .T. ) ;
#10674=CARTESIAN_POINT ( 'NONE',  ( -5.731347020009612645E-17, 0.2749999998482670627, 0.3119999999999999996 ) ) ;
#10676=CARTESIAN_POINT ( 'NONE',  ( -0.1370262819018738254, 5.125659746303123043, 0.2760471446584434330 ) ) ;
#10680=EDGE_CURVE ( 'NONE', #5059, #6423, #14115, .T. ) ;
#10682=CARTESIAN_POINT ( 'NONE',  ( 0.09537333962189972758, 5.097200745393280386, -0.2967035365653761803 ) ) ;
#10683=CARTESIAN_POINT ( 'NONE',  ( 0.2819296736111110424, 0.2541666665908000056, 0.1167790944451424923 ) ) ;
#10686=CARTESIAN_POINT ( 'NONE',  ( 0.2819296736111110424, 4.550777777853643791, -0.1167790944451423396 ) ) ;
#10690=CARTESIAN_POINT ( 'NONE',  ( -0.1292346314604057023, 4.116749999999998799, 0.3119999999999998885 ) ) ;
#10691=CARTESIAN_POINT ( 'NONE',  ( -0.2206173157302027676, 4.953555555707287894, 0.2206173157302028787 ) ) ;
#10695=CARTESIAN_POINT ( 'NONE',  ( -0.1892265952907544457, 4.882961343802892706, -0.2480685101248006896 ) ) ;
#10699=( BOUNDED_SURFACE ( )  B_SPLINE_SURFACE ( 1, 2, ( 
 ( #6923, #14485, #1315, #4842, #23609, #19968, #16311, #5199, #5329, #10951, #4962, #19841, #20090, #10590, #12429, #12794, #14361, #21910, #3025, #18017, #18260, #3379, #19722, #8739, #18378, #10472, #1673, #16195, #21791, #1196, #8628, #1555, #16073, #5080, #8993, #16436, #12548, #3255, #23846, #10706, #18141, #1438, #7166, #14609, #15942, #23724, #23368, #8870, #6677, #7049, #14122, #12308, #17902, #23485, #6801, #7766, #15209, #17032, #4101, #9358, #2039, #14859, #7288, #20452, #22276, #16800, #5571, #81, #3619, #13390, #20330, #13275, #16675, #1792, #20693, #11561, #3870, #9106, #9478, #5696, #326, #22644, #18621, #16911, #13159, #5930, #18498, #20812, #16555, #18988, #22518, #14739, #12919, #20573, #14973, #3748, #23977, #11312, #22154, #5451, #11069, #1914, #13036, #206, #11192, #18744, #9235, #24099, #7408, #7526, #22395, #7647, #15095, #5811, #3983, #11434, #18865, #2167, #9600, #14311, #17278, #15567, #21622, #22759, #17971, #3094, #17396, #6744, #22875, #9967, #10539, #8578, #1142, #10091, #1262, #13746, #8690, #22989, #11792, #13633, #23555, #17158, #6294, #16139, #6868, #21746, #5031, #2524, #19345, #8000, #448, #21051, #15452, #689, #6170, #8113, #20933, #12499, #13517, #14188, #9847, #19101, #4916, #2287, #21171, #9722, #2642, #4461, #7879, #15330, #19217, #17511, #11925, #6050, #11678, #4225, #2407, #564, #16018, #4341, #23435, #12378, #19795, #14556, #9299, #22100, #19920, #14918, #16739, #12743, #23795, #11019, #7117, #14683, #11137, #1855, #22, #1384, #22337, #12861, #20280, #21979, #7236, #5273, #5640, #23917, #10897, #7469, #10782, #9057, #14803, #16262, #18567, #20399, #18327, #24042, #16387, #18443, #20157, #8814, #3446, #5396, #3565, #9180, #3206, #10653, #18207, #1623, #16622, #16504, #1503, #18084, #1739, #7352, #6993, #22220, #5519, #12982, #23674, #8938, #14437, #21862, #5152, #3690, #12617, #20035, #3324, #9793, #13223, #22588, #19051, #507, #5873, #18935, #2352, #390, #11377, #3935, #4046, #7829, #17226, #17102, #7940, #15274, #15395, #11500, #11258, #13334, #22938, #270, #22822, #9664, #4287, #20756, #18805, #7709, #2100, #146, #6113, #20875, #13105, #3815, #13581, #4169, #9541, #22702, #5992, #16974, #13457, #15513, #7589, #15156, #11619, #1986, #15040, #2232, #20992, #11744, #19165, #2473, #9908, #17340, #633, #8064, #20633, #20518, #18684, #9422, #16861, #22463, #5762, #4407, #17458, #21359, #6716, #1112, #3062, #15754, #4759, #15634, #12114, #11871, #23166, #19284, #10398, #6478, #6597, #16110, #13929, #990, #8545, #6359, #10155, #19524, #2817, #6234, #2590, #4647, #12231, #23051, #10273, #17821, #14045, #21476, #21242, #11993, #17698, #17580, #10036, #13700, #8419, #869, #15867, #23283, #19641, #2940, #19406, #15987, #23408, #8302, #14161, #21591, #4884, #12349, #13806, #2704, #19766, #10510, #17940, #1236, #8661, #4530, #21117, #751, #8179, #14526, #14280, #20367, #18056, #10748, #11105, #1710, #3177, #18298, #7203, #14775, #8783, #3658, #23523, #22190, #12831, #5001, #10627, #10869, #5241, #18180, #12955, #1596, #6840, #18535, #1825, #16354, #3294, #14649, #1473, #9031, #5489, #9270, #21718, #12463, #19885, #16474, #23885, #8910, #22070, #23765, #1352, #3419, #21948, #16235, #14405, #12713, #18416, #23645, #6964, #24014, #20127, #3538, #20008, #5366, #7086, #21829, #20250, #10991, #9149, #16592, #5120, #12585, #7324, #20605, #13423 ),
 ( #7799, #7558, #22431, #5845, #3902, #14889, #24127, #2070, #11347, #15128, #22554, #11469, #2202, #5732, #4019, #5961, #18774, #358, #22672, #11592, #4135, #9393, #13191, #9511, #7910, #15242, #18902, #11710, #16833, #19133, #15362, #9755, #7678, #7442, #13551, #11226, #16944, #4259, #19023, #20486, #9635, #20845, #15011, #13308, #17065, #2318, #20723, #17192, #478, #22791, #6084, #22308, #243, #2437, #20965, #16710, #5606, #13071, #3782, #18654, #1947, #116, #8270, #15719, #4616, #19491, #15601, #21327, #23252, #11961, #17666, #15833, #4729, #21443, #2557, #23024, #21204, #1078, #8383, #12079, #4849, #10004, #12317, #8509, #2903, #841, #601, #6684, #4374, #4496, #21558, #12201, #13670, #2785, #952, #721, #23133, #10238, #6562, #13898, #14012, #19608, #10362, #6446, #8032, #2673, #19729, #19376, #17785, #15950, #23376, #17548, #8149, #10123, #6325, #21084, #14129, #9879, #17308, #15483, #22909, #6204, #13777, #11832, #19251, #17428, #3387, #5461, #21685, #18025, #5208, #16080, #4968, #8747, #7056, #14368, #21800, #6931, #20099, #9000, #18149, #5087, #10597, #12681, #10840, #16564, #22162, #1443, #6808, #1204, #14250, #8877, #3509, #22042, #23986, #12554, #1564, #12435, #16319, #8635, #19976, #23492, #7174, #3263, #18268, #12927, #10714, #21916, #5337, #3147, #23731, #14493, #16444, #3032, #19849, #23855, #14617, #1322, #12802, #20221, #10961, #18386, #16203, #23616, #1681, #9114, #7297, #14747, #10479, #17909, #15219, #333, #24106, #18629, #22766, #7416, #9729, #7532, #16808, #5578, #13043, #17039, #20460, #5704, #2175, #7773, #13166, #2047, #9609, #7654, #1922, #3877, #20820, #22651, #18874, #3991, #11569, #15102, #2294, #16918, #20580, #14981, #17167, #11077, #9486, #18996, #455, #4110, #15338, #11320, #13283, #9366, #18507, #22403, #88, #18751, #215, #22526, #14867, #7886, #22283, #5939, #3757, #11199, #13397, #6058, #5818, #20339, #20701, #11442, #3627, #1799, #9243, #16685, #10098, #4706, #22882, #10334, #13526, #12174, #2763, #19109, #17284, #814, #19351, #8123, #2875, #15695, #20940, #8482, #17761, #6301, #17403, #4593, #696, #8241, #19582, #1055, #15924, #2413, #23347, #6418, #13872, #15574, #23109, #22997, #4233, #17519, #4468, #11685, #4348, #2648, #8359, #9855, #572, #13989, #11932, #17640, #9976, #12052, #13754, #8007, #21179, #21300, #19465, #10214, #15459, #6177, #11802, #929, #15809, #23228, #19224, #13641, #6537, #21059, #2531, #21417, #23830, #21777, #21534, #3483, #1176, #18006, #18362, #8973, #10457, #1422, #14472, #21659, #5063, #18124, #3363, #10690, #10815, #8850, #18242, #12533, #4821, #23589, #16540, #1298, #1541, #3242, #22015, #14344, #4947, #8723, #12411, #17884, #16421, #21896, #6658, #12291, #7152, #5185, #19830, #16296, #23709, #3125, #7031, #9090, #8614, #10576, #12656, #19705, #16055, #16176, #20074, #6906, #19952, #14592, #5313, #12776, #20195, #10934, #14223, #1655, #14105, #3007, #23470, #6781, #3600, #22134, #11052, #14954, #303, #18842, #20788, #9339, #22496, #9219, #5675, #5435, #16775, #12900, #3965, #60, #183, #9698, #7506, #18721, #2139, #24080, #3729, #13140, #20553, #23958, #20316, #22374, #5791, #16658, #3848, #11409, #7623, #15074, #14840, #5553, #11293, #11176, #18481, #7272, #2020, #18603, #9457, #16890, #13255, #20672, #13018, #9577, #17010, #1896, #7743, #15187, #22624, #5910, #7388, #20433, #13367, #4079, #11534 ) ),
 .UNSPECIFIED., .F., .F., .F. ) 
 B_SPLINE_SURFACE_WITH_KNOTS ( ( 2, 2 ),
 ( 3, 2, 2, 2, 2, 2, 2, 2, 2, 2, 2, 2, 2, 2, 2, 2, 2, 2, 2, 2, 2, 2, 2, 2, 2, 2, 2, 2, 2, 2, 2, 2, 2, 2, 2, 2, 2, 2, 2, 2, 2, 2, 2, 2, 2, 2, 2, 2, 2, 2, 2, 2, 2, 2, 2, 2, 2, 2, 2, 2, 2, 2, 2, 2, 2, 2, 2, 2, 2, 2, 2, 2, 2, 2, 2, 2, 2, 2, 2, 2, 2, 2, 2, 2, 2, 2, 2, 2, 2, 2, 2, 2, 2, 2, 2, 2, 2, 2, 2, 2, 2, 2, 2, 2, 2, 2, 2, 2, 2, 2, 2, 2, 2, 2, 2, 2, 2, 2, 2, 2, 2, 2, 2, 2, 2, 2, 2, 2, 2, 2, 2, 2, 2, 2, 2, 2, 2, 2, 2, 2, 2, 2, 2, 2, 2, 2, 2, 2, 2, 2, 2, 2, 2, 2, 2, 2, 2, 2, 2, 2, 2, 2, 2, 2, 2, 2, 2, 2, 2, 2, 2, 2, 2, 2, 2, 2, 2, 2, 2, 2, 2, 2, 2, 2, 2, 2, 2, 2, 2, 2, 2, 2, 2, 2, 2, 2, 2, 2, 2, 2, 2, 2, 2, 2, 2, 2, 2, 2, 2, 2, 2, 2, 2, 2, 2, 2, 2, 2, 2, 2, 3 ),
 ( 0.000000000000000000, 1.000000000000000000 ),
 ( 0.000000000000000000, 0.004464285714285714038, 0.008928571428571428076, 0.01339285714285714211, 0.01785714285714285615, 0.02232142857142857192, 0.02678571428571428423, 0.03125000000000000000, 0.03571428571428571230, 0.04017857142857143155, 0.04464285714285714385, 0.04910714285714285615, 0.05357142857142856845, 0.05803571428571428770, 0.06250000000000000000, 0.06696428571428571230, 0.07142857142857142461, 0.07589285714285713691, 0.08035714285714286309, 0.08482142857142857539, 0.08928571428571428770, 0.09375000000000000000, 0.09821428571428571230, 0.1026785714285714246, 0.1071428571428571369, 0.1116071428571428631, 0.1160714285714285754, 0.1205357142857142877, 0.1250000000000000000, 0.1294642857142857262, 0.1339285714285714246, 0.1383928571428571508, 0.1428571428571428492, 0.1473214285714285754, 0.1517857142857142738, 0.1562500000000000000, 0.1607142857142857262, 0.1651785714285714246, 0.1696428571428571508, 0.1741071428571428492, 0.1785714285714285754, 0.1830357142857142738, 0.1875000000000000000, 0.1919642857142857262, 0.1964285714285714246, 0.2008928571428571508, 0.2053571428571428492, 0.2098214285714285754, 0.2142857142857142738, 0.2187500000000000000, 0.2232142857142857262, 0.2276785714285714246, 0.2321428571428571508, 0.2366071428571428492, 0.2410714285714285754, 0.2455357142857142738, 0.2500000000000000000, 0.2544642857142856984, 0.2589285714285714524, 0.2633928571428571508, 0.2678571428571428492, 0.2723214285714285476, 0.2767857142857143016, 0.2812500000000000000, 0.2857142857142856984, 0.2901785714285714524, 0.2946428571428571508, 0.2991071428571428492, 0.3035714285714285476, 0.3080357142857143016, 0.3125000000000000000, 0.3169642857142856984, 0.3214285714285714524, 0.3258928571428571508, 0.3303571428571428492, 0.3348214285714285476, 0.3392857142857143016, 0.3437500000000000000, 0.3482142857142856984, 0.3526785714285714524, 0.3571428571428571508, 0.3616071428571428492, 0.3660714285714285476, 0.3705357142857143016, 0.3750000000000000000, 0.3794642857142856984, 0.3839285714285714524, 0.3883928571428571508, 0.3928571428571428492, 0.3973214285714285476, 0.4017857142857143016, 0.4062500000000000000, 0.4107142857142856984, 0.4151785714285714524, 0.4196428571428571508, 0.4241071428571428492, 0.4285714285714285476, 0.4330357142857143016, 0.4375000000000000000, 0.4419642857142856984, 0.4464285714285714524, 0.4508928571428571508, 0.4553571428571428492, 0.4598214285714285476, 0.4642857142857143016, 0.4687500000000000000, 0.4732142857142856984, 0.4776785714285714524, 0.4821428571428571508, 0.4866071428571428492, 0.4910714285714285476, 0.4955357142857143016, 0.5000000000000000000, 0.5044642857142856984, 0.5089285714285713969, 0.5133928571428570953, 0.5178571428571429047, 0.5223214285714286031, 0.5267857142857143016, 0.5312500000000000000, 0.5357142857142856984, 0.5401785714285713969, 0.5446428571428570953, 0.5491071428571429047, 0.5535714285714286031, 0.5580357142857143016, 0.5625000000000000000, 0.5669642857142856984, 0.5714285714285713969, 0.5758928571428570953, 0.5803571428571429047, 0.5848214285714286031, 0.5892857142857143016, 0.5937500000000000000, 0.5982142857142856984, 0.6026785714285713969, 0.6071428571428570953, 0.6116071428571429047, 0.6160714285714286031, 0.6205357142857143016, 0.6250000000000000000, 0.6294642857142856984, 0.6339285714285713969, 0.6383928571428570953, 0.6428571428571429047, 0.6473214285714286031, 0.6517857142857143016, 0.6562500000000000000, 0.6607142857142856984, 0.6651785714285713969, 0.6696428571428570953, 0.6741071428571429047, 0.6785714285714286031, 0.6830357142857143016, 0.6875000000000000000, 0.6919642857142856984, 0.6964285714285713969, 0.7008928571428570953, 0.7053571428571429047, 0.7098214285714286031, 0.7142857142857143016, 0.7187500000000000000, 0.7232142857142856984, 0.7276785714285713969, 0.7321428571428570953, 0.7366071428571429047, 0.7410714285714286031, 0.7455357142857143016, 0.7500000000000000000, 0.7544642857142856984, 0.7589285714285713969, 0.7633928571428570953, 0.7678571428571429047, 0.7723214285714286031, 0.7767857142857143016, 0.7812500000000000000, 0.7857142857142856984, 0.7901785714285713969, 0.7946428571428570953, 0.7991071428571429047, 0.8035714285714286031, 0.8080357142857143016, 0.8125000000000000000, 0.8169642857142856984, 0.8214285714285713969, 0.8258928571428570953, 0.8303571428571429047, 0.8348214285714286031, 0.8392857142857143016, 0.8437500000000000000, 0.8482142857142856984, 0.8526785714285713969, 0.8571428571428570953, 0.8616071428571429047, 0.8660714285714286031, 0.8705357142857143016, 0.8750000000000000000, 0.8794642857142856984, 0.8839285714285713969, 0.8883928571428570953, 0.8928571428571429047, 0.8973214285714286031, 0.9017857142857143016, 0.9062500000000000000, 0.9107142857142856984, 0.9151785714285713969, 0.9196428571428570953, 0.9241071428571429047, 0.9285714285714286031, 0.9330357142857143016, 0.9375000000000000000, 0.9419642857142856984, 0.9464285714285713969, 0.9508928571428570953, 0.9553571428571429047, 0.9598214285714286031, 0.9642857142857143016, 0.9687500000000000000, 0.9732142857142856984, 0.9771335280684947389, 0.9869048633491797062 ),
 .UNSPECIFIED. ) 
 GEOMETRIC_REPRESENTATION_ITEM ( )  RATIONAL_B_SPLINE_SURFACE ( (
 ( 1.000000000000000000, 0.9238795325112867385, 1.000000000000000000, 0.9238795325112867385, 1.000000000000000000, 0.9238795325112867385, 1.000000000000000000, 0.9238795325112867385, 1.000000000000000000, 0.9238795325112867385, 1.000000000000000000, 0.9238795325112867385, 1.000000000000000000, 0.9238795325112867385, 1.000000000000000000, 0.9238795325112867385, 1.000000000000000000, 0.9238795325112867385, 1.000000000000000000, 0.9238795325112867385, 1.000000000000000000, 0.9238795325112867385, 1.000000000000000000, 0.9238795325112867385, 1.000000000000000000, 0.9238795325112867385, 1.000000000000000000, 0.9238795325112867385, 1.000000000000000000, 0.9238795325112867385, 1.000000000000000000, 0.9238795325112867385, 1.000000000000000000, 0.9238795325112867385, 1.000000000000000000, 0.9238795325112867385, 1.000000000000000000, 0.9238795325112867385, 1.000000000000000000, 0.9238795325112867385, 1.000000000000000000, 0.9238795325112867385, 1.000000000000000000, 0.9238795325112867385, 1.000000000000000000, 0.9238795325112867385, 1.000000000000000000, 0.9238795325112867385, 1.000000000000000000, 0.9238795325112867385, 1.000000000000000000, 0.9238795325112867385, 1.000000000000000000, 0.9238795325112867385, 1.000000000000000000, 0.9238795325112867385, 1.000000000000000000, 0.9238795325112867385, 1.000000000000000000, 0.9238795325112867385, 1.000000000000000000, 0.9238795325112867385, 1.000000000000000000, 0.9238795325112867385, 1.000000000000000000, 0.9238795325112867385, 1.000000000000000000, 0.9238795325112867385, 1.000000000000000000, 0.9238795325112867385, 1.000000000000000000, 0.9238795325112867385, 1.000000000000000000, 0.9238795325112867385, 1.000000000000000000, 0.9238795325112867385, 1.000000000000000000, 0.9238795325112867385, 1.000000000000000000, 0.9238795325112867385, 1.000000000000000000, 0.9238795325112867385, 1.000000000000000000, 0.9238795325112867385, 1.000000000000000000, 0.9238795325112867385, 1.000000000000000000, 0.9238795325112867385, 1.000000000000000000, 0.9238795325112867385, 1.000000000000000000, 0.9238795325112867385, 1.000000000000000000, 0.9238795325112867385, 1.000000000000000000, 0.9238795325112867385, 1.000000000000000000, 0.9238795325112867385, 1.000000000000000000, 0.9238795325112867385, 1.000000000000000000, 0.9238795325112867385, 1.000000000000000000, 0.9238795325112867385, 1.000000000000000000, 0.9238795325112867385, 1.000000000000000000, 0.9238795325112867385, 1.000000000000000000, 0.9238795325112867385, 1.000000000000000000, 0.9238795325112867385, 1.000000000000000000, 0.9238795325112867385, 1.000000000000000000, 0.9238795325112867385, 1.000000000000000000, 0.9238795325112867385, 1.000000000000000000, 0.9238795325112867385, 1.000000000000000000, 0.9238795325112867385, 1.000000000000000000, 0.9238795325112867385, 1.000000000000000000, 0.9238795325112867385, 1.000000000000000000, 0.9238795325112867385, 1.000000000000000000, 0.9238795325112867385, 1.000000000000000000, 0.9238795325112867385, 1.000000000000000000, 0.9238795325112867385, 1.000000000000000000, 0.9238795325112867385, 1.000000000000000000, 0.9238795325112867385, 1.000000000000000000, 0.9238795325112867385, 1.000000000000000000, 0.9238795325112867385, 1.000000000000000000, 0.9238795325112867385, 1.000000000000000000, 0.9238795325112867385, 1.000000000000000000, 0.9238795325112867385, 1.000000000000000000, 0.9238795325112867385, 1.000000000000000000, 0.9238795325112867385, 1.000000000000000000, 0.9238795325112867385, 1.000000000000000000, 0.9238795325112867385, 1.000000000000000000, 0.9238795325112867385, 1.000000000000000000, 0.9238795325112867385, 1.000000000000000000, 0.9238795325112867385, 1.000000000000000000, 0.9238795325112867385, 1.000000000000000000, 0.9238795325112867385, 1.000000000000000000, 0.9238795325112867385, 1.000000000000000000, 0.9238795325112867385, 1.000000000000000000, 0.9238795325112867385, 1.000000000000000000, 0.9238795325112867385, 1.000000000000000000, 0.9238795325112867385, 1.000000000000000000, 0.9238795325112867385, 1.000000000000000000, 0.9238795325112867385, 1.000000000000000000, 0.9238795325112867385, 1.000000000000000000, 0.9238795325112867385, 1.000000000000000000, 0.9238795325112867385, 1.000000000000000000, 0.9238795325112867385, 1.000000000000000000, 0.9238795325112867385, 1.000000000000000000, 0.9238795325112867385, 1.000000000000000000, 0.9238795325112867385, 1.000000000000000000, 0.9238795325112867385, 1.000000000000000000, 0.9238795325112867385, 1.000000000000000000, 0.9238795325112867385, 1.000000000000000000, 0.9238795325112867385, 1.000000000000000000, 0.9238795325112867385, 1.000000000000000000, 0.9238795325112867385, 1.000000000000000000, 0.9238795325112867385, 1.000000000000000000, 0.9238795325112867385, 1.000000000000000000, 0.9238795325112867385, 1.000000000000000000, 0.9238795325112867385, 1.000000000000000000, 0.9238795325112867385, 1.000000000000000000, 0.9238795325112867385, 1.000000000000000000, 0.9238795325112867385, 1.000000000000000000, 0.9238795325112867385, 1.000000000000000000, 0.9238795325112867385, 1.000000000000000000, 0.9238795325112867385, 1.000000000000000000, 0.9238795325112867385, 1.000000000000000000, 0.9238795325112867385, 1.000000000000000000, 0.9238795325112867385, 1.000000000000000000, 0.9238795325112867385, 1.000000000000000000, 0.9238795325112867385, 1.000000000000000000, 0.9238795325112867385, 1.000000000000000000, 0.9238795325112867385, 1.000000000000000000, 0.9238795325112867385, 1.000000000000000000, 0.9238795325112867385, 1.000000000000000000, 0.9238795325112867385, 1.000000000000000000, 0.9238795325112867385, 1.000000000000000000, 0.9238795325112867385, 1.000000000000000000, 0.9238795325112867385, 1.000000000000000000, 0.9238795325112867385, 1.000000000000000000, 0.9238795325112867385, 1.000000000000000000, 0.9238795325112867385, 1.000000000000000000, 0.9238795325112867385, 1.000000000000000000, 0.9238795325112867385, 1.000000000000000000, 0.9238795325112867385, 1.000000000000000000, 0.9238795325112867385, 1.000000000000000000, 0.9238795325112867385, 1.000000000000000000, 0.9238795325112867385, 1.000000000000000000, 0.9238795325112867385, 1.000000000000000000, 0.9238795325112867385, 1.000000000000000000, 0.9238795325112867385, 1.000000000000000000, 0.9238795325112867385, 1.000000000000000000, 0.9238795325112867385, 1.000000000000000000, 0.9238795325112867385, 1.000000000000000000, 0.9238795325112867385, 1.000000000000000000, 0.9238795325112867385, 1.000000000000000000, 0.9238795325112867385, 1.000000000000000000, 0.9238795325112867385, 1.000000000000000000, 0.9238795325112867385, 1.000000000000000000, 0.9238795325112867385, 1.000000000000000000, 0.9238795325112867385, 1.000000000000000000, 0.9238795325112867385, 1.000000000000000000, 0.9238795325112867385, 1.000000000000000000, 0.9238795325112867385, 1.000000000000000000, 0.9238795325112867385, 1.000000000000000000, 0.9238795325112867385, 1.000000000000000000, 0.9238795325112867385, 1.000000000000000000, 0.9238795325112867385, 1.000000000000000000, 0.9238795325112867385, 1.000000000000000000, 0.9238795325112867385, 1.000000000000000000, 0.9238795325112867385, 1.000000000000000000, 0.9238795325112867385, 1.000000000000000000, 0.9238795325112867385, 1.000000000000000000, 0.9238795325112867385, 1.000000000000000000, 0.9238795325112867385, 1.000000000000000000, 0.9238795325112867385, 1.000000000000000000, 0.9238795325112867385, 1.000000000000000000, 0.9238795325112867385, 1.000000000000000000, 0.9238795325112867385, 1.000000000000000000, 0.9238795325112867385, 1.000000000000000000, 0.9238795325112867385, 1.000000000000000000, 0.9238795325112867385, 1.000000000000000000, 0.9238795325112867385, 1.000000000000000000, 0.9238795325112867385, 1.000000000000000000, 0.9238795325112867385, 1.000000000000000000, 0.9238795325112867385, 1.000000000000000000, 0.9238795325112867385, 1.000000000000000000, 0.9238795325112867385, 1.000000000000000000, 0.9238795325112867385, 1.000000000000000000, 0.9238795325112867385, 1.000000000000000000, 0.9238795325112867385, 1.000000000000000000, 0.9238795325112867385, 1.000000000000000000, 0.9238795325112867385, 1.000000000000000000, 0.9238795325112867385, 1.000000000000000000, 0.9238795325112867385, 1.000000000000000000, 0.9238795325112867385, 1.000000000000000000, 0.9238795325112867385, 1.000000000000000000, 0.9238795325112867385, 1.000000000000000000, 0.9238795325112867385, 1.000000000000000000, 0.9238795325112867385, 1.000000000000000000, 0.9238795325112867385, 1.000000000000000000, 0.9238795325112867385, 1.000000000000000000, 0.9238795325112867385, 1.000000000000000000, 0.9238795325112867385, 1.000000000000000000, 0.9238795325112867385, 1.000000000000000000, 0.9238795325112867385, 1.000000000000000000, 0.9238795325112867385, 1.000000000000000000, 0.9238795325112867385, 1.000000000000000000, 0.9238795325112867385, 1.000000000000000000, 0.9238795325112867385, 1.000000000000000000, 0.9238795325112867385, 1.000000000000000000, 0.9238795325112867385, 1.000000000000000000, 0.9238795325112867385, 1.000000000000000000, 0.9238795325112867385, 1.000000000000000000, 0.9238795325112867385, 1.000000000000000000, 0.9238795325112867385, 1.000000000000000000, 0.9238795325112867385, 1.000000000000000000, 0.9238795325112867385, 1.000000000000000000, 0.9238795325112867385, 1.000000000000000000, 0.9238795325112867385, 1.000000000000000000, 0.9238795325112867385, 1.000000000000000000, 0.9238795325112867385, 1.000000000000000000, 0.9238795325112867385, 1.000000000000000000, 0.9238795325112867385, 1.000000000000000000, 0.9238795325112867385, 1.000000000000000000, 0.9238795325112867385, 1.000000000000000000, 0.9238795325112867385, 1.000000000000000000, 0.9238795325112867385, 1.000000000000000000, 0.9238795325112867385, 1.000000000000000000, 0.9238795325112867385, 1.000000000000000000, 0.9238795325112867385, 1.000000000000000000, 0.9331730585143133139, 0.9836822358325096882, 0.9836822358325096882, 0.9836822358325096882),
 ( 1.000000000000000000, 0.9238795325112867385, 1.000000000000000000, 0.9238795325112867385, 1.000000000000000000, 0.9238795325112867385, 1.000000000000000000, 0.9238795325112867385, 1.000000000000000000, 0.9238795325112867385, 1.000000000000000000, 0.9238795325112867385, 1.000000000000000000, 0.9238795325112867385, 1.000000000000000000, 0.9238795325112867385, 1.000000000000000000, 0.9238795325112867385, 1.000000000000000000, 0.9238795325112867385, 1.000000000000000000, 0.9238795325112867385, 1.000000000000000000, 0.9238795325112867385, 1.000000000000000000, 0.9238795325112867385, 1.000000000000000000, 0.9238795325112867385, 1.000000000000000000, 0.9238795325112867385, 1.000000000000000000, 0.9238795325112867385, 1.000000000000000000, 0.9238795325112867385, 1.000000000000000000, 0.9238795325112867385, 1.000000000000000000, 0.9238795325112867385, 1.000000000000000000, 0.9238795325112867385, 1.000000000000000000, 0.9238795325112867385, 1.000000000000000000, 0.9238795325112867385, 1.000000000000000000, 0.9238795325112867385, 1.000000000000000000, 0.9238795325112867385, 1.000000000000000000, 0.9238795325112867385, 1.000000000000000000, 0.9238795325112867385, 1.000000000000000000, 0.9238795325112867385, 1.000000000000000000, 0.9238795325112867385, 1.000000000000000000, 0.9238795325112867385, 1.000000000000000000, 0.9238795325112867385, 1.000000000000000000, 0.9238795325112867385, 1.000000000000000000, 0.9238795325112867385, 1.000000000000000000, 0.9238795325112867385, 1.000000000000000000, 0.9238795325112867385, 1.000000000000000000, 0.9238795325112867385, 1.000000000000000000, 0.9238795325112867385, 1.000000000000000000, 0.9238795325112867385, 1.000000000000000000, 0.9238795325112867385, 1.000000000000000000, 0.9238795325112867385, 1.000000000000000000, 0.9238795325112867385, 1.000000000000000000, 0.9238795325112867385, 1.000000000000000000, 0.9238795325112867385, 1.000000000000000000, 0.9238795325112867385, 1.000000000000000000, 0.9238795325112867385, 1.000000000000000000, 0.9238795325112867385, 1.000000000000000000, 0.9238795325112867385, 1.000000000000000000, 0.9238795325112867385, 1.000000000000000000, 0.9238795325112867385, 1.000000000000000000, 0.9238795325112867385, 1.000000000000000000, 0.9238795325112867385, 1.000000000000000000, 0.9238795325112867385, 1.000000000000000000, 0.9238795325112867385, 1.000000000000000000, 0.9238795325112867385, 1.000000000000000000, 0.9238795325112867385, 1.000000000000000000, 0.9238795325112867385, 1.000000000000000000, 0.9238795325112867385, 1.000000000000000000, 0.9238795325112867385, 1.000000000000000000, 0.9238795325112867385, 1.000000000000000000, 0.9238795325112867385, 1.000000000000000000, 0.9238795325112867385, 1.000000000000000000, 0.9238795325112867385, 1.000000000000000000, 0.9238795325112867385, 1.000000000000000000, 0.9238795325112867385, 1.000000000000000000, 0.9238795325112867385, 1.000000000000000000, 0.9238795325112867385, 1.000000000000000000, 0.9238795325112867385, 1.000000000000000000, 0.9238795325112867385, 1.000000000000000000, 0.9238795325112867385, 1.000000000000000000, 0.9238795325112867385, 1.000000000000000000, 0.9238795325112867385, 1.000000000000000000, 0.9238795325112867385, 1.000000000000000000, 0.9238795325112867385, 1.000000000000000000, 0.9238795325112867385, 1.000000000000000000, 0.9238795325112867385, 1.000000000000000000, 0.9238795325112867385, 1.000000000000000000, 0.9238795325112867385, 1.000000000000000000, 0.9238795325112867385, 1.000000000000000000, 0.9238795325112867385, 1.000000000000000000, 0.9238795325112867385, 1.000000000000000000, 0.9238795325112867385, 1.000000000000000000, 0.9238795325112867385, 1.000000000000000000, 0.9238795325112867385, 1.000000000000000000, 0.9238795325112867385, 1.000000000000000000, 0.9238795325112867385, 1.000000000000000000, 0.9238795325112867385, 1.000000000000000000, 0.9238795325112867385, 1.000000000000000000, 0.9238795325112867385, 1.000000000000000000, 0.9238795325112867385, 1.000000000000000000, 0.9238795325112867385, 1.000000000000000000, 0.9238795325112867385, 1.000000000000000000, 0.9238795325112867385, 1.000000000000000000, 0.9238795325112867385, 1.000000000000000000, 0.9238795325112867385, 1.000000000000000000, 0.9238795325112867385, 1.000000000000000000, 0.9238795325112867385, 1.000000000000000000, 0.9238795325112867385, 1.000000000000000000, 0.9238795325112867385, 1.000000000000000000, 0.9238795325112867385, 1.000000000000000000, 0.9238795325112867385, 1.000000000000000000, 0.9238795325112867385, 1.000000000000000000, 0.9238795325112867385, 1.000000000000000000, 0.9238795325112867385, 1.000000000000000000, 0.9238795325112867385, 1.000000000000000000, 0.9238795325112867385, 1.000000000000000000, 0.9238795325112867385, 1.000000000000000000, 0.9238795325112867385, 1.000000000000000000, 0.9238795325112867385, 1.000000000000000000, 0.9238795325112867385, 1.000000000000000000, 0.9238795325112867385, 1.000000000000000000, 0.9238795325112867385, 1.000000000000000000, 0.9238795325112867385, 1.000000000000000000, 0.9238795325112867385, 1.000000000000000000, 0.9238795325112867385, 1.000000000000000000, 0.9238795325112867385, 1.000000000000000000, 0.9238795325112867385, 1.000000000000000000, 0.9238795325112867385, 1.000000000000000000, 0.9238795325112867385, 1.000000000000000000, 0.9238795325112867385, 1.000000000000000000, 0.9238795325112867385, 1.000000000000000000, 0.9238795325112867385, 1.000000000000000000, 0.9238795325112867385, 1.000000000000000000, 0.9238795325112867385, 1.000000000000000000, 0.9238795325112867385, 1.000000000000000000, 0.9238795325112867385, 1.000000000000000000, 0.9238795325112867385, 1.000000000000000000, 0.9238795325112867385, 1.000000000000000000, 0.9238795325112867385, 1.000000000000000000, 0.9238795325112867385, 1.000000000000000000, 0.9238795325112867385, 1.000000000000000000, 0.9238795325112867385, 1.000000000000000000, 0.9238795325112867385, 1.000000000000000000, 0.9238795325112867385, 1.000000000000000000, 0.9238795325112867385, 1.000000000000000000, 0.9238795325112867385, 1.000000000000000000, 0.9238795325112867385, 1.000000000000000000, 0.9238795325112867385, 1.000000000000000000, 0.9238795325112867385, 1.000000000000000000, 0.9238795325112867385, 1.000000000000000000, 0.9238795325112867385, 1.000000000000000000, 0.9238795325112867385, 1.000000000000000000, 0.9238795325112867385, 1.000000000000000000, 0.9238795325112867385, 1.000000000000000000, 0.9238795325112867385, 1.000000000000000000, 0.9238795325112867385, 1.000000000000000000, 0.9238795325112867385, 1.000000000000000000, 0.9238795325112867385, 1.000000000000000000, 0.9238795325112867385, 1.000000000000000000, 0.9238795325112867385, 1.000000000000000000, 0.9238795325112867385, 1.000000000000000000, 0.9238795325112867385, 1.000000000000000000, 0.9238795325112867385, 1.000000000000000000, 0.9238795325112867385, 1.000000000000000000, 0.9238795325112867385, 1.000000000000000000, 0.9238795325112867385, 1.000000000000000000, 0.9238795325112867385, 1.000000000000000000, 0.9238795325112867385, 1.000000000000000000, 0.9238795325112867385, 1.000000000000000000, 0.9238795325112867385, 1.000000000000000000, 0.9238795325112867385, 1.000000000000000000, 0.9238795325112867385, 1.000000000000000000, 0.9238795325112867385, 1.000000000000000000, 0.9238795325112867385, 1.000000000000000000, 0.9238795325112867385, 1.000000000000000000, 0.9238795325112867385, 1.000000000000000000, 0.9238795325112867385, 1.000000000000000000, 0.9238795325112867385, 1.000000000000000000, 0.9238795325112867385, 1.000000000000000000, 0.9238795325112867385, 1.000000000000000000, 0.9238795325112867385, 1.000000000000000000, 0.9238795325112867385, 1.000000000000000000, 0.9238795325112867385, 1.000000000000000000, 0.9238795325112867385, 1.000000000000000000, 0.9238795325112867385, 1.000000000000000000, 0.9238795325112867385, 1.000000000000000000, 0.9238795325112867385, 1.000000000000000000, 0.9238795325112867385, 1.000000000000000000, 0.9238795325112867385, 1.000000000000000000, 0.9238795325112867385, 1.000000000000000000, 0.9238795325112867385, 1.000000000000000000, 0.9238795325112867385, 1.000000000000000000, 0.9238795325112867385, 1.000000000000000000, 0.9238795325112867385, 1.000000000000000000, 0.9238795325112867385, 1.000000000000000000, 0.9238795325112867385, 1.000000000000000000, 0.9238795325112867385, 1.000000000000000000, 0.9238795325112867385, 1.000000000000000000, 0.9238795325112867385, 1.000000000000000000, 0.9238795325112867385, 1.000000000000000000, 0.9238795325112867385, 1.000000000000000000, 0.9238795325112867385, 1.000000000000000000, 0.9238795325112867385, 1.000000000000000000, 0.9238795325112867385, 1.000000000000000000, 0.9238795325112867385, 1.000000000000000000, 0.9238795325112867385, 1.000000000000000000, 0.9238795325112867385, 1.000000000000000000, 0.9238795325112867385, 1.000000000000000000, 0.9238795325112867385, 1.000000000000000000, 0.9238795325112867385, 1.000000000000000000, 0.9238795325112867385, 1.000000000000000000, 0.9238795325112867385, 1.000000000000000000, 0.9238795325112867385, 1.000000000000000000, 0.9238795325112867385, 1.000000000000000000, 0.9238795325112867385, 1.000000000000000000, 0.9238795325112867385, 1.000000000000000000, 0.9238795325112867385, 1.000000000000000000, 0.9238795325112867385, 1.000000000000000000, 0.9238795325112867385, 1.000000000000000000, 0.9238795325112867385, 1.000000000000000000, 0.9238795325112867385, 1.000000000000000000, 0.9238795325112867385, 1.000000000000000000, 0.9238795325112867385, 1.000000000000000000, 0.9238795325112867385, 1.000000000000000000, 0.9238795325112867385, 1.000000000000000000, 0.9238795325112867385, 1.000000000000000000, 0.9238795325112867385, 1.000000000000000000, 0.9238795325112867385, 1.000000000000000000, 0.9238795325112867385, 1.000000000000000000, 0.9238795325112867385, 1.000000000000000000, 0.9331730585143133139, 0.9836822358325096882, 0.9836822358325096882, 0.9836822358325096882) ) ) 
 REPRESENTATION_ITEM ( '' )  SURFACE ( )  );
#10700=VECTOR ( 'NONE', #11269, 39.37007874015748143 ) ;
#10701=EDGE_CURVE ( 'NONE', #5752, #12807, #15626, .T. ) ;
#10704=CARTESIAN_POINT ( 'NONE',  ( -0.2819296736111111534, 0.2472222221463555580, 0.1167790944451422563 ) ) ;
#10706=CARTESIAN_POINT ( 'NONE',  ( 0.2819296736111110424, 5.120222222298088433, -0.1167790944451423396 ) ) ;
#10707=DIRECTION ( 'NONE',  ( -0.000000000000000000, -1.000000000000000000, -0.000000000000000000 ) ) ;
#10710=CARTESIAN_POINT ( 'NONE',  ( -1.910449006669871087E-17, 3.870222222222221564, -0.3119999999999999996 ) ) ;
#10711=CARTESIAN_POINT ( 'NONE',  ( -0.0006126656105341529409, 4.293815956690722579, 0.3119994368665558460 ) ) ;
#10714=CARTESIAN_POINT ( 'NONE',  ( 0.2206173157302027954, 4.696611111111110404, -0.2206173157302028232 ) ) ;
#10715=CARTESIAN_POINT ( 'NONE',  ( 0.1182602959184163444, 5.202871751913769494, 0.2584494713975609703 ) ) ;
#10716=CARTESIAN_POINT ( 'NONE',  ( -1.726321361862525858E-17, 3.894527777853643347, -0.2819296736111110979 ) ) ;
#10717=CARTESIAN_POINT ( 'NONE',  ( 0.1167790944451422702, 3.793833333409199149, -0.2819296736111110424 ) ) ;
#10722=ORIENTED_EDGE ( 'NONE', *, *, #21273, .T. ) ;
#10724=CARTESIAN_POINT ( 'NONE',  ( -0.2819296736111110424, 4.571611111186975940, -0.1167790944451423119 ) ) ;
#10725=CARTESIAN_POINT ( 'NONE',  ( -0.2450779571127529310, 4.508096002043260775, 0.1931108503236894369 ) ) ;
#10730=CARTESIAN_POINT ( 'NONE',  ( 0.2819296736111110979, 4.061194444520309865, -3.452642723725051716E-17 ) ) ;
#10731=CARTESIAN_POINT ( 'NONE',  ( -0.3098980794439091802, 4.834497018200990759, -0.03649681129806247454 ) ) ;
#10737=CARTESIAN_POINT ( 'NONE',  ( -0.2819296736111110979, 0.06319444436857780956, -3.452642723725051716E-17 ) ) ;
#10743=ORIENTED_EDGE ( 'NONE', *, *, #18460, .T. ) ;
#10746=CARTESIAN_POINT ( 'NONE',  ( 0.1993543840281266910, 0.5979166665908001166, -0.1993543840281266910 ) ) ;
#10747=CARTESIAN_POINT ( 'NONE',  ( -0.3119999999999999996, -0.009722222222222557178, -3.820898013339742174E-17 ) ) ;
#10748=CARTESIAN_POINT ( 'NONE',  ( 0.1167790944451424368, 3.939666666742532186, 0.2819296736111110424 ) ) ;
#10750=AXIS2_PLACEMENT_3D ( 'NONE', #11670, #20923, #4334 ) ;
#10751=CARTESIAN_POINT ( 'NONE',  ( 0.2819296736111110979, 4.394527777853643791, -3.452642723725051716E-17 ) ) ;
#10756=EDGE_CURVE ( 'NONE', #21992, #10917, #4640, .T. ) ;
#10757=CARTESIAN_POINT ( 'NONE',  ( 5.731347020009612645E-17, 3.738277777929510215, 0.3119999999999999996 ) ) ;
#10759=CARTESIAN_POINT ( 'NONE',  ( 0.03516597121239248974, 4.209501246269358177, -0.3101320692603155571 ) ) ;
#10760=B_SPLINE_CURVE_WITH_KNOTS ( 'NONE', 3,
 ( #12521, #22002, #13006, #14461, #18349, #10676, #5302, #18110, #1407, #12765, #3350, #18232, #1643, #1529, #8962, #7139, #9078, #12365, #16127, #4778, #21490, #23542, #10290, #23424, #5018, #17956, #8678, #8438, #23300, #6734, #12245, #15768, #885, #2957, #19659, #16005, #14177, #19782, #3082, #6612, #4903, #1130, #18071, #6857 ),
 .UNSPECIFIED., .F., .F.,
 ( 4, 2, 2, 2, 2, 2, 2, 2, 2, 2, 2, 2, 2, 2, 2, 2, 2, 2, 2, 2, 2, 4 ),
 ( 0.05299829238697165851, 0.05454307465341280692, 0.05608785691985395533, 0.05763263918629510374, 0.05840503031951568141, 0.05917742145273625909, 0.05994981258595682982, 0.06072220371917740750, 0.06226698598561855591, 0.06381176825205971126, 0.06535655051850086661, 0.06612894165172143734, 0.06690133278494202196, 0.06844611505138316343, 0.06999089731782431878, 0.07076328845104488952, 0.07153567958426546025, 0.07308046185070661560, 0.07462524411714777095, 0.07617002638358892630, 0.07694241751680949704, 0.07771480865003008165 ),
 .UNSPECIFIED. ) ;
#10764=CARTESIAN_POINT ( 'NONE',  ( 0.1167790944451422702, 5.002166666742532186, -0.2819296736111110979 ) ) ;
#10768=CARTESIAN_POINT ( 'NONE',  ( -0.02336201496938555139, 4.070985353836114484, 0.3119999969656189198 ) ) ;
#10770=VERTEX_POINT ( 'NONE', #11985 ) ;
#10771=CARTESIAN_POINT ( 'NONE',  ( 0.1167790944451423535, 0.2611111110352444808, 0.2819296736111110424 ) ) ;
#10773=CARTESIAN_POINT ( 'NONE',  ( -0.2819296736111110979, 0.02499999992413337591, 0.1167790944451422425 ) ) ;
#10777=CARTESIAN_POINT ( 'NONE',  ( -0.2206173157302027676, 4.502166666666665762, 0.2206173157302028787 ) ) ;
#10778=CARTESIAN_POINT ( 'NONE',  ( -0.1292346314603983470, 3.783416666666665762, 0.3120000000000073270 ) ) ;
#10779=LINE ( 'NONE', #14680, #1182 ) ;
#10781=CYLINDRICAL_SURFACE ( 'NONE', #15873, 0.3119999999999999996 ) ;
#10782=CARTESIAN_POINT ( 'NONE',  ( -0.2819296736111110979, 4.533416666742532186, 0.000000000000000000 ) ) ;
#10785=CARTESIAN_POINT ( 'NONE',  ( 0.1993543840281267465, 5.109805555631420582, 0.1993543840281266633 ) ) ;
#10786=CARTESIAN_POINT ( 'NONE',  ( -0.09735099498061879075, 0.04500432081407945706, -0.2786451087458969300 ) ) ;
#10790=CARTESIAN_POINT ( 'NONE',  ( -0.1292346314604057023, 4.290361111262844140, 0.3119999999999998885 ) ) ;
#10791=CARTESIAN_POINT ( 'NONE',  ( -0.2819296736111110979, 4.529944444520310753, -0.1167790944451422980 ) ) ;
#10792=CARTESIAN_POINT ( 'NONE',  ( -1.726321361862525858E-17, 3.894527777853643347, -0.2819296736111110979 ) ) ;
#10793=VERTEX_POINT ( 'NONE', #19398 ) ;
#10796=ORIENTED_EDGE ( 'NONE', *, *, #12915, .F. ) ;
#10801=CARTESIAN_POINT ( 'NONE',  ( 0.3119999999999999996, 0.3479166665149338034, -0.1292346314604056468 ) ) ;
#10803=CARTESIAN_POINT ( 'NONE',  ( -0.2214530096782409696, 4.384127800144598908, -0.2198004540226814463 ) ) ;
#10807=ORIENTED_EDGE ( 'NONE', *, *, #14190, .F. ) ;
#10808=CARTESIAN_POINT ( 'NONE',  ( 0.2253486499796795439, 5.092611837936364516, -0.2157528262157012711 ) ) ;
#10810=CARTESIAN_POINT ( 'NONE',  ( -0.2819296736111110979, 4.186194444520309865, 0.000000000000000000 ) ) ;
#10811=CARTESIAN_POINT ( 'NONE',  ( -0.1993543840281266910, 5.179250000075866112, -0.1993543840281266910 ) ) ;
#10814=CARTESIAN_POINT ( 'NONE',  ( -0.03304210309726871020, 4.237377706265436750, 0.3102558678455366592 ) ) ;
#10815=CARTESIAN_POINT ( 'NONE',  ( -0.2206173157302027676, 4.113277777777777366, 0.2206173157302028787 ) ) ;
#10817=CARTESIAN_POINT ( 'NONE',  ( 0.1292346314604058410, 4.963972222373953969, 0.3119999999999998885 ) ) ;
#10818=CARTESIAN_POINT ( 'NONE',  ( -0.2819296736111110979, 5.144527777853643791, 0.000000000000000000 ) ) ;
#10823=CARTESIAN_POINT ( 'NONE',  ( -0.0006132284040734684288, 4.877183144895580469, -0.3119999996348461480 ) ) ;
#10830=CARTESIAN_POINT ( 'NONE',  ( -0.1993543840281267465, 0.1951388888130222710, 0.1993543840281266633 ) ) ;
#10833=CARTESIAN_POINT ( 'NONE',  ( 0.3133630161831524874, 4.474762566377171957, -0.01146161691659670044 ) ) ;
#10834=VERTEX_POINT ( 'NONE', #2809 ) ;
#10835=CARTESIAN_POINT ( 'NONE',  ( -0.1005150341732207325, 3.768858437468117994, -0.2960704298912133492 ) ) ;
#10836=CARTESIAN_POINT ( 'NONE',  ( -0.1940126398823881770, 4.605354529194622515, -0.2443523765828770344 ) ) ;
#10838=CARTESIAN_POINT ( 'NONE',  ( 5.731347020009612645E-17, 4.842444444444443441, 0.3119999999999999996 ) ) ;
#10840=CARTESIAN_POINT ( 'NONE',  ( -0.3119999999999999996, 4.772999999999998799, 0.000000000000000000 ) ) ;
#10841=CARTESIAN_POINT ( 'NONE',  ( -0.1167790944451423535, 4.085500000075865223, 0.2819296736111110979 ) ) ;
#10842=CARTESIAN_POINT ( 'NONE',  ( 0.1993543840281267465, 3.776472222298087988, 0.1993543840281266633 ) ) ;
#10843=CARTESIAN_POINT ( 'NONE',  ( 0.2959623242263846321, 4.032775975072071972, -0.09874543881575856275 ) ) ;
#10844=EDGE_LOOP ( 'NONE', ( #11759, #10075, #14822, #23971, #16882, #17462, #13819, #18224, #12709, #3577, #20147, #3788, #4683, #20919, #7719, #16690, #8831, #23498, #6516, #7423, #10443, #23459, #2128, #7751, #9448 ) ) ;
#10845=FACE_OUTER_BOUND ( 'NONE', #18135, .T. ) ;
#10847=CARTESIAN_POINT ( 'NONE',  ( 0.2819296736111110979, 4.543833333409199149, 0.1167790944451422425 ) ) ;
#10849=CARTESIAN_POINT ( 'NONE',  ( -0.2019846619707756641, 4.509905506849337442, 0.2387847868100533566 ) ) ;
#10853=CARTESIAN_POINT ( 'NONE',  ( 0.1167790944451424506, 3.828555555631421470, 0.2819296736111110424 ) ) ;
#10855=CARTESIAN_POINT ( 'NONE',  ( 0.1522808163552602789, 5.156853442606030846, -0.2598339165385931127 ) ) ;
#10858=CARTESIAN_POINT ( 'NONE',  ( -0.1993543840281267465, 0.2368055554796889561, 0.1993543840281266633 ) ) ;
#10865=VERTEX_POINT ( 'NONE', #10028 ) ;
#10867=CARTESIAN_POINT ( 'NONE',  ( 5.731347020009612645E-17, 4.731333333333332725, 0.3119999999999999996 ) ) ;
#10868=CARTESIAN_POINT ( 'NONE',  ( 0.1292346314604057023, 0.1187499999999996614, 0.3119999999999998885 ) ) ;
#10869=CARTESIAN_POINT ( 'NONE',  ( 0.2819296736111110979, 3.891055555631421914, 0.1167790944451422425 ) ) ;
#10871=CARTESIAN_POINT ( 'NONE',  ( -0.2819296736111110424, 4.474388888964755395, -0.1167790944451423119 ) ) ;
#10872=CARTESIAN_POINT ( 'NONE',  ( 0.1292346314604057300, 0.1118055554038226290, 0.3119999999999998885 ) ) ;
#10877=CARTESIAN_POINT ( 'NONE',  ( 0.1993543840281266633, 5.109805555631420582, -0.1993543840281266910 ) ) ;
#10879=CARTESIAN_POINT ( 'NONE',  ( 0.2387648180985315616, 4.202823093931177922, -0.2008770064554694090 ) ) ;
#10883=CARTESIAN_POINT ( 'NONE',  ( -0.2819296736111110424, 4.634111111186976828, 0.1167790944451424923 ) ) ;
#10885=CARTESIAN_POINT ( 'NONE',  ( -0.2104324251216644903, 4.065027146098090682, 0.2311922143307865718 ) ) ;
#10887=CARTESIAN_POINT ( 'NONE',  ( -0.1167790944451422702, 0.2333333332574666907, -0.2819296736111110424 ) ) ;
#10889=CARTESIAN_POINT ( 'NONE',  ( -0.1167790944451424368, 0.1430555554796889284, 0.2819296736111110424 ) ) ;
#10890=DIRECTION ( 'NONE',  ( 0.000000000000000000, 0.000000000000000000, -1.000000000000000000 ) ) ;
#10891=CARTESIAN_POINT ( 'NONE',  ( -0.1324640314579201839, 5.193749668861634028, -0.2568599863705673947 ) ) ;
#10895=CARTESIAN_POINT ( 'NONE',  ( 0.1797084794423411680, 3.735609856212664948, -0.2172307604343298448 ) ) ;
#10896=CARTESIAN_POINT ( 'NONE',  ( 0.1167790944451423257, 0.1013888888130222432, -0.2819296736111110424 ) ) ;
#10897=CARTESIAN_POINT ( 'NONE',  ( -0.1993543840281266355, 4.540361111186976828, 0.1993543840281267465 ) ) ;
#10900=CARTESIAN_POINT ( 'NONE',  ( 0.2819296736111110979, 5.061194444520310753, -3.452642723725051716E-17 ) ) ;
#10902=CARTESIAN_POINT ( 'NONE',  ( -0.2621650492421670475, 0.04909780403330635951, -0.1442773403164986090 ) ) ;
#10903=CARTESIAN_POINT ( 'NONE',  ( 0.1113886448093519416, 3.762860911357303273, -0.2917950463651685089 ) ) ;
#10904=CARTESIAN_POINT ( 'NONE',  ( -0.2206173157302027954, 0.4763888887371559577, -0.2206173157302028232 ) ) ;
#10905=CIRCLE ( 'NONE', #17892, 0.3119999999999999996 ) ;
#10907=CARTESIAN_POINT ( 'NONE',  ( 0.1292346314604056190, 4.262583333485065573, -0.3119999999999999996 ) ) ;
#10908=CARTESIAN_POINT ( 'NONE',  ( -0.1167790944451423535, 4.543833333409198261, 0.2819296736111110979 ) ) ;
#10909=CARTESIAN_POINT ( 'NONE',  ( 5.178964085587577574E-17, 3.755638888964754951, 0.2819296736111110979 ) ) ;
#10917=VERTEX_POINT ( 'NONE', #3054 ) ;
#10918=CARTESIAN_POINT ( 'NONE',  ( -0.1292346314604058410, 0.2715277776260447973, 0.3119999999999998885 ) ) ;
#10919=CARTESIAN_POINT ( 'NONE',  ( -0.2801425706040142072, 4.395165469185563722, 0.1388625805350480191 ) ) ;
#10922=CARTESIAN_POINT ( 'NONE',  ( 5.731347020009612645E-17, 4.953555555555554157, 0.3119999999999999996 ) ) ;
#10923=CARTESIAN_POINT ( 'NONE',  ( -8.183246661411124563E-08, 3.960496777434589610, 0.3119999999999772400 ) ) ;
#10927=CARTESIAN_POINT ( 'NONE',  ( 0.1913867056871989270, 5.077500454502875904, 0.2465551918856197511 ) ) ;
#10930=CARTESIAN_POINT ( 'NONE',  ( 0.1993543840281267465, 4.262583333409199149, 0.1993543840281266633 ) ) ;
#10931=CARTESIAN_POINT ( 'NONE',  ( -1.726321361862525858E-17, 5.061194444520309865, -0.2819296736111110979 ) ) ;
#10933=CARTESIAN_POINT ( 'NONE',  ( -0.2052485393096138977, 4.231925960476026205, 0.2359794098173954580 ) ) ;
#10934=CARTESIAN_POINT ( 'NONE',  ( 0.3119999999999999996, 3.970916666666665762, -0.1292346314604056745 ) ) ;
#10935=CARTESIAN_POINT ( 'NONE',  ( -0.1292346314604056745, 4.936194444596176290, -0.3119999999999999996 ) ) ;
#10936=CARTESIAN_POINT ( 'NONE',  ( 0.2819296736111110979, 5.064666666742532186, -0.1167790944451423396 ) ) ;
#10938=CARTESIAN_POINT ( 'NONE',  ( -0.3119999999999999996, 4.161888888888888083, 0.000000000000000000 ) ) ;
#10939=VERTEX_POINT ( 'NONE', #12824 ) ;
#10941=CARTESIAN_POINT ( 'NONE',  ( 0.02274447101932148066, 0.04271007974323598466, -0.2915486118860042275 ) ) ;
#10944=CARTESIAN_POINT ( 'NONE',  ( 0.2819296736111110424, 5.217444444520309865, -0.1167790944451423396 ) ) ;
#10948=AXIS2_PLACEMENT_3D ( 'NONE', #1209, #23258, #21087 ) ;
#10949=CARTESIAN_POINT ( 'NONE',  ( 0.2819296736111110979, 0.2715277777019111660, 0.000000000000000000 ) ) ;
#10951=CARTESIAN_POINT ( 'NONE',  ( 0.2819296736111110979, 5.224388888964754507, 0.1167790944451422425 ) ) ;
#10953=ADVANCED_FACE ( 'NONE', ( #1702 ), #24006, .T. ) ;
#10955=B_SPLINE_CURVE_WITH_KNOTS ( 'NONE', 3,
 ( #17052, #5830, #708, #2542, #7897, #13296, #6312, #4006, #20951, #346, #11819, #7785, #4246, #587, #15232, #11696, #21070, #4361 ),
 .UNSPECIFIED., .F., .F.,
 ( 4, 2, 2, 2, 2, 2, 2, 2, 4 ),
 ( 0.5939386199298102298, 0.5962229759072257274, 0.5985073318846413359, 0.6007916878620569445, 0.6030760438394724421, 0.6053603998168879397, 0.6076447557943035482, 0.6099291117717191568, 0.6122134677491346544 ),
 .UNSPECIFIED. ) ;
#10956=CARTESIAN_POINT ( 'NONE',  ( 5.178964085587577574E-17, 4.977861111186976828, 0.2819296736111110979 ) ) ;
#10957=CARTESIAN_POINT ( 'NONE',  ( -0.3119612969836771388, 4.167620540232060300, -0.04114099006773573597 ) ) ;
#10958=CARTESIAN_POINT ( 'NONE',  ( -0.3119999999999999996, 5.047305555555555046, -0.1292346314604056468 ) ) ;
#10959=CARTESIAN_POINT ( 'NONE',  ( 0.3119999999999999996, 4.582027777777776478, -0.1292346314604056745 ) ) ;
#10961=CARTESIAN_POINT ( 'NONE',  ( -1.910449006669871087E-17, 4.647999999999998799, -0.3119999999999999996 ) ) ;
#10962=CARTESIAN_POINT ( 'NONE',  ( 0.1993543840281266633, 3.998694444520309865, -0.1993543840281266910 ) ) ;
#10963=CARTESIAN_POINT ( 'NONE',  ( 0.1015009281151166981, 3.738732047420452620, -0.2819296736111110979 ) ) ;
#10964=CARTESIAN_POINT ( 'NONE',  ( 0.02511968257364222828, 4.043153853174205281, -0.3113283232506174336 ) ) ;
#10967=ORIENTED_EDGE ( 'NONE', *, *, #10975, .T. ) ;
#10970=CARTESIAN_POINT ( 'NONE',  ( 0.1167790944451422702, 4.391055555631420582, -0.2819296736111110424 ) ) ;
#10971=CARTESIAN_POINT ( 'NONE',  ( -0.3037587743577567778, 4.111198837271344608, -0.07370139431766779825 ) ) ;
#10975=EDGE_CURVE ( 'NONE', #4825, #6378, #15003, .T. ) ;
#10976=CARTESIAN_POINT ( 'NONE',  ( -0.3120000142875944960, 3.947771082080143934, 0.04084060482829639932 ) ) ;
#10980=CARTESIAN_POINT ( 'NONE',  ( -0.2819296736111110979, 0.2298611110352444808, -3.452642723725051716E-17 ) ) ;
#10982=DIRECTION ( 'NONE',  ( -0.000000000000000000, 1.000000000000000000, -0.000000000000000000 ) ) ;
#10987=ORIENTED_EDGE ( 'NONE', *, *, #11833, .T. ) ;
#10989=CARTESIAN_POINT ( 'NONE',  ( 5.731347020009612645E-17, 4.342444444444443441, 0.3119999999999999996 ) ) ;
#10990=CARTESIAN_POINT ( 'NONE',  ( 0.1292346314604056745, -0.02708333333333366733, -0.3119999999999999996 ) ) ;
#10991=CARTESIAN_POINT ( 'NONE',  ( -0.2819296736111110424, 3.752166666742533074, -0.1167790944451423119 ) ) ;
#10993=CARTESIAN_POINT ( 'NONE',  ( -0.1993543840281266355, 4.373694444520309865, 0.1993543840281267465 ) ) ;
#10996=CARTESIAN_POINT ( 'NONE',  ( 0.2634491424827775097, 4.358245445987300570, 0.1671768415365145755 ) ) ;
#10997=CARTESIAN_POINT ( 'NONE',  ( 0.1167790944451424368, 4.870222222298087544, 0.2819296736111110424 ) ) ;
#10999=CARTESIAN_POINT ( 'NONE',  ( 0.2933062516910102668, 4.193495950309771736, 0.1074496315832312171 ) ) ;
#11001=CARTESIAN_POINT ( 'NONE',  ( 0.1993543840281266633, 4.609805555631420582, -0.1993543840281266910 ) ) ;
#11006=ORIENTED_EDGE ( 'NONE', *, *, #16283, .F. ) ;
#11007=CARTESIAN_POINT ( 'NONE',  ( -0.1167790944451422702, 0.2888888888130222710, -0.2819296736111110424 ) ) ;
#11009=CARTESIAN_POINT ( 'NONE',  ( -0.05541411813196098213, 4.712050423989051495, -0.3078451288426665711 ) ) ;
#11015=( BOUNDED_CURVE ( )  B_SPLINE_CURVE ( 2, ( #2534, #457, #5942, #7777, #17406, #11324, #7889, #19227, #9979 ),
 .UNSPECIFIED., .F., .F. ) 
 B_SPLINE_CURVE_WITH_KNOTS ( ( 3, 2, 2, 2, 3 ),
 ( 0.8125000000000002220, 0.8169642857142858094, 0.8214285714285713969, 0.8258928571428569843, 0.8303571428571426827 ),
 .UNSPECIFIED. ) 
 CURVE ( )  GEOMETRIC_REPRESENTATION_ITEM ( )  RATIONAL_B_SPLINE_CURVE ( ( 0.9999999999999962252, 0.9238795325112905132, 1.000000000000000000, 0.9238795325112867385, 1.000000000000000000, 0.9238795325112867385, 1.000000000000000000, 0.9238795325112905132, 0.9999999999999962252 ) ) 
 REPRESENTATION_ITEM ( '' )  );
#11016=CARTESIAN_POINT ( 'NONE',  ( -0.3119999999999999996, 3.769527777777777811, -0.1292346314604056468 ) ) ;
#11018=CARTESIAN_POINT ( 'NONE',  ( 0.1167790944451423535, 0.02499999992413337591, 0.2819296736111110424 ) ) ;
#11019=CARTESIAN_POINT ( 'NONE',  ( -0.2819296736111110424, 4.592444444520309865, 0.1167790944451424923 ) ) ;
#11022=CARTESIAN_POINT ( 'NONE',  ( -0.2819296736111110424, 5.196611111186976828, -0.1167790944451423119 ) ) ;
#11023=CARTESIAN_POINT ( 'NONE',  ( 0.1993543840281267465, 4.373694444520309865, 0.1993543840281266633 ) ) ;
#11024=CARTESIAN_POINT ( 'NONE',  ( 0.02043441368966909463, 4.932131780984220448, -0.3120000003117849863 ) ) ;
#11027=CARTESIAN_POINT ( 'NONE',  ( 0.1292346314604058410, 4.352861111262843252, 0.3119999999999998885 ) ) ;
#11028=CARTESIAN_POINT ( 'NONE',  ( 0.2819296736111110979, 4.564666666742532186, -0.1167790944451423396 ) ) ;
#11029=CARTESIAN_POINT ( 'NONE',  ( 0.2819296736111110979, 3.766055555631420582, 0.1167790944451422425 ) ) ;
#11032=ORIENTED_EDGE ( 'NONE', *, *, #16756, .T. ) ;
#11034=CARTESIAN_POINT ( 'NONE',  ( 0.2206173157302028787, 4.238277777777777366, 0.2206173157302027954 ) ) ;
#11035=DIRECTION ( 'NONE',  ( -0.000000000000000000, 1.000000000000000000, -0.000000000000000000 ) ) ;
#11036=EDGE_LOOP ( 'NONE', ( #23307, #6769, #6370, #3347 ) ) ;
#11037=CARTESIAN_POINT ( 'NONE',  ( -0.1292346314604056190, 0.4729166665149337478, -0.3119999999999999996 ) ) ;
#11039=CARTESIAN_POINT ( 'NONE',  ( -0.1072922602170164191, 3.735183360884210657, 0.2929731678372050618 ) ) ;
#11042=VERTEX_POINT ( 'NONE', #15355 ) ;
#11044=ORIENTED_EDGE ( 'NONE', *, *, #20955, .F. ) ;
#11045=CARTESIAN_POINT ( 'NONE',  ( 0.2726353606394136819, 5.081042968642144331, 0.1517956056947933619 ) ) ;
#11048=CARTESIAN_POINT ( 'NONE',  ( 0.1167790944451424368, 4.314666666742532186, 0.2819296736111110424 ) ) ;
#11049=CARTESIAN_POINT ( 'NONE',  ( -0.2819296736111110979, 5.071611111186976828, -0.1167790944451422980 ) ) ;
#11051=CARTESIAN_POINT ( 'NONE',  ( -0.3070831450522693573, 4.225926056666180486, 0.05521187652797088230 ) ) ;
#11052=CARTESIAN_POINT ( 'NONE',  ( -0.3119999999999999996, 3.939666666666666206, 0.000000000000000000 ) ) ;
#11053=CARTESIAN_POINT ( 'NONE',  ( -0.3119999999999998885, 4.894527777929509327, 0.1292346314604058410 ) ) ;
#11054=CARTESIAN_POINT ( 'NONE',  ( -1.726321361862525858E-17, 5.130638888964754507, -0.2819296736111110979 ) ) ;
#11057=EDGE_CURVE ( 'NONE', #7667, #16613, #18031, .T. ) ;
#11059=CARTESIAN_POINT ( 'NONE',  ( 0.2830627371972649908, 0.03488899866380682641, -0.02971062478493903189 ) ) ;
#11063=CARTESIAN_POINT ( 'NONE',  ( 0.2819296736111110979, 5.102861111186976828, -3.452642723725051716E-17 ) ) ;
#11067=CARTESIAN_POINT ( 'NONE',  ( 0.1993543840281266355, 0.3201388888130222710, 0.1993543840281267465 ) ) ;
#11069=CARTESIAN_POINT ( 'NONE',  ( -1.726321361862525858E-17, 4.908416666742532186, -0.2819296736111110979 ) ) ;
#11070=CARTESIAN_POINT ( 'NONE',  ( 0.3048113794607916205, 4.476554688488221245, -0.07360551287067333692 ) ) ;
#11072=CARTESIAN_POINT ( 'NONE',  ( 0.1993543840281266633, 4.832027777853643791, -0.1993543840281266910 ) ) ;
#11077=CARTESIAN_POINT ( 'NONE',  ( -0.3119999999999998885, 4.498694444444443441, 0.1292346314604058410 ) ) ;
#11078=CARTESIAN_POINT ( 'NONE',  ( 0.2819296736111111534, 3.988277777853643347, 0.1167790944451422563 ) ) ;
#11079=VECTOR ( 'NONE', #9520, 39.37007874015748143 ) ;
#11081=CARTESIAN_POINT ( 'NONE',  ( 0.3066522881518912169, 4.031597852227386980, -0.05855820888548868286 ) ) ;
#11082=CARTESIAN_POINT ( 'NONE',  ( 5.731347020009612645E-17, 4.397999999999999687, 0.3119999999999999996 ) ) ;
#11086=EDGE_CURVE ( 'NONE', #13879, #10939, #17060, .T. ) ;
#11091=CARTESIAN_POINT ( 'NONE',  ( -0.2495012331031523645, 4.440889594020191566, -0.1917320893305669016 ) ) ;
#11094=CARTESIAN_POINT ( 'NONE',  ( 0.2819296736111110424, 0.3097222221463555303, 0.1167790944451424923 ) ) ;
#11096=DIRECTION ( 'NONE',  ( -0.000000000000000000, -1.000000000000000000, -0.000000000000000000 ) ) ;
#11097=CYLINDRICAL_SURFACE ( 'NONE', #24128, 0.3119999999999999996 ) ;
#11100=VERTEX_POINT ( 'NONE', #18649 ) ;
#11104=CARTESIAN_POINT ( 'NONE',  ( 1.910449006669871087E-17, 0.03194444444444410891, -0.3119999999999999996 ) ) ;
#11105=CARTESIAN_POINT ( 'NONE',  ( 5.178964085587577574E-17, 3.936194444520310309, 0.2819296736111110979 ) ) ;
#11107=CARTESIAN_POINT ( 'NONE',  ( -0.1993543840281266355, 4.429250000075866112, 0.1993543840281267465 ) ) ;
#11109=ADVANCED_FACE ( 'NONE', ( #7551 ), #11097, .T. ) ;
#11111=ORIENTED_EDGE ( 'NONE', *, *, #5971, .T. ) ;
#11114=CARTESIAN_POINT ( 'NONE',  ( 0.1167790944451422702, 5.002166666742531298, -0.2819296736111110424 ) ) ;
#11116=CARTESIAN_POINT ( 'NONE',  ( -0.1507786080989017841, 5.147423691745167673, -0.2635463223593010884 ) ) ;
#11118=CARTESIAN_POINT ( 'NONE',  ( -0.3119999999999999996, 4.991749999999998799, -0.1292346314604056468 ) ) ;
#11120=CARTESIAN_POINT ( 'NONE',  ( -0.2819296736111110979, 4.682722222298087544, -0.1167790944451422980 ) ) ;
#11124=CARTESIAN_POINT ( 'NONE',  ( -0.1167790944451424368, 0.5319444443685777957, 0.2819296736111110424 ) ) ;
#11126=ORIENTED_EDGE ( 'NONE', *, *, #22890, .T. ) ;
#11127=CARTESIAN_POINT ( 'NONE',  ( -0.1993543840281266633, 0.2368055554796889006, -0.1993543840281266910 ) ) ;
#11134=CARTESIAN_POINT ( 'NONE',  ( -0.1235199187034025786, 3.880721340484976078, -0.2869016881843655109 ) ) ;
#11135=CARTESIAN_POINT ( 'NONE',  ( 0.2819296736111110979, 0.3131944443685777957, 0.000000000000000000 ) ) ;
#11136=CARTESIAN_POINT ( 'NONE',  ( 1.726321361862525858E-17, 0.04930555547968892144, -0.2819296736111110979 ) ) ;
#11137=CARTESIAN_POINT ( 'NONE',  ( -0.1993543840281266910, 4.582027777853643791, -0.1993543840281266910 ) ) ;
#11139=CARTESIAN_POINT ( 'NONE',  ( 0.04183867695277764670, 4.542642517705186123, -0.3092924480017552047 ) ) ;
#11140=CARTESIAN_POINT ( 'NONE',  ( -0.2819296736111110424, 5.036888888964754507, 0.1167790944451424923 ) ) ;
#11141=CARTESIAN_POINT ( 'NONE',  ( -0.2819296736111110424, 4.411888888964754507, 0.1167790944451424923 ) ) ;
#11142=CARTESIAN_POINT ( 'NONE',  ( 0.1307108517531567482, 3.742116710486879327, 0.2841574553316881246 ) ) ;
#11146=CARTESIAN_POINT ( 'NONE',  ( 0.3119999999999999996, 4.141055555707287894, -3.820898013339742174E-17 ) ) ;
#11147=CARTESIAN_POINT ( 'NONE',  ( -0.2819296736111110424, 4.425777777853642903, 0.1167790944451424923 ) ) ;
#11150=VECTOR ( 'NONE', #18836, 39.37007874015748143 ) ;
#11156=CARTESIAN_POINT ( 'NONE',  ( -0.09380593400082881672, 0.03242967361111052244, 0.2658661084243340578 ) ) ;
#11160=CARTESIAN_POINT ( 'NONE',  ( 0.3119999999999999996, 0.5701388887371559022, -0.1292346314604056468 ) ) ;
#11163=CARTESIAN_POINT ( 'NONE',  ( -0.2348053674301955052, 3.718086869336296729, -0.2057751470050347142 ) ) ;
#11166=ORIENTED_EDGE ( 'NONE', *, *, #11276, .F. ) ;
#11170=CARTESIAN_POINT ( 'NONE',  ( 0.1484364568374648974, 5.095438198970610344, -0.2736806903221176701 ) ) ;
#11172=CARTESIAN_POINT ( 'NONE',  ( -0.1993543840281266355, 4.248694444520309865, 0.1993543840281267465 ) ) ;
#11173=CARTESIAN_POINT ( 'NONE',  ( 0.2819296736111110979, 5.106333333409199149, -0.1167790944451423396 ) ) ;
#11176=CARTESIAN_POINT ( 'NONE',  ( -0.1292346314604056745, 3.818138888888887639, -0.3119999999999999996 ) ) ;
#11177=CARTESIAN_POINT ( 'NONE',  ( -0.3119999999999999996, 4.724388889040620931, 0.000000000000000000 ) ) ;
#11178=CARTESIAN_POINT ( 'NONE',  ( 0.1607903964422072729, 4.798635960660796229, 0.2688681601943798682 ) ) ;
#11182=CARTESIAN_POINT ( 'NONE',  ( 0.1515256109559866837, 0.04002383242775373051, -0.2469710999841635557 ) ) ;
#11187=CARTESIAN_POINT ( 'NONE',  ( 0.1993543840281267465, 5.095916666742532186, 0.1993543840281266633 ) ) ;
#11190=CARTESIAN_POINT ( 'NONE',  ( -0.1167790944451422702, 0.1777777777019111938, -0.2819296736111110979 ) ) ;
#11192=CARTESIAN_POINT ( 'NONE',  ( 0.2819296736111110979, 4.894527777853643791, -3.452642723725051716E-17 ) ) ;
#11193=CARTESIAN_POINT ( 'NONE',  ( 0.2594935920934202112, 4.479718426223786132, -0.1748956054335727706 ) ) ;
#11194=CARTESIAN_POINT ( 'NONE',  ( -0.1167790944451423535, 4.918833333409199149, 0.2819296736111110424 ) ) ;
#11195=CYLINDRICAL_SURFACE ( 'NONE', #2512, 0.3119999999999999996 ) ;
#11196=CARTESIAN_POINT ( 'NONE',  ( -5.731347020009612645E-17, 0.4972222220704892726, 0.3119999999999999996 ) ) ;
#11197=CARTESIAN_POINT ( 'NONE',  ( 0.2206173157302027954, 4.585499999999999687, -0.2206173157302028232 ) ) ;
#11199=CARTESIAN_POINT ( 'NONE',  ( -0.1292346314604056745, 4.429249999999999687, -0.3119999999999999996 ) ) ;
#11200=CARTESIAN_POINT ( 'NONE',  ( -0.1993543840281266355, 4.026472222298087544, 0.1993543840281267465 ) ) ;
#11204=CARTESIAN_POINT ( 'NONE',  ( -0.03716597311884842908, 3.737241779597674896, 0.3101143021802981181 ) ) ;
#11205=VERTEX_POINT ( 'NONE', #16703 ) ;
#11206=CARTESIAN_POINT ( 'NONE',  ( 0.3102328094856748320, 4.584584709764821575, 0.03329712396315245154 ) ) ;
#11211=DIRECTION ( 'NONE',  ( -0.000000000000000000, -1.000000000000000000, -0.000000000000000000 ) ) ;
#11212=CARTESIAN_POINT ( 'NONE',  ( -0.04082748817735452201, 4.459360436992971799, 0.3119999991102669901 ) ) ;
#11216=CARTESIAN_POINT ( 'NONE',  ( 0.1167790944451423257, 0.2680555554796889561, -0.2819296736111110424 ) ) ;
#11217=CARTESIAN_POINT ( 'NONE',  ( 0.08089722802934988521, 3.874934476269974670, -0.3020209484956946078 ) ) ;
#11218=DIRECTION ( 'NONE',  ( 0.000000000000000000, 0.000000000000000000, -1.000000000000000000 ) ) ;
#11222=ORIENTED_EDGE ( 'NONE', *, *, #2134, .T. ) ;
#11225=CARTESIAN_POINT ( 'NONE',  ( 0.2206173157302028232, 0.08055555555555521385, -0.2206173157302028232 ) ) ;
#11226=CARTESIAN_POINT ( 'NONE',  ( -0.1292346314604056745, 5.151472222222222008, -0.3119999999999999996 ) ) ;
#11229=CARTESIAN_POINT ( 'NONE',  ( 0.1993543840281266633, 4.290361111186976828, -0.1993543840281266910 ) ) ;
#11230=CARTESIAN_POINT ( 'NONE',  ( 0.000000000000000000, 5.384999999999999787, -0.3119999999999999996 ) ) ;
#11233=VERTEX_POINT ( 'NONE', #12071 ) ;
#11235=CARTESIAN_POINT ( 'NONE',  ( 0.2348386186658658059, 4.356861530419343431, 0.2064237969327863131 ) ) ;
#11236=CARTESIAN_POINT ( 'NONE',  ( -0.1993543840281266910, 5.012583333409199149, -0.1993543840281266910 ) ) ;
#11239=CARTESIAN_POINT ( 'NONE',  ( 0.03587150718080267531, 3.709525392854851056, -0.3100612275418990760 ) ) ;
#11240=CYLINDRICAL_SURFACE ( 'NONE', #8348, 0.3119999999999999996 ) ;
#11241=CARTESIAN_POINT ( 'NONE',  ( -0.2819296736111110424, 4.689666666742532186, 0.1167790944451424923 ) ) ;
#11244=CARTESIAN_POINT ( 'NONE',  ( -0.09380593400082881672, 0.03242967361111052244, 0.2658661084243340578 ) ) ;
#11245=CARTESIAN_POINT ( 'NONE',  ( -0.1993543840281266633, 0.5701388888130222155, -0.1993543840281266910 ) ) ;
#11246=ADVANCED_FACE ( 'NONE', ( #714 ), #17541, .T. ) ;
#11250=CARTESIAN_POINT ( 'NONE',  ( -0.2819296736111110979, 0.2993055554796889561, -3.452642723725051716E-17 ) ) ;
#11252=CYLINDRICAL_SURFACE ( 'NONE', #12121, 0.3119999999999999996 ) ;
#11257=CARTESIAN_POINT ( 'NONE',  ( -0.2819296736111110979, 0.2819444443685778512, -0.1167790944451423396 ) ) ;
#11258=CARTESIAN_POINT ( 'NONE',  ( 0.1993543840281267465, 4.332027777853642903, 0.1993543840281266633 ) ) ;
#11261=CARTESIAN_POINT ( 'NONE',  ( 5.178964085587577574E-17, 5.047305555631421470, 0.2819296736111110979 ) ) ;
#11262=CARTESIAN_POINT ( 'NONE',  ( -0.1993543840281266910, 4.401472222298088433, -0.1993543840281266910 ) ) ;
#11266=CARTESIAN_POINT ( 'NONE',  ( 0.3119999999999999996, 4.085500000151732536, -3.820898013339742174E-17 ) ) ;
#11268=AXIS2_PLACEMENT_3D ( 'NONE', #8622, #20081, #16063 ) ;
#11269=DIRECTION ( 'NONE',  ( -0.000000000000000000, -1.000000000000000000, -0.000000000000000000 ) ) ;
#11272=CARTESIAN_POINT ( 'NONE',  ( -0.1374632086698537592, 4.845340413058586648, 0.2800857552099924042 ) ) ;
#11274=ORIENTED_EDGE ( 'NONE', *, *, #10680, .F. ) ;
#11275=CARTESIAN_POINT ( 'NONE',  ( 0.1292346314604056745, 0.4104166665149336923, -0.3119999999999999996 ) ) ;
#11276=EDGE_CURVE ( 'NONE', #70, #5752, #11633, .T. ) ;
#11280=CARTESIAN_POINT ( 'NONE',  ( 0.2515573277093725024, 4.746441417219358527, 0.1886560052811415422 ) ) ;
#11282=CARTESIAN_POINT ( 'NONE',  ( 1.364852645245658621E-07, 4.377166663151471404, -0.3119999999999701346 ) ) ;
#11285=AXIS2_PLACEMENT_3D ( 'NONE', #17173, #13290, #11576 ) ;
#11288=CARTESIAN_POINT ( 'NONE',  ( -0.3127085332352448899, 4.668742369690864535, -0.005568702923292533601 ) ) ;
#11290=CARTESIAN_POINT ( 'NONE',  ( 0.2819296736111110979, 4.210500000075865223, 0.1167790944451422425 ) ) ;
#11293=CARTESIAN_POINT ( 'NONE',  ( -0.2206173157302028232, 3.821611111111110404, -0.2206173157302028232 ) ) ;
#11294=CARTESIAN_POINT ( 'NONE',  ( 0.2206173157302027954, 4.703555555707287894, -0.2206173157302028232 ) ) ;
#11295=CARTESIAN_POINT ( 'NONE',  ( 0.3080665527274119575, 4.806319477209046731, 0.05048669183540833300 ) ) ;
#11298=AXIS2_PLACEMENT_3D ( 'NONE', #3048, #2803, #1097 ) ;
#11299=CARTESIAN_POINT ( 'NONE',  ( -0.01971715691147114813, 0.06040120350305807490, 0.3099012035031042944 ) ) ;
#11301=EDGE_LOOP ( 'NONE', ( #5412, #21452, #2769, #13497 ) ) ;
#11304=CARTESIAN_POINT ( 'NONE',  ( 0.1167790944451424368, 5.092444444520309865, 0.2819296736111110424 ) ) ;
#11305=CARTESIAN_POINT ( 'NONE',  ( -0.1993543840281266355, 3.762583333409198705, 0.1993543840281267465 ) ) ;
#11309=CARTESIAN_POINT ( 'NONE',  ( 0.2819296736111110979, 0.4416666665908000611, -0.1167790944451422980 ) ) ;
#11312=CARTESIAN_POINT ( 'NONE',  ( -0.2819296736111110424, 4.918833333409199149, -0.1167790944451423119 ) ) ;
#11315=CARTESIAN_POINT ( 'NONE',  ( 0.1167790944451424368, 4.814666666742533074, 0.2819296736111110424 ) ) ;
#11317=CARTESIAN_POINT ( 'NONE',  ( 0.01223391761890406035, 4.876836776912257143, -0.3117956601136203099 ) ) ;
#11320=CARTESIAN_POINT ( 'NONE',  ( 0.1292346314604056190, 4.477861111111110404, -0.3119999999999999996 ) ) ;
#11322=CARTESIAN_POINT ( 'NONE',  ( 0.1797085267211815662, 3.721720965436318362, -0.2172307213220433242 ) ) ;
#11323=LINE ( 'NONE', #8213, #12844 ) ;
#11324=CARTESIAN_POINT ( 'NONE',  ( -0.3119999999999999996, 3.991749999999999243, -0.1292346314604056468 ) ) ;
#11325=CARTESIAN_POINT ( 'NONE',  ( -0.1051149507764515267, 3.735250598783638409, 0.2937598854384353420 ) ) ;
#11326=CARTESIAN_POINT ( 'NONE',  ( 0.3108826220787605510, 4.584778751626606308, 0.02638173060821461663 ) ) ;
#11328=CARTESIAN_POINT ( 'NONE',  ( -0.2926395827916415948, 4.110145192664806935, -0.1098333424203642578 ) ) ;
#11332=CARTESIAN_POINT ( 'NONE',  ( 3.820898013339742174E-17, 5.384999999999999787, 0.3119999999999999996 ) ) ;
#11333=CARTESIAN_POINT ( 'NONE',  ( 0.2880336597100306428, 5.149313696340753310, -0.09459580602892668499 ) ) ;
#11337=CARTESIAN_POINT ( 'NONE',  ( -0.1993543840281266633, 0.3340277777019111660, -0.1993543840281266910 ) ) ;
#11342=( BOUNDED_CURVE ( )  B_SPLINE_CURVE ( 2, ( #18748, #9240, #24103, #20218, #3624, #10958, #2044, #20336, #7294 ),
 .UNSPECIFIED., .F., .F. ) 
 B_SPLINE_CURVE_WITH_KNOTS ( ( 3, 2, 2, 2, 3 ),
 ( 0.1339285714285714246, 0.1383928571428570675, 0.1428571428571426827, 0.1473214285714283533, 0.1517857142857139685 ),
 .UNSPECIFIED. ) 
 CURVE ( )  GEOMETRIC_REPRESENTATION_ITEM ( )  RATIONAL_B_SPLINE_CURVE ( ( 1.000000000000000000, 0.9238795325112867385, 1.000000000000000000, 0.9238795325112867385, 1.000000000000000000, 0.9238795325112867385, 1.000000000000000000, 0.9238795325112919565, 0.9999999999999947820 ) ) 
 REPRESENTATION_ITEM ( '' )  );
#11343=CARTESIAN_POINT ( 'NONE',  ( 1.910449006669871087E-17, 0.6361111109593781121, -0.3119999999999999996 ) ) ;
#11344=( BOUNDED_CURVE ( )  B_SPLINE_CURVE ( 2, ( #9018, #18164, #23752, #14512, #5226, #23871, #22983 ),
 .UNSPECIFIED., .F., .F. ) 
 B_SPLINE_CURVE_WITH_KNOTS ( ( 3, 2, 2, 3 ),
 ( 0.07711994006981462424, 0.08333333333333332871, 0.09375000000000000000, 0.1041666666666666713 ),
 .UNSPECIFIED. ) 
 CURVE ( )  GEOMETRIC_REPRESENTATION_ITEM ( )  RATIONAL_B_SPLINE_CURVE ( ( 0.9633570533295530147, 0.9545952256086144283, 1.000000000000000000, 0.9238795325112867385, 1.000000000000000000, 0.9238795325112867385, 1.000000000000000000 ) ) 
 REPRESENTATION_ITEM ( '' )  );
#11346=CARTESIAN_POINT ( 'NONE',  ( 0.2206173157302027676, 0.2888888888888885287, 0.2206173157302028787 ) ) ;
#11347=CARTESIAN_POINT ( 'NONE',  ( 0.3119999999999999996, 5.245222222222222008, -3.820898013339742174E-17 ) ) ;
#11348=CARTESIAN_POINT ( 'NONE',  ( -0.1167790944451423257, 4.300777777853642903, -0.2819296736111110424 ) ) ;
#11351=ADVANCED_FACE ( 'NONE', ( #14242 ), #10699, .T. ) ;
#11352=ORIENTED_EDGE ( 'NONE', *, *, #23018, .F. ) ;
#11353=VERTEX_POINT ( 'NONE', #18967 ) ;
#11355=CARTESIAN_POINT ( 'NONE',  ( 0.1993543840281267465, 4.984805555631420582, 0.1993543840281266633 ) ) ;
#11360=CARTESIAN_POINT ( 'NONE',  ( -0.3120000000000000551, 0.2159722222222218713, 0.1292346314604056190 ) ) ;
#11361=CARTESIAN_POINT ( 'NONE',  ( 0.2819296736111110979, 4.661888888964753619, -0.1167790944451423396 ) ) ;
#11364=CARTESIAN_POINT ( 'NONE',  ( 0.000000000000000000, 5.384999999999999787, 1.910449006669871087E-17 ) ) ;
#11366=CARTESIAN_POINT ( 'NONE',  ( 0.1167790944451423535, 0.5944444443685777957, 0.2819296736111110424 ) ) ;
#11367=VERTEX_POINT ( 'NONE', #4562 ) ;
#11368=CARTESIAN_POINT ( 'NONE',  ( -0.2819296736111110979, 0.1916666665908000333, 0.1167790944451422425 ) ) ;
#11369=DIRECTION ( 'NONE',  ( -0.000000000000000000, -1.000000000000000000, -0.000000000000000000 ) ) ;
#11370=CARTESIAN_POINT ( 'NONE',  ( 3.429644138441397019E-17, 0.000000000000000000, -0.2495000000000007212 ) ) ;
#11375=CARTESIAN_POINT ( 'NONE',  ( -0.1167790944451422702, 0.2749999999241334314, -0.2819296736111110979 ) ) ;
#11376=CARTESIAN_POINT ( 'NONE',  ( -0.1993543840281267465, 0.07013888881302225708, 0.1993543840281266633 ) ) ;
#11377=CARTESIAN_POINT ( 'NONE',  ( -0.2819296736111110979, 4.366750000075866112, 0.000000000000000000 ) ) ;
#11379=CARTESIAN_POINT ( 'NONE',  ( -0.2819296736111110424, 4.814666666742533074, 0.1167790944451424923 ) ) ;
#11380=CARTESIAN_POINT ( 'NONE',  ( 0.1167790944451424506, 4.481333333409199149, 0.2819296736111110424 ) ) ;
#11383=CARTESIAN_POINT ( 'NONE',  ( -0.3119999999999998885, 4.061194444596176290, 0.1292346314604058410 ) ) ;
#11384=DIRECTION ( 'NONE',  ( -0.000000000000000000, -1.000000000000000000, -0.000000000000000000 ) ) ;
#11392=CARTESIAN_POINT ( 'NONE',  ( 3.820898013339742174E-17, 5.384999999999999787, 0.3119999999999999996 ) ) ;
#11394=CARTESIAN_POINT ( 'NONE',  ( -0.2206173157302027954, 0.4763888887371559577, -0.2206173157302028232 ) ) ;
#11398=CARTESIAN_POINT ( 'NONE',  ( -0.2206173157302027954, 0.5388888888888885287, -0.2206173157302028232 ) ) ;
#11400=CARTESIAN_POINT ( 'NONE',  ( 0.2727859317332818612, 3.978974379482379309, -0.1568535693789047114 ) ) ;
#11403=ORIENTED_EDGE ( 'NONE', *, *, #17380, .F. ) ;
#11405=CARTESIAN_POINT ( 'NONE',  ( -0.1909016353860534532, 4.676933550353267854, 0.2504354235555140140 ) ) ;
#11406=CARTESIAN_POINT ( 'NONE',  ( -1.726321361862525858E-17, 3.950083333409199149, -0.2819296736111110979 ) ) ;
#11408=CARTESIAN_POINT ( 'NONE',  ( -0.3119999999999998885, 4.832027777777777366, 0.1292346314604058410 ) ) ;
#11409=CARTESIAN_POINT ( 'NONE',  ( -0.1292346314604057023, 3.838972222222221564, 0.3119999999999998885 ) ) ;
#11410=CARTESIAN_POINT ( 'NONE',  ( -1.910449006669871087E-17, 4.710500000151732536, -0.3119999999999999996 ) ) ;
#11411=AXIS2_PLACEMENT_3D ( 'NONE', #20522, #4173, #17230 ) ;
#11412=CARTESIAN_POINT ( 'NONE',  ( -0.1167790944451423535, 4.932722222298088433, 0.2819296736111110979 ) ) ;
#11414=EDGE_CURVE ( 'NONE', #3381, #23182, #4953, .T. ) ;
#11415=CARTESIAN_POINT ( 'NONE',  ( 0.1993543840281266633, 4.332027777853642903, -0.1993543840281266910 ) ) ;
#11417=CARTESIAN_POINT ( 'NONE',  ( -0.2025283230813139379, 3.898705486534137066, 0.2391110646586180055 ) ) ;
#11418=ORIENTED_EDGE ( 'NONE', *, *, #21712, .T. ) ;
#11421=EDGE_LOOP ( 'NONE', ( #13935, #10967, #14584, #9653 ) ) ;
#11424=CARTESIAN_POINT ( 'NONE',  ( 0.000000000000000000, 5.072999999999999510, 0.000000000000000000 ) ) ;
#11425=CARTESIAN_POINT ( 'NONE',  ( -0.1167790944451423535, 5.029944444520310753, 0.2819296736111110424 ) ) ;
#11426=CARTESIAN_POINT ( 'NONE',  ( -0.2819296736111110979, 3.807722222298088877, -0.1167790944451422980 ) ) ;
#11432=CARTESIAN_POINT ( 'NONE',  ( -5.178964085587577574E-17, 0.4798611110352444253, 0.2819296736111110979 ) ) ;
#11434=CARTESIAN_POINT ( 'NONE',  ( -0.1167790944451423257, 4.856333333409199149, -0.2819296736111110424 ) ) ;
#11435=CARTESIAN_POINT ( 'NONE',  ( 0.2922484174926198719, 4.471234547107716395, 0.1097235258941094554 ) ) ;
#11436=CARTESIAN_POINT ( 'NONE',  ( 0.2819296736111110979, 4.932722222298088433, 0.1167790944451422425 ) ) ;
#11438=EDGE_CURVE ( 'NONE', #2426, #8700, #9334, .T. ) ;
#11439=CARTESIAN_POINT ( 'NONE',  ( 0.1976131576089550368, 4.855479579813982483, 0.2418934624741892470 ) ) ;
#11442=CARTESIAN_POINT ( 'NONE',  ( 0.3119999999999999996, 4.408416666666666650, 0.1292346314604056190 ) ) ;
#11443=CARTESIAN_POINT ( 'NONE',  ( -0.1167790944451423535, 3.863277777853643347, 0.2819296736111110979 ) ) ;
#11445=CARTESIAN_POINT ( 'NONE',  ( -0.3119999999999999996, 0.5388888887371559022, -3.820898013339742174E-17 ) ) ;
#11446=ORIENTED_EDGE ( 'NONE', *, *, #4410, .F. ) ;
#11447=CARTESIAN_POINT ( 'NONE',  ( 1.910449006669871087E-17, 0.08055555540382261515, -0.3119999999999999996 ) ) ;
#11454=B_SPLINE_CURVE_WITH_KNOTS ( 'NONE', 3,
 ( #18319, #18558, #21855, #21973, #10891, #21740, #5265, #12735, #20151, #3440, #1617, #9051, #16497, #9171, #23909, #16616, #7345, #14797, #22212, #3683, #8685, #16133, #5025, #20867, #22330, #17215, #2345, #16967 ),
 .UNSPECIFIED., .F., .F.,
 ( 4, 2, 2, 2, 2, 2, 2, 2, 2, 2, 2, 2, 2, 4 ),
 ( 0.1142854809683468142, 0.1163847642462578491, 0.1184840475241688840, 0.1195336891631243875, 0.1205833308020799050, 0.1216329724410354224, 0.1226826140799909398, 0.1237322557189464572, 0.1247818973579019747, 0.1258315389968574782, 0.1268811806358129957, 0.1279308222747685131, 0.1289804639137240305, 0.1310797471916350654 ),
 .UNSPECIFIED. ) ;
#11456=CARTESIAN_POINT ( 'NONE',  ( 0.2414151976196820815, 5.152793932359630347, -0.1819029909458831917 ) ) ;
#11457=EDGE_LOOP ( 'NONE', ( #21489, #7787, #6148, #12756 ) ) ;
#11459=CARTESIAN_POINT ( 'NONE',  ( -0.1993543840281267465, 0.5701388888130222155, 0.1993543840281266633 ) ) ;
#11464=AXIS2_PLACEMENT_3D ( 'NONE', #23466, #14469, #8355 ) ;
#11466=CARTESIAN_POINT ( 'NONE',  ( -0.2945206866155428704, 5.108041754680044733, 0.09890754808314189406 ) ) ;
#11468=CARTESIAN_POINT ( 'NONE',  ( 0.3119999999999998885, 0.3479166666666663188, 0.1292346314604058410 ) ) ;
#11469=CARTESIAN_POINT ( 'NONE',  ( 0.1292346314604058410, 5.234805555555554157, 0.3119999999999998885 ) ) ;
#11470=CARTESIAN_POINT ( 'NONE',  ( 5.178964085587577574E-17, 4.213972222298087544, 0.2819296736111110979 ) ) ;
#11474=CARTESIAN_POINT ( 'NONE',  ( 0.2206173157302027676, 0.3444444444444440534, 0.2206173157302028787 ) ) ;
#11475=CARTESIAN_POINT ( 'NONE',  ( 0.1993543840281266633, 4.887583333409199149, -0.1993543840281266910 ) ) ;
#11476=CARTESIAN_POINT ( 'NONE',  ( 0.01740894572980225888, 5.198436972620729790, 0.2852777632786984152 ) ) ;
#11477=CARTESIAN_POINT ( 'NONE',  ( -0.2195237376300352150, 5.149645692627588645, -0.2082703641299125108 ) ) ;
#11481=CARTESIAN_POINT ( 'NONE',  ( 0.2819296736111110979, 4.342444444520310753, -0.1167790944451423396 ) ) ;
#11484=CARTESIAN_POINT ( 'NONE',  ( -0.01981372967188622242, 4.044372679049708985, -0.3113707790481334281 ) ) ;
#11485=( BOUNDED_SURFACE ( )  B_SPLINE_SURFACE ( 1, 2, ( 
 ( #4668, #3315, #18076, #10295, #8443, #16132, #17964, #3198, #14304, #10773, #1376, #23787, #8930, #21614, #4908, #8805, #3087, #6861, #18199, #7107, #14547, #17717, #12137, #21738, #16254, #8683, #6984, #14427, #19544, #21853, #5142, #2835, #12609, #1013, #21493, #4782, #12250, #22454, #11, #260, #16496, #12853, #7459, #10889, #23907, #3557, #1846, #9169, #16614, #1731, #14908, #3804, #12972, #24033, #5388, #22328, #5629, #11368, #16965, #20388, #1614, #20149, #9049, #3681, #5753, #16850, #18795, #7343, #20509, #7227, #11127, #3438, #14795, #18317, #1975, #22210, #13095, #7700, #5510, #16731, #137, #22092, #18556, #14673, #13214, #11007, #21971, #9289, #11250, #20270, #18674, #9413, #7580, #15029, #18436, #20623, #3923, #2090, #9532, #5263, #12733, #2343, #13573, #20982, #9899, #624, #20866, #2460, #4396, #17213, #22930, #21107, #10026, #2578, #7820, #4159, #9781, #6348, #13689, #17330, #10146, #15265, #17570, #13798, #8170, #6103, #5864, #11983, #9654, #497, #2694, #17448, #18924, #8055, #6225, #5983, #4278, #15503, #11858, #19154, #19273, #742, #15624, #11733, #13323, #7931, #860, #15385, #23043, #21229, #4518, #22813, #13447, #19396, #11610, #2223, #15147, #22576, #20745, #4037, #11491, #17093, #19041, #379, #22692, #1100, #19995, #10615, #12103, #3051, #16099, #23274, #23397, #19756, #4990, #12340, #12454, #10498, #19873, #6705, #6466 ),
 ( #23513, #4873, #23636, #17687, #5108, #8291, #6953, #21706, #13920, #19513, #17928, #14149, #6829, #1224, #14394, #14270, #3283, #12574, #8533, #12220, #3165, #19630, #8650, #21818, #10737, #18167, #21348, #15745, #18045, #1341, #2929, #8771, #10387, #23156, #16224, #21578, #4638, #6586, #2806, #10261, #980, #8409, #15857, #14035, #21465, #4749, #17809, #15976, #7076, #9136, #5480, #1815, #14881, #15000, #5724, #23873, #5355, #22298, #12821, #7193, #16581, #20357, #24119, #20240, #3529, #20478, #5595, #5228, #14638, #3892, #12702, #22422, #10980, #22061, #10858, #18287, #13060, #1584, #18406, #7434, #3774, #1699, #7314, #11216, #12945, #24002, #14764, #1938, #18645, #9385, #9259, #16825, #3647, #7548, #22180, #11094, #18525, #13183, #16342, #16700, #107, #20596, #11337, #1463, #8898, #23754, #14514, #9020, #16461, #21935, #20117, #3408, #18766, #11701, #15352, #9993, #2545, #4127, #2428, #22781, #17418, #4011, #15591, #2061, #711, #8022, #234, #22546, #6075, #469, #17297, #4249, #8139, #590, #13767, #23013, #11584, #22664, #9870, #5953, #13541, #6315, #21193, #4484, #7670, #9502, #19124, #15473, #13412, #20956, #20835, #16936, #22899, #9746, #15120, #9624, #7900, #13659, #5837, #13300, #19241, #17183, #6193, #15235, #21074, #19013, #20715, #2309, #4364, #11822, #11459, #18892, #2193, #17057, #350, #7791, #23242, #17655, #19598, #6674, #10469 ) ),
 .UNSPECIFIED., .F., .F., .F. ) 
 B_SPLINE_SURFACE_WITH_KNOTS ( ( 2, 2 ),
 ( 3, 2, 2, 2, 2, 2, 2, 2, 2, 2, 2, 2, 2, 2, 2, 2, 2, 2, 2, 2, 2, 2, 2, 2, 2, 2, 2, 2, 2, 2, 2, 2, 2, 2, 2, 2, 2, 2, 2, 2, 2, 2, 2, 2, 2, 2, 2, 2, 2, 2, 2, 2, 2, 2, 2, 2, 2, 2, 2, 2, 2, 2, 2, 2, 2, 2, 2, 2, 2, 2, 2, 2, 2, 2, 2, 2, 2, 2, 2, 2, 2, 2, 2, 2, 2, 2, 2, 2, 2, 2, 3 ),
 ( 0.000000000000000000, 1.000000000000000000 ),
 ( 0.000000000000000000, 0.01041666666666666609, 0.02083333333333333218, 0.03125000000000000000, 0.04166666666666666435, 0.05208333333333333565, 0.06250000000000000000, 0.07291666666666667129, 0.08333333333333332871, 0.09375000000000000000, 0.1041666666666666713, 0.1145833333333333287, 0.1250000000000000000, 0.1354166666666666574, 0.1458333333333333426, 0.1562500000000000000, 0.1666666666666666574, 0.1770833333333333426, 0.1875000000000000000, 0.1979166666666666574, 0.2083333333333333426, 0.2187500000000000000, 0.2291666666666666574, 0.2395833333333333426, 0.2500000000000000000, 0.2604166666666666852, 0.2708333333333333148, 0.2812500000000000000, 0.2916666666666666852, 0.3020833333333333148, 0.3125000000000000000, 0.3229166666666666852, 0.3333333333333333148, 0.3437500000000000000, 0.3541666666666666852, 0.3645833333333333148, 0.3750000000000000000, 0.3854166666666666852, 0.3958333333333333148, 0.4062500000000000000, 0.4166666666666666852, 0.4270833333333333148, 0.4375000000000000000, 0.4479166666666666852, 0.4583333333333333148, 0.4687500000000000000, 0.4791666666666666852, 0.4895833333333333148, 0.5000000000000000000, 0.5104166666666666297, 0.5208333333333333703, 0.5312500000000000000, 0.5416666666666666297, 0.5520833333333333703, 0.5625000000000000000, 0.5729166666666666297, 0.5833333333333333703, 0.5937500000000000000, 0.6041666666666666297, 0.6145833333333333703, 0.6250000000000000000, 0.6354166666666666297, 0.6458333333333333703, 0.6562500000000000000, 0.6666666666666666297, 0.6770833333333333703, 0.6875000000000000000, 0.6979166666666666297, 0.7083333333333333703, 0.7187500000000000000, 0.7291666666666666297, 0.7395833333333333703, 0.7500000000000000000, 0.7604166666666666297, 0.7708333333333333703, 0.7812500000000000000, 0.7916666666666666297, 0.8020833333333333703, 0.8125000000000000000, 0.8229166666666666297, 0.8333333333333333703, 0.8437500000000000000, 0.8541666666666666297, 0.8645833333333333703, 0.8750000000000000000, 0.8854166666666666297, 0.8958333333333333703, 0.9062500000000000000, 0.9166666666666666297, 0.9270833333333333703, 0.9375000000000000000 ),
 .UNSPECIFIED. ) 
 GEOMETRIC_REPRESENTATION_ITEM ( )  RATIONAL_B_SPLINE_SURFACE ( (
 ( 1.000000000000000000, 0.9238795325112867385, 1.000000000000000000, 0.9238795325112867385, 1.000000000000000000, 0.9238795325112867385, 1.000000000000000000, 0.9238795325112867385, 1.000000000000000000, 0.9238795325112867385, 1.000000000000000000, 0.9238795325112867385, 1.000000000000000000, 0.9238795325112867385, 1.000000000000000000, 0.9238795325112867385, 1.000000000000000000, 0.9238795325112867385, 1.000000000000000000, 0.9238795325112867385, 1.000000000000000000, 0.9238795325112867385, 1.000000000000000000, 0.9238795325112867385, 1.000000000000000000, 0.9238795325112867385, 1.000000000000000000, 0.9238795325112867385, 1.000000000000000000, 0.9238795325112867385, 1.000000000000000000, 0.9238795325112867385, 1.000000000000000000, 0.9238795325112867385, 1.000000000000000000, 0.9238795325112867385, 1.000000000000000000, 0.9238795325112867385, 1.000000000000000000, 0.9238795325112867385, 1.000000000000000000, 0.9238795325112867385, 1.000000000000000000, 0.9238795325112867385, 1.000000000000000000, 0.9238795325112867385, 1.000000000000000000, 0.9238795325112867385, 1.000000000000000000, 0.9238795325112867385, 1.000000000000000000, 0.9238795325112867385, 1.000000000000000000, 0.9238795325112867385, 1.000000000000000000, 0.9238795325112867385, 1.000000000000000000, 0.9238795325112867385, 1.000000000000000000, 0.9238795325112867385, 1.000000000000000000, 0.9238795325112867385, 1.000000000000000000, 0.9238795325112867385, 1.000000000000000000, 0.9238795325112867385, 1.000000000000000000, 0.9238795325112867385, 1.000000000000000000, 0.9238795325112867385, 1.000000000000000000, 0.9238795325112867385, 1.000000000000000000, 0.9238795325112867385, 1.000000000000000000, 0.9238795325112867385, 1.000000000000000000, 0.9238795325112867385, 1.000000000000000000, 0.9238795325112867385, 1.000000000000000000, 0.9238795325112867385, 1.000000000000000000, 0.9238795325112867385, 1.000000000000000000, 0.9238795325112867385, 1.000000000000000000, 0.9238795325112867385, 1.000000000000000000, 0.9238795325112867385, 1.000000000000000000, 0.9238795325112867385, 1.000000000000000000, 0.9238795325112867385, 1.000000000000000000, 0.9238795325112867385, 1.000000000000000000, 0.9238795325112867385, 1.000000000000000000, 0.9238795325112867385, 1.000000000000000000, 0.9238795325112867385, 1.000000000000000000, 0.9238795325112867385, 1.000000000000000000, 0.9238795325112867385, 1.000000000000000000, 0.9238795325112867385, 1.000000000000000000, 0.9238795325112867385, 1.000000000000000000, 0.9238795325112867385, 1.000000000000000000, 0.9238795325112867385, 1.000000000000000000, 0.9238795325112867385, 1.000000000000000000, 0.9238795325112867385, 1.000000000000000000, 0.9238795325112867385, 1.000000000000000000, 0.9238795325112867385, 1.000000000000000000, 0.9238795325112867385, 1.000000000000000000, 0.9238795325112867385, 1.000000000000000000, 0.9238795325112867385, 1.000000000000000000, 0.9238795325112867385, 1.000000000000000000, 0.9238795325112867385, 1.000000000000000000, 0.9238795325112867385, 1.000000000000000000, 0.9238795325112867385, 1.000000000000000000, 0.9238795325112867385, 1.000000000000000000, 0.9238795325112867385, 1.000000000000000000, 0.9238795325112867385, 1.000000000000000000, 0.9238795325112867385, 1.000000000000000000, 0.9238795325112867385, 1.000000000000000000, 0.9238795325112867385, 1.000000000000000000, 0.9238795325112867385, 1.000000000000000000, 0.9238795325112867385, 1.000000000000000000, 0.9238795325112867385, 1.000000000000000000, 0.9238795325112867385, 1.000000000000000000, 0.9238795325112867385, 1.000000000000000000, 0.9238795325112867385, 1.000000000000000000, 0.9238795325112867385, 1.000000000000000000, 0.9238795325112867385, 1.000000000000000000, 0.9238795325112867385, 1.000000000000000000, 0.9238795325112867385, 1.000000000000000000, 0.9238795325112867385, 1.000000000000000000, 0.9238795325112867385, 1.000000000000000000, 0.9238795325112867385, 1.000000000000000000, 0.9238795325112867385, 1.000000000000000000, 0.9238795325112867385, 1.000000000000000000, 0.9238795325112867385, 1.000000000000000000),
 ( 1.000000000000000000, 0.9238795325112867385, 1.000000000000000000, 0.9238795325112867385, 1.000000000000000000, 0.9238795325112867385, 1.000000000000000000, 0.9238795325112867385, 1.000000000000000000, 0.9238795325112867385, 1.000000000000000000, 0.9238795325112867385, 1.000000000000000000, 0.9238795325112867385, 1.000000000000000000, 0.9238795325112867385, 1.000000000000000000, 0.9238795325112867385, 1.000000000000000000, 0.9238795325112867385, 1.000000000000000000, 0.9238795325112867385, 1.000000000000000000, 0.9238795325112867385, 1.000000000000000000, 0.9238795325112867385, 1.000000000000000000, 0.9238795325112867385, 1.000000000000000000, 0.9238795325112867385, 1.000000000000000000, 0.9238795325112867385, 1.000000000000000000, 0.9238795325112867385, 1.000000000000000000, 0.9238795325112867385, 1.000000000000000000, 0.9238795325112867385, 1.000000000000000000, 0.9238795325112867385, 1.000000000000000000, 0.9238795325112867385, 1.000000000000000000, 0.9238795325112867385, 1.000000000000000000, 0.9238795325112867385, 1.000000000000000000, 0.9238795325112867385, 1.000000000000000000, 0.9238795325112867385, 1.000000000000000000, 0.9238795325112867385, 1.000000000000000000, 0.9238795325112867385, 1.000000000000000000, 0.9238795325112867385, 1.000000000000000000, 0.9238795325112867385, 1.000000000000000000, 0.9238795325112867385, 1.000000000000000000, 0.9238795325112867385, 1.000000000000000000, 0.9238795325112867385, 1.000000000000000000, 0.9238795325112867385, 1.000000000000000000, 0.9238795325112867385, 1.000000000000000000, 0.9238795325112867385, 1.000000000000000000, 0.9238795325112867385, 1.000000000000000000, 0.9238795325112867385, 1.000000000000000000, 0.9238795325112867385, 1.000000000000000000, 0.9238795325112867385, 1.000000000000000000, 0.9238795325112867385, 1.000000000000000000, 0.9238795325112867385, 1.000000000000000000, 0.9238795325112867385, 1.000000000000000000, 0.9238795325112867385, 1.000000000000000000, 0.9238795325112867385, 1.000000000000000000, 0.9238795325112867385, 1.000000000000000000, 0.9238795325112867385, 1.000000000000000000, 0.9238795325112867385, 1.000000000000000000, 0.9238795325112867385, 1.000000000000000000, 0.9238795325112867385, 1.000000000000000000, 0.9238795325112867385, 1.000000000000000000, 0.9238795325112867385, 1.000000000000000000, 0.9238795325112867385, 1.000000000000000000, 0.9238795325112867385, 1.000000000000000000, 0.9238795325112867385, 1.000000000000000000, 0.9238795325112867385, 1.000000000000000000, 0.9238795325112867385, 1.000000000000000000, 0.9238795325112867385, 1.000000000000000000, 0.9238795325112867385, 1.000000000000000000, 0.9238795325112867385, 1.000000000000000000, 0.9238795325112867385, 1.000000000000000000, 0.9238795325112867385, 1.000000000000000000, 0.9238795325112867385, 1.000000000000000000, 0.9238795325112867385, 1.000000000000000000, 0.9238795325112867385, 1.000000000000000000, 0.9238795325112867385, 1.000000000000000000, 0.9238795325112867385, 1.000000000000000000, 0.9238795325112867385, 1.000000000000000000, 0.9238795325112867385, 1.000000000000000000, 0.9238795325112867385, 1.000000000000000000, 0.9238795325112867385, 1.000000000000000000, 0.9238795325112867385, 1.000000000000000000, 0.9238795325112867385, 1.000000000000000000, 0.9238795325112867385, 1.000000000000000000, 0.9238795325112867385, 1.000000000000000000, 0.9238795325112867385, 1.000000000000000000, 0.9238795325112867385, 1.000000000000000000, 0.9238795325112867385, 1.000000000000000000, 0.9238795325112867385, 1.000000000000000000, 0.9238795325112867385, 1.000000000000000000, 0.9238795325112867385, 1.000000000000000000, 0.9238795325112867385, 1.000000000000000000, 0.9238795325112867385, 1.000000000000000000, 0.9238795325112867385, 1.000000000000000000, 0.9238795325112867385, 1.000000000000000000, 0.9238795325112867385, 1.000000000000000000, 0.9238795325112867385, 1.000000000000000000, 0.9238795325112867385, 1.000000000000000000, 0.9238795325112867385, 1.000000000000000000, 0.9238795325112867385, 1.000000000000000000, 0.9238795325112867385, 1.000000000000000000) ) ) 
 REPRESENTATION_ITEM ( '' )  SURFACE ( )  );
#11489=CARTESIAN_POINT ( 'NONE',  ( 1.726321361862525858E-17, 0.4520833332574667462, -0.2819296736111110979 ) ) ;
#11491=CARTESIAN_POINT ( 'NONE',  ( 0.2819296736111110979, 0.5493055554796889561, 0.000000000000000000 ) ) ;
#11497=CARTESIAN_POINT ( 'NONE',  ( 0.1993543840281266910, 0.2090277777019111383, -0.1993543840281266910 ) ) ;
#11498=CARTESIAN_POINT ( 'NONE',  ( 0.1167790944451423257, 0.3236111110352444808, -0.2819296736111110424 ) ) ;
#11500=CARTESIAN_POINT ( 'NONE',  ( 0.2819296736111110979, 4.335500000075866112, 0.1167790944451422425 ) ) ;
#11503=CARTESIAN_POINT ( 'NONE',  ( -0.2819296736111110424, 4.925777777853643791, 0.1167790944451424923 ) ) ;
#11504=CARTESIAN_POINT ( 'NONE',  ( 0.2819296736111111534, 4.543833333409198261, 0.1167790944451422563 ) ) ;
#11507=CARTESIAN_POINT ( 'NONE',  ( 0.3119999999999999996, 4.029944444596176290, -3.820898013339742174E-17 ) ) ;
#11518=CARTESIAN_POINT ( 'NONE',  ( -5.731347020009612645E-17, 0.6083333331816004330, 0.3119999999999999996 ) ) ;
#11520=CARTESIAN_POINT ( 'NONE',  ( 0.1670718646175240740, 4.261161593087173571, -0.2643034011721546173 ) ) ;
#11521=CYLINDRICAL_SURFACE ( 'NONE', #1091, 0.3119999999999999996 ) ;
#11522=CARTESIAN_POINT ( 'NONE',  ( 0.3037029041911168403, 4.749794205331636654, 0.08231968813497411719 ) ) ;
#11524=CARTESIAN_POINT ( 'NONE',  ( 0.1300715219937130795, 5.170735578853760117, 0.2669230633663410290 ) ) ;
#11525=ORIENTED_EDGE ( 'NONE', *, *, #18697, .F. ) ;
#11530=EDGE_CURVE ( 'NONE', #9562, #23454, #3796, .T. ) ;
#11531=CARTESIAN_POINT ( 'NONE',  ( -0.2819296736111110424, 3.967444444520310309, 0.1167790944451424923 ) ) ;
#11534=CARTESIAN_POINT ( 'NONE',  ( 0.6082799348109491078, 3.738202056031992182, 0.09828638484944851594 ) ) ;
#11535=CLOSED_SHELL ( 'NONE', ( #2329, #23180, #19884, #23316, #7030, #3704, #19612, #433, #11246, #8235, #3444, #10953, #19859, #5017, #16304, #8630, #18907, #22563, #1525, #20020, #1716, #4927, #20050, #15328, #12606, #23916, #5222, #23451, #14573, #1392, #7497, #11109, #23962, #13230, #17660, #14079, #13089, #8326, #17068, #23010, #62, #1961, #2332, #18063, #13559, #17085, #12066, #19201, #9011, #22741, #19597, #8705, #10666, #3368, #10649, #7224, #12156, #15604, #824, #19596, #30, #4254, #6004, #2963, #12607, #15035, #8865, #5499, #16028, #13789, #5548, #21429, #15138, #17026, #8569, #22113, #21340, #5615, #14235, #1311, #3196, #13625, #17986, #16595, #11351, #7521, #20132 ) ) ;
#11536=CARTESIAN_POINT ( 'NONE',  ( -0.2206173157302028232, 4.773000000151731648, -0.2206173157302028232 ) ) ;
#11538=CARTESIAN_POINT ( 'NONE',  ( 0.1993543840281267465, 4.998694444520309865, 0.1993543840281266633 ) ) ;
#11539=VERTEX_POINT ( 'NONE', #6750 ) ;
#11540=CARTESIAN_POINT ( 'NONE',  ( 0.2819296736111110424, 4.384111111186976828, -0.1167790944451423396 ) ) ;
#11541=ORIENTED_EDGE ( 'NONE', *, *, #10374, .F. ) ;
#11548=CYLINDRICAL_SURFACE ( 'NONE', #5385, 0.3119999999999999996 ) ;
#11549=CARTESIAN_POINT ( 'NONE',  ( 0.1993543840281266633, 3.901472222298087988, -0.1993543840281266910 ) ) ;
#11550=AXIS2_PLACEMENT_3D ( 'NONE', #3088, #14428, #1136 ) ;
#11553=EDGE_CURVE ( 'NONE', #10865, #7634, #3212, .T. ) ;
#11558=CARTESIAN_POINT ( 'NONE',  ( 0.2819296736111110979, 0.4972222221463556413, -0.1167790944451422980 ) ) ;
#11560=VERTEX_POINT ( 'NONE', #23319 ) ;
#11561=CARTESIAN_POINT ( 'NONE',  ( 0.1167790944451424368, 4.995222222298087544, 0.2819296736111110424 ) ) ;
#11562=CARTESIAN_POINT ( 'NONE',  ( 5.731347020009612645E-17, 3.953555555555555046, 0.3119999999999999996 ) ) ;
#11563=CARTESIAN_POINT ( 'NONE',  ( 0.2819296736111110979, 4.769527777853642903, -3.452642723725051716E-17 ) ) ;
#11565=CARTESIAN_POINT ( 'NONE',  ( 0.1679725729491048092, 4.872240167009049827, -0.2637599262370826092 ) ) ;
#11569=CARTESIAN_POINT ( 'NONE',  ( 0.3119999999999999996, 4.522999999999999687, -3.820898013339742174E-17 ) ) ;
#11570=CARTESIAN_POINT ( 'NONE',  ( -0.1993543840281266355, 3.748694444520309865, 0.1993543840281267465 ) ) ;
#11573=CARTESIAN_POINT ( 'NONE',  ( -0.2206173157302027954, 0.5319444442927114824, -0.2206173157302028232 ) ) ;
#11574=ORIENTED_EDGE ( 'NONE', *, *, #8448, .F. ) ;
#11576=DIRECTION ( 'NONE',  ( 0.000000000000000000, 0.000000000000000000, -1.000000000000000000 ) ) ;
#11578=CARTESIAN_POINT ( 'NONE',  ( 0.2824805458792227220, 4.700498842312279990, -0.1324723342704639539 ) ) ;
#11584=CARTESIAN_POINT ( 'NONE',  ( -0.2819296736111110979, 0.4520833332574666907, -3.452642723725051716E-17 ) ) ;
#11585=CARTESIAN_POINT ( 'NONE',  ( -0.1950097289954165203, 5.206640035683668621, 0.2045561157895784965 ) ) ;
#11587=CARTESIAN_POINT ( 'NONE',  ( -0.1292346314604058410, 0.1673611111111107941, 0.3119999999999998885 ) ) ;
#11591=CARTESIAN_POINT ( 'NONE',  ( 0.3119999999999999996, 0.2402777777777774515, 0.000000000000000000 ) ) ;
#11592=CARTESIAN_POINT ( 'NONE',  ( -0.1292346314604056745, 5.207027777777777366, -0.3119999999999999996 ) ) ;
#11593=CARTESIAN_POINT ( 'NONE',  ( 0.1167790944451422702, 4.182722222298087544, -0.2819296736111110424 ) ) ;
#11598=CARTESIAN_POINT ( 'NONE',  ( 1.910449006669871087E-17, 0.3652777777777774237, -0.3119999999999999996 ) ) ;
#11599=CARTESIAN_POINT ( 'NONE',  ( 0.1993543840281267465, 4.707027777853643791, 0.1993543840281266633 ) ) ;
#11605=CARTESIAN_POINT ( 'NONE',  ( -0.1167790944451423119, 4.356333333409199149, -0.2819296736111110979 ) ) ;
#11607=CARTESIAN_POINT ( 'NONE',  ( -0.3105842280018246138, 4.056716673947225793, -0.03562418879921332854 ) ) ;
#11610=CARTESIAN_POINT ( 'NONE',  ( -0.1993543840281267465, 0.5284722221463555858, 0.1993543840281266633 ) ) ;
#11616=CARTESIAN_POINT ( 'NONE',  ( -0.1167790944451424506, 0.4624999999241333759, 0.2819296736111110424 ) ) ;
#11617=CARTESIAN_POINT ( 'NONE',  ( 0.2819296736111110424, 0.2541666665908000056, 0.1167790944451424923 ) ) ;
#11619=CARTESIAN_POINT ( 'NONE',  ( -1.726321361862525858E-17, 4.241750000075866112, -0.2819296736111110979 ) ) ;
#11623=CARTESIAN_POINT ( 'NONE',  ( 5.178964085587577574E-17, 4.825083333409199149, 0.2819296736111110979 ) ) ;
#11625=CARTESIAN_POINT ( 'NONE',  ( -0.1993543840281266910, 4.123694444520309865, -0.1993543840281266910 ) ) ;
#11628=CARTESIAN_POINT ( 'NONE',  ( 0.000000000000000000, 5.384999999999999787, 0.000000000000000000 ) ) ;
#11629=CARTESIAN_POINT ( 'NONE',  ( 0.3119999999999999996, 4.144527777929510215, -0.1292346314604056745 ) ) ;
#11633=( BOUNDED_CURVE ( )  B_SPLINE_CURVE ( 2, ( #6196, #8262, #6437, #12194, #22784, #21196, #2431, #20959, #9873 ),
 .UNSPECIFIED., .F., .F. ) 
 B_SPLINE_CURVE_WITH_KNOTS ( ( 3, 2, 2, 2, 3 ),
 ( 0.8125000000000000000, 0.8229166666666666297, 0.8333333333333333703, 0.8437500000000000000, 0.8541666666666666297 ),
 .UNSPECIFIED. ) 
 CURVE ( )  GEOMETRIC_REPRESENTATION_ITEM ( )  RATIONAL_B_SPLINE_CURVE ( ( 1.000000000000000000, 0.9238795325112867385, 1.000000000000000000, 0.9238795325112867385, 1.000000000000000000, 0.9238795325112867385, 1.000000000000000000, 0.9238795325112867385, 1.000000000000000000 ) ) 
 REPRESENTATION_ITEM ( '' )  );
#11637=CARTESIAN_POINT ( 'NONE',  ( 6.089848770316828444E-07, 4.238302053322364316, 0.3119999999987258521 ) ) ;
#11638=CARTESIAN_POINT ( 'NONE',  ( -0.07934877013414777525, 5.013721278816293037, 0.3045045899376126464 ) ) ;
#11640=CARTESIAN_POINT ( 'NONE',  ( 0.1167790944451423257, 0.004166666590800036790, -0.2819296736111110424 ) ) ;
#11641=ORIENTED_EDGE ( 'NONE', *, *, #17053, .T. ) ;
#11642=LINE ( 'NONE', #413, #9345 ) ;
#11643=FACE_OUTER_BOUND ( 'NONE', #588, .T. ) ;
#11644=CARTESIAN_POINT ( 'NONE',  ( -0.3119999999999999996, 0.5458333333333329485, -3.820898013339742174E-17 ) ) ;
#11646=CARTESIAN_POINT ( 'NONE',  ( 0.2934911225613386909, 5.179109063580405348, -0.006257992997124091177 ) ) ;
#11648=ORIENTED_EDGE ( 'NONE', *, *, #20695, .F. ) ;
#11652=CARTESIAN_POINT ( 'NONE',  ( -1.726321361862525858E-17, 4.005638888964754507, -0.2819296736111110979 ) ) ;
#11654=CARTESIAN_POINT ( 'NONE',  ( 0.04000452085013941200, 5.119333780138143553, 0.3065892211030125658 ) ) ;
#11655=CARTESIAN_POINT ( 'NONE',  ( -0.2909981737311249095, 5.180927869648259687, 0.03329044010142344356 ) ) ;
#11657=CARTESIAN_POINT ( 'NONE',  ( 0.3119999999999999996, 4.748694444596176290, 0.1292346314604056190 ) ) ;
#11658=CARTESIAN_POINT ( 'NONE',  ( -0.1167790944451423119, 5.023000000075866112, -0.2819296736111110979 ) ) ;
#11660=CARTESIAN_POINT ( 'NONE',  ( -0.2819296736111110424, 4.300777777853642903, 0.1167790944451424923 ) ) ;
#11668=CARTESIAN_POINT ( 'NONE',  ( -0.1167790944451423535, 3.821611111186977272, 0.2819296736111110979 ) ) ;
#11670=CARTESIAN_POINT ( 'NONE',  ( 0.000000000000000000, 5.384999999999999787, 0.000000000000000000 ) ) ;
#11671=LINE ( 'NONE', #6895, #1517 ) ;
#11675=CARTESIAN_POINT ( 'NONE',  ( -0.2819296736111110979, 0.5215277777019110550, -3.452642723725051716E-17 ) ) ;
#11677=ORIENTED_EDGE ( 'NONE', *, *, #14388, .T. ) ;
#11678=CARTESIAN_POINT ( 'NONE',  ( -0.1993543840281266355, 4.651472222298087544, 0.1993543840281267465 ) ) ;
#11679=CARTESIAN_POINT ( 'NONE',  ( -0.1292346314604057300, 3.950083333333332281, 0.3119999999999998885 ) ) ;
#11680=CARTESIAN_POINT ( 'NONE',  ( 5.178964085587577574E-17, 4.755638888964754507, 0.2819296736111110979 ) ) ;
#11681=CARTESIAN_POINT ( 'NONE',  ( -0.08061050724763124675, 4.157245614755926688, -0.3020926103485261915 ) ) ;
#11682=CARTESIAN_POINT ( 'NONE',  ( 7.515426412127797749E-07, 4.849418923572540230, 0.3119999999980542227 ) ) ;
#11685=CARTESIAN_POINT ( 'NONE',  ( -0.3119999999999999996, 4.269527777777777366, -0.1292346314604056468 ) ) ;
#11687=CARTESIAN_POINT ( 'NONE',  ( -0.2206173157302028787, 0.5458333331816004330, 0.2206173157302027954 ) ) ;
#11689=ORIENTED_EDGE ( 'NONE', *, *, #18990, .F. ) ;
#11690=CARTESIAN_POINT ( 'NONE',  ( 0.3108774165693796721, 4.584777046742110507, 0.02644302458017251320 ) ) ;
#11691=ORIENTED_EDGE ( 'NONE', *, *, #22118, .T. ) ;
#11694=CARTESIAN_POINT ( 'NONE',  ( 0.1907340935051382025, 4.133015612144294693, 0.2469099182623766542 ) ) ;
#11696=CARTESIAN_POINT ( 'NONE',  ( 0.08154560721408028734, 4.296146448903024329, 0.3039036348046776359 ) ) ;
#11701=CARTESIAN_POINT ( 'NONE',  ( 0.2819296736111110424, 0.3722222221463555858, -0.1167790944451423119 ) ) ;
#11702=DIRECTION ( 'NONE',  ( 1.000000000000000000, 0.000000000000000000, 0.000000000000000000 ) ) ;
#11706=CARTESIAN_POINT ( 'NONE',  ( -0.1528469870339583259, 4.622614882896163735, 0.2719999503001284125 ) ) ;
#11709=CARTESIAN_POINT ( 'NONE',  ( -0.3119999999999999996, 0.1534722222222218990, -0.1292346314604056745 ) ) ;
#11710=CARTESIAN_POINT ( 'NONE',  ( 0.1292346314604058410, 5.179249999999998799, 0.3119999999999998885 ) ) ;
#11711=CARTESIAN_POINT ( 'NONE',  ( 0.2819296736111110979, 4.113277777853643791, 0.1167790944451422425 ) ) ;
#11717=CARTESIAN_POINT ( 'NONE',  ( -1.726321361862525858E-17, 4.672305555631421470, -0.2819296736111110979 ) ) ;
#11719=AXIS2_PLACEMENT_3D ( 'NONE', #16019, #13956, #13723 ) ;
#11720=CARTESIAN_POINT ( 'NONE',  ( -0.03098226891380893508, 4.515206242287482574, 0.3104630823214994950 ) ) ;
#11725=CARTESIAN_POINT ( 'NONE',  ( 0.3119999999999999996, 0.6256944442927114824, -0.1292346314604056468 ) ) ;
#11726=CARTESIAN_POINT ( 'NONE',  ( -0.1993543840281266355, 4.318138888964754507, 0.1993543840281267465 ) ) ;
#11729=CARTESIAN_POINT ( 'NONE',  ( -0.2670672243593699702, 4.052874141853025414, -0.1660684718339069943 ) ) ;
#11731=CYLINDRICAL_SURFACE ( 'NONE', #23476, 0.3119999999999999996 ) ;
#11733=CARTESIAN_POINT ( 'NONE',  ( 0.2819296736111110424, 0.4902777777019112215, 0.1167790944451424923 ) ) ;
#11734=CARTESIAN_POINT ( 'NONE',  ( 0.1292346314604058410, 4.123694444444444329, 0.3119999999999998885 ) ) ;
#11735=DIRECTION ( 'NONE',  ( -0.000000000000000000, -1.000000000000000000, -0.000000000000000000 ) ) ;
#11738=DIRECTION ( 'NONE',  ( -0.000000000000000000, -1.000000000000000000, -0.000000000000000000 ) ) ;
#11739=CARTESIAN_POINT ( 'NONE',  ( 0.3119999999999999996, 5.026472222222221120, -0.1292346314604056745 ) ) ;
#11740=CARTESIAN_POINT ( 'NONE',  ( -0.2819296736111111534, 0.4555555554796890116, 0.1167790944451422563 ) ) ;
#11741=CARTESIAN_POINT ( 'NONE',  ( -0.1993543840281266633, 0.2229166665908000333, -0.1993543840281266910 ) ) ;
#11742=ORIENTED_EDGE ( 'NONE', *, *, #7094, .T. ) ;
#11744=CARTESIAN_POINT ( 'NONE',  ( 0.2819296736111110979, 4.224388888964755395, 0.1167790944451422425 ) ) ;
#11746=CARTESIAN_POINT ( 'NONE',  ( 0.2819296736111110979, 4.894527777853643791, -3.452642723725051716E-17 ) ) ;
#11747=CARTESIAN_POINT ( 'NONE',  ( -1.726321361862525858E-17, 4.283416666742532186, -0.2819296736111110979 ) ) ;
#11751=CARTESIAN_POINT ( 'NONE',  ( -1.910449006669871087E-17, 3.932722222373954413, -0.3119999999999999996 ) ) ;
#11752=CARTESIAN_POINT ( 'NONE',  ( -5.731347020009612645E-17, 0.1152777777777774515, 0.3119999999999999996 ) ) ;
#11759=ORIENTED_EDGE ( 'NONE', *, *, #13694, .T. ) ;
#11760=CARTESIAN_POINT ( 'NONE',  ( 0.2206173157302027676, 0.6152777776260449638, 0.2206173157302028787 ) ) ;
#11762=CARTESIAN_POINT ( 'NONE',  ( 0.2837750196973463646, 4.255964866207376573, -0.1296761943110192605 ) ) ;
#11766=CARTESIAN_POINT ( 'NONE',  ( 0.07599768514248278484, 5.169247371546412673, 0.2875240573393413879 ) ) ;
#11767=ORIENTED_EDGE ( 'NONE', *, *, #11870, .F. ) ;
#11771=CARTESIAN_POINT ( 'NONE',  ( 0.1993543840281266633, 3.943138888964754507, -0.1993543840281266910 ) ) ;
#11773=CARTESIAN_POINT ( 'NONE',  ( -0.1211763616584382586, 5.192648849054667615, 0.2616024314742874113 ) ) ;
#11774=CARTESIAN_POINT ( 'NONE',  ( -1.910449006669871087E-17, 4.432722222373953969, -0.3119999999999999996 ) ) ;
#11775=CARTESIAN_POINT ( 'NONE',  ( 0.1167790944451424506, 4.939666666742532186, 0.2819296736111110424 ) ) ;
#11776=VERTEX_POINT ( 'NONE', #17196 ) ;
#11777=CARTESIAN_POINT ( 'NONE',  ( 0.2819296736111110979, 4.380638888964754507, -3.452642723725051716E-17 ) ) ;
#11780=ORIENTED_EDGE ( 'NONE', *, *, #3305, .T. ) ;
#11783=DIRECTION ( 'NONE',  ( 0.000000000000000000, 0.000000000000000000, -1.000000000000000000 ) ) ;
#11784=CARTESIAN_POINT ( 'NONE',  ( -0.2819296736111110979, 3.752166666742532630, -0.1167790944451422980 ) ) ;
#11785=CARTESIAN_POINT ( 'NONE',  ( 0.07355958478172115733, 4.407018638961537782, 0.3032090396793259424 ) ) ;
#11789=CARTESIAN_POINT ( 'NONE',  ( -0.1993543840281266633, 0.5701388888130222155, -0.1993543840281266910 ) ) ;
#11792=CARTESIAN_POINT ( 'NONE',  ( 0.1993543840281267465, 4.776472222298088433, 0.1993543840281266633 ) ) ;
#11794=VECTOR ( 'NONE', #15100, 39.37007874015748143 ) ;
#11795=CARTESIAN_POINT ( 'NONE',  ( -1.726321361862525858E-17, 4.616750000075865223, -0.2819296736111110979 ) ) ;
#11797=( BOUNDED_CURVE ( )  B_SPLINE_CURVE ( 2, ( #18925, #2461, #4279, #11859, #19274, #20746, #2224, #11734, #17094 ),
 .UNSPECIFIED., .F., .F. ) 
 B_SPLINE_CURVE_WITH_KNOTS ( ( 3, 2, 2, 2, 3 ),
 ( 0.7232142857142858094, 0.7276785714285715079, 0.7321428571428572063, 0.7366071428571429047, 0.7410714285714286031 ),
 .UNSPECIFIED. ) 
 CURVE ( )  GEOMETRIC_REPRESENTATION_ITEM ( )  RATIONAL_B_SPLINE_CURVE ( ( 0.9999999999999981126, 0.9238795325112886259, 1.000000000000000000, 0.9238795325112867385, 1.000000000000000000, 0.9238795325112867385, 1.000000000000000000, 0.9238795325112867385, 1.000000000000000000 ) ) 
 REPRESENTATION_ITEM ( '' )  );
#11799=CARTESIAN_POINT ( 'NONE',  ( 0.04546508165698102955, 4.850751077471080919, 0.3093939345129879115 ) ) ;
#11800=DIRECTION ( 'NONE',  ( 0.000000000000000000, 0.000000000000000000, -1.000000000000000000 ) ) ;
#11802=CARTESIAN_POINT ( 'NONE',  ( -1.910449006669871087E-17, 4.203555555555555046, -0.3119999999999999996 ) ) ;
#11805=CARTESIAN_POINT ( 'NONE',  ( 0.1292346314604058410, 5.186194444596176290, 0.3119999999999998885 ) ) ;
#11813=CARTESIAN_POINT ( 'NONE',  ( 0.006135078556594095005, 4.710334877597526670, -0.3119484483264631236 ) ) ;
#11814=VECTOR ( 'NONE', #9454, 39.37007874015748143 ) ;
#11815=CARTESIAN_POINT ( 'NONE',  ( 0.1873983838916965794, 4.132896614991455664, 0.2494675077111220274 ) ) ;
#11817=B_SPLINE_CURVE_WITH_KNOTS ( 'NONE', 3,
 ( #14706, #14825, #9931, #9685, #4306, #21378, #22843, #8202, #8080, #2723, #19183, #9811, #6132, #2375, #22722, #23070, #19307, #11520, #2251, #6379, #2610, #10054, #21136, #17599, #17478, #6500, #8320, #11762, #15415, #770, #13599, #6256, #10177, #890, #15772, #17124, #13950, #4425, #11891, #21012, #22953, #15651, #13827, #23191 ),
 .UNSPECIFIED., .F., .F.,
 ( 4, 2, 1, 1, 1, 1, 1, 1, 2, 2, 2, 2, 2, 2, 2, 2, 2, 2, 1, 1, 2, 2, 2, 2, 2, 4 ),
 ( 0.6304885228263440444, 0.6304929868432944673, 0.6304974508602450012, 0.6305063788941459579, 0.6305242349619478714, 0.6305599470975516985, 0.6306313713687593525, 0.6307742199111745496, 0.6310599169960051658, 0.6316313111656661761, 0.6327740995049883077, 0.6339168878443105504, 0.6350596761836326820, 0.6362024645229548137, 0.6367738586926158240, 0.6370595557774464401, 0.6371309800486540942, 0.6371488361164560077, 0.6371666921842579212, 0.6372024043198616372, 0.6373452528622769453, 0.6396308295409212086, 0.6419164062195654719, 0.6442019828982096241, 0.6464875595768538874, 0.6487731362554981507 ),
 .UNSPECIFIED. ) ;
#11819=CARTESIAN_POINT ( 'NONE',  ( 0.3037735703191254411, 4.305353122071822192, 0.08207324121115516791 ) ) ;
#11822=CARTESIAN_POINT ( 'NONE',  ( -0.2819296736111110979, 0.5666666665908001166, 0.1167790944451422425 ) ) ;
#11826=ORIENTED_EDGE ( 'NONE', *, *, #6913, .F. ) ;
#11828=EDGE_CURVE ( 'NONE', #22848, #14521, #13209, .T. ) ;
#11831=CARTESIAN_POINT ( 'NONE',  ( -0.2206173157302027954, 0.1499999999999996336, -0.2206173157302028232 ) ) ;
#11832=CARTESIAN_POINT ( 'NONE',  ( 0.1292346314604058410, 4.845916666666666650, 0.3119999999999998885 ) ) ;
#11833=EDGE_CURVE ( 'NONE', #13967, #6423, #9187, .T. ) ;
#11835=CARTESIAN_POINT ( 'NONE',  ( -0.2819296736111110424, 3.918833333409198705, -0.1167790944451423119 ) ) ;
#11836=CARTESIAN_POINT ( 'NONE',  ( 0.000000000000000000, 5.384999999999999787, -0.3119999999999999996 ) ) ;
#11837=CARTESIAN_POINT ( 'NONE',  ( -0.2206173157302028232, 3.877166666666666206, -0.2206173157302028232 ) ) ;
#11838=CARTESIAN_POINT ( 'NONE',  ( 0.03502586135503213405, 4.820592410594939814, -0.3119999852544549923 ) ) ;
#11841=SPHERICAL_SURFACE ( 'NONE', #14392, 0.3119999999999999996 ) ;
#11842=CARTESIAN_POINT ( 'NONE',  ( 5.178964085587577574E-17, 4.700083333409199149, 0.2819296736111110979 ) ) ;
#11851=CARTESIAN_POINT ( 'NONE',  ( -0.1993543840281266910, 4.304250000075866112, -0.1993543840281266910 ) ) ;
#11854=CARTESIAN_POINT ( 'NONE',  ( -0.1209015717334110257, 4.047309448929498288, -0.2883025095971109009 ) ) ;
#11858=CARTESIAN_POINT ( 'NONE',  ( -0.1993543840281267465, 0.4729166665907999501, 0.1993543840281266633 ) ) ;
#11859=CARTESIAN_POINT ( 'NONE',  ( 0.3119999999999999996, 4.137583333333332725, -0.1292346314604056745 ) ) ;
#11860=DIRECTION ( 'NONE',  ( -0.000000000000000000, -1.000000000000000000, -0.000000000000000000 ) ) ;
#11861=CARTESIAN_POINT ( 'NONE',  ( 3.820898013339742174E-17, 5.384999999999999787, 0.3119999999999999996 ) ) ;
#11865=EDGE_CURVE ( 'NONE', #14830, #17235, #15682, .T. ) ;
#11867=CARTESIAN_POINT ( 'NONE',  ( -0.2819296736111110979, 0.5041666665908000056, -0.1167790944451423396 ) ) ;
#11868=CARTESIAN_POINT ( 'NONE',  ( -0.2819296736111110424, 0.2263888888130222710, -0.1167790944451423396 ) ) ;
#11870=EDGE_CURVE ( 'NONE', #10582, #9441, #13295, .T. ) ;
#11871=CARTESIAN_POINT ( 'NONE',  ( -0.2819296736111110424, 4.141055555631421470, -0.1167790944451423119 ) ) ;
#11873=CARTESIAN_POINT ( 'NONE',  ( 0.2819296736111110979, 4.779944444520310753, 0.1167790944451422425 ) ) ;
#11874=CARTESIAN_POINT ( 'NONE',  ( 1.910449006669871087E-17, 0.4138888887371559577, -0.3119999999999999996 ) ) ;
#11875=VERTEX_POINT ( 'NONE', #8387 ) ;
#11877=CARTESIAN_POINT ( 'NONE',  ( -0.3119999999999999996, 3.835500000151732536, 0.000000000000000000 ) ) ;
#11878=AXIS2_PLACEMENT_3D ( 'NONE', #8631, #1074, #16076 ) ;
#11879=EDGE_CURVE ( 'NONE', #17381, #23806, #18177, .T. ) ;
#11884=ORIENTED_EDGE ( 'NONE', *, *, #14082, .F. ) ;
#11887=CARTESIAN_POINT ( 'NONE',  ( -0.2297546890400682940, 5.008753309236311679, 0.2110849256844293531 ) ) ;
#11889=CARTESIAN_POINT ( 'NONE',  ( 0.2819296736111110424, 0.1569444443685778234, 0.1167790944451424923 ) ) ;
#11891=CARTESIAN_POINT ( 'NONE',  ( 0.2492517591117642817, 4.246397638743545144, 0.1920442392552785815 ) ) ;
#11896=CARTESIAN_POINT ( 'NONE',  ( 0.2330253964033324743, 5.174051372064914389, 0.1822079934528198497 ) ) ;
#11900=CARTESIAN_POINT ( 'NONE',  ( 0.1167790944451424368, 3.981333333409199593, 0.2819296736111110424 ) ) ;
#11903=CARTESIAN_POINT ( 'NONE',  ( -0.2911802280149716204, 5.178089509600573237, -0.04337890609128645242 ) ) ;
#11904=CARTESIAN_POINT ( 'NONE',  ( 0.2206173157302028787, 4.411888889040620931, 0.2206173157302027954 ) ) ;
#11905=CARTESIAN_POINT ( 'NONE',  ( 0.1167790944451424506, 5.050777777853643791, 0.2819296736111110424 ) ) ;
#11907=CARTESIAN_POINT ( 'NONE',  ( -0.2819296736111110979, 3.963972222298087544, 0.000000000000000000 ) ) ;
#11908=ORIENTED_EDGE ( 'NONE', *, *, #4078, .T. ) ;
#11909=ORIENTED_EDGE ( 'NONE', *, *, #13812, .F. ) ;
#11915=EDGE_LOOP ( 'NONE', ( #10632, #10031, #17963, #7395 ) ) ;
#11916=CARTESIAN_POINT ( 'NONE',  ( -0.1292346314604058410, 0.04930555540382262208, 0.3119999999999998885 ) ) ;
#11917=CARTESIAN_POINT ( 'NONE',  ( 0.009944027729119363224, 5.130526759350952481, 0.3066508893901822574 ) ) ;
#11919=CARTESIAN_POINT ( 'NONE',  ( 0.000000000000000000, 5.384999999999999787, -0.3119999999999999996 ) ) ;
#11922=CARTESIAN_POINT ( 'NONE',  ( -0.1993543840281267465, 0.1256944443685777957, 0.1993543840281266633 ) ) ;
#11925=CARTESIAN_POINT ( 'NONE',  ( 5.178964085587577574E-17, 4.658416666742532186, 0.2819296736111110979 ) ) ;
#11927=CARTESIAN_POINT ( 'NONE',  ( 5.178964085587577574E-17, 4.588972222298087544, 0.2819296736111110979 ) ) ;
#11929=CARTESIAN_POINT ( 'NONE',  ( 0.3084778088542702301, 4.861392285864870821, 0.06361362161637863777 ) ) ;
#11932=CARTESIAN_POINT ( 'NONE',  ( 0.3119999999999999996, 4.245222222222222008, -3.820898013339742174E-17 ) ) ;
#11934=CARTESIAN_POINT ( 'NONE',  ( -0.3119999999999998885, 5.116750000151732536, 0.1292346314604058410 ) ) ;
#11936=CARTESIAN_POINT ( 'NONE',  ( 0.06194388087313247582, 4.962233402074594402, 0.3057891118530218222 ) ) ;
#11938=ORIENTED_EDGE ( 'NONE', *, *, #4244, .T. ) ;
#11941=CARTESIAN_POINT ( 'NONE',  ( 0.2372985009168012693, 4.702956468199077200, -0.2041371284000717268 ) ) ;
#11944=CARTESIAN_POINT ( 'NONE',  ( 1.201146141948970407E-06, 4.904991752689871198, 0.3119999999951060254 ) ) ;
#11947=CARTESIAN_POINT ( 'NONE',  ( -0.1571289607070218142, 3.937354179263907294, -0.2726214474784059982 ) ) ;
#11948=( BOUNDED_CURVE ( )  B_SPLINE_CURVE ( 2, ( #2748, #20921, #2398, #19334, #9836, #4214, #19449, #6158, #21160 ),
 .UNSPECIFIED., .F., .T. ) 
 B_SPLINE_CURVE_WITH_KNOTS ( ( 3, 2, 2, 2, 3 ),
 ( 0.4791666666666666852, 0.4895833333333333148, 0.5000000000000000000, 0.5104166666666666297, 0.5208333333333333703 ),
 .UNSPECIFIED. ) 
 CURVE ( )  GEOMETRIC_REPRESENTATION_ITEM ( )  RATIONAL_B_SPLINE_CURVE ( ( 1.000000000000000000, 0.9238795325112867385, 1.000000000000000000, 0.9238795325112867385, 1.000000000000000000, 0.9238795325112867385, 1.000000000000000000, 0.9238795325112867385, 1.000000000000000000 ) ) 
 REPRESENTATION_ITEM ( '' )  );
#11955=CARTESIAN_POINT ( 'NONE',  ( 1.726321361862525858E-17, 0.6187499999241333759, -0.2819296736111110979 ) ) ;
#11957=CARTESIAN_POINT ( 'NONE',  ( -0.1556145064993704752, 5.113981281356894115, 0.2680637230490377498 ) ) ;
#11958=DIRECTION ( 'NONE',  ( 0.000000000000000000, 1.000000000000000000, 0.000000000000000000 ) ) ;
#11960=CARTESIAN_POINT ( 'NONE',  ( -0.1292346314604058410, 0.5562499999999995781, 0.3119999999999998885 ) ) ;
#11961=CARTESIAN_POINT ( 'NONE',  ( 0.1292346314604056190, 5.033416666666665762, -0.3119999999999999996 ) ) ;
#11962=VECTOR ( 'NONE', #7542, 39.37007874015748143 ) ;
#11963=CARTESIAN_POINT ( 'NONE',  ( -0.2819296736111110979, 4.088972222298088433, 0.000000000000000000 ) ) ;
#11964=CARTESIAN_POINT ( 'NONE',  ( -0.3119999999999999996, 3.828555555555555046, 0.000000000000000000 ) ) ;
#11965=CARTESIAN_POINT ( 'NONE',  ( -0.1292346314604057300, 3.894527777777776478, 0.3119999999999998885 ) ) ;
#11969=DIRECTION ( 'NONE',  ( 0.000000000000000000, 0.000000000000000000, -1.000000000000000000 ) ) ;
#11970=CARTESIAN_POINT ( 'NONE',  ( 0.1993543840281267465, 4.651472222298087544, 0.1993543840281266633 ) ) ;
#11974=FACE_OUTER_BOUND ( 'NONE', #8127, .T. ) ;
#11977=AXIS2_PLACEMENT_3D ( 'NONE', #3924, #11369, #14272 ) ;
#11978=CARTESIAN_POINT ( 'NONE',  ( -0.1167790944451423119, 4.411888888964754507, -0.2819296736111110979 ) ) ;
#11982=VERTEX_POINT ( 'NONE', #14622 ) ;
#11983=CARTESIAN_POINT ( 'NONE',  ( 0.2819296736111110424, 0.4347222221463555303, 0.1167790944451424923 ) ) ;
#11984=CARTESIAN_POINT ( 'NONE',  ( -0.3119999999999999996, 0.1013888888888885564, -3.820898013339742174E-17 ) ) ;
#11985=CARTESIAN_POINT ( 'NONE',  ( -5.428794840643969700E-10, 4.321611111277808170, -0.3119999999999999996 ) ) ;
#11988=EDGE_CURVE ( 'NONE', #14521, #12807, #12147, .T. ) ;
#11990=CARTESIAN_POINT ( 'NONE',  ( -0.002220744026976864509, 3.766115247783142550, -0.3119932384635896727 ) ) ;
#11991=CARTESIAN_POINT ( 'NONE',  ( -0.1993543840281266633, 0.5562499999241333759, -0.1993543840281266910 ) ) ;
#11992=CARTESIAN_POINT ( 'NONE',  ( 0.1993543840281266910, 0.1534722221463555858, -0.1993543840281266910 ) ) ;
#11993=CARTESIAN_POINT ( 'NONE',  ( 0.2819296736111110979, 4.057722222298088433, 0.1167790944451422425 ) ) ;
#11995=CARTESIAN_POINT ( 'NONE',  ( 0.1167790944451424368, 4.606333333409200037, 0.2819296736111110424 ) ) ;
#11999=DIRECTION ( 'NONE',  ( 0.000000000000000000, 0.000000000000000000, -1.000000000000000000 ) ) ;
#12000=CARTESIAN_POINT ( 'NONE',  ( 0.3119999999999999996, 3.915361111262843252, 0.1292346314604056190 ) ) ;
#12003=CARTESIAN_POINT ( 'NONE',  ( 0.02897014736687301972, 0.03242967361111054325, 0.2808128927374478612 ) ) ;
#12008=CARTESIAN_POINT ( 'NONE',  ( -0.2890875887038242276, 4.998758336917366485, -0.1173658538989466454 ) ) ;
#12009=VERTEX_POINT ( 'NONE', #12806 ) ;
#12010=CARTESIAN_POINT ( 'NONE',  ( -0.1167790944451424368, 0.08749999992413336203, 0.2819296736111110424 ) ) ;
#12012=ORIENTED_EDGE ( 'NONE', *, *, #20793, .F. ) ;
#12014=CARTESIAN_POINT ( 'NONE',  ( -0.2950224166209188259, 4.727389069448219239, 0.1057762073105751044 ) ) ;
#12017=EDGE_CURVE ( 'NONE', #6354, #16467, #9632, .T. ) ;
#12020=CARTESIAN_POINT ( 'NONE',  ( -0.1993543840281266355, 3.804250000075865223, 0.1993543840281267465 ) ) ;
#12021=CARTESIAN_POINT ( 'NONE',  ( -0.1552887038618610549, 5.191068077878869147, 0.2436830441765351074 ) ) ;
#12022=CARTESIAN_POINT ( 'NONE',  ( 0.000000000000000000, 5.384999999999999787, -0.3119999999999999996 ) ) ;
#12023=CARTESIAN_POINT ( 'NONE',  ( 0.2206173157302028787, 4.467444444596176290, 0.2206173157302027954 ) ) ;
#12024=CARTESIAN_POINT ( 'NONE',  ( -0.2819296736111110979, 4.641055555631421470, -0.1167790944451422980 ) ) ;
#12025=ORIENTED_EDGE ( 'NONE', *, *, #525, .F. ) ;
#12027=CARTESIAN_POINT ( 'NONE',  ( -0.1167790944451423257, 4.120222222298087544, -0.2819296736111110424 ) ) ;
#12029=ORIENTED_EDGE ( 'NONE', *, *, #2235, .T. ) ;
#12033=EDGE_CURVE ( 'NONE', #8220, #3381, #21069, .T. ) ;
#12037=CARTESIAN_POINT ( 'NONE',  ( 0.1797084794423411680, 3.735609856212664948, -0.2172307604343298448 ) ) ;
#12038=CARTESIAN_POINT ( 'NONE',  ( 0.2729403726835234467, 5.150705085961851282, -0.1311526151795892881 ) ) ;
#12043=CARTESIAN_POINT ( 'NONE',  ( -5.178964085587577574E-17, 0.1326388888130222710, 0.2819296736111110979 ) ) ;
#12047=CARTESIAN_POINT ( 'NONE',  ( -0.2819296736111110979, 4.575083333409199149, 0.000000000000000000 ) ) ;
#12052=CARTESIAN_POINT ( 'NONE',  ( 0.1292346314604058410, 4.234805555555554157, 0.3119999999999998885 ) ) ;
#12054=CARTESIAN_POINT ( 'NONE',  ( 0.3108937553010620025, 4.973671289738724965, 0.02625051856199436470 ) ) ;
#12056=ORIENTED_EDGE ( 'NONE', *, *, #15637, .F. ) ;
#12057=CARTESIAN_POINT ( 'NONE',  ( 0.07200204255845482626, 4.573693138600060770, 0.3053374176464236367 ) ) ;
#12066=ADVANCED_FACE ( 'NONE', ( #22166 ), #18511, .T. ) ;
#12068=CARTESIAN_POINT ( 'NONE',  ( 0.2819296736111110979, 0.1604166665908000333, 0.000000000000000000 ) ) ;
#12071=CARTESIAN_POINT ( 'NONE',  ( 5.731347020009612645E-17, 5.009111111111110404, 0.3119999999999999996 ) ) ;
#12074=CARTESIAN_POINT ( 'NONE',  ( -0.1377698178703422593, 5.114529494886277838, 0.2775902850408615286 ) ) ;
#12075=CARTESIAN_POINT ( 'NONE',  ( -0.2168203832546517218, 4.272808835557615481, -0.2252774235831185579 ) ) ;
#12077=CARTESIAN_POINT ( 'NONE',  ( 0.3119999999999998885, 0.4034722222222218435, 0.1292346314604058410 ) ) ;
#12078=B_SPLINE_CURVE_WITH_KNOTS ( 'NONE', 3,
 ( #20547, #22367, #18598, #24073, #10682, #23701, #5669, #11170, #18116, #18474, #7382, #10808, #20188, #14833, #22249, #3477, #16533, #5546, #22127, #8966, #18356, #1768, #13011, #20426, #3723, #3355, #7266, #1649, #5428, #11045, #12894, #13134, #18236, #1413, #8841, #14586, #10927, #23952, #7499, #12649, #5307, #12770, #23824, #9083 ),
 .UNSPECIFIED., .F., .F.,
 ( 4, 2, 2, 2, 2, 2, 2, 2, 2, 2, 2, 2, 2, 2, 2, 2, 2, 2, 2, 2, 2, 4 ),
 ( 0.07771480865003008165, 0.07919108110018341362, 0.08066735355033674559, 0.08140548977541341158, 0.08214362600049006369, 0.08361989845064339566, 0.08509617090079674151, 0.08657244335095005960, 0.08731057957602672559, 0.08804871580110339158, 0.08952498825125672355, 0.09026312447633338953, 0.09100126070141005552, 0.09247753315156338749, 0.09395380560171671946, 0.09469194182679338545, 0.09543007805187005144, 0.09690635050202339729, 0.09764448672710004939, 0.09838262295217671538, 0.09985889540233004735, 0.1013351678524833793 ),
 .UNSPECIFIED. ) ;
#12079=CARTESIAN_POINT ( 'NONE',  ( -0.3119999999999998885, 4.998694444444444329, 0.1292346314604058410 ) ) ;
#12081=B_SPLINE_CURVE_WITH_KNOTS ( 'NONE', 3,
 ( #463, #14876, #22414, #5717, #13176, #8015, #2883, #12185, #2657, #15818, #8133, #10222, #21189, #8490, #19591, #15584, #23236, #937, #1062, #15933, #9988, #4478, #4359, #13883, #6187, #823, #8252, #11694, #15467, #19359, #17648, #11815, #17532, #6667, #17770, #10109, #6310, #17412, #15704, #23007 ),
 .UNSPECIFIED., .F., .F.,
 ( 4, 2, 2, 2, 2, 2, 2, 2, 2, 2, 2, 1, 2, 2, 1, 1, 1, 2, 2, 2, 2, 4 ),
 ( 0.7035887612132493141, 0.7060454443609081032, 0.7085021275085668924, 0.7109588106562256815, 0.7121871522300550206, 0.7134154938038844707, 0.7146438353777138097, 0.7158721769515432598, 0.7171005185253725989, 0.7177146893122873239, 0.7180217747057446864, 0.7180409675428357508, 0.7180457657521085446, 0.7180505639613813385, 0.7180601603799268151, 0.7180985460541091658, 0.7181753174024736452, 0.7183288600992028261, 0.7195572016730356069, 0.7207855432468683876, 0.7220138848207011684, 0.7232422263945339491 ),
 .UNSPECIFIED. ) ;
#12082=CARTESIAN_POINT ( 'NONE',  ( 0.2819296736111110979, 4.061194444520309865, -3.452642723725051716E-17 ) ) ;
#12085=CARTESIAN_POINT ( 'NONE',  ( 0.1788910854725163091, 4.816197864334125001, -0.2589896416955246305 ) ) ;
#12088=CARTESIAN_POINT ( 'NONE',  ( -0.1571291513240659632, 4.011495724926215978, 0.2726213359419245585 ) ) ;
#12089=CARTESIAN_POINT ( 'NONE',  ( -0.1993543840281266910, 4.623694444520309865, -0.1993543840281266910 ) ) ;
#12090=CARTESIAN_POINT ( 'NONE',  ( -0.01469736539579117630, 4.515659913531111513, 0.3117060488516621986 ) ) ;
#12097=CARTESIAN_POINT ( 'NONE',  ( 0.2819296736111110979, 4.009111111186976828, -0.1167790944451423396 ) ) ;
#12099=CARTESIAN_POINT ( 'NONE',  ( -0.2929336088530244964, 4.832415422266893579, -0.1092304483702396245 ) ) ;
#12100=CARTESIAN_POINT ( 'NONE',  ( 0.01548350045596276134, 5.071997560486030565, 0.3119999982137058314 ) ) ;
#12103=CARTESIAN_POINT ( 'NONE',  ( -0.2819296736111110979, 0.5770833332574666352, -3.452642723725051716E-17 ) ) ;
#12106=CARTESIAN_POINT ( 'NONE',  ( 0.2206173157302028787, 4.460499999999998799, 0.2206173157302027954 ) ) ;
#12107=DIRECTION ( 'NONE',  ( 0.000000000000000000, 0.000000000000000000, 1.000000000000000000 ) ) ;
#12110=CARTESIAN_POINT ( 'NONE',  ( -1.910449006669871087E-17, 3.981333333333332725, -0.3119999999999999996 ) ) ;
#12112=CARTESIAN_POINT ( 'NONE',  ( 0.1993543840281266355, 0.4173611110352444808, 0.1993543840281267465 ) ) ;
#12113=CARTESIAN_POINT ( 'NONE',  ( -0.1993543840281267465, 0.4590277777019111105, 0.1993543840281266633 ) ) ;
#12114=CARTESIAN_POINT ( 'NONE',  ( -0.2819296736111110979, 4.144527777853643791, 0.000000000000000000 ) ) ;
#12117=CARTESIAN_POINT ( 'NONE',  ( -0.2819296736111110979, 4.700083333409199149, 0.000000000000000000 ) ) ;
#12120=CARTESIAN_POINT ( 'NONE',  ( 0.2085465366998034975, 5.085798565832035933, -0.2321456212477118752 ) ) ;
#12121=AXIS2_PLACEMENT_3D ( 'NONE', #13, #1977, #9656 ) ;
#12125=CARTESIAN_POINT ( 'NONE',  ( -0.1292346314604056745, 3.769527777929509327, -0.3119999999999999996 ) ) ;
#12129=CARTESIAN_POINT ( 'NONE',  ( 1.910449006669871087E-17, 0.5874999999999996891, -0.3119999999999999996 ) ) ;
#12132=CARTESIAN_POINT ( 'NONE',  ( -0.2206173157302028787, 0.3236111109593782231, 0.2206173157302027954 ) ) ;
#12134=CARTESIAN_POINT ( 'NONE',  ( 0.1993543840281266910, 0.1673611110352444808, -0.1993543840281266910 ) ) ;
#12136=ORIENTED_EDGE ( 'NONE', *, *, #11530, .T. ) ;
#12137=CARTESIAN_POINT ( 'NONE',  ( -0.1993543840281266633, 0.07013888881302225708, -0.1993543840281266910 ) ) ;
#12138=CARTESIAN_POINT ( 'NONE',  ( -0.2837606913901806194, 4.720503326065920824, -0.1316857305938944622 ) ) ;
#12139=CARTESIAN_POINT ( 'NONE',  ( 5.574357792518489764E-07, 4.071633398088104094, 0.3119999999989289674 ) ) ;
#12141=CARTESIAN_POINT ( 'NONE',  ( -0.2249462833042268628, 5.064501476579637895, 0.2162079342807830262 ) ) ;
#12142=FACE_OUTER_BOUND ( 'NONE', #10602, .T. ) ;
#12144=ORIENTED_EDGE ( 'NONE', *, *, #4085, .F. ) ;
#12145=CARTESIAN_POINT ( 'NONE',  ( 0.1167790944451422702, 5.238277777853643791, -0.2819296736111110424 ) ) ;
#12146=( BOUNDED_CURVE ( )  B_SPLINE_CURVE ( 2, ( #22097, #12858, #6866, #12494, #5270, #19914, #14309, #16259, #3321 ),
 .UNSPECIFIED., .F., .T. ) 
 B_SPLINE_CURVE_WITH_KNOTS ( ( 3, 2, 2, 2, 3 ),
 ( 0.6875000000000001110, 0.6919642857142858094, 0.6964285714285713969, 0.7008928571428570953, 0.7053571428571429047 ),
 .UNSPECIFIED. ) 
 CURVE ( )  GEOMETRIC_REPRESENTATION_ITEM ( )  RATIONAL_B_SPLINE_CURVE ( ( 0.9999999999999981126, 0.9238795325112886259, 1.000000000000000000, 0.9238795325112867385, 1.000000000000000000, 0.9238795325112867385, 1.000000000000000000, 0.9238795325112867385, 1.000000000000000000 ) ) 
 REPRESENTATION_ITEM ( '' )  );
#12147=( BOUNDED_CURVE ( )  B_SPLINE_CURVE ( 2, ( #3268, #22046, #16689, #8752, #5092, #16448, #3152, #16207, #19980 ),
 .UNSPECIFIED., .F., .T. ) 
 B_SPLINE_CURVE_WITH_KNOTS ( ( 3, 2, 2, 2, 3 ),
 ( 0.7291666666666666297, 0.7395833333333333703, 0.7500000000000000000, 0.7604166666666666297, 0.7708333333333333703 ),
 .UNSPECIFIED. ) 
 CURVE ( )  GEOMETRIC_REPRESENTATION_ITEM ( )  RATIONAL_B_SPLINE_CURVE ( ( 1.000000000000000000, 0.9238795325112867385, 1.000000000000000000, 0.9238795325112867385, 1.000000000000000000, 0.9238795325112867385, 1.000000000000000000, 0.9238795325112867385, 1.000000000000000000 ) ) 
 REPRESENTATION_ITEM ( '' )  );
#12148=CARTESIAN_POINT ( 'NONE',  ( 0.000000000000000000, 5.072999999999999510, 0.000000000000000000 ) ) ;
#12150=CARTESIAN_POINT ( 'NONE',  ( -0.3009862200524689446, 4.777363621821248962, -0.09131534522726025838 ) ) ;
#12151=CARTESIAN_POINT ( 'NONE',  ( -1.910449006669871087E-17, 4.599388889040620931, -0.3119999999999999996 ) ) ;
#12152=CARTESIAN_POINT ( 'NONE',  ( 0.2819296736111110979, 4.616750000075865223, -3.452642723725051716E-17 ) ) ;
#12154=CARTESIAN_POINT ( 'NONE',  ( 0.2819296736111110979, 3.991750000075865223, -3.452642723725051716E-17 ) ) ;
#12155=EDGE_LOOP ( 'NONE', ( #23623, #20004, #1872, #17554 ) ) ;
#12156=ADVANCED_FACE ( 'NONE', ( #13171 ), #14985, .T. ) ;
#12160=CARTESIAN_POINT ( 'NONE',  ( -0.1993543840281266910, 3.748694444520310309, -0.1993543840281266910 ) ) ;
#12163=CARTESIAN_POINT ( 'NONE',  ( 0.1292346314604043700, 4.644527777777777366, -0.3120000000000012763 ) ) ;
#12165=CARTESIAN_POINT ( 'NONE',  ( 0.2819296736111110979, 0.1499999999241333482, -0.1167790944451422980 ) ) ;
#12169=CARTESIAN_POINT ( 'NONE',  ( 0.1167790944451422702, 4.391055555631420582, -0.2819296736111110424 ) ) ;
#12173=CARTESIAN_POINT ( 'NONE',  ( 1.910449006669871087E-17, 0.4694444442927115380, -0.3119999999999999996 ) ) ;
#12174=CARTESIAN_POINT ( 'NONE',  ( -0.1292346314604056745, 4.373694444444443441, -0.3119999999999999996 ) ) ;
#12175=EDGE_CURVE ( 'NONE', #10865, #8265, #15720, .T. ) ;
#12176=CARTESIAN_POINT ( 'NONE',  ( 0.3119999999999999996, 5.141055555707287894, -3.820898013339742174E-17 ) ) ;
#12177=CARTESIAN_POINT ( 'NONE',  ( 0.3011001227036403383, 4.972027705505035478, 0.08342311245020585242 ) ) ;
#12181=VERTEX_POINT ( 'NONE', #14707 ) ;
#12185=CARTESIAN_POINT ( 'NONE',  ( 0.2853639214901735333, 4.144740996897934515, -0.1280573243343183787 ) ) ;
#12187=FACE_OUTER_BOUND ( 'NONE', #16760, .T. ) ;
#12192=CARTESIAN_POINT ( 'NONE',  ( 0.2819296736111110979, 0.05277777770191114520, -0.1167790944451422980 ) ) ;
#12194=CARTESIAN_POINT ( 'NONE',  ( 0.3119999999999998885, 0.5145833333333330595, 0.1292346314604058410 ) ) ;
#12196=ORIENTED_EDGE ( 'NONE', *, *, #12544, .F. ) ;
#12198=CARTESIAN_POINT ( 'NONE',  ( -0.2024076084730564995, 4.272264278896607870, -0.2381172270738897701 ) ) ;
#12200=CARTESIAN_POINT ( 'NONE',  ( -0.1292346314604056190, 0.3687499999999996891, -0.3119999999999999996 ) ) ;
#12201=CARTESIAN_POINT ( 'NONE',  ( 0.1292346314604058410, 4.957027777777776478, 0.3119999999999998885 ) ) ;
#12202=CARTESIAN_POINT ( 'NONE',  ( 0.1167790944451422702, 4.168833333409199149, -0.2819296736111110979 ) ) ;
#12203=CARTESIAN_POINT ( 'NONE',  ( -0.2819296736111110979, 4.033416666742532186, 0.000000000000000000 ) ) ;
#12205=CARTESIAN_POINT ( 'NONE',  ( -0.3119999999999999996, 3.884111111111110404, 0.000000000000000000 ) ) ;
#12207=ORIENTED_EDGE ( 'NONE', *, *, #9829, .T. ) ;
#12209=CARTESIAN_POINT ( 'NONE',  ( -0.2819296736111110424, 4.411888888964753619, 0.1167790944451424923 ) ) ;
#12211=CARTESIAN_POINT ( 'NONE',  ( -0.3119999999999998885, 4.109805555555554157, 0.1292346314604058410 ) ) ;
#12215=CARTESIAN_POINT ( 'NONE',  ( 0.2819296736111110979, 4.172305555631421470, -3.452642723725051716E-17 ) ) ;
#12216=CARTESIAN_POINT ( 'NONE',  ( -0.004360456888021747683, 4.821737920469208127, -0.3119738819052217949 ) ) ;
#12220=CARTESIAN_POINT ( 'NONE',  ( 0.1167790944451423257, 0.04583333325746669074, -0.2819296736111110424 ) ) ;
#12228=CARTESIAN_POINT ( 'NONE',  ( -0.2494851997466753513, 3.774217015172883993, -0.1917528079887330095 ) ) ;
#12230=CARTESIAN_POINT ( 'NONE',  ( 0.1993543840281266910, 0.3756944443685777957, -0.1993543840281266910 ) ) ;
#12231=CARTESIAN_POINT ( 'NONE',  ( -0.1993543840281266910, 4.082027777853643791, -0.1993543840281266910 ) ) ;
#12234=CARTESIAN_POINT ( 'NONE',  ( 0.2819296736111110979, 4.613277777853643791, 0.1167790944451422425 ) ) ;
#12235=CARTESIAN_POINT ( 'NONE',  ( 0.09881506494190155088, 5.140796054993752584, -0.2887599643961580864 ) ) ;
#12239=CARTESIAN_POINT ( 'NONE',  ( -0.2819296736111110424, 5.238277777853643791, -0.1167790944451423119 ) ) ;
#12243=CARTESIAN_POINT ( 'NONE',  ( 0.2819296736111110979, 4.825083333409199149, -3.452642723725051716E-17 ) ) ;
#12245=CARTESIAN_POINT ( 'NONE',  ( -0.2453579118455930796, 5.108600672401633069, -0.1896813902191237244 ) ) ;
#12246=CARTESIAN_POINT ( 'NONE',  ( 4.589747744727345336E-07, 4.571629220806286753, 0.3119999999992840722 ) ) ;
#12248=CARTESIAN_POINT ( 'NONE',  ( 0.2819296736111110979, 0.3270833332574666907, 0.000000000000000000 ) ) ;
#12249=ORIENTED_EDGE ( 'NONE', *, *, #15547, .T. ) ;
#12250=CARTESIAN_POINT ( 'NONE',  ( 1.726321361862525858E-17, 0.1187499999241333620, -0.2819296736111110979 ) ) ;
#12254=CARTESIAN_POINT ( 'NONE',  ( -0.01714907257191002066, 5.044294090511437290, -0.3120000000000000551 ) ) ;
#12256=CARTESIAN_POINT ( 'NONE',  ( -0.08123984940749030825, 4.657242163357344644, -0.3039884212747680503 ) ) ;
#12257=CARTESIAN_POINT ( 'NONE',  ( 0.1167790944451424368, 3.814666666742532630, 0.2819296736111110424 ) ) ;
#12258=CARTESIAN_POINT ( 'NONE',  ( -0.2399726197094832481, 0.04835313003952727146, -0.1767124178163874682 ) ) ;
#12259=FACE_OUTER_BOUND ( 'NONE', #4116, .T. ) ;
#12261=CARTESIAN_POINT ( 'NONE',  ( -0.3071176021544892443, 4.781885710250458388, 0.06789679950010621412 ) ) ;
#12262=CARTESIAN_POINT ( 'NONE',  ( -1.910449006669871087E-17, 4.488277777929509327, -0.3119999999999999996 ) ) ;
#12263=CARTESIAN_POINT ( 'NONE',  ( -0.1167790944451423119, 4.800777777853643791, -0.2819296736111110979 ) ) ;
#12265=CARTESIAN_POINT ( 'NONE',  ( 0.2819296736111110979, 4.043833333409200037, 0.1167790944451422425 ) ) ;
#12274=CARTESIAN_POINT ( 'NONE',  ( 0.3119999999999999996, 0.1256944442927115102, -0.1292346314604056468 ) ) ;
#12275=CARTESIAN_POINT ( 'NONE',  ( -0.2276520258992634771, 4.384388760381654926, -0.2133517376713266744 ) ) ;
#12282=DIRECTION ( 'NONE',  ( -0.000000000000000000, -1.000000000000000000, -0.000000000000000000 ) ) ;
#12283=CARTESIAN_POINT ( 'NONE',  ( 0.000000000000000000, 5.384999999999999787, 0.000000000000000000 ) ) ;
#12285=EDGE_CURVE ( 'NONE', #5345, #13418, #10760, .T. ) ;
#12286=CARTESIAN_POINT ( 'NONE',  ( -0.2819296736111110424, 4.516055555631421470, -0.1167790944451423119 ) ) ;
#12287=CARTESIAN_POINT ( 'NONE',  ( 0.000000000000000000, 5.384999999999999787, 0.000000000000000000 ) ) ;
#12291=CARTESIAN_POINT ( 'NONE',  ( -0.3119999999999999996, 4.047305555555555046, -0.1292346314604056468 ) ) ;
#12292=CARTESIAN_POINT ( 'NONE',  ( 5.731347020009612645E-17, 5.064666666666665762, 0.3119999999999999996 ) ) ;
#12294=CARTESIAN_POINT ( 'NONE',  ( 0.07550810074049957299, 4.962629998519987318, 0.3027891987685060182 ) ) ;
#12303=CARTESIAN_POINT ( 'NONE',  ( 0.2494962160978485000, 3.813449145089014003, -0.1917383745809272677 ) ) ;
#12305=CARTESIAN_POINT ( 'NONE',  ( -1.910449006669871087E-17, 4.814666666666665762, -0.3119999999999999996 ) ) ;
#12308=CARTESIAN_POINT ( 'NONE',  ( -0.1167790944451423257, 5.078555555631421470, -0.2819296736111110424 ) ) ;
#12311=ORIENTED_EDGE ( 'NONE', *, *, #5739, .T. ) ;
#12312=CARTESIAN_POINT ( 'NONE',  ( -0.1360472109712710653, 4.603413381864274179, -0.2814923986826167734 ) ) ;
#12313=CARTESIAN_POINT ( 'NONE',  ( -0.0003030584613339698703, 4.293824744644136437, 0.3119998912175568351 ) ) ;
#12316=CARTESIAN_POINT ( 'NONE',  ( 0.3119999999999999996, 0.4104166666666663188, -0.1292346314604056468 ) ) ;
#12317=CARTESIAN_POINT ( 'NONE',  ( -0.2206173157302028232, 4.988277777777777366, -0.2206173157302028232 ) ) ;
#12318=CARTESIAN_POINT ( 'NONE',  ( -1.726321361862525858E-17, 4.172305555631420582, -0.2819296736111110979 ) ) ;
#12319=CARTESIAN_POINT ( 'NONE',  ( -1.726321361862525858E-17, 3.908416666742532630, -0.2819296736111110979 ) ) ;
#12325=CARTESIAN_POINT ( 'NONE',  ( -0.1993543840281266910, 4.401472222298088433, -0.1993543840281266910 ) ) ;
#12327=CARTESIAN_POINT ( 'NONE',  ( -0.3094355579546126944, 4.501065253622277496, -0.03993151788800097801 ) ) ;
#12330=EDGE_CURVE ( 'NONE', #16668, #6378, #23777, .T. ) ;
#12333=CARTESIAN_POINT ( 'NONE',  ( 0.1993543840281267465, 4.054250000075865223, 0.1993543840281266633 ) ) ;
#12336=CARTESIAN_POINT ( 'NONE',  ( 0.2658661084243346684, 0.03242967361111057795, 0.09380593400082704036 ) ) ;
#12340=CARTESIAN_POINT ( 'NONE',  ( 0.2819296736111110424, 0.6013888888130223265, 0.1167790944451424923 ) ) ;
#12347=CARTESIAN_POINT ( 'NONE',  ( 0.000000000000000000, 5.384999999999999787, -0.3119999999999999996 ) ) ;
#12348=CARTESIAN_POINT ( 'NONE',  ( 0.1167790944451423535, 0.4694444443685777957, 0.2819296736111110424 ) ) ;
#12349=CARTESIAN_POINT ( 'NONE',  ( 0.1167790944451424368, 3.995222222298087988, 0.2819296736111110424 ) ) ;
#12352=CARTESIAN_POINT ( 'NONE',  ( -0.1167790944451423535, 4.599388888964754507, 0.2819296736111110424 ) ) ;
#12353=CARTESIAN_POINT ( 'NONE',  ( 0.1533627255593470462, 5.139211491064951787, -0.2637066568091733787 ) ) ;
#12356=CARTESIAN_POINT ( 'NONE',  ( 0.2206173157302027954, 4.029944444444443441, -0.2206173157302028232 ) ) ;
#12357=CARTESIAN_POINT ( 'NONE',  ( 0.2819296736111110979, 5.213972222298088433, -3.452642723725051716E-17 ) ) ;
#12358=CARTESIAN_POINT ( 'NONE',  ( 0.2650429728237971294, 4.191665852671973447, 0.1646101441917078023 ) ) ;
#12360=CARTESIAN_POINT ( 'NONE',  ( 0.1386474987925107871, 0.03242967361111057795, 0.2459144974368996650 ) ) ;
#12361=CARTESIAN_POINT ( 'NONE',  ( 0.01738314693924293206, 5.206640035683670398, 0.2819296736111598367 ) ) ;
#12362=CARTESIAN_POINT ( 'NONE',  ( -0.1993543840281266910, 4.957027777853642903, -0.1993543840281266910 ) ) ;
#12365=CARTESIAN_POINT ( 'NONE',  ( -0.2934150973083375913, 5.117997740190176614, 0.09815118981130775688 ) ) ;
#12367=ORIENTED_EDGE ( 'NONE', *, *, #7039, .F. ) ;
#12368=CARTESIAN_POINT ( 'NONE',  ( -0.2819296736111110424, 0.4069444443685779067, -0.1167790944451423396 ) ) ;
#12369=DIRECTION ( 'NONE',  ( -0.000000000000000000, -1.000000000000000000, -0.000000000000000000 ) ) ;
#12374=CARTESIAN_POINT ( 'NONE',  ( -0.2301007481662196430, 5.064294881705610152, 0.2107077067205023468 ) ) ;
#12376=CARTESIAN_POINT ( 'NONE',  ( 5.731347020009612645E-17, 3.786888888888888527, 0.3119999999999999996 ) ) ;
#12378=CARTESIAN_POINT ( 'NONE',  ( 0.1167790944451422702, 4.627166666742533074, -0.2819296736111110424 ) ) ;
#12382=CARTESIAN_POINT ( 'NONE',  ( -0.1167790944451423535, 3.752166666742532630, 0.2819296736111110424 ) ) ;
#12383=CARTESIAN_POINT ( 'NONE',  ( -0.1844930076592919965, 0.04690905832487239635, -0.2328264863501848803 ) ) ;
#12384=CARTESIAN_POINT ( 'NONE',  ( 0.03899446768531367874, 5.017119825889835738, 0.3095914530902155737 ) ) ;
#12386=CARTESIAN_POINT ( 'NONE',  ( -0.03821043196831897665, 4.792783218731831774, 0.3097114644149256968 ) ) ;
#12387=CARTESIAN_POINT ( 'NONE',  ( 0.3119999999999999996, 4.193138889040620931, 0.1292346314604056190 ) ) ;
#12388=CARTESIAN_POINT ( 'NONE',  ( 0.1993543840281267465, 4.665361111186976828, 0.1993543840281266633 ) ) ;
#12389=CARTESIAN_POINT ( 'NONE',  ( 5.178964085587577574E-17, 4.033416666742532186, 0.2819296736111110979 ) ) ;
#12392=VERTEX_POINT ( 'NONE', #12602 ) ;
#12398=CARTESIAN_POINT ( 'NONE',  ( -0.3119999999999999996, 0.3687499998482670627, -0.1292346314604056745 ) ) ;
#12399=CARTESIAN_POINT ( 'NONE',  ( -0.04075253542306750409, 4.403731456933130950, 0.3120000054653133126 ) ) ;
#12402=VERTEX_POINT ( 'NONE', #23186 ) ;
#12403=DIRECTION ( 'NONE',  ( 0.000000000000000000, 0.000000000000000000, -1.000000000000000000 ) ) ;
#12404=CARTESIAN_POINT ( 'NONE',  ( 1.726321361862525858E-17, 0.6187499999241333759, -0.2819296736111110979 ) ) ;
#12406=CARTESIAN_POINT ( 'NONE',  ( -0.2819296736111110424, 4.460500000075867000, -0.1167790944451423119 ) ) ;
#12411=CARTESIAN_POINT ( 'NONE',  ( 5.731347020009612645E-17, 4.064666666666665762, 0.3119999999999999996 ) ) ;
#12413=CARTESIAN_POINT ( 'NONE',  ( 0.3119999999999999996, 4.977861111262843252, -0.1292346314604056745 ) ) ;
#12414=CARTESIAN_POINT ( 'NONE',  ( -1.910449006669871087E-17, 4.870222222222222008, -0.3119999999999999996 ) ) ;
#12416=CARTESIAN_POINT ( 'NONE',  ( 0.04357916212451937166, 5.199516353566889570, 0.2819848337134137628 ) ) ;
#12417=CARTESIAN_POINT ( 'NONE',  ( -0.1904734272879128332, 4.883006184772527902, -0.2471112552497352621 ) ) ;
#12420=CARTESIAN_POINT ( 'NONE',  ( -0.1993543840281266910, 5.234805555631421470, -0.1993543840281266910 ) ) ;
#12423=CARTESIAN_POINT ( 'NONE',  ( 0.2494960010015663254, 3.801995302344789440, 0.1917386440423899940 ) ) ;
#12426=CARTESIAN_POINT ( 'NONE',  ( -0.2819296736111111534, 0.1361111110352444808, 0.1167790944451422563 ) ) ;
#12429=CARTESIAN_POINT ( 'NONE',  ( -0.1993543840281266355, 5.207027777853642903, 0.1993543840281267465 ) ) ;
#12432=CARTESIAN_POINT ( 'NONE',  ( -0.2968342663916302970, 4.282823203675612866, 0.1006737699901302241 ) ) ;
#12433=DIRECTION ( 'NONE',  ( -0.000000000000000000, -1.000000000000000000, -0.000000000000000000 ) ) ;
#12434=CARTESIAN_POINT ( 'NONE',  ( -0.2206173157302027954, 0.5388888888888885287, -0.2206173157302028232 ) ) ;
#12435=CARTESIAN_POINT ( 'NONE',  ( -0.1292346314604057023, 4.727861111111110404, 0.3119999999999998885 ) ) ;
#12436=CARTESIAN_POINT ( 'NONE',  ( 5.178964085587577574E-17, 4.200083333409199149, 0.2819296736111110979 ) ) ;
#12443=CARTESIAN_POINT ( 'NONE',  ( -1.726321361862525858E-17, 4.561194444520309865, -0.2819296736111110979 ) ) ;
#12449=CARTESIAN_POINT ( 'NONE',  ( 0.2819296736111110979, 4.116750000075866112, -3.452642723725051716E-17 ) ) ;
#12450=CARTESIAN_POINT ( 'NONE',  ( -0.3061149493775596753, 4.833804916956971454, -0.06113088645964446372 ) ) ;
#12454=CARTESIAN_POINT ( 'NONE',  ( 0.2819296736111110979, 0.6048611110352444253, 0.000000000000000000 ) ) ;
#12456=LINE ( 'NONE', #10263, #19730 ) ;
#12462=CARTESIAN_POINT ( 'NONE',  ( -0.1167790944451424368, 0.4624999999241333759, 0.2819296736111110424 ) ) ;
#12463=CARTESIAN_POINT ( 'NONE',  ( 0.2819296736111110979, 3.835500000075866556, 0.1167790944451422425 ) ) ;
#12466=CARTESIAN_POINT ( 'NONE',  ( 0.2819296736111110424, 4.564666666742532186, -0.1167790944451423396 ) ) ;
#12467=CARTESIAN_POINT ( 'NONE',  ( 0.3045549119083980627, 5.129919930104686721, 0.04183624683181733084 ) ) ;
#12469=CARTESIAN_POINT ( 'NONE',  ( -0.1292346314604069513, 4.616749999999999687, 0.3119999999999986673 ) ) ;
#12473=CARTESIAN_POINT ( 'NONE',  ( 0.2206173157302028787, 4.016055555555555046, 0.2206173157302027954 ) ) ;
#12474=CARTESIAN_POINT ( 'NONE',  ( 5.178964085587577574E-17, 5.200083333409199149, 0.2819296736111110979 ) ) ;
#12475=CARTESIAN_POINT ( 'NONE',  ( 0.2621946814482496446, 4.191512508530529146, 0.1691344502069037914 ) ) ;
#12477=EDGE_CURVE ( 'NONE', #12402, #20545, #7144, .T. ) ;
#12480=CARTESIAN_POINT ( 'NONE',  ( 0.2819296736111110979, 4.884111111186975940, -0.1167790944451423396 ) ) ;
#12483=CARTESIAN_POINT ( 'NONE',  ( -0.3119999999999999996, 0.3131944442927115380, -0.1292346314604056745 ) ) ;
#12484=CARTESIAN_POINT ( 'NONE',  ( -0.3102354826482426331, 4.556271949145164868, -0.05181833945654303747 ) ) ;
#12486=CARTESIAN_POINT ( 'NONE',  ( 1.726321361862525858E-17, 0.2854166665908000056, -0.2819296736111110979 ) ) ;
#12487=ORIENTED_EDGE ( 'NONE', *, *, #20646, .T. ) ;
#12492=CARTESIAN_POINT ( 'NONE',  ( -0.1422641812239349990, 5.047914731991645532, -0.2787100512567418087 ) ) ;
#12493=EDGE_CURVE ( 'NONE', #14703, #13879, #22108, .T. ) ;
#12494=CARTESIAN_POINT ( 'NONE',  ( 0.3119999999999999996, 4.193138888888888083, -0.1292346314604056745 ) ) ;
#12495=AXIS2_PLACEMENT_3D ( 'NONE', #12283, #3001, #8350 ) ;
#12496=CARTESIAN_POINT ( 'NONE',  ( -0.1385637893017130362, 3.881186881039875303, -0.2801137187350042357 ) ) ;
#12497=DIRECTION ( 'NONE',  ( 0.000000000000000000, 0.000000000000000000, -1.000000000000000000 ) ) ;
#12499=CARTESIAN_POINT ( 'NONE',  ( -0.1167790944451423535, 4.710500000075865223, 0.2819296736111110424 ) ) ;
#12500=CARTESIAN_POINT ( 'NONE',  ( -1.910449006669871087E-17, 4.759111111111110404, -0.3119999999999999996 ) ) ;
#12501=CARTESIAN_POINT ( 'NONE',  ( -0.1993543840281266355, 3.859805555631421026, 0.1993543840281267465 ) ) ;
#12502=CARTESIAN_POINT ( 'NONE',  ( -0.2458244892731747677, 0.04853829241537972738, -0.1688004682141546475 ) ) ;
#12503=CARTESIAN_POINT ( 'NONE',  ( 0.2792459877652407330, 5.034052277606470227, -0.1393239653528951794 ) ) ;
#12505=CARTESIAN_POINT ( 'NONE',  ( -0.01780161371572347787, 4.793364628393688598, 0.3116243167563513272 ) ) ;
#12506=CARTESIAN_POINT ( 'NONE',  ( 0.3119999999999999996, 4.366750000151731648, -0.1292346314604056745 ) ) ;
#12507=CARTESIAN_POINT ( 'NONE',  ( 0.2819296736111110979, 4.672305555631421470, -3.452642723725051716E-17 ) ) ;
#12508=CARTESIAN_POINT ( 'NONE',  ( 0.1993543840281267465, 3.873694444520310309, 0.1993543840281266633 ) ) ;
#12509=VERTEX_POINT ( 'NONE', #11364 ) ;
#12510=EDGE_CURVE ( 'NONE', #8566, #4354, #2300, .T. ) ;
#12516=CARTESIAN_POINT ( 'NONE',  ( -0.04088287987717395544, 4.933903511193491909, -0.3119999993762155310 ) ) ;
#12519=CARTESIAN_POINT ( 'NONE',  ( -0.1292346314604056190, 0.2506944442927114824, -0.3119999999999999996 ) ) ;
#12520=CARTESIAN_POINT ( 'NONE',  ( -0.2236462712880645243, 4.384219027667765722, -0.2175689465940933709 ) ) ;
#12521=CARTESIAN_POINT ( 'NONE',  ( 1.145733547534701715E-12, 5.130222168000691418, 0.3067077167097377322 ) ) ;
#12522=CARTESIAN_POINT ( 'NONE',  ( -0.3119999999999999996, 0.2680555555555552139, -3.820898013339742174E-17 ) ) ;
#12526=CARTESIAN_POINT ( 'NONE',  ( 0.1292346314604057300, 0.2229166665149337201, 0.3119999999999998885 ) ) ;
#12527=CARTESIAN_POINT ( 'NONE',  ( 0.2819296736111110979, 0.3722222221463555858, -0.1167790944451422980 ) ) ;
#12529=CARTESIAN_POINT ( 'NONE',  ( -0.1993543840281266910, 4.345916666742532186, -0.1993543840281266910 ) ) ;
#12530=CARTESIAN_POINT ( 'NONE',  ( 0.2206173157302027676, 0.1777777777777774515, 0.2206173157302028787 ) ) ;
#12532=CARTESIAN_POINT ( 'NONE',  ( -0.05138680331271978929, 4.236846235768294555, 0.3078081964070191745 ) ) ;
#12533=CARTESIAN_POINT ( 'NONE',  ( -0.3119999999999999996, 4.102861111111110404, -0.1292346314604056468 ) ) ;
#12535=CARTESIAN_POINT ( 'NONE',  ( 0.3119999999999999996, 4.859805555707287894, 0.1292346314604056190 ) ) ;
#12537=CARTESIAN_POINT ( 'NONE',  ( 0.2530624153226711526, 5.072996518863750026, 0.1824922298374807572 ) ) ;
#12540=CARTESIAN_POINT ( 'NONE',  ( -0.1899746975659765691, 4.882988235955101786, -0.2474948752168808219 ) ) ;
#12542=CARTESIAN_POINT ( 'NONE',  ( -0.1167790944451423257, 5.231333333409198261, -0.2819296736111110424 ) ) ;
#12543=CARTESIAN_POINT ( 'NONE',  ( 5.731347020009612645E-17, 3.953555555555555046, 0.3119999999999999996 ) ) ;
#12544=EDGE_CURVE ( 'NONE', #7025, #19443, #8710, .T. ) ;
#12546=CARTESIAN_POINT ( 'NONE',  ( 0.2819296736111110424, 0.3236111110352444808, 0.1167790944451424923 ) ) ;
#12548=CARTESIAN_POINT ( 'NONE',  ( -1.726321361862525858E-17, 5.130638888964754507, -0.2819296736111110979 ) ) ;
#12549=CARTESIAN_POINT ( 'NONE',  ( 0.3059100320596817579, 4.472671705659782226, 0.06139557928590994029 ) ) ;
#12551=DIRECTION ( 'NONE',  ( -0.000000000000000000, -1.000000000000000000, -0.000000000000000000 ) ) ;
#12554=CARTESIAN_POINT ( 'NONE',  ( 0.1292346314604058410, 4.734805555555555046, 0.3119999999999998885 ) ) ;
#12555=CARTESIAN_POINT ( 'NONE',  ( 0.1772105346487870270, 5.205904791023236555, 0.2204285013117096848 ) ) ;
#12557=CARTESIAN_POINT ( 'NONE',  ( -0.2819296736111110979, 3.904944444520309865, -0.1167790944451422980 ) ) ;
#12558=CARTESIAN_POINT ( 'NONE',  ( -0.1993543840281266355, 3.762583333409198705, 0.1993543840281267465 ) ) ;
#12559=CARTESIAN_POINT ( 'NONE',  ( -0.2206173157302028787, 0.6013888887371559022, 0.2206173157302027954 ) ) ;
#12562=CARTESIAN_POINT ( 'NONE',  ( 0.3119999999999999996, 3.915361111111110848, -0.1292346314604056745 ) ) ;
#12563=CARTESIAN_POINT ( 'NONE',  ( 0.1993543840281267465, 4.484805555631420582, 0.1993543840281266633 ) ) ;
#12564=CARTESIAN_POINT ( 'NONE',  ( -0.05415793351760116864, 4.489840156517192149, -0.3074561344383239803 ) ) ;
#12565=AXIS2_PLACEMENT_3D ( 'NONE', #20097, #13041, #16682 ) ;
#12569=CARTESIAN_POINT ( 'NONE',  ( -0.1167790944451423119, 4.078555555631421470, -0.2819296736111110979 ) ) ;
#12570=DIRECTION ( 'NONE',  ( 1.000000000000000000, 0.000000000000000000, 0.000000000000000000 ) ) ;
#12574=CARTESIAN_POINT ( 'NONE',  ( 0.2819296736111110424, 0.03888888881302225708, -0.1167790944451423119 ) ) ;
#12581=ORIENTED_EDGE ( 'NONE', *, *, #1428, .F. ) ;
#12584=CARTESIAN_POINT ( 'NONE',  ( -0.3119999999999999996, 0.09791666666666633267, -0.1292346314604056745 ) ) ;
#12585=CARTESIAN_POINT ( 'NONE',  ( 0.1015005499617950280, 3.738732058664179903, -0.2819296736111110424 ) ) ;
#12589=CARTESIAN_POINT ( 'NONE',  ( 0.2819296736111110424, 4.453555555631421470, -0.1167790944451423396 ) ) ;
#12592=B_SPLINE_CURVE_WITH_KNOTS ( 'NONE', 3,
 ( #8729, #14351, #16186, #8981, #23354, #16426, #5191, #23712, #4952, #21424, #3371, #1061, #17891, #18249, #8857, #17767, #21782, #5070, #21541, #12417, #12540, #10695, #14111, #6666, #18131, #6544, #3247, #13994, #1429, #16301, #12661, #19833, #1185, #10823, #10583 ),
 .UNSPECIFIED., .F., .F.,
 ( 4, 2, 2, 2, 2, 2, 2, 2, 1, 2, 2, 1, 1, 2, 2, 2, 2, 2, 4 ),
 ( 0.2101647747907265662, 0.2124489175043063061, 0.2147330602178860459, 0.2170172029314657858, 0.2193013456450455256, 0.2215854883586252655, 0.2238696310722050054, 0.2244406667505999264, 0.2245834256701986775, 0.2246191154000983514, 0.2246280378325732907, 0.2246369602650482022, 0.2246548051299980531, 0.2247261845897974286, 0.2250117024289949308, 0.2255827381073899907, 0.2261537737857850228, 0.2272958451425751147, 0.2284379164993652067 ),
 .UNSPECIFIED. ) ;
#12593=VERTEX_POINT ( 'NONE', #12336 ) ;
#12594=CARTESIAN_POINT ( 'NONE',  ( 0.006680993209926284343, 4.376987163322225705, -0.3119999970774108844 ) ) ;
#12595=CARTESIAN_POINT ( 'NONE',  ( -0.3119999999999999996, 3.720916666818399055, -0.1292346314604056468 ) ) ;
#12596=CARTESIAN_POINT ( 'NONE',  ( 0.01571168205836896356, 4.210054417711290853, -0.3116595364661075007 ) ) ;
#12598=CARTESIAN_POINT ( 'NONE',  ( -0.2819296736111110979, 4.852861111186976828, 0.000000000000000000 ) ) ;
#12602=CARTESIAN_POINT ( 'NONE',  ( -4.760580627680044823E-09, 4.932722222506802368, -0.3119999999999999996 ) ) ;
#12605=CARTESIAN_POINT ( 'NONE',  ( -0.2819296736111110979, 0.2993055554796889561, -3.452642723725051716E-17 ) ) ;
#12606=ADVANCED_FACE ( 'NONE', ( #10258 ), #16096, .T. ) ;
#12607=ADVANCED_FACE ( 'NONE', ( #21575 ), #23510, .T. ) ;
#12609=CARTESIAN_POINT ( 'NONE',  ( 0.2819296736111110979, 0.1048611110352444808, 0.000000000000000000 ) ) ;
#12615=CARTESIAN_POINT ( 'NONE',  ( -0.2579334647780821554, 3.885737390849240747, -0.1755419818098827023 ) ) ;
#12617=CARTESIAN_POINT ( 'NONE',  ( -1.726321361862525858E-17, 4.408416666742533074, -0.2819296736111110979 ) ) ;
#12619=CARTESIAN_POINT ( 'NONE',  ( 0.003701402432584371873, 4.543728254411404599, -0.3119811817425749978 ) ) ;
#12621=CARTESIAN_POINT ( 'NONE',  ( -0.1993543840281266910, 5.082027777853643791, -0.1993543840281266910 ) ) ;
#12623=CARTESIAN_POINT ( 'NONE',  ( 0.3119835370037090105, 3.753046293522503074, -0.02992120370447185970 ) ) ;
#12624=CARTESIAN_POINT ( 'NONE',  ( 0.2468659554013261648, 0.05872605207754656720, 0.1866057693320590238 ) ) ;
#12625=ORIENTED_EDGE ( 'NONE', *, *, #4146, .T. ) ;
#12627=CARTESIAN_POINT ( 'NONE',  ( -0.2206173157302028232, 4.273000000151732536, -0.2206173157302028232 ) ) ;
#12629=CARTESIAN_POINT ( 'NONE',  ( 0.2819296736111111534, 4.557722222298087544, 0.1167790944451422563 ) ) ;
#12630=CARTESIAN_POINT ( 'NONE',  ( -0.1167790944451423535, 3.807722222298087988, 0.2819296736111110424 ) ) ;
#12632=ORIENTED_EDGE ( 'NONE', *, *, #10547, .F. ) ;
#12636=DIRECTION ( 'NONE',  ( -0.000000000000000000, -1.000000000000000000, -0.000000000000000000 ) ) ;
#12638=ADVANCED_BREP_SHAPE_REPRESENTATION ( '', ( #1448, #9127 ), #15765 ) ;
#12639=CARTESIAN_POINT ( 'NONE',  ( -0.3119999999999999996, 0.2611111109593781676, -3.820898013339742174E-17 ) ) ;
#12641=CARTESIAN_POINT ( 'NONE',  ( 0.1797085267211815662, 3.721720965436318362, -0.2172307213220433242 ) ) ;
#12642=CARTESIAN_POINT ( 'NONE',  ( -0.01491610195037358991, 3.710900762300672007, -0.3119999571456253951 ) ) ;
#12643=VECTOR ( 'NONE', #14432, 39.37007874015748143 ) ;
#12647=ORIENTED_EDGE ( 'NONE', *, *, #12033, .T. ) ;
#12649=CARTESIAN_POINT ( 'NONE',  ( 0.1425746527767651484, 5.075825272696307344, 0.2781771577023212649 ) ) ;
#12652=CARTESIAN_POINT ( 'NONE',  ( -0.2819296736111110424, 4.134111111186976828, 0.1167790944451424923 ) ) ;
#12653=CARTESIAN_POINT ( 'NONE',  ( -0.2819296736111110424, 5.023000000075866112, 0.1167790944451424923 ) ) ;
#12655=CARTESIAN_POINT ( 'NONE',  ( -0.1099743054185288865, 4.235112341272140313, 0.2928703655857898824 ) ) ;
#12656=CARTESIAN_POINT ( 'NONE',  ( 5.731347020009612645E-17, 4.009111111111109516, 0.3119999999999999996 ) ) ;
#12657=CARTESIAN_POINT ( 'NONE',  ( -0.2206173157302028232, 5.050777777929510215, -0.2206173157302028232 ) ) ;
#12658=CARTESIAN_POINT ( 'NONE',  ( -0.3119999999999999996, 4.158416666666665762, -0.1292346314604056468 ) ) ;
#12659=ORIENTED_EDGE ( 'NONE', *, *, #20051, .T. ) ;
#12661=CARTESIAN_POINT ( 'NONE',  ( -0.05059632256427344654, 4.878606678054476120, -0.3088345630771059946 ) ) ;
#12668=CARTESIAN_POINT ( 'NONE',  ( -0.1167790944451422702, 0.2333333332574666907, -0.2819296736111110979 ) ) ;
#12677=CARTESIAN_POINT ( 'NONE',  ( -0.005017074662756174433, 4.599534034751092015, -0.3119621811286065194 ) ) ;
#12678=CARTESIAN_POINT ( 'NONE',  ( 0.06049446539525574207, 4.875506709053786913, -0.3065030800618469553 ) ) ;
#12679=CARTESIAN_POINT ( 'NONE',  ( 8.375559671162349491E-15, 3.988277777929486678, -0.3119999999999999996 ) ) ;
#12681=CARTESIAN_POINT ( 'NONE',  ( -0.3119999999999998885, 4.776472222222222008, 0.1292346314604058410 ) ) ;
#12682=CARTESIAN_POINT ( 'NONE',  ( -0.1993543840281266910, 4.012583333409198261, -0.1993543840281266910 ) ) ;
#12683=CARTESIAN_POINT ( 'NONE',  ( 0.2819296736111110424, 3.842444444520310309, -0.1167790944451423396 ) ) ;
#12684=CARTESIAN_POINT ( 'NONE',  ( 0.2935269953798502751, 4.032991781582652813, -0.1057786308535565989 ) ) ;
#12689=CARTESIAN_POINT ( 'NONE',  ( -0.2819296736111110979, 4.519527777853643791, 0.000000000000000000 ) ) ;
#12690=CARTESIAN_POINT ( 'NONE',  ( 0.2206173157302027954, 3.807722222222221564, -0.2206173157302028232 ) ) ;
#12694=CARTESIAN_POINT ( 'NONE',  ( -0.1167790944451423119, 3.800777777853643347, -0.2819296736111110979 ) ) ;
#12696=CARTESIAN_POINT ( 'NONE',  ( 0.07873564497862947653, 5.159726166786684054, -0.2898521741972847621 ) ) ;
#12699=B_SPLINE_CURVE_WITH_KNOTS ( 'NONE', 3,
 ( #2024, #7628, #5796, #20677, #3969, #11417, #2146, #17015, #19916, #1852, #23672, #16384, #16736, #7349, #8811, #23913, #12859, #20033, #20155, #16502, #1737, #12615, #21860, #16620, #7466, #7234, #5029, #22098, #1621, #20396, #12979, #14553, #20277, #9055, #3687, #14434, #9296, #12496, #11134, #18441, #10651, #24040, #3563, #3322, #18324, #16260 ),
 .UNSPECIFIED., .F., .F.,
 ( 4, 2, 2, 2, 2, 2, 2, 2, 2, 2, 2, 1, 1, 2, 2, 1, 1, 1, 1, 2, 2, 2, 2, 2, 2, 4 ),
 ( 0.8613901642458987595, 0.8629494678102641592, 0.8645087713746295588, 0.8660680749389949584, 0.8676273785033603581, 0.8691866820677257577, 0.8707459856320911573, 0.8723052891964565569, 0.8738645927608219566, 0.8769831998895527558, 0.8801018070182835551, 0.8804916329093749328, 0.8806865458549205661, 0.8807109099731137425, 0.8807139554878878895, 0.8807170010026620366, 0.8807230920322103307, 0.8807352740913069189, 0.8807840023276931607, 0.8808814588004657553, 0.8816611105826461792, 0.8824407623648266030, 0.8832204141470070269, 0.8840000659291875618, 0.8847797177113679856, 0.8863390212757288333 ),
 .UNSPECIFIED. ) ;
#12702=CARTESIAN_POINT ( 'NONE',  ( -0.1993543840281266633, 0.2229166665908000333, -0.1993543840281266910 ) ) ;
#12703=CARTESIAN_POINT ( 'NONE',  ( 2.034975993999860866E-05, 3.877166120065549837, -0.3120000000214913638 ) ) ;
#12709=ORIENTED_EDGE ( 'NONE', *, *, #3707, .F. ) ;
#12712=CARTESIAN_POINT ( 'NONE',  ( 0.1993543840281266910, 0.5979166665908001166, -0.1993543840281266910 ) ) ;
#12713=CARTESIAN_POINT ( 'NONE',  ( 0.1167790944451422702, 3.793833333409199149, -0.2819296736111110424 ) ) ;
#12716=CARTESIAN_POINT ( 'NONE',  ( -0.1993543840281266910, 4.359805555631421470, -0.1993543840281266910 ) ) ;
#12717=CARTESIAN_POINT ( 'NONE',  ( 0.1292346314604039537, 4.957027777777777366, 0.3120000000000016649 ) ) ;
#12718=CARTESIAN_POINT ( 'NONE',  ( -0.3119999999999999996, 4.606333333333332725, 0.000000000000000000 ) ) ;
#12719=ORIENTED_EDGE ( 'NONE', *, *, #18544, .T. ) ;
#12720=CARTESIAN_POINT ( 'NONE',  ( 0.2246729631343395983, 4.370108299028268917, -0.2176007414103741100 ) ) ;
#12721=CARTESIAN_POINT ( 'NONE',  ( -1.726321361862525858E-17, 5.227861111186975940, -0.2819296736111110979 ) ) ;
#12723=CARTESIAN_POINT ( 'NONE',  ( 0.0009908759922620817475, 4.210471905009121052, -0.3119986526024096096 ) ) ;
#12724=CARTESIAN_POINT ( 'NONE',  ( -0.2206173157302028232, 4.988277777777777366, -0.2206173157302028232 ) ) ;
#12726=CARTESIAN_POINT ( 'NONE',  ( 0.1167790944451424506, 4.814666666742533074, 0.2819296736111110424 ) ) ;
#12728=EDGE_CURVE ( 'NONE', #16124, #3616, #19589, .T. ) ;
#12729=CARTESIAN_POINT ( 'NONE',  ( -0.1794086211558035826, 4.066157371076530858, 0.2554475641543275666 ) ) ;
#12732=CARTESIAN_POINT ( 'NONE',  ( -0.2819296736111110979, 0.3027777777019111660, 0.1167790944451422425 ) ) ;
#12733=CARTESIAN_POINT ( 'NONE',  ( 1.726321361862525858E-17, 0.3409722221463556413, -0.2819296736111110979 ) ) ;
#12734=CARTESIAN_POINT ( 'NONE',  ( -0.09855069764300931900, 4.713304858131104780, -0.2968621023885956167 ) ) ;
#12735=CARTESIAN_POINT ( 'NONE',  ( -0.1985766828738846912, 5.195784807567790153, -0.2074211384348365605 ) ) ;
#12742=CARTESIAN_POINT ( 'NONE',  ( 0.1993543840281266355, 0.08402777770191115214, 0.1993543840281267465 ) ) ;
#12743=CARTESIAN_POINT ( 'NONE',  ( -0.1167790944451423535, 4.599388888964754507, 0.2819296736111110424 ) ) ;
#12745=CARTESIAN_POINT ( 'NONE',  ( 0.3128595373675272517, 4.529777549056624331, 0.005372927980562640198 ) ) ;
#12746=CARTESIAN_POINT ( 'NONE',  ( 0.1167790944451422702, 5.016055555631420582, -0.2819296736111110424 ) ) ;
#12748=CARTESIAN_POINT ( 'NONE',  ( 0.2497132334490027028, 4.924618274614680047, -0.1914511699637774511 ) ) ;
#12749=CARTESIAN_POINT ( 'NONE',  ( 0.02752505417202956439, 0.04140457188012223316, 0.2899247665489211312 ) ) ;
#12752=CARTESIAN_POINT ( 'NONE',  ( -0.3119999999999998885, 4.394527777929509327, 0.1292346314604058410 ) ) ;
#12753=CARTESIAN_POINT ( 'NONE',  ( 0.1167790944451424506, 4.550777777853644679, 0.2819296736111110424 ) ) ;
#12754=CARTESIAN_POINT ( 'NONE',  ( -0.1167790944451423535, 3.918833333409198705, 0.2819296736111110424 ) ) ;
#12755=ORIENTED_EDGE ( 'NONE', *, *, #23237, .F. ) ;
#12756=ORIENTED_EDGE ( 'NONE', *, *, #24094, .F. ) ;
#12759=CARTESIAN_POINT ( 'NONE',  ( -0.1919110571530789344, 4.938596203506701698, -0.2493703182469045598 ) ) ;
#12762=CARTESIAN_POINT ( 'NONE',  ( 0.2206173157302027676, 0.2819444442927114824, 0.2206173157302028787 ) ) ;
#12765=CARTESIAN_POINT ( 'NONE',  ( -0.2041014093529595619, 5.123076492009982275, 0.2308277784739024285 ) ) ;
#12769=ORIENTED_EDGE ( 'NONE', *, *, #16756, .F. ) ;
#12770=CARTESIAN_POINT ( 'NONE',  ( 0.08891876399603607095, 5.074138123154654068, 0.2996821340870129413 ) ) ;
#12772=CARTESIAN_POINT ( 'NONE',  ( 0.2819296736111110979, 4.321611111186976828, 0.1167790944451422425 ) ) ;
#12773=CARTESIAN_POINT ( 'NONE',  ( -0.1167790944451423119, 5.064666666742532186, -0.2819296736111110979 ) ) ;
#12776=CARTESIAN_POINT ( 'NONE',  ( 0.1292346314604056190, 3.977861111111111292, -0.3119999999999999996 ) ) ;
#12777=CARTESIAN_POINT ( 'NONE',  ( -0.3119999999999999996, 4.998694444596177178, -0.1292346314604056468 ) ) ;
#12778=CARTESIAN_POINT ( 'NONE',  ( 0.1167790944451422702, 5.071611111186976828, -0.2819296736111110979 ) ) ;
#12779=EDGE_CURVE ( 'NONE', #7806, #17266, #21802, .T. ) ;
#12780=AXIS2_PLACEMENT_3D ( 'NONE', #7531, #17038, #9365 ) ;
#12783=( BOUNDED_SURFACE ( )  B_SPLINE_SURFACE ( 1, 2, ( 
 ( #6660, #19583, #21660, #2532, #4822, #2876, #10099, #21302, #13755, #4595, #13990, #11805, #6302, #2650, #4708, #6539, #13873, #9978, #19226, #17405, #23471, #19466, #21180, #17762, #12176, #10335, #19352, #1056, #8484, #8616, #698, #11934, #15926, #19706, #3008, #10459, #17885, #16056, #15575, #22999, #17521, #816, #15696, #3126, #21897, #10579, #9091, #5187, #5314, #14842, #12657, #23831, #23960, #5064, #8852, #16178, #12901, #18125, #7389, #16298, #20075, #1424, #16659, #3601, #18244, #12777, #16423, #19954, #23591, #7032, #21778, #12413, #14474, #23710, #3364, #10817, #7153, #14594, #10691, #22016, #18363, #1542, #20197, #10935, #7273, #3484, #20317, #14721, #18007, #1656, #4948, #8974, #1775, #19831, #16541, #11053, #18482, #9221, #24082, #22136, #5436, #1300, #8724, #6907, #14346, #12535, #3243, #22497, #16776, #2387, #9340, #2265, #5676, #14955, #9700, #542, #17011, #22258, #15188, #9578, #20909, #13257, #16891, #5911, #18844, #13495, #7507, #19080, #5554, #4203, #11536, #3730, #1898, #304, #3966, #20789, #7745, #11657, #4080, #17258, #9824, #15075, #2021, #7624, #11177, #18605, #17139, #7978, #11410, #63, #11294, #22625, #13368, #9459, #18968, #184, #13019, #2141, #20673, #5793, #426, #20434, #22375, #13141, #20554, #22738, #7860, #15309, #18723, #6026, #3850, #21027, #23082, #19437, #15785, #4681, #4796, #19677, #13727, #19324, #12151, #2622, #21149, #6391, #10188, #13962, #10065, #8456, #17490, #19557, #21392, #23321, #2848, #15429, #4319, #10434, #15899, #22856, #23203, #10307, #15546, #784, #17731, #1025, #8214, #21272, #6629, #2737, #4437, #13843, #14077, #21506, #12262, #2980, #15663, #9944, #17858, #4564, #12023, #22968, #902, #6514, #1150, #6145, #17374, #17612, #8334, #13612, #11774, #19194, #2504, #664, #8093, #6269, #11904, #14446, #6752, #1393, #14197, #12752, #8824, #8947, #18453, #16270, #3333, #3455, #8697, #12506, #19803, #16512, #21753, #11027, #19927, #23682, #5039, #20289, #7246, #21870, #16395, #20044, #23564, #3100, #10660, #1271, #16025, #18092, #3214, #7003, #5161, #10790, #18217, #14320, #1512, #21989, #12627, #23803, #14564, #10907, #20168, #16149, #7124, #5284, #18336, #1631, #9065, #3574, #6878, #8588, #23926, #14692, #22110, #23441, #5405, #10546, #12872, #21631, #4923, #12387, #17980, #9550, #16749, #16868, #13229, #22596, #5769, #5880, #20642, #13340, #155, #24051, #18693, #11629, #11146, #15281, #7597, #16633, #9430, #31, #20526, #7478, #12992, #20762, #16985, #1748, #7361, #4053, #277, #14926, #11266, #3699, #1993, #3941, #4175, #20406, #22345, #11383, #22472, #3823, #14812, #20881, #9190, #2240, #7716, #15163, #11507, #17109, #18943, #22228, #9672, #5528, #13112, #22709, #18576, #15049, #399, #7835, #5999, #1867, #18812, #2109, #5647, #9307, #13465, #8069, #19292, #15521, #2597, #13589, #23292, #6121, #23177, #2480, #11751, #6487, #21483, #13815, #19056, #12000, #6367, #17705, #10043, #13706, #2711, #15642, #10283, #4295, #15875, #2360, #999, #8310, #514, #22831, #21249, #757, #17587, #4538, #8429, #879, #14053, #6605, #11877, #22943, #4415, #7948, #15402, #13938, #4768, #8188, #21001, #6243, #19412, #10164, #21124, #15761, #17466, #9800, #23059, #21368, #4654, #12125, #17232, #19174, #9915, #17346, #19532, #2826, #640, #8668, #10757, #21727, #17832, #19894, #16242, #12595, #1483, #1605, #16484, #10517, #16119 ),
 ( #8920, #12239, #1121, #7211, #12721, #19651, #20015, #16362, #12357, #5011, #18187, #23773, #12474, #18061, #7096, #23654, #17950, #3185, #21840, #3302, #9039, #14657, #14169, #1361, #5128, #14534, #10634, #20137, #21956, #23893, #8790, #5250, #21600, #6972, #10407, #14414, #8555, #3427, #10877, #18306, #22078, #2949, #15998, #23416, #19776, #23532, #6727, #4894, #1243, #3072, #6849, #14290, #1833, #17074, #4027, #18662, #13199, #16840, #20376, #24021, #7449, #22198, #12840, #14896, #16719, #3790, #11236, #125, #15018, #11114, #7568, #18782, #22316, #20613, #11355, #250, #16952, #5498, #1957, #20495, #22440, #5740, #3910, #366, #12962, #7808, #20730, #22562, #9401, #20259, #2210, #7332, #4125, #15249, #7685, #9156, #2079, #9518, #3666, #15136, #5853, #13314, #11475, #18908, #9641, #5374, #3546, #10997, #5614, #18425, #14783, #1718, #16601, #18543, #13078, #9278, #17316, #13560, #9764, #10132, #6332, #8393, #13432, #17556, #13787, #20971, #8041, #486, #15490, #730, #963, #17201, #4268, #8158, #19260, #609, #20853, #17676, #5969, #10248, #9888, #7919, #4505, #13678, #22919, #6091, #850, #19499, #6213, #21214, #15371, #4384, #4145, #21092, #11599, #2682, #11842, #23031, #22679, #2564, #17435, #8278, #22798, #2447, #11717, #6454, #19141, #19031, #10012, #15611, #11970, #2327, #21335, #19384, #15729, #23143, #13907, #4624, #12089, #2794, #23263, #1211, #3039, #14258, #21692, #10604, #1330, #21566, #3154, #5095, #17917, #23624, #21807, #10724, #3271, #8520, #12443, #6815, #18033, #16211, #8756, #10847, #15960, #18277, #7064, #8886, #4974, #6573, #12689, #10370, #10486, #3397, #18156, #19618, #6938, #14377, #6691, #19858, #12563, #19983, #1452, #16329, #23739, #14502, #21924, #14023, #8641, #1572, #1088, #5215, #20107, #21454, #23500, #14136, #16088, #4859, #2913, #15844, #4737, #12209, #17795, #23383, #12325, #19740, #18847, #10970, #2145, #11540, #11777, #3519, #186, #18971, #5914, #3968, #23863, #4323, #16451, #21030, #20676, #18394, #15313, #308, #11415, #16894, #2268, #9703, #22859, #19198, #1690, #15191, #17142, #11660, #7748, #9827, #22629, #9582, #430, #13373, #545, #9124, #6149, #9008, #7980, #22742, #14627, #12810, #20794, #4083, #7863, #6031, #15433, #13498, #7185, #13615, #17014, #13260, #20913, #22050, #5346, #4206, #20230, #19083, #7627, #22498, #2391, #17262, #15078, #5795, #13846, #4926, #6517, #17615, #21276, #4800, #16029, #21634, #22971, #17861, #2983, #907, #6633, #23086, #1029, #12027, #8096, #10192, #13965, #2852, #15902, #23445, #6756, #788, #6394, #23324, #4567, #8217, #8336, #21396, #8459, #19440, #19680, #2740, #14081, #21509, #10437, #12265, #2507, #15550, #12389, #1153, #9947, #10312, #8591, #2625, #15788, #14202, #17377, #23205, #4684, #669, #12154, #15667, #19561, #6273, #13730, #21153, #17734, #4440, #11907, #19327, #10069, #17493, #7005, #16635, #10550, #8949, #18456, #1751, #3576, #14814, #20046, #12754, #1395, #17983, #14448, #8826, #3336, #16272, #10792, #14322, #24053, #6882, #23932, #3217, #12508, #7248, #22233, #14568, #19806, #20170, #7126, #9193, #5286, #22112, #18220, #20291, #14694, #7363, #5164, #18338, #5041, #1516, #1274, #12630, #8702, #5407, #16397, #3458, #5530, #23805, #21991, #12874, #19931, #23684, #21755, #11029, #21872, #3103, #10909, #1633, #9067, #16152, #23567, #16515, #10663, #18096, #3825, #7481, #15050 ) ),
 .UNSPECIFIED., .F., .F., .T. ) 
 B_SPLINE_SURFACE_WITH_KNOTS ( ( 2, 2 ),
 ( 3, 2, 2, 2, 2, 2, 2, 2, 2, 2, 2, 2, 2, 2, 2, 2, 2, 2, 2, 2, 2, 2, 2, 2, 2, 2, 2, 2, 2, 2, 2, 2, 2, 2, 2, 2, 2, 2, 2, 2, 2, 2, 2, 2, 2, 2, 2, 2, 2, 2, 2, 2, 2, 2, 2, 2, 2, 2, 2, 2, 2, 2, 2, 2, 2, 2, 2, 2, 2, 2, 2, 2, 2, 2, 2, 2, 2, 2, 2, 2, 2, 2, 2, 2, 2, 2, 2, 2, 2, 2, 2, 2, 2, 2, 2, 2, 2, 2, 2, 2, 2, 2, 2, 2, 2, 2, 2, 2, 2, 2, 2, 2, 2, 2, 2, 2, 2, 2, 2, 2, 2, 2, 2, 2, 2, 2, 2, 2, 2, 2, 2, 2, 2, 2, 2, 2, 2, 2, 2, 2, 2, 2, 2, 2, 2, 2, 2, 2, 2, 2, 2, 2, 2, 2, 2, 2, 2, 2, 2, 2, 2, 2, 2, 2, 2, 2, 2, 2, 2, 2, 2, 2, 2, 2, 2, 2, 2, 2, 2, 2, 2, 2, 2, 2, 2, 2, 2, 2, 2, 2, 2, 2, 2, 2, 2, 2, 2, 2, 2, 2, 2, 2, 2, 2, 2, 2, 2, 2, 2, 2, 2, 2, 2, 2, 2, 2, 2, 2, 2, 3 ),
 ( 0.000000000000000000, 1.000000000000000000 ),
 ( 0.000000000000000000, 0.004464285714285714038, 0.008928571428571428076, 0.01339285714285714211, 0.01785714285714285615, 0.02232142857142857192, 0.02678571428571428423, 0.03125000000000000000, 0.03571428571428571230, 0.04017857142857143155, 0.04464285714285714385, 0.04910714285714285615, 0.05357142857142856845, 0.05803571428571428770, 0.06250000000000000000, 0.06696428571428571230, 0.07142857142857142461, 0.07589285714285713691, 0.08035714285714286309, 0.08482142857142857539, 0.08928571428571428770, 0.09375000000000000000, 0.09821428571428571230, 0.1026785714285714246, 0.1071428571428571369, 0.1116071428571428631, 0.1160714285714285754, 0.1205357142857142877, 0.1250000000000000000, 0.1294642857142857262, 0.1339285714285714246, 0.1383928571428571508, 0.1428571428571428492, 0.1473214285714285754, 0.1517857142857142738, 0.1562500000000000000, 0.1607142857142857262, 0.1651785714285714246, 0.1696428571428571508, 0.1741071428571428492, 0.1785714285714285754, 0.1830357142857142738, 0.1875000000000000000, 0.1919642857142857262, 0.1964285714285714246, 0.2008928571428571508, 0.2053571428571428492, 0.2098214285714285754, 0.2142857142857142738, 0.2187500000000000000, 0.2232142857142857262, 0.2276785714285714246, 0.2321428571428571508, 0.2366071428571428492, 0.2410714285714285754, 0.2455357142857142738, 0.2500000000000000000, 0.2544642857142856984, 0.2589285714285714524, 0.2633928571428571508, 0.2678571428571428492, 0.2723214285714285476, 0.2767857142857143016, 0.2812500000000000000, 0.2857142857142856984, 0.2901785714285714524, 0.2946428571428571508, 0.2991071428571428492, 0.3035714285714285476, 0.3080357142857143016, 0.3125000000000000000, 0.3169642857142856984, 0.3214285714285714524, 0.3258928571428571508, 0.3303571428571428492, 0.3348214285714285476, 0.3392857142857143016, 0.3437500000000000000, 0.3482142857142856984, 0.3526785714285714524, 0.3571428571428571508, 0.3616071428571428492, 0.3660714285714285476, 0.3705357142857143016, 0.3750000000000000000, 0.3794642857142856984, 0.3839285714285714524, 0.3883928571428571508, 0.3928571428571428492, 0.3973214285714285476, 0.4017857142857143016, 0.4062500000000000000, 0.4107142857142856984, 0.4151785714285714524, 0.4196428571428571508, 0.4241071428571428492, 0.4285714285714285476, 0.4330357142857143016, 0.4375000000000000000, 0.4419642857142856984, 0.4464285714285714524, 0.4508928571428571508, 0.4553571428571428492, 0.4598214285714285476, 0.4642857142857143016, 0.4687500000000000000, 0.4732142857142856984, 0.4776785714285714524, 0.4821428571428571508, 0.4866071428571428492, 0.4910714285714285476, 0.4955357142857143016, 0.5000000000000000000, 0.5044642857142856984, 0.5089285714285713969, 0.5133928571428570953, 0.5178571428571429047, 0.5223214285714286031, 0.5267857142857143016, 0.5312500000000000000, 0.5357142857142856984, 0.5401785714285713969, 0.5446428571428570953, 0.5491071428571429047, 0.5535714285714286031, 0.5580357142857143016, 0.5625000000000000000, 0.5669642857142856984, 0.5714285714285713969, 0.5758928571428570953, 0.5803571428571429047, 0.5848214285714286031, 0.5892857142857143016, 0.5937500000000000000, 0.5982142857142856984, 0.6026785714285713969, 0.6071428571428570953, 0.6116071428571429047, 0.6160714285714286031, 0.6205357142857143016, 0.6250000000000000000, 0.6294642857142856984, 0.6339285714285713969, 0.6383928571428570953, 0.6428571428571429047, 0.6473214285714286031, 0.6517857142857143016, 0.6562500000000000000, 0.6607142857142856984, 0.6651785714285713969, 0.6696428571428570953, 0.6741071428571429047, 0.6785714285714286031, 0.6830357142857143016, 0.6875000000000000000, 0.6919642857142856984, 0.6964285714285713969, 0.7008928571428570953, 0.7053571428571429047, 0.7098214285714286031, 0.7142857142857143016, 0.7187500000000000000, 0.7232142857142856984, 0.7276785714285713969, 0.7321428571428570953, 0.7366071428571429047, 0.7410714285714286031, 0.7455357142857143016, 0.7500000000000000000, 0.7544642857142856984, 0.7589285714285713969, 0.7633928571428570953, 0.7678571428571429047, 0.7723214285714286031, 0.7767857142857143016, 0.7812500000000000000, 0.7857142857142856984, 0.7901785714285713969, 0.7946428571428570953, 0.7991071428571429047, 0.8035714285714286031, 0.8080357142857143016, 0.8125000000000000000, 0.8169642857142856984, 0.8214285714285713969, 0.8258928571428570953, 0.8303571428571429047, 0.8348214285714286031, 0.8392857142857143016, 0.8437500000000000000, 0.8482142857142856984, 0.8526785714285713969, 0.8571428571428570953, 0.8616071428571429047, 0.8660714285714286031, 0.8705357142857143016, 0.8750000000000000000, 0.8794642857142856984, 0.8839285714285713969, 0.8883928571428570953, 0.8928571428571429047, 0.8973214285714286031, 0.9017857142857143016, 0.9062500000000000000, 0.9107142857142856984, 0.9151785714285713969, 0.9196428571428570953, 0.9241071428571429047, 0.9285714285714286031, 0.9330357142857143016, 0.9375000000000000000, 0.9419642857142856984, 0.9464285714285713969, 0.9508928571428570953, 0.9553571428571429047, 0.9598214285714286031, 0.9642857142857143016, 0.9687500000000000000, 0.9732142857142856984, 0.9771335305660339143 ),
 .UNSPECIFIED. ) 
 GEOMETRIC_REPRESENTATION_ITEM ( )  RATIONAL_B_SPLINE_SURFACE ( (
 ( 1.000000000000000000, 0.9238795325112867385, 1.000000000000000000, 0.9238795325112867385, 1.000000000000000000, 0.9238795325112867385, 1.000000000000000000, 0.9238795325112867385, 1.000000000000000000, 0.9238795325112867385, 1.000000000000000000, 0.9238795325112867385, 1.000000000000000000, 0.9238795325112867385, 1.000000000000000000, 0.9238795325112867385, 1.000000000000000000, 0.9238795325112867385, 1.000000000000000000, 0.9238795325112867385, 1.000000000000000000, 0.9238795325112867385, 1.000000000000000000, 0.9238795325112867385, 1.000000000000000000, 0.9238795325112867385, 1.000000000000000000, 0.9238795325112867385, 1.000000000000000000, 0.9238795325112867385, 1.000000000000000000, 0.9238795325112867385, 1.000000000000000000, 0.9238795325112867385, 1.000000000000000000, 0.9238795325112867385, 1.000000000000000000, 0.9238795325112867385, 1.000000000000000000, 0.9238795325112867385, 1.000000000000000000, 0.9238795325112867385, 1.000000000000000000, 0.9238795325112867385, 1.000000000000000000, 0.9238795325112867385, 1.000000000000000000, 0.9238795325112867385, 1.000000000000000000, 0.9238795325112867385, 1.000000000000000000, 0.9238795325112867385, 1.000000000000000000, 0.9238795325112867385, 1.000000000000000000, 0.9238795325112867385, 1.000000000000000000, 0.9238795325112867385, 1.000000000000000000, 0.9238795325112867385, 1.000000000000000000, 0.9238795325112867385, 1.000000000000000000, 0.9238795325112867385, 1.000000000000000000, 0.9238795325112867385, 1.000000000000000000, 0.9238795325112867385, 1.000000000000000000, 0.9238795325112867385, 1.000000000000000000, 0.9238795325112867385, 1.000000000000000000, 0.9238795325112867385, 1.000000000000000000, 0.9238795325112867385, 1.000000000000000000, 0.9238795325112867385, 1.000000000000000000, 0.9238795325112867385, 1.000000000000000000, 0.9238795325112867385, 1.000000000000000000, 0.9238795325112867385, 1.000000000000000000, 0.9238795325112867385, 1.000000000000000000, 0.9238795325112867385, 1.000000000000000000, 0.9238795325112867385, 1.000000000000000000, 0.9238795325112867385, 1.000000000000000000, 0.9238795325112867385, 1.000000000000000000, 0.9238795325112867385, 1.000000000000000000, 0.9238795325112867385, 1.000000000000000000, 0.9238795325112867385, 1.000000000000000000, 0.9238795325112867385, 1.000000000000000000, 0.9238795325112867385, 1.000000000000000000, 0.9238795325112867385, 1.000000000000000000, 0.9238795325112867385, 1.000000000000000000, 0.9238795325112867385, 1.000000000000000000, 0.9238795325112867385, 1.000000000000000000, 0.9238795325112867385, 1.000000000000000000, 0.9238795325112867385, 1.000000000000000000, 0.9238795325112867385, 1.000000000000000000, 0.9238795325112867385, 1.000000000000000000, 0.9238795325112867385, 1.000000000000000000, 0.9238795325112867385, 1.000000000000000000, 0.9238795325112867385, 1.000000000000000000, 0.9238795325112867385, 1.000000000000000000, 0.9238795325112867385, 1.000000000000000000, 0.9238795325112867385, 1.000000000000000000, 0.9238795325112867385, 1.000000000000000000, 0.9238795325112867385, 1.000000000000000000, 0.9238795325112867385, 1.000000000000000000, 0.9238795325112867385, 1.000000000000000000, 0.9238795325112867385, 1.000000000000000000, 0.9238795325112867385, 1.000000000000000000, 0.9238795325112867385, 1.000000000000000000, 0.9238795325112867385, 1.000000000000000000, 0.9238795325112867385, 1.000000000000000000, 0.9238795325112867385, 1.000000000000000000, 0.9238795325112867385, 1.000000000000000000, 0.9238795325112867385, 1.000000000000000000, 0.9238795325112867385, 1.000000000000000000, 0.9238795325112867385, 1.000000000000000000, 0.9238795325112867385, 1.000000000000000000, 0.9238795325112867385, 1.000000000000000000, 0.9238795325112867385, 1.000000000000000000, 0.9238795325112867385, 1.000000000000000000, 0.9238795325112867385, 1.000000000000000000, 0.9238795325112867385, 1.000000000000000000, 0.9238795325112867385, 1.000000000000000000, 0.9238795325112867385, 1.000000000000000000, 0.9238795325112867385, 1.000000000000000000, 0.9238795325112867385, 1.000000000000000000, 0.9238795325112867385, 1.000000000000000000, 0.9238795325112867385, 1.000000000000000000, 0.9238795325112867385, 1.000000000000000000, 0.9238795325112867385, 1.000000000000000000, 0.9238795325112867385, 1.000000000000000000, 0.9238795325112867385, 1.000000000000000000, 0.9238795325112867385, 1.000000000000000000, 0.9238795325112867385, 1.000000000000000000, 0.9238795325112867385, 1.000000000000000000, 0.9238795325112867385, 1.000000000000000000, 0.9238795325112867385, 1.000000000000000000, 0.9238795325112867385, 1.000000000000000000, 0.9238795325112867385, 1.000000000000000000, 0.9238795325112867385, 1.000000000000000000, 0.9238795325112867385, 1.000000000000000000, 0.9238795325112867385, 1.000000000000000000, 0.9238795325112867385, 1.000000000000000000, 0.9238795325112867385, 1.000000000000000000, 0.9238795325112867385, 1.000000000000000000, 0.9238795325112867385, 1.000000000000000000, 0.9238795325112867385, 1.000000000000000000, 0.9238795325112867385, 1.000000000000000000, 0.9238795325112867385, 1.000000000000000000, 0.9238795325112867385, 1.000000000000000000, 0.9238795325112867385, 1.000000000000000000, 0.9238795325112867385, 1.000000000000000000, 0.9238795325112867385, 1.000000000000000000, 0.9238795325112867385, 1.000000000000000000, 0.9238795325112867385, 1.000000000000000000, 0.9238795325112867385, 1.000000000000000000, 0.9238795325112867385, 1.000000000000000000, 0.9238795325112867385, 1.000000000000000000, 0.9238795325112867385, 1.000000000000000000, 0.9238795325112867385, 1.000000000000000000, 0.9238795325112867385, 1.000000000000000000, 0.9238795325112867385, 1.000000000000000000, 0.9238795325112867385, 1.000000000000000000, 0.9238795325112867385, 1.000000000000000000, 0.9238795325112867385, 1.000000000000000000, 0.9238795325112867385, 1.000000000000000000, 0.9238795325112867385, 1.000000000000000000, 0.9238795325112867385, 1.000000000000000000, 0.9238795325112867385, 1.000000000000000000, 0.9238795325112867385, 1.000000000000000000, 0.9238795325112867385, 1.000000000000000000, 0.9238795325112867385, 1.000000000000000000, 0.9238795325112867385, 1.000000000000000000, 0.9238795325112867385, 1.000000000000000000, 0.9238795325112867385, 1.000000000000000000, 0.9238795325112867385, 1.000000000000000000, 0.9238795325112867385, 1.000000000000000000, 0.9238795325112867385, 1.000000000000000000, 0.9238795325112867385, 1.000000000000000000, 0.9238795325112867385, 1.000000000000000000, 0.9238795325112867385, 1.000000000000000000, 0.9238795325112867385, 1.000000000000000000, 0.9238795325112867385, 1.000000000000000000, 0.9238795325112867385, 1.000000000000000000, 0.9238795325112867385, 1.000000000000000000, 0.9238795325112867385, 1.000000000000000000, 0.9238795325112867385, 1.000000000000000000, 0.9238795325112867385, 1.000000000000000000, 0.9238795325112867385, 1.000000000000000000, 0.9238795325112867385, 1.000000000000000000, 0.9238795325112867385, 1.000000000000000000, 0.9238795325112867385, 1.000000000000000000, 0.9238795325112867385, 1.000000000000000000, 0.9238795325112867385, 1.000000000000000000, 0.9238795325112867385, 1.000000000000000000, 0.9238795325112867385, 1.000000000000000000, 0.9238795325112867385, 1.000000000000000000, 0.9238795325112867385, 1.000000000000000000, 0.9238795325112867385, 1.000000000000000000, 0.9238795325112867385, 1.000000000000000000, 0.9238795325112867385, 1.000000000000000000, 0.9238795325112867385, 1.000000000000000000, 0.9238795325112867385, 1.000000000000000000, 0.9238795325112867385, 1.000000000000000000, 0.9238795325112867385, 1.000000000000000000, 0.9238795325112867385, 1.000000000000000000, 0.9238795325112867385, 1.000000000000000000, 0.9238795325112867385, 1.000000000000000000, 0.9238795325112867385, 1.000000000000000000, 0.9238795325112867385, 1.000000000000000000, 0.9238795325112867385, 1.000000000000000000, 0.9238795325112867385, 1.000000000000000000, 0.9238795325112867385, 1.000000000000000000, 0.9238795325112867385, 1.000000000000000000, 0.9238795325112867385, 1.000000000000000000, 0.9238795325112867385, 1.000000000000000000, 0.9238795325112867385, 1.000000000000000000, 0.9238795325112867385, 1.000000000000000000, 0.9238795325112867385, 1.000000000000000000, 0.9238795325112867385, 1.000000000000000000, 0.9238795325112867385, 1.000000000000000000, 0.9238795325112867385, 1.000000000000000000, 0.9238795325112867385, 1.000000000000000000, 0.9238795325112867385, 1.000000000000000000, 0.9238795325112867385, 1.000000000000000000, 0.9238795325112867385, 1.000000000000000000, 0.9238795325112867385, 1.000000000000000000, 0.9238795325112867385, 1.000000000000000000, 0.9238795325112867385, 1.000000000000000000, 0.9238795325112867385, 1.000000000000000000, 0.9238795325112867385, 1.000000000000000000, 0.9238795325112867385, 1.000000000000000000, 0.9238795325112867385, 1.000000000000000000, 0.9238795325112867385, 1.000000000000000000, 0.9238795325112867385, 1.000000000000000000, 0.9238795325112867385, 1.000000000000000000, 0.9238795325112867385, 1.000000000000000000, 0.9238795325112867385, 1.000000000000000000, 0.9238795325112867385, 1.000000000000000000, 0.9238795325112867385, 1.000000000000000000, 0.9238795325112867385, 1.000000000000000000, 0.9238795325112867385, 1.000000000000000000, 0.9238795325112867385, 1.000000000000000000, 0.9238795325112867385, 1.000000000000000000, 0.9238795325112867385, 1.000000000000000000, 0.9238795325112867385, 1.000000000000000000, 0.9238795325112867385, 1.000000000000000000, 0.9238795325112867385, 1.000000000000000000, 0.9238795325112867385, 1.000000000000000000, 0.9238795325112867385, 1.000000000000000000, 0.9238795325112867385, 1.000000000000000000, 0.9238795325112867385, 1.000000000000000000, 0.9238795325112867385, 1.000000000000000000, 0.9238795325112867385, 1.000000000000000000, 0.9331730159288109672, 0.9836823002065551158),
 ( 1.000000000000000000, 0.9238795325112867385, 1.000000000000000000, 0.9238795325112867385, 1.000000000000000000, 0.9238795325112867385, 1.000000000000000000, 0.9238795325112867385, 1.000000000000000000, 0.9238795325112867385, 1.000000000000000000, 0.9238795325112867385, 1.000000000000000000, 0.9238795325112867385, 1.000000000000000000, 0.9238795325112867385, 1.000000000000000000, 0.9238795325112867385, 1.000000000000000000, 0.9238795325112867385, 1.000000000000000000, 0.9238795325112867385, 1.000000000000000000, 0.9238795325112867385, 1.000000000000000000, 0.9238795325112867385, 1.000000000000000000, 0.9238795325112867385, 1.000000000000000000, 0.9238795325112867385, 1.000000000000000000, 0.9238795325112867385, 1.000000000000000000, 0.9238795325112867385, 1.000000000000000000, 0.9238795325112867385, 1.000000000000000000, 0.9238795325112867385, 1.000000000000000000, 0.9238795325112867385, 1.000000000000000000, 0.9238795325112867385, 1.000000000000000000, 0.9238795325112867385, 1.000000000000000000, 0.9238795325112867385, 1.000000000000000000, 0.9238795325112867385, 1.000000000000000000, 0.9238795325112867385, 1.000000000000000000, 0.9238795325112867385, 1.000000000000000000, 0.9238795325112867385, 1.000000000000000000, 0.9238795325112867385, 1.000000000000000000, 0.9238795325112867385, 1.000000000000000000, 0.9238795325112867385, 1.000000000000000000, 0.9238795325112867385, 1.000000000000000000, 0.9238795325112867385, 1.000000000000000000, 0.9238795325112867385, 1.000000000000000000, 0.9238795325112867385, 1.000000000000000000, 0.9238795325112867385, 1.000000000000000000, 0.9238795325112867385, 1.000000000000000000, 0.9238795325112867385, 1.000000000000000000, 0.9238795325112867385, 1.000000000000000000, 0.9238795325112867385, 1.000000000000000000, 0.9238795325112867385, 1.000000000000000000, 0.9238795325112867385, 1.000000000000000000, 0.9238795325112867385, 1.000000000000000000, 0.9238795325112867385, 1.000000000000000000, 0.9238795325112867385, 1.000000000000000000, 0.9238795325112867385, 1.000000000000000000, 0.9238795325112867385, 1.000000000000000000, 0.9238795325112867385, 1.000000000000000000, 0.9238795325112867385, 1.000000000000000000, 0.9238795325112867385, 1.000000000000000000, 0.9238795325112867385, 1.000000000000000000, 0.9238795325112867385, 1.000000000000000000, 0.9238795325112867385, 1.000000000000000000, 0.9238795325112867385, 1.000000000000000000, 0.9238795325112867385, 1.000000000000000000, 0.9238795325112867385, 1.000000000000000000, 0.9238795325112867385, 1.000000000000000000, 0.9238795325112867385, 1.000000000000000000, 0.9238795325112867385, 1.000000000000000000, 0.9238795325112867385, 1.000000000000000000, 0.9238795325112867385, 1.000000000000000000, 0.9238795325112867385, 1.000000000000000000, 0.9238795325112867385, 1.000000000000000000, 0.9238795325112867385, 1.000000000000000000, 0.9238795325112867385, 1.000000000000000000, 0.9238795325112867385, 1.000000000000000000, 0.9238795325112867385, 1.000000000000000000, 0.9238795325112867385, 1.000000000000000000, 0.9238795325112867385, 1.000000000000000000, 0.9238795325112867385, 1.000000000000000000, 0.9238795325112867385, 1.000000000000000000, 0.9238795325112867385, 1.000000000000000000, 0.9238795325112867385, 1.000000000000000000, 0.9238795325112867385, 1.000000000000000000, 0.9238795325112867385, 1.000000000000000000, 0.9238795325112867385, 1.000000000000000000, 0.9238795325112867385, 1.000000000000000000, 0.9238795325112867385, 1.000000000000000000, 0.9238795325112867385, 1.000000000000000000, 0.9238795325112867385, 1.000000000000000000, 0.9238795325112867385, 1.000000000000000000, 0.9238795325112867385, 1.000000000000000000, 0.9238795325112867385, 1.000000000000000000, 0.9238795325112867385, 1.000000000000000000, 0.9238795325112867385, 1.000000000000000000, 0.9238795325112867385, 1.000000000000000000, 0.9238795325112867385, 1.000000000000000000, 0.9238795325112867385, 1.000000000000000000, 0.9238795325112867385, 1.000000000000000000, 0.9238795325112867385, 1.000000000000000000, 0.9238795325112867385, 1.000000000000000000, 0.9238795325112867385, 1.000000000000000000, 0.9238795325112867385, 1.000000000000000000, 0.9238795325112867385, 1.000000000000000000, 0.9238795325112867385, 1.000000000000000000, 0.9238795325112867385, 1.000000000000000000, 0.9238795325112867385, 1.000000000000000000, 0.9238795325112867385, 1.000000000000000000, 0.9238795325112867385, 1.000000000000000000, 0.9238795325112867385, 1.000000000000000000, 0.9238795325112867385, 1.000000000000000000, 0.9238795325112867385, 1.000000000000000000, 0.9238795325112867385, 1.000000000000000000, 0.9238795325112867385, 1.000000000000000000, 0.9238795325112867385, 1.000000000000000000, 0.9238795325112867385, 1.000000000000000000, 0.9238795325112867385, 1.000000000000000000, 0.9238795325112867385, 1.000000000000000000, 0.9238795325112867385, 1.000000000000000000, 0.9238795325112867385, 1.000000000000000000, 0.9238795325112867385, 1.000000000000000000, 0.9238795325112867385, 1.000000000000000000, 0.9238795325112867385, 1.000000000000000000, 0.9238795325112867385, 1.000000000000000000, 0.9238795325112867385, 1.000000000000000000, 0.9238795325112867385, 1.000000000000000000, 0.9238795325112867385, 1.000000000000000000, 0.9238795325112867385, 1.000000000000000000, 0.9238795325112867385, 1.000000000000000000, 0.9238795325112867385, 1.000000000000000000, 0.9238795325112867385, 1.000000000000000000, 0.9238795325112867385, 1.000000000000000000, 0.9238795325112867385, 1.000000000000000000, 0.9238795325112867385, 1.000000000000000000, 0.9238795325112867385, 1.000000000000000000, 0.9238795325112867385, 1.000000000000000000, 0.9238795325112867385, 1.000000000000000000, 0.9238795325112867385, 1.000000000000000000, 0.9238795325112867385, 1.000000000000000000, 0.9238795325112867385, 1.000000000000000000, 0.9238795325112867385, 1.000000000000000000, 0.9238795325112867385, 1.000000000000000000, 0.9238795325112867385, 1.000000000000000000, 0.9238795325112867385, 1.000000000000000000, 0.9238795325112867385, 1.000000000000000000, 0.9238795325112867385, 1.000000000000000000, 0.9238795325112867385, 1.000000000000000000, 0.9238795325112867385, 1.000000000000000000, 0.9238795325112867385, 1.000000000000000000, 0.9238795325112867385, 1.000000000000000000, 0.9238795325112867385, 1.000000000000000000, 0.9238795325112867385, 1.000000000000000000, 0.9238795325112867385, 1.000000000000000000, 0.9238795325112867385, 1.000000000000000000, 0.9238795325112867385, 1.000000000000000000, 0.9238795325112867385, 1.000000000000000000, 0.9238795325112867385, 1.000000000000000000, 0.9238795325112867385, 1.000000000000000000, 0.9238795325112867385, 1.000000000000000000, 0.9238795325112867385, 1.000000000000000000, 0.9238795325112867385, 1.000000000000000000, 0.9238795325112867385, 1.000000000000000000, 0.9238795325112867385, 1.000000000000000000, 0.9238795325112867385, 1.000000000000000000, 0.9238795325112867385, 1.000000000000000000, 0.9238795325112867385, 1.000000000000000000, 0.9238795325112867385, 1.000000000000000000, 0.9238795325112867385, 1.000000000000000000, 0.9238795325112867385, 1.000000000000000000, 0.9238795325112867385, 1.000000000000000000, 0.9238795325112867385, 1.000000000000000000, 0.9238795325112867385, 1.000000000000000000, 0.9238795325112867385, 1.000000000000000000, 0.9238795325112867385, 1.000000000000000000, 0.9238795325112867385, 1.000000000000000000, 0.9238795325112867385, 1.000000000000000000, 0.9238795325112867385, 1.000000000000000000, 0.9238795325112867385, 1.000000000000000000, 0.9238795325112867385, 1.000000000000000000, 0.9238795325112867385, 1.000000000000000000, 0.9238795325112867385, 1.000000000000000000, 0.9238795325112867385, 1.000000000000000000, 0.9238795325112867385, 1.000000000000000000, 0.9238795325112867385, 1.000000000000000000, 0.9238795325112867385, 1.000000000000000000, 0.9238795325112867385, 1.000000000000000000, 0.9238795325112867385, 1.000000000000000000, 0.9238795325112867385, 1.000000000000000000, 0.9238795325112867385, 1.000000000000000000, 0.9238795325112867385, 1.000000000000000000, 0.9238795325112867385, 1.000000000000000000, 0.9238795325112867385, 1.000000000000000000, 0.9238795325112867385, 1.000000000000000000, 0.9238795325112867385, 1.000000000000000000, 0.9238795325112867385, 1.000000000000000000, 0.9238795325112867385, 1.000000000000000000, 0.9238795325112867385, 1.000000000000000000, 0.9238795325112867385, 1.000000000000000000, 0.9238795325112867385, 1.000000000000000000, 0.9238795325112867385, 1.000000000000000000, 0.9238795325112867385, 1.000000000000000000, 0.9238795325112867385, 1.000000000000000000, 0.9238795325112867385, 1.000000000000000000, 0.9238795325112867385, 1.000000000000000000, 0.9238795325112867385, 1.000000000000000000, 0.9238795325112867385, 1.000000000000000000, 0.9238795325112867385, 1.000000000000000000, 0.9238795325112867385, 1.000000000000000000, 0.9238795325112867385, 1.000000000000000000, 0.9238795325112867385, 1.000000000000000000, 0.9238795325112867385, 1.000000000000000000, 0.9238795325112867385, 1.000000000000000000, 0.9238795325112867385, 1.000000000000000000, 0.9238795325112867385, 1.000000000000000000, 0.9238795325112867385, 1.000000000000000000, 0.9238795325112867385, 1.000000000000000000, 0.9238795325112867385, 1.000000000000000000, 0.9238795325112867385, 1.000000000000000000, 0.9238795325112867385, 1.000000000000000000, 0.9238795325112867385, 1.000000000000000000, 0.9238795325112867385, 1.000000000000000000, 0.9238795325112867385, 1.000000000000000000, 0.9238795325112867385, 1.000000000000000000, 0.9238795325112867385, 1.000000000000000000, 0.9238795325112867385, 1.000000000000000000, 0.9238795325112867385, 1.000000000000000000, 0.9238795325112867385, 1.000000000000000000, 0.9238795325112867385, 1.000000000000000000, 0.9238795325112867385, 1.000000000000000000, 0.9331730159288109672, 0.9836823002065551158) ) ) 
 REPRESENTATION_ITEM ( '' )  SURFACE ( )  );
#12784=CARTESIAN_POINT ( 'NONE',  ( -0.1983289933404564775, 0.05677534557590641767, 0.2335968120589810293 ) ) ;
#12788=CARTESIAN_POINT ( 'NONE',  ( -0.1993543840281266355, 5.026472222298088433, 0.1993543840281267465 ) ) ;
#12791=VECTOR ( 'NONE', #19378, 39.37007874015748143 ) ;
#12792=CARTESIAN_POINT ( 'NONE',  ( 0.1993543840281266355, 0.2090277777019111383, 0.1993543840281267465 ) ) ;
#12794=CARTESIAN_POINT ( 'NONE',  ( -0.2819296736111110424, 5.203555555631421470, 0.1167790944451424923 ) ) ;
#12795=CARTESIAN_POINT ( 'NONE',  ( 0.05068837741648516554, 5.073009555618063438, 0.3078549794868774558 ) ) ;
#12796=VERTEX_POINT ( 'NONE', #14760 ) ;
#12797=CARTESIAN_POINT ( 'NONE',  ( 0.2819296736111110424, 4.995222222298087544, -0.1167790944451423396 ) ) ;
#12798=CARTESIAN_POINT ( 'NONE',  ( -0.2495230188188473364, 4.174703235102065868, 0.1917148675851489681 ) ) ;
#12799=CARTESIAN_POINT ( 'NONE',  ( 0.07748689081482018626, 4.875025410756610889, -0.3027932829829018124 ) ) ;
#12800=CARTESIAN_POINT ( 'NONE',  ( 0.1292346314604033708, 4.568138888888888971, 0.3120000000000023865 ) ) ;
#12802=CARTESIAN_POINT ( 'NONE',  ( -0.2206173157302028232, 4.654944444444443441, -0.2206173157302028232 ) ) ;
#12803=CARTESIAN_POINT ( 'NONE',  ( 0.2819296736111110979, 4.106333333409199149, -0.1167790944451423396 ) ) ;
#12804=CARTESIAN_POINT ( 'NONE',  ( -0.2819296736111110979, 3.755638888964754951, 0.000000000000000000 ) ) ;
#12805=CARTESIAN_POINT ( 'NONE',  ( 0.2961762452215840891, 4.032756265542360552, -0.09810037269422101913 ) ) ;
#12806=CARTESIAN_POINT ( 'NONE',  ( -5.731347020009612645E-17, 0.2749999998482670627, 0.3119999999999999996 ) ) ;
#12807=VERTEX_POINT ( 'NONE', #9017 ) ;
#12808=CARTESIAN_POINT ( 'NONE',  ( 5.731347020009612645E-17, 3.897999999999999243, 0.3119999999999999996 ) ) ;
#12810=CARTESIAN_POINT ( 'NONE',  ( -0.1167790944451423535, 4.252166666742533074, 0.2819296736111110424 ) ) ;
#12811=CARTESIAN_POINT ( 'NONE',  ( -0.3096714640854181244, 4.501118225121650163, -0.03805883575092474519 ) ) ;
#12812=CONICAL_SURFACE ( 'NONE', #8483, 0.3119999999999999996, 0.7853981633974450594 ) ;
#12814=EDGE_CURVE ( 'NONE', #13967, #8952, #19470, .T. ) ;
#12817=CARTESIAN_POINT ( 'NONE',  ( -0.2494960936497209736, 3.952398630088741260, 0.1917385281361134730 ) ) ;
#12818=CARTESIAN_POINT ( 'NONE',  ( -0.04084137789490534937, 4.433892237992067997, -0.3099887041510316910 ) ) ;
#12821=CARTESIAN_POINT ( 'NONE',  ( -0.1993543840281267465, 0.1812499999241333759, 0.1993543840281266633 ) ) ;
#12822=CARTESIAN_POINT ( 'NONE',  ( 0.1917423854131830863, 3.871439620893523337, -0.2494933204621729017 ) ) ;
#12824=CARTESIAN_POINT ( 'NONE',  ( -1.910449006669871087E-17, 4.036888888888888083, -0.3119999999999999996 ) ) ;
#12828=CARTESIAN_POINT ( 'NONE',  ( -0.1807484698107602594, 5.097407819853565059, -0.2533385039640153047 ) ) ;
#12830=CARTESIAN_POINT ( 'NONE',  ( -5.178964085587577574E-17, 0.5770833332574667462, 0.2819296736111110979 ) ) ;
#12831=CARTESIAN_POINT ( 'NONE',  ( 0.1993543840281266633, 3.901472222298087988, -0.1993543840281266910 ) ) ;
#12835=CARTESIAN_POINT ( 'NONE',  ( 0.1993543840281267465, 4.498694444520309865, 0.1993543840281266633 ) ) ;
#12837=CARTESIAN_POINT ( 'NONE',  ( -1.910449006669871087E-17, 4.592444444444443441, -0.3119999999999999996 ) ) ;
#12839=CARTESIAN_POINT ( 'NONE',  ( 0.2778757787820582137, 4.359068954902455495, 0.1421744276038705013 ) ) ;
#12840=CARTESIAN_POINT ( 'NONE',  ( -0.1993543840281266355, 5.026472222298088433, 0.1993543840281267465 ) ) ;
#12841=CARTESIAN_POINT ( 'NONE',  ( 0.3068634962433764435, 4.194799344920210338, 0.06402122387849780438 ) ) ;
#12842=( CONVERSION_BASED_UNIT ( 'INCH', #5376 ) LENGTH_UNIT ( ) NAMED_UNIT ( #19748 ) );
#12843=CARTESIAN_POINT ( 'NONE',  ( -0.3119999999999999996, 4.995222222222221120, 0.000000000000000000 ) ) ;
#12844=VECTOR ( 'NONE', #13287, 39.37007874015748143 ) ;
#12845=CARTESIAN_POINT ( 'NONE',  ( 0.2819296736111110979, 4.713972222298087544, -3.452642723725051716E-17 ) ) ;
#12847=CARTESIAN_POINT ( 'NONE',  ( -1.910449006669871087E-17, 4.759111111111110404, -0.3119999999999999996 ) ) ;
#12848=CARTESIAN_POINT ( 'NONE',  ( -2.750539236387841874E-07, 4.266055563097283176, -0.3119999999998787632 ) ) ;
#12850=CARTESIAN_POINT ( 'NONE',  ( -0.2819296736111110979, 0.4694444443685776847, 0.1167790944451422425 ) ) ;
#12852=ORIENTED_EDGE ( 'NONE', *, *, #23208, .F. ) ;
#12853=CARTESIAN_POINT ( 'NONE',  ( -0.2819296736111110979, 0.1361111110352444808, 0.1167790944451422425 ) ) ;
#12854=CARTESIAN_POINT ( 'NONE',  ( -0.3119999999999999996, 4.328555555555554157, 0.000000000000000000 ) ) ;
#12858=CARTESIAN_POINT ( 'NONE',  ( 0.1292346314604080892, 4.200083333333331836, -0.3119999999999975016 ) ) ;
#12859=CARTESIAN_POINT ( 'NONE',  ( -0.3042511176241679549, 3.889013863588333564, -0.07042807391908939563 ) ) ;
#12860=CARTESIAN_POINT ( 'NONE',  ( 5.731347020009612645E-17, 4.009111111111109516, 0.3119999999999999996 ) ) ;
#12861=CARTESIAN_POINT ( 'NONE',  ( 0.2819296736111110424, 4.564666666742532186, -0.1167790944451423396 ) ) ;
#12863=CARTESIAN_POINT ( 'NONE',  ( 0.1292346314604043700, 4.755638888888888083, -0.3120000000000012763 ) ) ;
#12865=CARTESIAN_POINT ( 'NONE',  ( -1.726321361862525858E-17, 5.186194444520309865, -0.2819296736111110979 ) ) ;
#12866=CARTESIAN_POINT ( 'NONE',  ( 0.1167790944451422702, 4.557722222298087544, -0.2819296736111110979 ) ) ;
#12867=CARTESIAN_POINT ( 'NONE',  ( 0.2494037671505511811, 4.913117397265690300, 0.1918541382674933959 ) ) ;
#12872=CARTESIAN_POINT ( 'NONE',  ( 0.2206173157302027954, 4.203555555707287894, -0.2206173157302028232 ) ) ;
#12873=CARTESIAN_POINT ( 'NONE',  ( -0.2819296736111110424, 4.592444444520309865, 0.1167790944451424923 ) ) ;
#12874=CARTESIAN_POINT ( 'NONE',  ( 0.1167790944451422702, 3.779944444520310309, -0.2819296736111110424 ) ) ;
#12882=CARTESIAN_POINT ( 'NONE',  ( 0.2206173157302027954, 4.252166666666665762, -0.2206173157302028232 ) ) ;
#12884=ORIENTED_EDGE ( 'NONE', *, *, #22259, .T. ) ;
#12885=CARTESIAN_POINT ( 'NONE',  ( 0.2206173157302028232, 0.1847222220704893003, -0.2206173157302028232 ) ) ;
#12888=CARTESIAN_POINT ( 'NONE',  ( -0.1224332991792908831, 3.734713384307907447, 0.2872374373138953940 ) ) ;
#12890=CARTESIAN_POINT ( 'NONE',  ( 0.009632836665255781541, 5.167574349600237760, 0.2973209551366967074 ) ) ;
#12893=ORIENTED_EDGE ( 'NONE', *, *, #2449, .T. ) ;
#12894=CARTESIAN_POINT ( 'NONE',  ( 0.2678247992155382007, 5.080760836019062587, 0.1601480313148006818 ) ) ;
#12896=CARTESIAN_POINT ( 'NONE',  ( -1.726321361862525858E-17, 4.227861111186976828, -0.2819296736111110979 ) ) ;
#12897=CARTESIAN_POINT ( 'NONE',  ( -0.1993543840281266910, 5.123694444520309865, -0.1993543840281266910 ) ) ;
#12899=CARTESIAN_POINT ( 'NONE',  ( -0.2491998977626836975, 4.218580871723631276, -0.1921089702143923827 ) ) ;
#12900=CARTESIAN_POINT ( 'NONE',  ( 0.1292346314604058410, 3.901472222222222008, 0.3119999999999998885 ) ) ;
#12901=CARTESIAN_POINT ( 'NONE',  ( 0.3119999999999999996, 5.029944444596177178, -3.820898013339742174E-17 ) ) ;
#12903=CARTESIAN_POINT ( 'NONE',  ( 0.2819296736111110979, 5.175777777853643791, -0.1167790944451423396 ) ) ;
#12904=AXIS2_PLACEMENT_3D ( 'NONE', #7792, #11702, #20716 ) ;
#12907=CARTESIAN_POINT ( 'NONE',  ( -0.2386252316775615556, 0.05573247922623769668, 0.1905836568333658665 ) ) ;
#12909=CARTESIAN_POINT ( 'NONE',  ( 0.1167790944451422702, 5.002166666742531298, -0.2819296736111110424 ) ) ;
#12915=EDGE_CURVE ( 'NONE', #23182, #5345, #5826, .T. ) ;
#12917=CARTESIAN_POINT ( 'NONE',  ( -0.1993543840281266633, 0.2923611110352444808, -0.1993543840281266910 ) ) ;
#12919=CARTESIAN_POINT ( 'NONE',  ( 5.178964085587577574E-17, 4.936194444520309865, 0.2819296736111110979 ) ) ;
#12920=CARTESIAN_POINT ( 'NONE',  ( 0.02020074157040065502, 4.487702955821844419, -0.3115091454018745210 ) ) ;
#12922=CARTESIAN_POINT ( 'NONE',  ( -0.1167790944451423257, 4.953555555631421470, -0.2819296736111110424 ) ) ;
#12923=FACE_OUTER_BOUND ( 'NONE', #7954, .T. ) ;
#12927=CARTESIAN_POINT ( 'NONE',  ( 0.1292346314604056190, 4.700083333333332725, -0.3119999999999999996 ) ) ;
#12928=CARTESIAN_POINT ( 'NONE',  ( -0.2819296736111110424, 4.078555555631420582, 0.1167790944451424923 ) ) ;
#12929=DIRECTION ( 'NONE',  ( -0.000000000000000000, -1.000000000000000000, -0.000000000000000000 ) ) ;
#12930=EDGE_CURVE ( 'NONE', #10368, #16166, #799, .T. ) ;
#12932=CARTESIAN_POINT ( 'NONE',  ( 0.2963938556121599732, 4.032736175004294488, -0.09744095219179720047 ) ) ;
#12933=DIRECTION ( 'NONE',  ( 0.000000000000000000, 0.000000000000000000, 1.000000000000000000 ) ) ;
#12934=EDGE_LOOP ( 'NONE', ( #3194, #23403, #19088, #21065 ) ) ;
#12935=DIRECTION ( 'NONE',  ( 0.000000000000000000, 0.000000000000000000, -1.000000000000000000 ) ) ;
#12941=DIRECTION ( 'NONE',  ( -0.000000000000000000, -1.000000000000000000, -0.000000000000000000 ) ) ;
#12945=CARTESIAN_POINT ( 'NONE',  ( 1.726321361862525858E-17, 0.2715277777019111660, -0.2819296736111110979 ) ) ;
#12946=CARTESIAN_POINT ( 'NONE',  ( 0.02550031897004510079, 3.876477113958451515, -0.3109980661668607094 ) ) ;
#12947=DIRECTION ( 'NONE',  ( -0.000000000000000000, -1.000000000000000000, -0.000000000000000000 ) ) ;
#12948=DIRECTION ( 'NONE',  ( -0.000000000000000000, -1.000000000000000000, -0.000000000000000000 ) ) ;
#12952=CARTESIAN_POINT ( 'NONE',  ( -0.2944222112592022600, 5.102614573065762826, -0.1009617277478159353 ) ) ;
#12953=CARTESIAN_POINT ( 'NONE',  ( -1.910449006669871087E-17, 4.370222222222221120, -0.3119999999999999996 ) ) ;
#12954=CARTESIAN_POINT ( 'NONE',  ( -0.2819296736111110979, 0.5666666665908001166, 0.1167790944451422425 ) ) ;
#12955=CARTESIAN_POINT ( 'NONE',  ( 5.178964085587577574E-17, 3.880638888964754951, 0.2819296736111110979 ) ) ;
#12957=CARTESIAN_POINT ( 'NONE',  ( 0.1167790944451422702, 4.349388888964754507, -0.2819296736111110424 ) ) ;
#12959=CARTESIAN_POINT ( 'NONE',  ( -0.1292346314604044533, 4.595916666666665762, -0.3120000000000012763 ) ) ;
#12960=ORIENTED_EDGE ( 'NONE', *, *, #9559, .T. ) ;
#12961=CARTESIAN_POINT ( 'NONE',  ( -7.331754493858430024E-07, 4.349360015129621004, 0.3119999999981767358 ) ) ;
#12962=CARTESIAN_POINT ( 'NONE',  ( -1.726321361862525858E-17, 4.950083333409199149, -0.2819296736111110979 ) ) ;
#12963=CARTESIAN_POINT ( 'NONE',  ( -0.2969476826539968473, 5.154194855657474150, -0.05166938045060873175 ) ) ;
#12965=CARTESIAN_POINT ( 'NONE',  ( 0.1993543840281267465, 4.651472222298087544, 0.1993543840281266633 ) ) ;
#12966=( BOUNDED_CURVE ( )  B_SPLINE_CURVE ( 2, ( #23224, #6533, #13986, #21413, #6654, #23955, #18359, #16536, #10811, #18239, #20430, #16772, #5431, #8969, #3480, #9216, #16655, #1652, #3597, #9087, #13137, #7503, #5672, #7149, #12897, #1771, #3726, #14717, #18601, #11173, #14951, #7269, #7385, #14589, #20313, #3359, #22130, #1538, #5550, #11049, #24076, #12773, #10931, #13015, #18478, #20191, #14836, #22254, #1893, #9336, #56, #22370, #20550, #12653, #20071, #16418, #23827, #22012, #5310, #10764, #10287, #2954, #17711, #19779, #21606, #8673, #16125, #5014, #19899, #16002, #21730, #23658, #12362, #18067, #16247, #5134, #21845, #10411, #23420, #4899, #1487, #3079, #7101, #1005, #23539, #8924, #16369, #18191, #5256, #10522, #3188, #6731, #8435, #12480, #23778, #1246, #17953, #1369, #6854, #14539, #19656, #21487, #12598, #8795, #20144, #15880, #20018, #6976, #8561, #14296, #12243, #10636, #14419, #12726, #4774, #1127, #3307, #21962, #23297, #6609, #14057, #17836, #14174, #16606, #20502, #3797, #7336, #14900, #14788, #5859, #7452, #18550, #22204, #5746, #16959, #22570, #23899, #18789, #3917, #1839, #7574, #1967, #12845, #9282, #1609, #20381, #9043, #15022, #3673, #11241, #13318, #11120, #22321, #22446, #3550, #5503, #14664, #11361, #24026, #3430, #12965, #13204, #9406, #2084, #16844, #10883, #16489, #18312, #9526, #7218, #18668, #131, #11001, #16724, #20617, #254, #4, #5622, #7694, #13087, #1724, #15141, #22084, #5379, #20265, #18428, #9162, #12866, #20637, #393, #1862, #11504, #5400, #3819, #13337, #20759, #22591, #9668, #14923, #7594, #20402, #2236, #16979, #18447, #9425, #22466, #5524, #5644, #1989, #11380, #18687, #18808, #16864, #2104, #13108, #20285, #7474, #151, #17105, #7357, #14687, #4049, #5877, #22105, #22342, #15044, #3695, #3570, #9303, #11141, #20521, #18571, #11262, #9184, #18938, #1744, #9546, #22224, #14807, #273, #11023, #16628, #5766, #24047, #12988, #16744, #13226, #26, #3938, #7713, #15159, #22826, #19054, #19731, #15952, #18026, #22705, #3033, #23377, #6116, #17667, #14251, #6685, #3149, #4969, #953, #11747, #8384, #13461, #20878, #10480, #6809, #14014, #2355, #20997, #1079, #8511, #19168, #19609, #2786, #10598, #21686, #7832, #9796, #21444, #17787, #17912, #23254, #8636, #1205, #12436, #15836, #14130, #17229, #4730, #5995, #6563, #4172, #12318, #12202, #21559, #2904, #10363, #16081, #7943, #10239, #511, #23493, #4290, #15278, #4850, #19852, #11625, #15399, #13585, #14618, #9116, #12803, #16320, #19977, #3389, #22163, #1445, #10841, #7299, #12928, #18269, #7176, #14748, #20222, #23733, #9001, #1800, #5464, #23987, #16565, #16686, #20340, #23618, #3628, #11200, #18150, #8749, #1566, #12682, #23856, #22043, #3511, #10962, #7057, #18387, #11078, #16445, #18508, #9245, #24107, #7418, #8879, #5339, #1682, #14869, #20100, #22284, #16204, #5579, #13044, #20461, #3758, #1323, #6932, #14370, #14496, #21803, #5089, #21919, #12557, #5209, #3264, #10716, #22885, #5705, #22652, #22767, #5940, #6059, #17041, #16809, #11443, #4349, #3878, #8008, #9610, #9368, #2176, #16919, #13286, #9487, #13168, #13528, #2295, #18630, #22404, #13398, #334, #17170, #4112, #573, #456, #13642, #15460, #18876, #22527, #3992, #90, #7533, #20942, #17285, #7774, #20581, #7655, #11570, #15221, #20702, #2048, #18998, #9730, #6179, #21061, #11322 ),
 .UNSPECIFIED., .F., .T. ) 
 B_SPLINE_CURVE_WITH_KNOTS ( ( 3, 2, 2, 2, 2, 2, 2, 2, 2, 2, 2, 2, 2, 2, 2, 2, 2, 2, 2, 2, 2, 2, 2, 2, 2, 2, 2, 2, 2, 2, 2, 2, 2, 2, 2, 2, 2, 2, 2, 2, 2, 2, 2, 2, 2, 2, 2, 2, 2, 2, 2, 2, 2, 2, 2, 2, 2, 2, 2, 2, 2, 2, 2, 2, 2, 2, 2, 2, 2, 2, 2, 2, 2, 2, 2, 2, 2, 2, 2, 2, 2, 2, 2, 2, 2, 2, 2, 2, 2, 2, 2, 2, 2, 2, 2, 2, 2, 2, 2, 2, 2, 2, 2, 2, 2, 2, 2, 2, 2, 2, 2, 2, 2, 2, 2, 2, 2, 2, 2, 2, 2, 2, 2, 2, 2, 2, 2, 2, 2, 2, 2, 2, 2, 2, 2, 2, 2, 2, 2, 2, 2, 2, 2, 2, 2, 2, 2, 2, 2, 2, 2, 2, 2, 2, 2, 2, 2, 2, 2, 2, 2, 2, 2, 2, 2, 2, 2, 2, 2, 2, 2, 2, 2, 2, 2, 2, 2, 2, 2, 2, 2, 2, 2, 2, 2, 2, 2, 2, 2, 2, 2, 2, 2, 2, 2, 2, 2, 2, 2, 2, 2, 2, 2, 2, 2, 2, 2, 2, 2, 2, 2, 2, 2, 2, 3 ),
 ( 0.02311620385524515431, 0.02741254234740052656, 0.03198129940530199805, 0.03655005646320347301, 0.04111881352110494797, 0.04568757057900641599, 0.05025632763690789095, 0.05482508469480935898, 0.05939384175271084088, 0.06396259881061230890, 0.06853135586851377692, 0.07310011292641524494, 0.07766886998431671296, 0.08223762704221820874, 0.08680638410011967676, 0.09137514115802114478, 0.09594389821592259893, 0.1005126552738240808, 0.1050814123317255488, 0.1096501693896270169, 0.1142189264475284988, 0.1187876835054299807, 0.1233564405633314487, 0.1279251976212329167, 0.1324939546791343847, 0.1370627117370358805, 0.1416314687949373208, 0.1462002258528387888, 0.1507689829107402846, 0.1553377399686417248, 0.1599064970265432206, 0.1644752540844447164, 0.1690440111423461567, 0.1736127682002476524, 0.1781815252581490927, 0.1827502823160505885, 0.1873190393739520565, 0.1918877964318535245, 0.1964565534897550203, 0.2010253105476564883, 0.2055940676055579563, 0.2101628246634593966, 0.2147315817213608646, 0.2193003387792623327, 0.2238690958371638284, 0.2284378528950652965, 0.2330066099529667645, 0.2375753670108682603, 0.2421441240687697005, 0.2467128811266711963, 0.2512816381845726088, 0.2558503952424741046, 0.2604191523003756004, 0.2649879093582770961, 0.2695566664161785919, 0.2741254234740800322, 0.2786941805319814724, 0.2832629375898830237, 0.2878316946477844640, 0.2924004517056859043, 0.2969692087635873445, 0.3015379658214888403, 0.3061067228793902806, 0.3106754799372917208, 0.3152442369951933276, 0.3198129940530947679, 0.3243817511109962082, 0.3289505081688977040, 0.3335192652267991442, 0.3380880222847005845, 0.3426567793426020248, 0.3472255364005036316, 0.3517942934584050718, 0.3563630505163065121, 0.3609318075742080079, 0.3655005646321094481, 0.3700693216900108884, 0.3746380787479123842, 0.3792068358058139355, 0.3837755928637153757, 0.3883443499216168715, 0.3929131069795183118, 0.3974818640374197520, 0.4020506210953212478, 0.4066193781532226881, 0.4111881352111242394, 0.4157568922690256796, 0.4203256493269271754, 0.4248944063848286157, 0.4294631634427300004, 0.4340319205006314962, 0.4386006775585329365, 0.4431694346164344878, 0.4477381916743359835, 0.4523069487322374238, 0.4568757057901388641, 0.4614444628480403598, 0.4660132199059418001, 0.4705819769638432404, 0.4751507340217447917, 0.4797194910796462874, 0.4842882481375477277, 0.4888570051954491680, 0.4934257622533506638, 0.4979945193112521040, 0.5025632763691535443, 0.5071320334270551511, 0.5117007904849566469, 0.5162695475428580316, 0.5208383046007595274, 0.5254070616586609122, 0.5299758187165625190, 0.5345445757744640147, 0.5391133328323653995, 0.5436820898902668953, 0.5482508469481683910, 0.5528196040060697758, 0.5573883610639712716, 0.5619571181218727673, 0.5665258751797742631, 0.5710946322376757589, 0.5756633892955772547, 0.5802321463534786394, 0.5848009034113801352, 0.5893696604692815200, 0.5939384175271831268, 0.5985071745850845115, 0.6030759316429861183, 0.6076446887008875031, 0.6122134457587889989, 0.6167822028166903836, 0.6213509598745918794, 0.6259197169324933752, 0.6304884739903949820, 0.6350572310482963667, 0.6396259881061978625, 0.6441947451640992472, 0.6487635022220007430, 0.6533322592799021278, 0.6579010163378037346, 0.6624697733957052304, 0.6670385304536067261, 0.6716072875115081109, 0.6761760445694096067, 0.6807448016273109914, 0.6853135586852124872, 0.6898823157431140940, 0.6944510728010155898, 0.6990198298589169745, 0.7035885869168184703, 0.7081573439747198551, 0.7127261010326212398, 0.7172948580905228466, 0.7218636151484243424, 0.7264323722063258382, 0.7310011292642272229, 0.7355698863221287187, 0.7401386433800301035, 0.7447074004379315992, 0.7492761574958330950, 0.7538449145537347018, 0.7584136716116360866, 0.7629824286695375823, 0.7675511857274389671, 0.7721199427853404629, 0.7766886998432419587, 0.7812574569011434544, 0.7858262139590449502, 0.7903949710169464460, 0.7949637280748478307, 0.7995324851327493265, 0.8041012421906508223, 0.8086699992485523181, 0.8132387563064537028, 0.8178075133643553096, 0.8223762704222566944, 0.8269450274801581902, 0.8315137845380595749, 0.8360825415959611817, 0.8406512986538625665, 0.8452200557117640622, 0.8497888127696655580, 0.8543575698275670538, 0.8589263268854684386, 0.8634950839433700454, 0.8680638410012714301, 0.8726325980591729259, 0.8772013551170743106, 0.8817701121749759174, 0.8863388692328773022, 0.8909076262907786870, 0.8954763833486802938, 0.9000451404065816785, 0.9046138974644831743, 0.9091826545223845590, 0.9137514115802861658, 0.9183201686381875506, 0.9228889256960891574, 0.9274576827539905421, 0.9320264398118920379, 0.9365951968697934227, 0.9411639539276949185, 0.9457327109855964142, 0.9503014680434979100, 0.9548702251013994058, 0.9594389821593009016, 0.9640077392172022863, 0.9685764962751037821, 0.9731452533330051669, 0.9777140103909067737, 0.9822827674488082694, 0.9868515245067097652, 0.9914202815646111500, 0.9959890386225126457, 1.000000000000000000 ),
 .UNSPECIFIED. ) 
 CURVE ( )  GEOMETRIC_REPRESENTATION_ITEM ( )  RATIONAL_B_SPLINE_CURVE ( ( 0.9914636835865335840, 0.9284183224522696287, 1.000000000000000000, 0.9238795325112867385, 1.000000000000000000, 0.9238795325112867385, 1.000000000000000000, 0.9238795325112867385, 1.000000000000000000, 0.9238795325112867385, 1.000000000000000000, 0.9238795325112867385, 1.000000000000000000, 0.9238795325112867385, 1.000000000000000000, 0.9238795325112867385, 1.000000000000000000, 0.9238795325112867385, 1.000000000000000000, 0.9238795325112867385, 1.000000000000000000, 0.9238795325112867385, 1.000000000000000000, 0.9238795325112867385, 1.000000000000000000, 0.9238795325112867385, 1.000000000000000000, 0.9238795325112867385, 1.000000000000000000, 0.9238795325112867385, 1.000000000000000000, 0.9238795325112867385, 1.000000000000000000, 0.9238795325112867385, 1.000000000000000000, 0.9238795325112867385, 1.000000000000000000, 0.9238795325112867385, 1.000000000000000000, 0.9238795325112867385, 1.000000000000000000, 0.9238795325112867385, 1.000000000000000000, 0.9238795325112867385, 1.000000000000000000, 0.9238795325112867385, 1.000000000000000000, 0.9238795325112867385, 1.000000000000000000, 0.9238795325112867385, 1.000000000000000000, 0.9238795325112867385, 1.000000000000000000, 0.9238795325112867385, 1.000000000000000000, 0.9238795325112867385, 1.000000000000000000, 0.9238795325112867385, 1.000000000000000000, 0.9238795325112867385, 1.000000000000000000, 0.9238795325112867385, 1.000000000000000000, 0.9238795325112867385, 1.000000000000000000, 0.9238795325112867385, 1.000000000000000000, 0.9238795325112867385, 1.000000000000000000, 0.9238795325112867385, 1.000000000000000000, 0.9238795325112867385, 1.000000000000000000, 0.9238795325112867385, 1.000000000000000000, 0.9238795325112867385, 1.000000000000000000, 0.9238795325112867385, 1.000000000000000000, 0.9238795325112867385, 1.000000000000000000, 0.9238795325112867385, 1.000000000000000000, 0.9238795325112867385, 1.000000000000000000, 0.9238795325112867385, 1.000000000000000000, 0.9238795325112867385, 1.000000000000000000, 0.9238795325112867385, 1.000000000000000000, 0.9238795325112867385, 1.000000000000000000, 0.9238795325112867385, 1.000000000000000000, 0.9238795325112867385, 1.000000000000000000, 0.9238795325112867385, 1.000000000000000000, 0.9238795325112867385, 1.000000000000000000, 0.9238795325112867385, 1.000000000000000000, 0.9238795325112867385, 1.000000000000000000, 0.9238795325112867385, 1.000000000000000000, 0.9238795325112867385, 1.000000000000000000, 0.9238795325112867385, 1.000000000000000000, 0.9238795325112867385, 1.000000000000000000, 0.9238795325112867385, 1.000000000000000000, 0.9238795325112867385, 1.000000000000000000, 0.9238795325112867385, 1.000000000000000000, 0.9238795325112867385, 1.000000000000000000, 0.9238795325112867385, 1.000000000000000000, 0.9238795325112867385, 1.000000000000000000, 0.9238795325112867385, 1.000000000000000000, 0.9238795325112867385, 1.000000000000000000, 0.9238795325112867385, 1.000000000000000000, 0.9238795325112867385, 1.000000000000000000, 0.9238795325112867385, 1.000000000000000000, 0.9238795325112867385, 1.000000000000000000, 0.9238795325112867385, 1.000000000000000000, 0.9238795325112867385, 1.000000000000000000, 0.9238795325112867385, 1.000000000000000000, 0.9238795325112867385, 1.000000000000000000, 0.9238795325112867385, 1.000000000000000000, 0.9238795325112867385, 1.000000000000000000, 0.9238795325112867385, 1.000000000000000000, 0.9238795325112867385, 1.000000000000000000, 0.9238795325112867385, 1.000000000000000000, 0.9238795325112867385, 1.000000000000000000, 0.9238795325112867385, 1.000000000000000000, 0.9238795325112867385, 1.000000000000000000, 0.9238795325112867385, 1.000000000000000000, 0.9238795325112867385, 1.000000000000000000, 0.9238795325112867385, 1.000000000000000000, 0.9238795325112867385, 1.000000000000000000, 0.9238795325112867385, 1.000000000000000000, 0.9238795325112867385, 1.000000000000000000, 0.9238795325112867385, 1.000000000000000000, 0.9238795325112867385, 1.000000000000000000, 0.9238795325112867385, 1.000000000000000000, 0.9238795325112867385, 1.000000000000000000, 0.9238795325112867385, 1.000000000000000000, 0.9238795325112867385, 1.000000000000000000, 0.9238795325112867385, 1.000000000000000000, 0.9238795325112867385, 1.000000000000000000, 0.9238795325112867385, 1.000000000000000000, 0.9238795325112867385, 1.000000000000000000, 0.9238795325112867385, 1.000000000000000000, 0.9238795325112867385, 1.000000000000000000, 0.9238795325112867385, 1.000000000000000000, 0.9238795325112867385, 1.000000000000000000, 0.9238795325112867385, 1.000000000000000000, 0.9238795325112867385, 1.000000000000000000, 0.9238795325112867385, 1.000000000000000000, 0.9238795325112867385, 1.000000000000000000, 0.9238795325112867385, 1.000000000000000000, 0.9238795325112867385, 1.000000000000000000, 0.9238795325112867385, 1.000000000000000000, 0.9238795325112867385, 1.000000000000000000, 0.9238795325112867385, 1.000000000000000000, 0.9238795325112867385, 1.000000000000000000, 0.9238795325112867385, 1.000000000000000000, 0.9238795325112867385, 1.000000000000000000, 0.9238795325112867385, 1.000000000000000000, 0.9238795325112867385, 1.000000000000000000, 0.9238795325112867385, 1.000000000000000000, 0.9238795325112867385, 1.000000000000000000, 0.9238795325112867385, 1.000000000000000000, 0.9238795325112867385, 1.000000000000000000, 0.9238795325112867385, 1.000000000000000000, 0.9238795325112867385, 1.000000000000000000, 0.9238795325112867385, 1.000000000000000000, 0.9238795325112867385, 1.000000000000000000, 0.9238795325112867385, 1.000000000000000000, 0.9238795325112867385, 1.000000000000000000, 0.9238795325112867385, 1.000000000000000000, 0.9238795325112867385, 1.000000000000000000, 0.9238795325112867385, 1.000000000000000000, 0.9238795325112867385, 1.000000000000000000, 0.9238795325112867385, 1.000000000000000000, 0.9238795325112867385, 1.000000000000000000, 0.9238795325112867385, 1.000000000000000000, 0.9238795325112867385, 1.000000000000000000, 0.9238795325112867385, 1.000000000000000000, 0.9238795325112867385, 1.000000000000000000, 0.9238795325112867385, 1.000000000000000000, 0.9238795325112867385, 1.000000000000000000, 0.9238795325112867385, 1.000000000000000000, 0.9238795325112867385, 1.000000000000000000, 0.9238795325112867385, 1.000000000000000000, 0.9238795325112867385, 1.000000000000000000, 0.9238795325112867385, 1.000000000000000000, 0.9238795325112867385, 1.000000000000000000, 0.9238795325112867385, 1.000000000000000000, 0.9238795325112867385, 1.000000000000000000, 0.9238795325112867385, 1.000000000000000000, 0.9238795325112867385, 1.000000000000000000, 0.9238795325112867385, 1.000000000000000000, 0.9238795325112867385, 1.000000000000000000, 0.9238795325112867385, 1.000000000000000000, 0.9238795325112867385, 1.000000000000000000, 0.9238795325112867385, 1.000000000000000000, 0.9238795325112867385, 1.000000000000000000, 0.9238795325112867385, 1.000000000000000000, 0.9238795325112867385, 1.000000000000000000, 0.9238795325112867385, 1.000000000000000000, 0.9238795325112867385, 1.000000000000000000, 0.9238795325112867385, 1.000000000000000000, 0.9238795325112867385, 1.000000000000000000, 0.9238795325112867385, 1.000000000000000000, 0.9238795325112867385, 1.000000000000000000, 0.9238795325112867385, 1.000000000000000000, 0.9238795325112867385, 1.000000000000000000, 0.9238795325112867385, 1.000000000000000000, 0.9238795325112867385, 1.000000000000000000, 0.9238795325112867385, 1.000000000000000000, 0.9238795325112867385, 1.000000000000000000, 0.9238795325112867385, 1.000000000000000000, 0.9238795325112867385, 1.000000000000000000, 0.9238795325112867385, 1.000000000000000000, 0.9238795325112867385, 1.000000000000000000, 0.9238795325112867385, 1.000000000000000000, 0.9238795325112867385, 1.000000000000000000, 0.9238795325112867385, 1.000000000000000000, 0.9238795325112867385, 1.000000000000000000, 0.9238795325112867385, 1.000000000000000000, 0.9238795325112867385, 1.000000000000000000, 0.9238795325112867385, 1.000000000000000000, 0.9238795325112867385, 1.000000000000000000, 0.9238795325112867385, 1.000000000000000000, 0.9238795325112867385, 1.000000000000000000, 0.9238795325112867385, 1.000000000000000000, 0.9238795325112867385, 1.000000000000000000, 0.9238795325112867385, 1.000000000000000000, 0.9238795325112867385, 1.000000000000000000, 0.9238795325112867385, 1.000000000000000000, 0.9238795325112867385, 1.000000000000000000, 0.9238795325112867385, 1.000000000000000000, 0.9238795325112867385, 1.000000000000000000, 0.9238795325112867385, 1.000000000000000000, 0.9238795325112867385, 1.000000000000000000, 0.9238795325112867385, 1.000000000000000000, 0.9238795325112867385, 1.000000000000000000, 0.9238795325112867385, 1.000000000000000000, 0.9238795325112867385, 1.000000000000000000, 0.9238795325112867385, 1.000000000000000000, 0.9238795325112867385, 1.000000000000000000, 0.9238795325112867385, 1.000000000000000000, 0.9238795325112867385, 1.000000000000000000, 0.9238795325112867385, 1.000000000000000000, 0.9238795325112867385, 1.000000000000000000, 0.9238795325112867385, 1.000000000000000000, 0.9238795325112867385, 1.000000000000000000, 0.9238795325112867385, 1.000000000000000000, 0.9238795325112867385, 1.000000000000000000, 0.9238795325112867385, 1.000000000000000000, 0.9238795325112867385, 1.000000000000000000, 0.9238795325112867385, 1.000000000000000000, 0.9238795325112867385, 1.000000000000000000, 0.9238795325112867385, 1.000000000000000000, 0.9238795325112867385, 1.000000000000000000, 0.9238795325112867385, 1.000000000000000000, 0.9238795325112867385, 1.000000000000000000, 0.9238795325112867385, 1.000000000000000000, 0.9331730159288109672, 0.9836823002065551158 ) ) 
 REPRESENTATION_ITEM ( '' )  );
#12969=CARTESIAN_POINT ( 'NONE',  ( -0.3119999999999999996, 0.4277777776260448528, -3.820898013339742174E-17 ) ) ;
#12970=CARTESIAN_POINT ( 'NONE',  ( 0.2819296736111110424, 0.5527777777019112770, -0.1167790944451423119 ) ) ;
#12971=VERTEX_POINT ( 'NONE', #19452 ) ;
#12972=CARTESIAN_POINT ( 'NONE',  ( 1.726321361862525858E-17, 0.1743055554796889284, -0.2819296736111110979 ) ) ;
#12979=CARTESIAN_POINT ( 'NONE',  ( -0.2546317497922950812, 3.885572683902586366, -0.1803043470822305872 ) ) ;
#12980=CARTESIAN_POINT ( 'NONE',  ( 0.1167790944451423535, 0.2472222221463555580, 0.2819296736111110979 ) ) ;
#12981=CARTESIAN_POINT ( 'NONE',  ( -0.2819296736111110424, 0.004166666590800034188, -0.1167790944451423396 ) ) ;
#12982=CARTESIAN_POINT ( 'NONE',  ( -0.1167790944451423535, 4.432722222298088433, 0.2819296736111110424 ) ) ;
#12983=VERTEX_POINT ( 'NONE', #8226 ) ;
#12985=CARTESIAN_POINT ( 'NONE',  ( 0.2631688084094599978, 4.535002051990153937, -0.1700533999623941861 ) ) ;
#12986=CARTESIAN_POINT ( 'NONE',  ( 0.1167790944451422702, 5.071611111186976828, -0.2819296736111110424 ) ) ;
#12988=CARTESIAN_POINT ( 'NONE',  ( -0.1993543840281266355, 4.359805555631421470, 0.1993543840281267465 ) ) ;
#12989=CARTESIAN_POINT ( 'NONE',  ( 0.2225846330532430251, 3.759095655877711106, -0.2199039815225819205 ) ) ;
#12992=CARTESIAN_POINT ( 'NONE',  ( -0.3119999999999999996, 4.113277777929510215, 0.000000000000000000 ) ) ;
#12993=CARTESIAN_POINT ( 'NONE',  ( -0.1167790944451423535, 4.432722222298088433, 0.2819296736111110979 ) ) ;
#12997=ORIENTED_EDGE ( 'NONE', *, *, #14198, .T. ) ;
#13003=CARTESIAN_POINT ( 'NONE',  ( 0.3119999999999999996, 0.5666666665149336923, 0.000000000000000000 ) ) ;
#13006=CARTESIAN_POINT ( 'NONE',  ( -0.04033405356528133034, 5.128963404656787795, 0.3049483761492560174 ) ) ;
#13007=CARTESIAN_POINT ( 'NONE',  ( -0.2206173157302027954, 0.2611111111111107386, -0.2206173157302028232 ) ) ;
#13008=CARTESIAN_POINT ( 'NONE',  ( -0.2206173157302027954, 0.4833333333333329485, -0.2206173157302028232 ) ) ;
#13011=CARTESIAN_POINT ( 'NONE',  ( 0.3118346153924759778, 5.085807044887113548, -0.005734882727686576101 ) ) ;
#13014=CARTESIAN_POINT ( 'NONE',  ( 0.1167790944451422702, 4.168833333409199149, -0.2819296736111110424 ) ) ;
#13015=CARTESIAN_POINT ( 'NONE',  ( 0.1167790944451422702, 5.057722222298087544, -0.2819296736111110979 ) ) ;
#13018=CARTESIAN_POINT ( 'NONE',  ( 5.731347020009612645E-17, 3.786888888888888527, 0.3119999999999999996 ) ) ;
#13019=CARTESIAN_POINT ( 'NONE',  ( 5.731347020009612645E-17, 4.682722222373953969, 0.3119999999999999996 ) ) ;
#13020=CARTESIAN_POINT ( 'NONE',  ( 0.2819296736111110979, 5.120222222298088433, -0.1167790944451423396 ) ) ;
#13022=ORIENTED_EDGE ( 'NONE', *, *, #13812, .T. ) ;
#13025=CARTESIAN_POINT ( 'NONE',  ( 0.1416419608836146093, 0.04025187610558324247, -0.2530322881355697162 ) ) ;
#13030=CARTESIAN_POINT ( 'NONE',  ( -0.1993543840281266355, 5.137583333409198261, 0.1993543840281267465 ) ) ;
#13034=CARTESIAN_POINT ( 'NONE',  ( -0.1993543840281266633, 0.1812499999241333482, -0.1993543840281266910 ) ) ;
#13036=CARTESIAN_POINT ( 'NONE',  ( 0.1993543840281266633, 4.901472222298088433, -0.1993543840281266910 ) ) ;
#13037=CARTESIAN_POINT ( 'NONE',  ( 0.04820796449995154442, 5.072973651020436847, 0.3082531300064171864 ) ) ;
#13038=CARTESIAN_POINT ( 'NONE',  ( -0.2819296736111110979, 4.908416666742532186, 0.000000000000000000 ) ) ;
#13041=DIRECTION ( 'NONE',  ( -1.000000000000000000, 0.000000000000000000, 0.000000000000000000 ) ) ;
#13042=CARTESIAN_POINT ( 'NONE',  ( 0.1357687531234556544, 0.06249999999999967387, 0.2838640674724194901 ) ) ;
#13043=CARTESIAN_POINT ( 'NONE',  ( 0.3119999999999999996, 4.578555555555555046, -3.820898013339742174E-17 ) ) ;
#13044=CARTESIAN_POINT ( 'NONE',  ( 0.2819296736111110979, 3.939666666742531742, -0.1167790944451423396 ) ) ;
#13047=CARTESIAN_POINT ( 'NONE',  ( 0.3127134533877636846, 4.029674673160470455, 0.009354555642908121346 ) ) ;
#13050=EDGE_LOOP ( 'NONE', ( #6843, #13371, #21521, #19644 ) ) ;
#13051=EDGE_CURVE ( 'NONE', #10504, #14830, #8050, .T. ) ;
#13052=CARTESIAN_POINT ( 'NONE',  ( -0.2077028099651906379, 4.120735818351255020, 0.2358420112239252020 ) ) ;
#13060=CARTESIAN_POINT ( 'NONE',  ( -5.178964085587577574E-17, 0.2437499999241333204, 0.2819296736111110979 ) ) ;
#13061=CARTESIAN_POINT ( 'NONE',  ( 0.05085440012827255329, 3.875780013435167426, -0.3079968891009477461 ) ) ;
#13065=( BOUNDED_CURVE ( )  B_SPLINE_CURVE ( 2, ( #2663, #10113, #14239, #3022, #942, #4719, #13888, #12192, #19719, #831, #6434, #2775, #17898, #8259, #4606, #8372, #15939, #6551, #14001, #15823, #1193, #8625, #2891, #16070, #10351, #15709, #21674, #17775, #23607, #8499, #4959, #12426, #23123, #3139, #1313, #8737, #16193, #6921, #12068, #19482, #79, #18376, #3746, #11190, #13034, #7524, #5327, #22152, #10830, #3253, #16434, #18258, #12792, #1553, #20211, #23722, #9356, #16309, #9233, #12668, #21907, #16672, #3499, #10704, #22030, #14971, #23844, #1790, #1671, #20450, #10949, #3377, #7164, #20088, #7047, #24097, #12917, #5078, #19966, #7406, #20328, #3617, #14737, #18619, #11067, #12546, #1911, #9103, #8991, #18496, #14607, #23975, #16798, #18139, #1436, #8868, #14483, #5449, #14857, #16553, #7285, #22274, #5569, #5197, #17393, #20810, #2037, #20571, #9476, #13387, #22872, #17275, #19214, #7763, #20929, #7645, #4099, #3868, #15207, #11309, #2404, #22756, #8110, #22642, #17155, #560, #22516, #2165, #16909, #6167, #11432, #686, #5927, #4222, #15093, #11558, #9844, #6047, #13514, #13273, #20690, #22393, #11675, #19098, #5809, #18985, #7997, #15449, #2285, #9719, #13630, #445, #3981, #7876, #21048, #4338, #11789, #2521, #9963, #15326, #5694, #13157, #18742, #204, #18863, #9598, #17030, #324, #6772, #804, #12404 ),
 .UNSPECIFIED., .F., .F. ) 
 B_SPLINE_CURVE_WITH_KNOTS ( ( 3, 2, 2, 2, 2, 2, 2, 2, 2, 2, 2, 2, 2, 2, 2, 2, 2, 2, 2, 2, 2, 2, 2, 2, 2, 2, 2, 2, 2, 2, 2, 2, 2, 2, 2, 2, 2, 2, 2, 2, 2, 2, 2, 2, 2, 2, 2, 2, 2, 2, 2, 2, 2, 2, 2, 2, 2, 2, 2, 2, 2, 2, 2, 2, 2, 2, 2, 2, 2, 2, 2, 2, 2, 2, 2, 2, 2, 2, 2, 2, 2, 2, 2, 2, 2, 3 ),
 ( 0.05799230993249919475, 0.06250000000000000000, 0.07291666666666667129, 0.08333333333333332871, 0.09375000000000000000, 0.1041666666666666713, 0.1145833333333333287, 0.1250000000000000000, 0.1354166666666666574, 0.1458333333333333426, 0.1562500000000000000, 0.1666666666666666574, 0.1770833333333333426, 0.1875000000000000000, 0.1979166666666666852, 0.2083333333333333703, 0.2187500000000000000, 0.2291666666666666852, 0.2395833333333333703, 0.2500000000000000000, 0.2604166666666666852, 0.2708333333333333148, 0.2812500000000000000, 0.2916666666666666852, 0.3020833333333333148, 0.3125000000000000000, 0.3229166666666666852, 0.3333333333333333148, 0.3437500000000000000, 0.3541666666666666852, 0.3645833333333333148, 0.3750000000000000000, 0.3854166666666666852, 0.3958333333333333148, 0.4062500000000000000, 0.4166666666666666852, 0.4270833333333333148, 0.4375000000000000000, 0.4479166666666666852, 0.4583333333333333148, 0.4687500000000000000, 0.4791666666666666852, 0.4895833333333333148, 0.5000000000000000000, 0.5104166666666666297, 0.5208333333333333703, 0.5312500000000000000, 0.5416666666666666297, 0.5520833333333333703, 0.5625000000000000000, 0.5729166666666666297, 0.5833333333333333703, 0.5937500000000000000, 0.6041666666666666297, 0.6145833333333333703, 0.6250000000000000000, 0.6354166666666666297, 0.6458333333333333703, 0.6562500000000000000, 0.6666666666666666297, 0.6770833333333333703, 0.6875000000000000000, 0.6979166666666666297, 0.7083333333333333703, 0.7187500000000000000, 0.7291666666666666297, 0.7395833333333333703, 0.7500000000000000000, 0.7604166666666666297, 0.7708333333333333703, 0.7812500000000000000, 0.7916666666666666297, 0.8020833333333333703, 0.8125000000000000000, 0.8229166666666666297, 0.8333333333333333703, 0.8437500000000000000, 0.8541666666666666297, 0.8645833333333333703, 0.8750000000000000000, 0.8854166666666666297, 0.8958333333333333703, 0.9062500000000000000, 0.9166666666666666297, 0.9270833333333333703, 0.9375000000000000000 ),
 .UNSPECIFIED. ) 
 CURVE ( )  GEOMETRIC_REPRESENTATION_ITEM ( )  RATIONAL_B_SPLINE_CURVE ( ( 0.9626285260900115937, 0.9670597623776904239, 1.000000000000000000, 0.9238795325112867385, 1.000000000000000000, 0.9238795325112867385, 1.000000000000000000, 0.9238795325112867385, 1.000000000000000000, 0.9238795325112867385, 1.000000000000000000, 0.9238795325112867385, 1.000000000000000000, 0.9238795325112867385, 1.000000000000000000, 0.9238795325112867385, 1.000000000000000000, 0.9238795325112867385, 1.000000000000000000, 0.9238795325112867385, 1.000000000000000000, 0.9238795325112867385, 1.000000000000000000, 0.9238795325112867385, 1.000000000000000000, 0.9238795325112867385, 1.000000000000000000, 0.9238795325112867385, 1.000000000000000000, 0.9238795325112867385, 1.000000000000000000, 0.9238795325112867385, 1.000000000000000000, 0.9238795325112867385, 1.000000000000000000, 0.9238795325112867385, 1.000000000000000000, 0.9238795325112867385, 1.000000000000000000, 0.9238795325112867385, 1.000000000000000000, 0.9238795325112867385, 1.000000000000000000, 0.9238795325112867385, 1.000000000000000000, 0.9238795325112867385, 1.000000000000000000, 0.9238795325112867385, 1.000000000000000000, 0.9238795325112867385, 1.000000000000000000, 0.9238795325112867385, 1.000000000000000000, 0.9238795325112867385, 1.000000000000000000, 0.9238795325112867385, 1.000000000000000000, 0.9238795325112867385, 1.000000000000000000, 0.9238795325112867385, 1.000000000000000000, 0.9238795325112867385, 1.000000000000000000, 0.9238795325112867385, 1.000000000000000000, 0.9238795325112867385, 1.000000000000000000, 0.9238795325112867385, 1.000000000000000000, 0.9238795325112867385, 1.000000000000000000, 0.9238795325112867385, 1.000000000000000000, 0.9238795325112867385, 1.000000000000000000, 0.9238795325112867385, 1.000000000000000000, 0.9238795325112867385, 1.000000000000000000, 0.9238795325112867385, 1.000000000000000000, 0.9238795325112867385, 1.000000000000000000, 0.9238795325112867385, 1.000000000000000000, 0.9238795325112867385, 1.000000000000000000, 0.9238795325112867385, 1.000000000000000000, 0.9238795325112867385, 1.000000000000000000, 0.9238795325112867385, 1.000000000000000000, 0.9238795325112867385, 1.000000000000000000, 0.9238795325112867385, 1.000000000000000000, 0.9238795325112867385, 1.000000000000000000, 0.9238795325112867385, 1.000000000000000000, 0.9238795325112867385, 1.000000000000000000, 0.9238795325112867385, 1.000000000000000000, 0.9238795325112867385, 1.000000000000000000, 0.9238795325112867385, 1.000000000000000000, 0.9238795325112867385, 1.000000000000000000, 0.9238795325112867385, 1.000000000000000000, 0.9238795325112867385, 1.000000000000000000, 0.9238795325112867385, 1.000000000000000000, 0.9238795325112867385, 1.000000000000000000, 0.9238795325112867385, 1.000000000000000000, 0.9238795325112867385, 1.000000000000000000, 0.9238795325112867385, 1.000000000000000000, 0.9238795325112867385, 1.000000000000000000, 0.9238795325112867385, 1.000000000000000000, 0.9238795325112867385, 1.000000000000000000, 0.9238795325112867385, 1.000000000000000000, 0.9238795325112867385, 1.000000000000000000, 0.9238795325112867385, 1.000000000000000000, 0.9238795325112867385, 1.000000000000000000, 0.9238795325112867385, 1.000000000000000000, 0.9238795325112867385, 1.000000000000000000, 0.9238795325112867385, 1.000000000000000000, 0.9238795325112867385, 1.000000000000000000, 0.9238795325112867385, 1.000000000000000000, 0.9238795325112867385, 1.000000000000000000, 0.9238795325112867385, 1.000000000000000000, 0.9238795325112867385, 1.000000000000000000, 0.9238795325112867385, 1.000000000000000000, 0.9238795325112867385, 1.000000000000000000, 0.9238795325112867385, 1.000000000000000000, 0.9238795325112867385, 1.000000000000000000, 0.9238795325112867385, 1.000000000000000000, 0.9238795325112867385, 1.000000000000000000, 0.9238795325112867385, 1.000000000000000000, 0.9238795325112867385, 1.000000000000000000 ) ) 
 REPRESENTATION_ITEM ( '' )  );
#13068=CARTESIAN_POINT ( 'NONE',  ( 0.2206173157302027954, 4.363277777777777366, -0.2206173157302028232 ) ) ;
#13070=CARTESIAN_POINT ( 'NONE',  ( 0.3119999999999999996, 0.07361111111111078020, 0.000000000000000000 ) ) ;
#13071=CARTESIAN_POINT ( 'NONE',  ( 0.3119999999999999996, 5.075083333333332725, 0.1292346314604056190 ) ) ;
#13073=CARTESIAN_POINT ( 'NONE',  ( -0.1993543840281266355, 4.151472222298088433, 0.1993543840281267465 ) ) ;
#13074=DIRECTION ( 'NONE',  ( -0.000000000000000000, -1.000000000000000000, -0.000000000000000000 ) ) ;
#13078=CARTESIAN_POINT ( 'NONE',  ( -0.1993543840281266910, 4.845916666742532186, -0.1993543840281266910 ) ) ;
#13080=EDGE_CURVE ( 'NONE', #5177, #6611, #17404, .T. ) ;
#13084=CARTESIAN_POINT ( 'NONE',  ( 0.003929474433554183514, 3.710394323774880654, -0.3119787920919602220 ) ) ;
#13085=CARTESIAN_POINT ( 'NONE',  ( -0.1292346314604118085, 4.984805555555555934, -0.3119999999999938378 ) ) ;
#13087=CARTESIAN_POINT ( 'NONE',  ( -0.1167790944451423535, 4.585500000075865223, 0.2819296736111110979 ) ) ;
#13089=ADVANCED_FACE ( 'NONE', ( #8603 ), #3713, .T. ) ;
#13092=CARTESIAN_POINT ( 'NONE',  ( -0.1993543840281267465, 0.5284722221463555858, 0.1993543840281266633 ) ) ;
#13093=ORIENTED_EDGE ( 'NONE', *, *, #14388, .F. ) ;
#13095=CARTESIAN_POINT ( 'NONE',  ( -5.178964085587577574E-17, 0.2576388888130222155, 0.2819296736111110979 ) ) ;
#13096=CARTESIAN_POINT ( 'NONE',  ( -0.003672251724678134415, 4.710598665704982757, -0.3119999984746245070 ) ) ;
#13103=CARTESIAN_POINT ( 'NONE',  ( -0.1167790944451424506, 0.3513888888130222155, 0.2819296736111110424 ) ) ;
#13105=CARTESIAN_POINT ( 'NONE',  ( 0.2819296736111110979, 4.283416666742533074, -3.452642723725051716E-17 ) ) ;
#13107=CARTESIAN_POINT ( 'NONE',  ( 5.178964085587577574E-17, 5.158416666742532186, 0.2819296736111110979 ) ) ;
#13108=CARTESIAN_POINT ( 'NONE',  ( -0.2819296736111110979, 4.463972222298087544, 0.000000000000000000 ) ) ;
#13109=CARTESIAN_POINT ( 'NONE',  ( 0.04095097312172040621, 4.931542214948650305, -0.3099778603826239265 ) ) ;
#13112=CARTESIAN_POINT ( 'NONE',  ( -0.2206173157302027676, 4.009111111262843252, 0.2206173157302028787 ) ) ;
#13113=LINE ( 'NONE', #18694, #551 ) ;
#13121=CARTESIAN_POINT ( 'NONE',  ( -0.1363718491207122907, 4.845375667118064555, 0.2806196265496272435 ) ) ;
#13123=ORIENTED_EDGE ( 'NONE', *, *, #11553, .T. ) ;
#13124=CARTESIAN_POINT ( 'NONE',  ( -0.2206173157302027954, 0.5874999998482670627, -0.2206173157302028232 ) ) ;
#13134=CARTESIAN_POINT ( 'NONE',  ( 0.2573919081827345523, 5.080198807860221599, 0.1764520568086606067 ) ) ;
#13135=CARTESIAN_POINT ( 'NONE',  ( -0.3104533523723745359, 4.669988699611968386, 0.03789925079919458095 ) ) ;
#13136=CARTESIAN_POINT ( 'NONE',  ( 5.178964085587577574E-17, 4.255638888964754507, 0.2819296736111110979 ) ) ;
#13137=CARTESIAN_POINT ( 'NONE',  ( -0.1993543840281266355, 5.137583333409198261, 0.1993543840281267465 ) ) ;
#13140=CARTESIAN_POINT ( 'NONE',  ( 0.1292346314604056190, 3.866749999999999243, -0.3119999999999999996 ) ) ;
#13141=CARTESIAN_POINT ( 'NONE',  ( -0.1292346314604056745, 4.658416666818398610, -0.3119999999999999996 ) ) ;
#13142=CARTESIAN_POINT ( 'NONE',  ( 0.2819296736111111534, 5.168833333409199149, 0.1167790944451422563 ) ) ;
#13147=VECTOR ( 'NONE', #12947, 39.37007874015748143 ) ;
#13151=CARTESIAN_POINT ( 'NONE',  ( -0.2819296736111110979, 5.130638888964754507, 0.000000000000000000 ) ) ;
#13152=CARTESIAN_POINT ( 'NONE',  ( -0.1993543840281266355, 3.818138888964754507, 0.1993543840281267465 ) ) ;
#13153=CARTESIAN_POINT ( 'NONE',  ( 0.02036138964301281717, 4.405474440628344368, 0.3119999972693427437 ) ) ;
#13157=CARTESIAN_POINT ( 'NONE',  ( -0.1167790944451424506, 0.5874999999241332649, 0.2819296736111110424 ) ) ;
#13159=CARTESIAN_POINT ( 'NONE',  ( -1.726321361862525858E-17, 4.963972222298088433, -0.2819296736111110979 ) ) ;
#13161=CARTESIAN_POINT ( 'NONE',  ( 0.1993543840281267465, 4.873694444520309865, 0.1993543840281266633 ) ) ;
#13163=CARTESIAN_POINT ( 'NONE',  ( 2.268515911781130585E-06, 4.877166605860494109, -0.3120000000014063746 ) ) ;
#13164=CARTESIAN_POINT ( 'NONE',  ( -1.910449006669871087E-17, 4.092444444444444329, -0.3119999999999999996 ) ) ;
#13165=CARTESIAN_POINT ( 'NONE',  ( 5.253288188650943643E-17, 5.197747365142496356, 0.2859756893339090444 ) ) ;
#13166=CARTESIAN_POINT ( 'NONE',  ( -0.2206173157302027676, 4.557722222222221120, 0.2206173157302028787 ) ) ;
#13168=CARTESIAN_POINT ( 'NONE',  ( 0.2819296736111110979, 3.828555555631420582, -0.1167790944451423396 ) ) ;
#13169=CARTESIAN_POINT ( 'NONE',  ( -0.2206173157302027676, 4.224388888888888083, 0.2206173157302028787 ) ) ;
#13170=CARTESIAN_POINT ( 'NONE',  ( 0.1874014852520086982, 4.021786705011994201, 0.2494495279341875649 ) ) ;
#13171=FACE_OUTER_BOUND ( 'NONE', #15551, .T. ) ;
#13172=CARTESIAN_POINT ( 'NONE',  ( 0.1892591419382505802, 4.593624869007159717, -0.2515320889428918072 ) ) ;
#13176=CARTESIAN_POINT ( 'NONE',  ( 0.1641670432182899542, 4.150053599719361053, -0.2682616677331741695 ) ) ;
#13178=AXIS2_PLACEMENT_3D ( 'NONE', #16836, #14653, #9273 ) ;
#13180=CARTESIAN_POINT ( 'NONE',  ( 0.1518731547439844121, 5.135423329234196643, 0.2660310188109448193 ) ) ;
#13183=CARTESIAN_POINT ( 'NONE',  ( 0.2819296736111110424, 0.3166666665908000056, -0.1167790944451423119 ) ) ;
#13186=DIRECTION ( 'NONE',  ( 0.000000000000000000, 0.000000000000000000, -1.000000000000000000 ) ) ;
#13188=CARTESIAN_POINT ( 'NONE',  ( -0.08047735155459137535, 5.094302086351763847, -0.3013681618867503076 ) ) ;
#13189=CARTESIAN_POINT ( 'NONE',  ( -0.1292346314604044810, 4.727861111111109516, 0.3120000000000012208 ) ) ;
#13190=CARTESIAN_POINT ( 'NONE',  ( -0.1292346314604056190, 0.1465277777777774515, -0.3119999999999999996 ) ) ;
#13191=CARTESIAN_POINT ( 'NONE',  ( 0.2206173157302027954, 5.196611111111110404, -0.2206173157302028232 ) ) ;
#13193=CARTESIAN_POINT ( 'NONE',  ( 0.1993543840281267465, 4.165361111186976828, 0.1993543840281266633 ) ) ;
#13199=CARTESIAN_POINT ( 'NONE',  ( 0.2819296736111110979, 5.047305555631421470, -3.452642723725051716E-17 ) ) ;
#13204=CARTESIAN_POINT ( 'NONE',  ( 0.1167790944451424506, 4.648000000075865223, 0.2819296736111110424 ) ) ;
#13209=( BOUNDED_CURVE ( )  B_SPLINE_CURVE ( 2, ( #20287, #4263, #10904, #15486, #18334, #14689, #22107, #18450, #1746 ),
 .UNSPECIFIED., .F., .F. ) 
 B_SPLINE_CURVE_WITH_KNOTS ( ( 3, 2, 2, 2, 3 ),
 ( 0.6875000000000000000, 0.6979166666666666297, 0.7083333333333333703, 0.7187500000000000000, 0.7291666666666666297 ),
 .UNSPECIFIED. ) 
 CURVE ( )  GEOMETRIC_REPRESENTATION_ITEM ( )  RATIONAL_B_SPLINE_CURVE ( ( 1.000000000000000000, 0.9238795325112867385, 1.000000000000000000, 0.9238795325112867385, 1.000000000000000000, 0.9238795325112867385, 1.000000000000000000, 0.9238795325112867385, 1.000000000000000000 ) ) 
 REPRESENTATION_ITEM ( '' )  );
#13210=CARTESIAN_POINT ( 'NONE',  ( -0.1993543840281266633, 0.4590277777019111105, -0.1993543840281266910 ) ) ;
#13213=ORIENTED_EDGE ( 'NONE', *, *, #12930, .F. ) ;
#13214=CARTESIAN_POINT ( 'NONE',  ( 1.726321361862525858E-17, 0.2854166665908000056, -0.2819296736111110979 ) ) ;
#13216=FACE_OUTER_BOUND ( 'NONE', #13050, .T. ) ;
#13220=CARTESIAN_POINT ( 'NONE',  ( 0.1993543840281266910, 0.2645833332574666907, -0.1993543840281266910 ) ) ;
#13221=CARTESIAN_POINT ( 'NONE',  ( 0.2819296736111110424, 0.08749999992413336203, 0.1167790944451424923 ) ) ;
#13223=CARTESIAN_POINT ( 'NONE',  ( 0.2819296736111110979, 4.394527777853643791, -3.452642723725051716E-17 ) ) ;
#13225=CARTESIAN_POINT ( 'NONE',  ( 0.1167790944451424368, 4.939666666742532186, 0.2819296736111110424 ) ) ;
#13226=CARTESIAN_POINT ( 'NONE',  ( -0.2819296736111110979, 4.352861111186976828, 0.000000000000000000 ) ) ;
#13228=CARTESIAN_POINT ( 'NONE',  ( 0.1615724546837533915, 3.909701830292296787, 0.2693711506783711407 ) ) ;
#13229=CARTESIAN_POINT ( 'NONE',  ( -0.2206173157302027676, 4.175777777929510215, 0.2206173157302028787 ) ) ;
#13230=ADVANCED_FACE ( 'NONE', ( #5780 ), #20775, .T. ) ;
#13238=LINE ( 'NONE', #11392, #13582 ) ;
#13240=CARTESIAN_POINT ( 'NONE',  ( -0.1292346314604056190, 0.5284722220704892726, -0.3119999999999999996 ) ) ;
#13243=CARTESIAN_POINT ( 'NONE',  ( 0.05904265200914168149, 4.764370636974210704, -0.3065873589144272882 ) ) ;
#13245=LINE ( 'NONE', #3589, #19807 ) ;
#13248=AXIS2_PLACEMENT_3D ( 'NONE', #10485, #21565, #11969 ) ;
#13251=CARTESIAN_POINT ( 'NONE',  ( -0.2983457502834188646, 4.666223328268666037, -0.09148694476314270241 ) ) ;
#13252=CARTESIAN_POINT ( 'NONE',  ( 0.1167790944451422702, 3.891055555631421914, -0.2819296736111110424 ) ) ;
#13255=CARTESIAN_POINT ( 'NONE',  ( 0.2206173157302028787, 3.793833333333332725, 0.2206173157302027954 ) ) ;
#13257=CARTESIAN_POINT ( 'NONE',  ( 0.3119999999999999996, 4.804250000151731648, 0.1292346314604056190 ) ) ;
#13259=CARTESIAN_POINT ( 'NONE',  ( 0.1167790944451424506, 5.161888888964753619, 0.2819296736111110424 ) ) ;
#13260=CARTESIAN_POINT ( 'NONE',  ( 0.2819296736111110424, 4.217444444520310753, -0.1167790944451423396 ) ) ;
#13268=CARTESIAN_POINT ( 'NONE',  ( 0.1167790944451424368, 5.036888888964754507, 0.2819296736111110424 ) ) ;
#13269=CARTESIAN_POINT ( 'NONE',  ( -0.2819296736111110979, 3.922305555631421914, 0.000000000000000000 ) ) ;
#13270=CARTESIAN_POINT ( 'NONE',  ( 0.2152754385359916256, 4.411674947035939987, 0.2271887073179320593 ) ) ;
#13273=CARTESIAN_POINT ( 'NONE',  ( -0.1167790944451422702, 0.5111111110352445364, -0.2819296736111110979 ) ) ;
#13275=CARTESIAN_POINT ( 'NONE',  ( 0.2819296736111110424, 5.009111111186976828, -0.1167790944451423396 ) ) ;
#13277=CARTESIAN_POINT ( 'NONE',  ( 0.2819296736111110424, 4.939666666742532186, -0.1167790944451423396 ) ) ;
#13283=CARTESIAN_POINT ( 'NONE',  ( 0.2206173157302027954, 4.474388888888888083, -0.2206173157302028232 ) ) ;
#13284=CARTESIAN_POINT ( 'NONE',  ( 0.1900105704308386045, 5.206640035683666845, 0.2082794372640154323 ) ) ;
#13286=CARTESIAN_POINT ( 'NONE',  ( 0.1167790944451422702, 3.835500000075866112, -0.2819296736111110979 ) ) ;
#13287=DIRECTION ( 'NONE',  ( -0.000000000000000000, -1.000000000000000000, -0.000000000000000000 ) ) ;
#13288=CARTESIAN_POINT ( 'NONE',  ( 0.000000000000000000, 5.384999999999999787, 0.000000000000000000 ) ) ;
#13289=CARTESIAN_POINT ( 'NONE',  ( 0.000000000000000000, 5.384999999999999787, 0.000000000000000000 ) ) ;
#13290=DIRECTION ( 'NONE',  ( -0.000000000000000000, -1.000000000000000000, -0.000000000000000000 ) ) ;
#13291=CARTESIAN_POINT ( 'NONE',  ( -0.1462652582317430505, 4.103741065394783227, -0.2781719402188991275 ) ) ;
#13292=CARTESIAN_POINT ( 'NONE',  ( 0.09033206243994013063, 4.629811855264434506, 0.3017044624047845458 ) ) ;
#13295=CIRCLE ( 'NONE', #10948, 0.2495000000000007212 ) ;
#13296=CARTESIAN_POINT ( 'NONE',  ( 0.2496269975438151767, 4.313450179719811928, -0.1915744269021862900 ) ) ;
#13297=CARTESIAN_POINT ( 'NONE',  ( 0.1769619725182808578, 5.155811688406484627, -0.2434508416669157460 ) ) ;
#13300=CARTESIAN_POINT ( 'NONE',  ( 0.2819296736111110424, 0.5319444443685777957, 0.1167790944451424923 ) ) ;
#13301=CARTESIAN_POINT ( 'NONE',  ( -7.892860322346445127E-13, 5.206640035683665957, 0.2819296736111106538 ) ) ;
#13307=CARTESIAN_POINT ( 'NONE',  ( -0.1292346314604058410, 0.2229166666666664021, 0.3119999999999998885 ) ) ;
#13308=CARTESIAN_POINT ( 'NONE',  ( 0.1292346314604058410, 5.123694444444443441, 0.3119999999999998885 ) ) ;
#13309=CARTESIAN_POINT ( 'NONE',  ( 0.2819296736111110979, 4.168833333409199149, 0.1167790944451422425 ) ) ;
#13314=CARTESIAN_POINT ( 'NONE',  ( 0.1167790944451422702, 4.891055555631421470, -0.2819296736111110424 ) ) ;
#13315=CARTESIAN_POINT ( 'NONE',  ( 0.2346572839409867828, 4.190181929725985022, 0.2066278427949707619 ) ) ;
#13318=CARTESIAN_POINT ( 'NONE',  ( -0.2819296736111110979, 4.686194444520309865, 0.000000000000000000 ) ) ;
#13321=CARTESIAN_POINT ( 'NONE',  ( 0.2819296736111110979, 0.6048611110352445364, 0.000000000000000000 ) ) ;
#13323=CARTESIAN_POINT ( 'NONE',  ( 0.2819296736111110979, 0.4937499999241333204, 0.000000000000000000 ) ) ;
#13325=CYLINDRICAL_SURFACE ( 'NONE', #4304, 0.3119999999999999996 ) ;
#13331=CARTESIAN_POINT ( 'NONE',  ( 0.2819296736111110979, 0.2576388888130222155, 0.000000000000000000 ) ) ;
#13332=CARTESIAN_POINT ( 'NONE',  ( -0.1167790944451424368, 0.1847222221463556413, 0.2819296736111110424 ) ) ;
#13334=CARTESIAN_POINT ( 'NONE',  ( 0.1167790944451424368, 4.328555555631420582, 0.2819296736111110424 ) ) ;
#13336=CARTESIAN_POINT ( 'NONE',  ( -0.2819296736111110979, 4.977861111186976828, 0.000000000000000000 ) ) ;
#13337=CARTESIAN_POINT ( 'NONE',  ( 5.178964085587577574E-17, 4.533416666742532186, 0.2819296736111110979 ) ) ;
#13340=CARTESIAN_POINT ( 'NONE',  ( -0.1292346314604056745, 4.158416666818398610, -0.3119999999999999996 ) ) ;
#13342=ORIENTED_EDGE ( 'NONE', *, *, #22582, .F. ) ;
#13352=CARTESIAN_POINT ( 'NONE',  ( -0.3119999999999999996, 0.5979166665149336923, 0.1292346314604056190 ) ) ;
#13355=CARTESIAN_POINT ( 'NONE',  ( 0.000000000000000000, 5.384999999999999787, -0.3119999999999999996 ) ) ;
#13356=CARTESIAN_POINT ( 'NONE',  ( 0.02086467461746857599, 4.765462960542953041, -0.3114012365584180042 ) ) ;
#13360=ORIENTED_EDGE ( 'NONE', *, *, #2235, .F. ) ;
#13364=CARTESIAN_POINT ( 'NONE',  ( -0.1993543840281266355, 3.915361111186976384, 0.1993543840281267465 ) ) ;
#13365=CARTESIAN_POINT ( 'NONE',  ( 0.2206290632986846467, 5.036984000381125703, -0.2218005928150467154 ) ) ;
#13366=CARTESIAN_POINT ( 'NONE',  ( -0.1292346314604093660, 4.818138888888888083, -0.3119999999999962803 ) ) ;
#13367=CARTESIAN_POINT ( 'NONE',  ( 0.1988757138996042617, 3.752970977545328601, -0.2404006040361021113 ) ) ;
#13368=CARTESIAN_POINT ( 'NONE',  ( 0.3119999999999999996, 4.696611111262843252, -3.820898013339742174E-17 ) ) ;
#13370=CARTESIAN_POINT ( 'NONE',  ( -1.726321361862525858E-17, 4.908416666742532186, -0.2819296736111110979 ) ) ;
#13371=ORIENTED_EDGE ( 'NONE', *, *, #12493, .T. ) ;
#13372=EDGE_CURVE ( 'NONE', #6049, #21992, #11817, .T. ) ;
#13373=CARTESIAN_POINT ( 'NONE',  ( 0.1167790944451422702, 4.279944444520310753, -0.2819296736111110424 ) ) ;
#13374=ORIENTED_EDGE ( 'NONE', *, *, #15539, .T. ) ;
#13377=ORIENTED_EDGE ( 'NONE', *, *, #11870, .T. ) ;
#13381=CARTESIAN_POINT ( 'NONE',  ( -0.1167790944451423535, 3.932722222298087988, 0.2819296736111110979 ) ) ;
#13385=ORIENTED_EDGE ( 'NONE', *, *, #8726, .T. ) ;
#13387=CARTESIAN_POINT ( 'NONE',  ( -0.2819296736111110979, 0.4069444443685778512, -0.1167790944451423396 ) ) ;
#13390=CARTESIAN_POINT ( 'NONE',  ( 0.1167790944451422702, 5.016055555631420582, -0.2819296736111110424 ) ) ;
#13391=CARTESIAN_POINT ( 'NONE',  ( 0.2496181645126293036, 4.468611226231085531, 0.1915855071014845590 ) ) ;
#13392=CARTESIAN_POINT ( 'NONE',  ( -0.2819296736111110424, 4.627166666742532186, -0.1167790944451423119 ) ) ;
#13394=CARTESIAN_POINT ( 'NONE',  ( 0.2099978738425454516, 4.855935259588629371, 0.2307503733689650338 ) ) ;
#13397=CARTESIAN_POINT ( 'NONE',  ( -1.910449006669871087E-17, 4.425777777777777366, -0.3119999999999999996 ) ) ;
#13398=CARTESIAN_POINT ( 'NONE',  ( 5.178964085587577574E-17, 3.811194444520309865, 0.2819296736111110979 ) ) ;
#13399=CARTESIAN_POINT ( 'NONE',  ( 0.3119999999999998885, 0.3409722220704892726, 0.1292346314604058410 ) ) ;
#13401=ORIENTED_EDGE ( 'NONE', *, *, #8496, .F. ) ;
#13402=CARTESIAN_POINT ( 'NONE',  ( 0.3109988355630948775, 4.584817533366577713, 0.02498716424996858324 ) ) ;
#13408=CARTESIAN_POINT ( 'NONE',  ( -0.3038794427342524362, 3.944299538033225527, -0.08166546517153733253 ) ) ;
#13410=ORIENTED_EDGE ( 'NONE', *, *, #10342, .T. ) ;
#13412=CARTESIAN_POINT ( 'NONE',  ( 1.726321361862525858E-17, 0.4937499999241333759, -0.2819296736111110979 ) ) ;
#13418=VERTEX_POINT ( 'NONE', #18953 ) ;
#13419=CARTESIAN_POINT ( 'NONE',  ( -0.04423000916681948252, 4.625947756500051078, 0.3119999933242569301 ) ) ;
#13422=CARTESIAN_POINT ( 'NONE',  ( 0.1292346314604056745, 0.3062499999999996336, -0.3119999999999999996 ) ) ;
#13423=CARTESIAN_POINT ( 'NONE',  ( 0.5496543701456371167, 3.720840944996751887, 0.08881361666993904669 ) ) ;
#13425=CARTESIAN_POINT ( 'NONE',  ( 0.2819296736111110979, 4.227861111186976828, -3.452642723725051716E-17 ) ) ;
#13426=CARTESIAN_POINT ( 'NONE',  ( -0.04081697132525561461, 4.348175715971974498, 0.3120000054304696846 ) ) ;
#13428=FACE_OUTER_BOUND ( 'NONE', #1664, .T. ) ;
#13430=ORIENTED_EDGE ( 'NONE', *, *, #19549, .F. ) ;
#13432=CARTESIAN_POINT ( 'NONE',  ( 0.1993543840281267465, 4.818138888964754507, 0.1993543840281266633 ) ) ;
#13437=CARTESIAN_POINT ( 'NONE',  ( 0.1395004180248995140, 3.706493199255800786, -0.2813810779009488505 ) ) ;
#13440=CARTESIAN_POINT ( 'NONE',  ( 5.178964085587577574E-17, 4.213972222298087544, 0.2819296736111110979 ) ) ;
#13442=CARTESIAN_POINT ( 'NONE',  ( -0.2023794242524271647, 4.050101341561973989, -0.2374638867795466346 ) ) ;
#13445=LINE ( 'NONE', #20863, #10661 ) ;
#13447=CARTESIAN_POINT ( 'NONE',  ( -0.2819296736111110979, 0.5215277777019111660, -3.452642723725051716E-17 ) ) ;
#13448=DIRECTION ( 'NONE',  ( -0.000000000000000000, -1.000000000000000000, -0.000000000000000000 ) ) ;
#13453=CARTESIAN_POINT ( 'NONE',  ( 0.1292346314604045920, 5.012583333333331836, 0.3120000000000012208 ) ) ;
#13454=CARTESIAN_POINT ( 'NONE',  ( 0.1993543840281266355, 0.5284722221463555858, 0.1993543840281267465 ) ) ;
#13455=B_SPLINE_CURVE_WITH_KNOTS ( 'NONE', 3,
 ( #2116, #22717, #20413, #9557, #18585, #9318, #16758, #14934, #22353, #5657, #13121, #11272, #18703, #2002, #9439, #163, #7605, #8894, #15972, #17924, #18040, #4745, #6700, #1219, #21702, #10382, #19991, #17683, #23151, #10731, #6949, #12450, #6462, #12099, #18162, #23631, #13916, #6824, #19869, #23270, #8528, #21574, #4868, #8647, #16095, #12216, #10494, #3161, #1096, #14265, #4985 ),
 .UNSPECIFIED., .F., .F.,
 ( 4, 2, 2, 2, 1, 1, 2, 2, 1, 2, 2, 2, 2, 1, 1, 2, 2, 2, 2, 2, 2, 2, 2, 2, 1, 1, 1, 1, 2, 4 ),
 ( 0.2471660779490366389, 0.2482799422568952308, 0.2488368744108245545, 0.2491153404877891886, 0.2492545735262715334, 0.2493241900455126780, 0.2493589983051332781, 0.2493764024349435504, 0.2493938065647538505, 0.2516215351804711453, 0.2538492637961884957, 0.2549631281040471431, 0.2560769924119057905, 0.2562162254503881353, 0.2562858419696293355, 0.2563206502292498801, 0.2563554584888704801, 0.2566339245658351698, 0.2571908567197644935, 0.2583047210276230854, 0.2605324496433403803, 0.2627601782590576751, 0.2638740425669163225, 0.2644309747208456463, 0.2647094407978103359, 0.2648486738362926252, 0.2649182903555338253, 0.2649530986151543699, 0.2649705027449646977, 0.2649879068747749700 ),
 .UNSPECIFIED. ) ;
#13456=CARTESIAN_POINT ( 'NONE',  ( 0.1167790944451423257, 0.1569444443685778234, -0.2819296736111110424 ) ) ;
#13457=CARTESIAN_POINT ( 'NONE',  ( -0.2819296736111110979, 4.255638888964754507, 0.000000000000000000 ) ) ;
#13460=CARTESIAN_POINT ( 'NONE',  ( -0.1993543840281266910, 4.859805555631421470, -0.1993543840281266910 ) ) ;
#13461=CARTESIAN_POINT ( 'NONE',  ( 0.1993543840281266633, 4.276472222298087544, -0.1993543840281266910 ) ) ;
#13462=EDGE_CURVE ( 'NONE', #19562, #11776, #11642, .T. ) ;
#13465=CARTESIAN_POINT ( 'NONE',  ( 0.2206173157302028787, 3.967444444596176734, 0.2206173157302027954 ) ) ;
#13466=CARTESIAN_POINT ( 'NONE',  ( 0.2206173157302028232, 0.1361111111111107663, -0.2206173157302028232 ) ) ;
#13478=CARTESIAN_POINT ( 'NONE',  ( 0.1292346314604056745, 0.4659722220704892726, -0.3119999999999999996 ) ) ;
#13484=CARTESIAN_POINT ( 'NONE',  ( 0.1712376643660483699, 5.185778304708162700, -0.2353596117731020232 ) ) ;
#13490=CARTESIAN_POINT ( 'NONE',  ( 5.178964085587577574E-17, 3.977861111186976384, 0.2819296736111110979 ) ) ;
#13492=CARTESIAN_POINT ( 'NONE',  ( 0.09872962232722692910, 5.120942621315136556, 0.2927443173902372076 ) ) ;
#13493=CARTESIAN_POINT ( 'NONE',  ( -0.2541070255160559066, 5.173678042950717426, -0.1516883682263707178 ) ) ;
#13495=CARTESIAN_POINT ( 'NONE',  ( -0.1292346314604057023, 4.790361111262843252, 0.3119999999999998885 ) ) ;
#13496=CARTESIAN_POINT ( 'NONE',  ( -0.1993543840281266355, 4.929250000075866112, 0.1993543840281267465 ) ) ;
#13497=ORIENTED_EDGE ( 'NONE', *, *, #20764, .F. ) ;
#13498=CARTESIAN_POINT ( 'NONE',  ( -0.1167790944451423257, 4.231333333409199149, -0.2819296736111110424 ) ) ;
#13508=CARTESIAN_POINT ( 'NONE',  ( -0.1993543840281266910, 3.859805555631421470, -0.1993543840281266910 ) ) ;
#13509=AXIS2_PLACEMENT_3D ( 'NONE', #3316, #22093, #10890 ) ;
#13510=CARTESIAN_POINT ( 'NONE',  ( 0.3140227130263654187, 4.419434873055135604, -0.01898951124202318680 ) ) ;
#13514=CARTESIAN_POINT ( 'NONE',  ( 1.726321361862525858E-17, 0.5076388888130222155, -0.2819296736111110979 ) ) ;
#13517=CARTESIAN_POINT ( 'NONE',  ( -0.1993543840281266355, 4.707027777853643791, 0.1993543840281267465 ) ) ;
#13519=CARTESIAN_POINT ( 'NONE',  ( 0.1993543840281266633, 4.776472222298087544, -0.1993543840281266910 ) ) ;
#13520=CARTESIAN_POINT ( 'NONE',  ( 3.887228417612631703E-07, 4.154944433789834690, -0.3119999999997578044 ) ) ;
#13521=( BOUNDED_CURVE ( )  B_SPLINE_CURVE ( 2, ( #4709, #10337, #17763, #3009, #10460, #23348, #17886, #22723, #4066 ),
 .UNSPECIFIED., .F., .F. ) 
 B_SPLINE_CURVE_WITH_KNOTS ( ( 3, 2, 2, 2, 3 ),
 ( 0.3839285714285713969, 0.3883928571428570953, 0.3928571428571427937, 0.3973214285714284921, 0.4017857142857142461 ),
 .UNSPECIFIED. ) 
 CURVE ( )  GEOMETRIC_REPRESENTATION_ITEM ( )  RATIONAL_B_SPLINE_CURVE ( ( 1.000000000000000888, 0.9238795325112857393, 1.000000000000000000, 0.9238795325112867385, 1.000000000000000000, 0.9238795325112867385, 1.000000000000000000, 0.9238795325112877377, 0.9999999999999990008 ) ) 
 REPRESENTATION_ITEM ( '' )  );
#13526=CARTESIAN_POINT ( 'NONE',  ( -0.2206173157302028232, 4.377166666666665762, -0.2206173157302028232 ) ) ;
#13528=CARTESIAN_POINT ( 'NONE',  ( 0.2819296736111110979, 3.825083333409198705, -3.452642723725051716E-17 ) ) ;
#13531=CARTESIAN_POINT ( 'NONE',  ( 0.3053277220128169378, 4.587655388424375147, -0.07727936894157313996 ) ) ;
#13532=ORIENTED_EDGE ( 'NONE', *, *, #12175, .F. ) ;
#13534=CARTESIAN_POINT ( 'NONE',  ( -1.296004783052830448E-07, 4.710500003633881327, -0.3119999999999730766 ) ) ;
#13535=CARTESIAN_POINT ( 'NONE',  ( 0.002698052836345287992, 4.654867065270698490, -0.3119899994661654574 ) ) ;
#13541=CARTESIAN_POINT ( 'NONE',  ( -5.178964085587577574E-17, 0.4659722221463555858, 0.2819296736111110979 ) ) ;
#13542=CARTESIAN_POINT ( 'NONE',  ( 0.08166507714107607008, 3.851613536341646160, 0.3038795024021940239 ) ) ;
#13547=CARTESIAN_POINT ( 'NONE',  ( -0.2669838093744815177, 4.608413313809449185, -0.1638134789338530906 ) ) ;
#13550=CARTESIAN_POINT ( 'NONE',  ( 0.2206173157302028232, 0.1361111111111107663, -0.2206173157302028232 ) ) ;
#13551=CARTESIAN_POINT ( 'NONE',  ( -0.2206173157302028232, 5.154944444444443441, -0.2206173157302028232 ) ) ;
#13552=CARTESIAN_POINT ( 'NONE',  ( -0.2819296736111110424, 4.196611111186976828, -0.1167790944451423119 ) ) ;
#13556=ORIENTED_EDGE ( 'NONE', *, *, #1913, .F. ) ;
#13559=ADVANCED_FACE ( 'NONE', ( #8570 ), #16011, .T. ) ;
#13560=CARTESIAN_POINT ( 'NONE',  ( 0.1167790944451422702, 4.835500000075865223, -0.2819296736111110424 ) ) ;
#13562=CARTESIAN_POINT ( 'NONE',  ( -0.07787416272928887606, 5.165394585812085992, 0.2883211566397950176 ) ) ;
#13566=CARTESIAN_POINT ( 'NONE',  ( 0.01571813568754789822, 3.710075998628030725, -0.3116604989128209935 ) ) ;
#13567=DIRECTION ( 'NONE',  ( 0.000000000000000000, 0.000000000000000000, -1.000000000000000000 ) ) ;
#13568=CARTESIAN_POINT ( 'NONE',  ( -0.2819296736111110424, 4.370222222298088433, 0.1167790944451424923 ) ) ;
#13570=CARTESIAN_POINT ( 'NONE',  ( -0.2827572605903787006, 4.061666605139203412, 0.1376332577019660497 ) ) ;
#13572=DIRECTION ( 'NONE',  ( 0.000000000000000000, 0.000000000000000000, -1.000000000000000000 ) ) ;
#13573=CARTESIAN_POINT ( 'NONE',  ( -0.1993543840281266633, 0.3479166665908000611, -0.1993543840281266910 ) ) ;
#13574=DIRECTION ( 'NONE',  ( -0.000000000000000000, -1.000000000000000000, -0.000000000000000000 ) ) ;
#13579=CARTESIAN_POINT ( 'NONE',  ( 0.1167790944451423535, 0.4138888888130222155, 0.2819296736111110979 ) ) ;
#13580=CARTESIAN_POINT ( 'NONE',  ( -0.2819296736111110979, 0.1222222221463555719, 0.1167790944451422425 ) ) ;
#13581=CARTESIAN_POINT ( 'NONE',  ( 0.1993543840281267465, 4.276472222298088433, 0.1993543840281266633 ) ) ;
#13582=VECTOR ( 'NONE', #24061, 39.37007874015748143 ) ;
#13584=CARTESIAN_POINT ( 'NONE',  ( 0.1993543840281267465, 4.943138888964754507, 0.1993543840281266633 ) ) ;
#13585=CARTESIAN_POINT ( 'NONE',  ( -1.726321361862525858E-17, 4.116750000075865223, -0.2819296736111110979 ) ) ;
#13586=DIRECTION ( 'NONE',  ( -0.000000000000000000, -1.000000000000000000, -0.000000000000000000 ) ) ;
#13588=CARTESIAN_POINT ( 'NONE',  ( 0.3120000000000000551, 4.519527777777776478, 0.1292346314604056190 ) ) ;
#13589=CARTESIAN_POINT ( 'NONE',  ( -0.3119999999999998885, 3.950083333485065573, 0.1292346314604058410 ) ) ;
#13595=CARTESIAN_POINT ( 'NONE',  ( -0.2228772273359933276, 5.009026790445733290, 0.2183502748428790829 ) ) ;
#13597=CARTESIAN_POINT ( 'NONE',  ( 0.2819296736111110424, -0.002777777853644406401, -0.1167790944451423119 ) ) ;
#13599=CARTESIAN_POINT ( 'NONE',  ( 0.2846063461394666150, 4.255906380294286251, -0.1278434303317485254 ) ) ;
#13603=CARTESIAN_POINT ( 'NONE',  ( 0.07617771740037646011, 5.188451671420351907, -0.2803169692743197605 ) ) ;
#13604=ORIENTED_EDGE ( 'NONE', *, *, #22118, .F. ) ;
#13607=CARTESIAN_POINT ( 'NONE',  ( -0.03922894998300566205, 4.681526571591189345, 0.3120000079934041604 ) ) ;
#13609=CARTESIAN_POINT ( 'NONE',  ( 0.1167790944451424368, 4.036888888964754507, 0.2819296736111110424 ) ) ;
#13611=CARTESIAN_POINT ( 'NONE',  ( -0.1031275500757723590, 5.166304435049627664, -0.2794537332880138725 ) ) ;
#13612=CARTESIAN_POINT ( 'NONE',  ( -0.1292346314604056745, 4.436194444596177178, -0.3119999999999999996 ) ) ;
#13613=CARTESIAN_POINT ( 'NONE',  ( -0.1993543840281266355, 4.873694444520310753, 0.1993543840281267465 ) ) ;
#13615=CARTESIAN_POINT ( 'NONE',  ( 0.1167790944451422702, 4.224388888964755395, -0.2819296736111110424 ) ) ;
#13625=ADVANCED_FACE ( 'NONE', ( #1135 ), #11485, .T. ) ;
#13626=CARTESIAN_POINT ( 'NONE',  ( 0.1081575060082094752, 4.408054576103176636, 0.2929456441888016460 ) ) ;
#13630=CARTESIAN_POINT ( 'NONE',  ( 0.2819296736111110979, 0.5493055554796889561, 0.000000000000000000 ) ) ;
#13632=ORIENTED_EDGE ( 'NONE', *, *, #14082, .T. ) ;
#13633=CARTESIAN_POINT ( 'NONE',  ( 0.1167790944451424368, 4.773000000075866112, 0.2819296736111110424 ) ) ;
#13636=CARTESIAN_POINT ( 'NONE',  ( -0.1993543840281266910, 4.734805555631420582, -0.1993543840281266910 ) ) ;
#13637=CARTESIAN_POINT ( 'NONE',  ( -0.02540882200436479776, 4.155671449734249734, -0.3110052518984787739 ) ) ;
#13638=CARTESIAN_POINT ( 'NONE',  ( 0.1409648704857156543, 4.853596617052923001, 0.2789902241728853260 ) ) ;
#13641=CARTESIAN_POINT ( 'NONE',  ( 0.3119999999999999996, 4.186194444444444329, 0.1292346314604056190 ) ) ;
#13642=CARTESIAN_POINT ( 'NONE',  ( -0.1993543840281266910, 3.790361111186976828, -0.1993543840281266910 ) ) ;
#13646=CARTESIAN_POINT ( 'NONE',  ( 0.3104769350984191711, 4.584653674997469786, 0.03084955884225352996 ) ) ;
#13647=ORIENTED_EDGE ( 'NONE', *, *, #19318, .T. ) ;
#13648=CARTESIAN_POINT ( 'NONE',  ( 0.2859729506740118499, 4.700254050761267344, -0.1247996014322190345 ) ) ;
#13656=( BOUNDED_CURVE ( )  B_SPLINE_CURVE ( 2, ( #3640, #20109, #16092, #1574, #21926, #7306, #9129, #8891, #9012 ),
 .UNSPECIFIED., .F., .F. ) 
 B_SPLINE_CURVE_WITH_KNOTS ( ( 3, 2, 2, 2, 3 ),
 ( 0.1500366067892652533, 0.1562500000000000000, 0.1666666666666666574, 0.1770833333333333426, 0.1875000000000000000 ),
 .UNSPECIFIED. ) 
 CURVE ( )  GEOMETRIC_REPRESENTATION_ITEM ( )  RATIONAL_B_SPLINE_CURVE ( ( 0.9633570531806863180, 0.9545952259943366602, 1.000000000000000000, 0.9238795325112867385, 1.000000000000000000, 0.9238795325112867385, 1.000000000000000000, 0.9238795325112867385, 1.000000000000000000 ) ) 
 REPRESENTATION_ITEM ( '' )  );
#13659=CARTESIAN_POINT ( 'NONE',  ( 0.1167790944451423535, 0.5249999999241333759, 0.2819296736111110424 ) ) ;
#13660=FACE_OUTER_BOUND ( 'NONE', #7607, .T. ) ;
#13666=CARTESIAN_POINT ( 'NONE',  ( -0.1582747645997409358, 4.622434822458711068, 0.2689245564580552972 ) ) ;
#13669=CARTESIAN_POINT ( 'NONE',  ( -0.1292346314604056190, 0.2576388888888885287, -0.3119999999999999996 ) ) ;
#13670=CARTESIAN_POINT ( 'NONE',  ( 5.731347020009612645E-17, 4.953555555555554157, 0.3119999999999999996 ) ) ;
#13671=CARTESIAN_POINT ( 'NONE',  ( -1.726321361862525858E-17, 4.075083333409199149, -0.2819296736111110979 ) ) ;
#13672=CARTESIAN_POINT ( 'NONE',  ( -0.1916416111016578661, 4.343568013825621854, 0.2495666673098946020 ) ) ;
#13675=VERTEX_POINT ( 'NONE', #12305 ) ;
#13676=ORIENTED_EDGE ( 'NONE', *, *, #22775, .T. ) ;
#13678=CARTESIAN_POINT ( 'NONE',  ( -0.2819296736111110424, 4.745222222298088433, 0.1167790944451424923 ) ) ;
#13680=AXIS2_PLACEMENT_3D ( 'NONE', #6055, #15571, #18870 ) ;
#13681=CARTESIAN_POINT ( 'NONE',  ( -0.2206173157302028232, 4.099388888888888083, -0.2206173157302028232 ) ) ;
#13685=CARTESIAN_POINT ( 'NONE',  ( -1.726321361862525858E-17, 4.352861111186976828, -0.2819296736111110979 ) ) ;
#13689=CARTESIAN_POINT ( 'NONE',  ( -0.1993543840281266633, 0.4034722221463555858, -0.1993543840281266910 ) ) ;
#13694=EDGE_CURVE ( 'NONE', #6119, #7025, #13065, .T. ) ;
#13697=CARTESIAN_POINT ( 'NONE',  ( -5.178964085587577574E-17, 0.4104166665908000056, 0.2819296736111110979 ) ) ;
#13698=CARTESIAN_POINT ( 'NONE',  ( 0.1993543840281266355, 0.1395833332574667185, 0.1993543840281267465 ) ) ;
#13699=AXIS2_PLACEMENT_3D ( 'NONE', #1327, #18273, #12933 ) ;
#13700=CARTESIAN_POINT ( 'NONE',  ( -0.1167790944451423535, 4.043833333409200037, 0.2819296736111110424 ) ) ;
#13702=CARTESIAN_POINT ( 'NONE',  ( 0.1167790944451422702, 4.849388888964755395, -0.2819296736111110424 ) ) ;
#13703=CARTESIAN_POINT ( 'NONE',  ( 0.1292346314604056745, 0.4104166665149337478, -0.3119999999999999996 ) ) ;
#13705=CYLINDRICAL_SURFACE ( 'NONE', #8557, 0.3119999999999999996 ) ;
#13706=CARTESIAN_POINT ( 'NONE',  ( -0.1292346314604057023, 3.901472222373954857, 0.3119999999999998885 ) ) ;
#13714=CARTESIAN_POINT ( 'NONE',  ( 0.1993543840281266910, 0.05624999992413336897, -0.1993543840281266910 ) ) ;
#13718=CARTESIAN_POINT ( 'NONE',  ( 0.04915613994164541589, 4.073065570104705380, 0.3089926667392805526 ) ) ;
#13723=DIRECTION ( 'NONE',  ( 0.000000000000000000, 0.000000000000000000, -1.000000000000000000 ) ) ;
#13724=CARTESIAN_POINT ( 'NONE',  ( 0.1167790944451422702, 3.946611111186976384, -0.2819296736111110424 ) ) ;
#13726=CARTESIAN_POINT ( 'NONE',  ( -0.01909785675588383455, 5.196999109626997182, 0.2863020908690515620 ) ) ;
#13727=CARTESIAN_POINT ( 'NONE',  ( -0.2206173157302028232, 4.606333333485065573, -0.2206173157302028232 ) ) ;
#13728=CARTESIAN_POINT ( 'NONE',  ( 0.2819296736111110979, 4.842444444520309865, -0.1167790944451423396 ) ) ;
#13730=CARTESIAN_POINT ( 'NONE',  ( 5.178964085587577574E-17, 3.977861111186976384, 0.2819296736111110979 ) ) ;
#13738=CARTESIAN_POINT ( 'NONE',  ( -5.731347020009612645E-17, 0.05277777762604484585, 0.3119999999999999996 ) ) ;
#13739=CARTESIAN_POINT ( 'NONE',  ( 0.2629417729398952353, 5.140591734628677578, 0.1550161288497664824 ) ) ;
#13740=CARTESIAN_POINT ( 'NONE',  ( 0.2206173157302027676, 0.1708333331816004053, 0.2206173157302028787 ) ) ;
#13742=CARTESIAN_POINT ( 'NONE',  ( 0.09694982473845883963, 0.06249891840240667101, 0.2965547697865978938 ) ) ;
#13744=CARTESIAN_POINT ( 'NONE',  ( -0.2819296736111110979, 0.1152777777019111383, -0.1167790944451423396 ) ) ;
#13746=CARTESIAN_POINT ( 'NONE',  ( 0.2819296736111110424, 4.786888888964755395, -0.1167790944451423396 ) ) ;
#13749=CARTESIAN_POINT ( 'NONE',  ( -0.1993543840281266355, 4.748694444520309865, 0.1993543840281267465 ) ) ;
#13750=CARTESIAN_POINT ( 'NONE',  ( -0.1002000441541520542, 4.157805295584717342, -0.2961774115687041964 ) ) ;
#13751=CARTESIAN_POINT ( 'NONE',  ( 0.1851001322554625683, 4.855041628199087356, 0.2517309871580742375 ) ) ;
#13752=CARTESIAN_POINT ( 'NONE',  ( 0.000000000000000000, 5.384999999999999787, 0.000000000000000000 ) ) ;
#13754=CARTESIAN_POINT ( 'NONE',  ( 5.731347020009612645E-17, 4.231333333333332725, 0.3119999999999999996 ) ) ;
#13755=CARTESIAN_POINT ( 'NONE',  ( 0.3119999999999999996, 5.196611111262844140, -3.820898013339742174E-17 ) ) ;
#13756=CARTESIAN_POINT ( 'NONE',  ( 0.2905230268857740272, 4.971080770670708304, 0.1149655184485972731 ) ) ;
#13760=CARTESIAN_POINT ( 'NONE',  ( 0.02915501805629885923, 4.709709316167313808, -0.3107256135361845528 ) ) ;
#13767=CARTESIAN_POINT ( 'NONE',  ( -0.1993543840281266633, 0.4451388888130222710, -0.1993543840281266910 ) ) ;
#13768=CARTESIAN_POINT ( 'NONE',  ( -0.1486148644933975860, 5.206640035683666845, 0.2403663825195851700 ) ) ;
#13773=CARTESIAN_POINT ( 'NONE',  ( -0.1500997534610212791, 4.622705627101820980, 0.2735216599064862475 ) ) ;
#13774=DIRECTION ( 'NONE',  ( 0.000000000000000000, -0.000000000000000000, 1.000000000000000000 ) ) ;
#13776=CARTESIAN_POINT ( 'NONE',  ( 0.1292346314604056745, 0.4729166666666663188, -0.3119999999999999996 ) ) ;
#13777=CARTESIAN_POINT ( 'NONE',  ( 0.2206173157302028787, 4.849388888888888083, 0.2206173157302027954 ) ) ;
#13778=CARTESIAN_POINT ( 'NONE',  ( 0.1993543840281267465, 3.943138888964754951, 0.1993543840281266633 ) ) ;
#13779=CARTESIAN_POINT ( 'NONE',  ( -0.1292346314604057300, 3.838972222222221564, 0.3119999999999998885 ) ) ;
#13786=CARTESIAN_POINT ( 'NONE',  ( 0.000000000000000000, 5.384999999999999787, -0.3119999999999999996 ) ) ;
#13787=CARTESIAN_POINT ( 'NONE',  ( 5.178964085587577574E-17, 4.811194444520309865, 0.2819296736111110979 ) ) ;
#13789=ADVANCED_FACE ( 'NONE', ( #2866 ), #920, .T. ) ;
#13792=CARTESIAN_POINT ( 'NONE',  ( -5.731347020009612645E-17, 0.2263888888888885564, 0.3119999999999999996 ) ) ;
#13793=CARTESIAN_POINT ( 'NONE',  ( 0.2819296736111110979, 4.231333333409199149, -0.1167790944451423396 ) ) ;
#13796=CARTESIAN_POINT ( 'NONE',  ( -0.0005878709530763284643, 4.043849134038319804, -0.3119994809580396988 ) ) ;
#13798=CARTESIAN_POINT ( 'NONE',  ( -0.1167790944451424368, 0.4208333332574665797, 0.2819296736111110424 ) ) ;
#13800=CARTESIAN_POINT ( 'NONE',  ( 0.3119999999999999996, 4.467444444444443441, -3.820898013339742174E-17 ) ) ;
#13804=CARTESIAN_POINT ( 'NONE',  ( -0.1167790944451422702, 0.5527777777019111660, -0.2819296736111110979 ) ) ;
#13805=CARTESIAN_POINT ( 'NONE',  ( 0.1167790944451423535, 0.3027777777019111105, 0.2819296736111110424 ) ) ;
#13806=CARTESIAN_POINT ( 'NONE',  ( 5.178964085587577574E-17, 3.991750000075865223, 0.2819296736111110979 ) ) ;
#13808=CARTESIAN_POINT ( 'NONE',  ( -0.2819296736111110979, 4.644527777853643791, 0.000000000000000000 ) ) ;
#13810=CARTESIAN_POINT ( 'NONE',  ( -0.2206173157302027954, 0.1430555554038226151, -0.2206173157302028232 ) ) ;
#13812=EDGE_CURVE ( 'NONE', #12593, #11100, #17254, .T. ) ;
#13815=CARTESIAN_POINT ( 'NONE',  ( 0.3119999999999999996, 3.922305555707287006, -0.1292346314604056745 ) ) ;
#13819=ORIENTED_EDGE ( 'NONE', *, *, #11988, .F. ) ;
#13823=CARTESIAN_POINT ( 'NONE',  ( -0.3115931849604412496, 5.001428069419088018, -0.02819374845571557750 ) ) ;
#13825=CARTESIAN_POINT ( 'NONE',  ( -0.1167790944451424368, 0.03194444436857781650, 0.2819296736111110424 ) ) ;
#13827=CARTESIAN_POINT ( 'NONE',  ( 0.04078511732514260996, 4.239493367616026909, 0.3120000055331293431 ) ) ;
#13832=CARTESIAN_POINT ( 'NONE',  ( 0.1784294693753899486, 5.172189122700864061, 0.2361384720919713631 ) ) ;
#13835=CARTESIAN_POINT ( 'NONE',  ( -0.1993543840281266355, 5.207027777853642903, 0.1993543840281267465 ) ) ;
#13841=CARTESIAN_POINT ( 'NONE',  ( 5.253288188650943643E-17, 5.197747365142496356, 0.2859756893339090444 ) ) ;
#13842=CARTESIAN_POINT ( 'NONE',  ( 0.2206173157302028232, 0.3513888887371559577, -0.2206173157302028232 ) ) ;
#13843=CARTESIAN_POINT ( 'NONE',  ( -0.3119999999999999996, 4.498694444596177178, -0.1292346314604056468 ) ) ;
#13844=CARTESIAN_POINT ( 'NONE',  ( -0.2819296736111110979, 4.977861111186976828, 0.000000000000000000 ) ) ;
#13846=CARTESIAN_POINT ( 'NONE',  ( -1.726321361862525858E-17, 4.172305555631420582, -0.2819296736111110979 ) ) ;
#13850=ORIENTED_EDGE ( 'NONE', *, *, #11865, .T. ) ;
#13853=FACE_OUTER_BOUND ( 'NONE', #21732, .T. ) ;
#13855=ORIENTED_EDGE ( 'NONE', *, *, #8117, .T. ) ;
#13856=FACE_OUTER_BOUND ( 'NONE', #10844, .T. ) ;
#13858=CARTESIAN_POINT ( 'NONE',  ( 0.1988757138996042617, 3.752970977545328157, -0.2404006040361021113 ) ) ;
#13862=CARTESIAN_POINT ( 'NONE',  ( 0.2658661084243346684, 0.03242967361111057795, 0.09380593400082704036 ) ) ;
#13866=AXIS2_PLACEMENT_3D ( 'NONE', #5053, #8963, #1530 ) ;
#13867=CARTESIAN_POINT ( 'NONE',  ( 0.2819296736111110424, 4.606333333409200037, -0.1167790944451423396 ) ) ;
#13870=DIRECTION ( 'NONE',  ( -0.6374213576849414586, 0.000000000000000000, 0.7705154202007158393 ) ) ;
#13872=CARTESIAN_POINT ( 'NONE',  ( 0.2206173157302028787, 4.293833333333332725, 0.2206173157302027954 ) ) ;
#13873=CARTESIAN_POINT ( 'NONE',  ( -0.3119999999999999996, 5.168833333485065573, 0.000000000000000000 ) ) ;
#13874=CARTESIAN_POINT ( 'NONE',  ( -5.488040394358968970E-07, 4.960478275469978549, 0.3119999999989728212 ) ) ;
#13879=VERTEX_POINT ( 'NONE', #3292 ) ;
#13880=CARTESIAN_POINT ( 'NONE',  ( 0.05352797175791356582, 4.684214349109525166, 0.3073846428649295581 ) ) ;
#13882=UNCERTAINTY_MEASURE_WITH_UNIT (LENGTH_MEASURE( 1.000000000000000082E-05 ), #12842, 'distance_accuracy_value', 'NONE');
#13883=CARTESIAN_POINT ( 'NONE',  ( 0.1909493018183467117, 4.133023247099400166, 0.2467435441855950762 ) ) ;
#13886=ORIENTED_EDGE ( 'NONE', *, *, #12510, .T. ) ;
#13888=CARTESIAN_POINT ( 'NONE',  ( 0.2819296736111110979, 0.04930555547968892144, 0.000000000000000000 ) ) ;
#13892=CYLINDRICAL_SURFACE ( 'NONE', #14375, 0.3119999999999999996 ) ;
#13895=CARTESIAN_POINT ( 'NONE',  ( -0.3129426082665457964, 4.280301605886003280, 0.01319854631990339047 ) ) ;
#13896=CARTESIAN_POINT ( 'NONE',  ( 0.000000000000000000, 5.384999999999999787, 0.000000000000000000 ) ) ;
#13897=CARTESIAN_POINT ( 'NONE',  ( 0.2206173157302027676, 0.5111111111111107386, 0.2206173157302028787 ) ) ;
#13898=CARTESIAN_POINT ( 'NONE',  ( -0.1292346314604056745, 4.929249999999999687, -0.3119999999999999996 ) ) ;
#13900=CARTESIAN_POINT ( 'NONE',  ( -0.1167790944451423257, 3.967444444520310309, -0.2819296736111110424 ) ) ;
#13907=CARTESIAN_POINT ( 'NONE',  ( -0.2819296736111110979, 4.630638888964754507, 0.000000000000000000 ) ) ;
#13914=CARTESIAN_POINT ( 'NONE',  ( -1.726321361862525858E-17, 4.019527777853643791, -0.2819296736111110979 ) ) ;
#13916=CARTESIAN_POINT ( 'NONE',  ( -0.1877440169500084466, 4.827352557465903082, -0.2523603461020555438 ) ) ;
#13920=CARTESIAN_POINT ( 'NONE',  ( -0.2819296736111110979, 0.007638888813022256218, -3.452642723725051716E-17 ) ) ;
#13921=CARTESIAN_POINT ( 'NONE',  ( 1.910449006669871087E-17, 0.4208333333333330040, -0.3119999999999999996 ) ) ;
#13927=CARTESIAN_POINT ( 'NONE',  ( 0.2819296736111110979, 0.4277777777019111660, -0.1167790944451422980 ) ) ;
#13928=CARTESIAN_POINT ( 'NONE',  ( 0.1167790944451423535, 0.5249999999241333759, 0.2819296736111110424 ) ) ;
#13929=CARTESIAN_POINT ( 'NONE',  ( 0.2819296736111110979, 4.116750000075866112, -3.452642723725051716E-17 ) ) ;
#13932=CARTESIAN_POINT ( 'NONE',  ( -0.2819296736111110424, 4.752166666742533074, -0.1167790944451423119 ) ) ;
#13935=ORIENTED_EDGE ( 'NONE', *, *, #8548, .F. ) ;
#13938=CARTESIAN_POINT ( 'NONE',  ( 0.1292346314604056190, 3.818138889040621375, -0.3119999999999999996 ) ) ;
#13940=ORIENTED_EDGE ( 'NONE', *, *, #13051, .F. ) ;
#13941=CARTESIAN_POINT ( 'NONE',  ( 0.06864889549624120235, 5.206640035683666845, 0.2739922474530114282 ) ) ;
#13945=ORIENTED_EDGE ( 'NONE', *, *, #4146, .F. ) ;
#13946=CARTESIAN_POINT ( 'NONE',  ( -0.1993543840281267465, 0.1395833332574666907, 0.1993543840281266633 ) ) ;
#13950=CARTESIAN_POINT ( 'NONE',  ( 0.3037827064340575256, 4.249802897613654373, 0.08205749792799824083 ) ) ;
#13951=CARTESIAN_POINT ( 'NONE',  ( -4.974594353761572974E-07, 4.738258141874186258, 0.3119999999991586170 ) ) ;
#13952=CARTESIAN_POINT ( 'NONE',  ( 0.3016382822107275818, 4.083242817246184764, 0.07973931868136807655 ) ) ;
#13954=CARTESIAN_POINT ( 'NONE',  ( -0.2296906778660977588, 5.064311450068244014, 0.2111546458865629639 ) ) ;
#13956=DIRECTION ( 'NONE',  ( -0.000000000000000000, -1.000000000000000000, -0.000000000000000000 ) ) ;
#13957=EDGE_CURVE ( 'NONE', #21366, #9589, #3084, .T. ) ;
#13958=CARTESIAN_POINT ( 'NONE',  ( 0.1167790944451424368, 5.217444444520309865, 0.2819296736111110424 ) ) ;
#13959=CARTESIAN_POINT ( 'NONE',  ( 0.2373038722028483205, 5.036289568926800797, -0.2041309936366799416 ) ) ;
#13961=CARTESIAN_POINT ( 'NONE',  ( -0.2802017012671415008, 4.784146520345384346, 0.1428922795062084750 ) ) ;
#13962=CARTESIAN_POINT ( 'NONE',  ( 0.3119999999999999996, 4.582027777929510215, 0.1292346314604056190 ) ) ;
#13963=CARTESIAN_POINT ( 'NONE',  ( 0.2819296736111110979, 4.620222222298088433, -0.1167790944451423396 ) ) ;
#13964=VERTEX_POINT ( 'NONE', #21474 ) ;
#13965=CARTESIAN_POINT ( 'NONE',  ( 0.1993543840281266633, 4.109805555631420582, -0.1993543840281266910 ) ) ;
#13967=VERTEX_POINT ( 'NONE', #23521 ) ;
#13971=CYLINDRICAL_SURFACE ( 'NONE', #22135, 0.3119999999999999996 ) ;
#13972=CARTESIAN_POINT ( 'NONE',  ( -0.1167790944451423119, 3.745222222298088433, -0.2819296736111110979 ) ) ;
#13975=LINE ( 'NONE', #11919, #19417 ) ;
#13977=( BOUNDED_CURVE ( )  B_SPLINE_CURVE ( 2, ( #12795, #1915, #13037 ),
 .UNSPECIFIED., .F., .F. ) 
 B_SPLINE_CURVE_WITH_KNOTS ( ( 3, 3 ),
 ( 0.09727559839650132267, 0.09732137976955804182 ),
 .UNSPECIFIED. ) 
 CURVE ( )  GEOMETRIC_REPRESENTATION_ITEM ( )  RATIONAL_B_SPLINE_CURVE ( ( 0.9747197555285191939, 0.9751720984492913136, 0.9756404518778661883 ) ) 
 REPRESENTATION_ITEM ( '' )  );
#13980=DIRECTION ( 'NONE',  ( -0.000000000000000000, -1.000000000000000000, -0.000000000000000000 ) ) ;
#13981=CARTESIAN_POINT ( 'NONE',  ( 0.1167790944451423535, 0.1361111110352444808, 0.2819296736111110979 ) ) ;
#13985=CARTESIAN_POINT ( 'NONE',  ( 0.2819296736111110424, 4.495222222298087544, -0.1167790944451423396 ) ) ;
#13986=CARTESIAN_POINT ( 'NONE',  ( 5.178964085587577574E-17, 5.200083333409199149, 0.2819296736111110979 ) ) ;
#13989=CARTESIAN_POINT ( 'NONE',  ( 0.3119999999999999996, 4.248694444444443441, -0.1292346314604056745 ) ) ;
#13990=CARTESIAN_POINT ( 'NONE',  ( 0.2206173157302028787, 5.189666666818398610, 0.2206173157302027954 ) ) ;
#13994=CARTESIAN_POINT ( 'NONE',  ( -0.1275151006136568121, 4.880904689916613748, -0.2851559274793544763 ) ) ;
#13995=AXIS2_PLACEMENT_3D ( 'NONE', #15918, #8476, #8939 ) ;
#14001=CARTESIAN_POINT ( 'NONE',  ( -5.178964085587577574E-17, 0.09097222214635558579, 0.2819296736111110979 ) ) ;
#14009=CARTESIAN_POINT ( 'NONE',  ( -0.001077020842221716127, 4.293802776323909498, 0.3119984097836999148 ) ) ;
#14010=DIRECTION ( 'NONE',  ( 0.000000000000000000, 0.000000000000000000, -1.000000000000000000 ) ) ;
#14011=CARTESIAN_POINT ( 'NONE',  ( 0.2206173157302028232, 0.4694444444444441089, -0.2206173157302028232 ) ) ;
#14012=CARTESIAN_POINT ( 'NONE',  ( -1.910449006669871087E-17, 4.925777777777777366, -0.3119999999999999996 ) ) ;
#14014=CARTESIAN_POINT ( 'NONE',  ( 0.1993543840281267465, 4.262583333409199149, 0.1993543840281266633 ) ) ;
#14015=CARTESIAN_POINT ( 'NONE',  ( -0.2819296736111110424, 4.036888888964754507, 0.1167790944451424923 ) ) ;
#14020=VERTEX_POINT ( 'NONE', #1109 ) ;
#14022=CARTESIAN_POINT ( 'NONE',  ( -0.1917385696898717407, 3.994101739603878265, -0.2494960598862051016 ) ) ;
#14023=CARTESIAN_POINT ( 'NONE',  ( -0.2819296736111110424, 4.460500000075867000, -0.1167790944451423119 ) ) ;
#14025=CARTESIAN_POINT ( 'NONE',  ( -0.02639353809836864767, 4.515333978748262034, 0.3108816215404409111 ) ) ;
#14030=CARTESIAN_POINT ( 'NONE',  ( 5.178964085587577574E-17, 4.158416666742532186, 0.2819296736111110979 ) ) ;
#14031=DIRECTION ( 'NONE',  ( -0.000000000000000000, -1.000000000000000000, -0.000000000000000000 ) ) ;
#14035=CARTESIAN_POINT ( 'NONE',  ( -0.1167790944451424368, 0.1291666665908000611, 0.2819296736111110424 ) ) ;
#14037=CARTESIAN_POINT ( 'NONE',  ( -5.731347020009612645E-17, 0.4486111111111107386, 0.3119999999999999996 ) ) ;
#14039=LINE ( 'NONE', #19157, #9969 ) ;
#14042=CARTESIAN_POINT ( 'NONE',  ( -0.2726133089392542286, 3.775404533184292699, -0.1571433413004071078 ) ) ;
#14044=CARTESIAN_POINT ( 'NONE',  ( -0.1993543840281267465, 0.4034722221463555858, 0.1993543840281266633 ) ) ;
#14045=CARTESIAN_POINT ( 'NONE',  ( 0.1993543840281266633, 4.068138888964754507, -0.1993543840281266910 ) ) ;
#14047=CARTESIAN_POINT ( 'NONE',  ( -0.2819296736111110979, 4.755638888964754507, 0.000000000000000000 ) ) ;
#14048=CARTESIAN_POINT ( 'NONE',  ( 0.3065813772506288948, 5.131179073402218016, -0.008293487530610424083 ) ) ;
#14049=CARTESIAN_POINT ( 'NONE',  ( 0.2472629257724013041, 5.084277803960305597, -0.1904837651393340436 ) ) ;
#14051=ORIENTED_EDGE ( 'NONE', *, *, #14992, .T. ) ;
#14052=CYLINDRICAL_SURFACE ( 'NONE', #1162, 0.3119999999999999996 ) ;
#14053=CARTESIAN_POINT ( 'NONE',  ( -0.2206173157302027676, 3.842444444596176290, 0.2206173157302028787 ) ) ;
#14054=CARTESIAN_POINT ( 'NONE',  ( 5.731347020009612645E-17, 5.064666666666665762, 0.3119999999999999996 ) ) ;
#14057=CARTESIAN_POINT ( 'NONE',  ( -0.1993543840281266910, 4.790361111186976828, -0.1993543840281266910 ) ) ;
#14061=CARTESIAN_POINT ( 'NONE',  ( 1.910449006669871087E-17, 0.1916666665149337478, -0.3119999999999999996 ) ) ;
#14063=CARTESIAN_POINT ( 'NONE',  ( 0.2819296736111110424, 0.1013888888130222432, 0.1167790944451424923 ) ) ;
#14070=CARTESIAN_POINT ( 'NONE',  ( -0.2904724470272674886, 5.054419505141493296, -0.1139996456453155477 ) ) ;
#14071=CARTESIAN_POINT ( 'NONE',  ( 0.000000000000000000, 5.384999999999999787, 0.000000000000000000 ) ) ;
#14073=CARTESIAN_POINT ( 'NONE',  ( 0.2819296736111110979, 3.877166666742531742, 0.1167790944451422425 ) ) ;
#14075=CARTESIAN_POINT ( 'NONE',  ( 0.2639837978753995507, 0.06059161645832044502, 0.1650549759726013255 ) ) ;
#14077=CARTESIAN_POINT ( 'NONE',  ( -0.2206173157302028232, 4.495222222373953969, -0.2206173157302028232 ) ) ;
#14078=CARTESIAN_POINT ( 'NONE',  ( -0.2819296736111110979, 4.752166666742531298, -0.1167790944451422980 ) ) ;
#14079=ADVANCED_FACE ( 'NONE', ( #2068 ), #22188, .T. ) ;
#14081=CARTESIAN_POINT ( 'NONE',  ( 0.1993543840281266633, 4.054250000075865223, -0.1993543840281266910 ) ) ;
#14082=EDGE_CURVE ( 'NONE', #14348, #11367, #15403, .T. ) ;
#14084=ORIENTED_EDGE ( 'NONE', *, *, #9762, .F. ) ;
#14087=EDGE_CURVE ( 'NONE', #9930, #4893, #21446, .T. ) ;
#14090=CARTESIAN_POINT ( 'NONE',  ( -5.731347020009612645E-17, 0.1083333331816004053, 0.3119999999999999996 ) ) ;
#14099=ORIENTED_EDGE ( 'NONE', *, *, #21909, .T. ) ;
#14100=CARTESIAN_POINT ( 'NONE',  ( 0.1167790944451422702, 4.446611111186975940, -0.2819296736111110424 ) ) ;
#14104=CARTESIAN_POINT ( 'NONE',  ( -5.731347020009612645E-17, 0.4416666665149336923, 0.3119999999999999996 ) ) ;
#14105=CARTESIAN_POINT ( 'NONE',  ( 0.2206173157302028787, 3.960499999999999243, 0.2206173157302027954 ) ) ;
#14106=CARTESIAN_POINT ( 'NONE',  ( 0.2206173157302028787, 5.071611111111109516, 0.2206173157302027954 ) ) ;
#14107=CARTESIAN_POINT ( 'NONE',  ( 0.3107178308811224254, 4.973614215416888307, 0.02829828600566403063 ) ) ;
#14110=ORIENTED_EDGE ( 'NONE', *, *, #1036, .F. ) ;
#14111=CARTESIAN_POINT ( 'NONE',  ( -0.1864835714138413370, 4.882863081058048671, -0.2501521505361365971 ) ) ;
#14115=( BOUNDED_CURVE ( )  B_SPLINE_CURVE ( 2, ( #21109, #744, #23158, #6350, #13800, #21231, #12106, #983, #10148 ),
 .UNSPECIFIED., .F., .F. ) 
 B_SPLINE_CURVE_WITH_KNOTS ( ( 3, 2, 2, 2, 3 ),
 ( 0.5089285714285716189, 0.5133928571428572063, 0.5178571428571429047, 0.5223214285714284921, 0.5267857142857140795 ),
 .UNSPECIFIED. ) 
 CURVE ( )  GEOMETRIC_REPRESENTATION_ITEM ( )  RATIONAL_B_SPLINE_CURVE ( ( 0.9999999999999962252, 0.9238795325112905132, 1.000000000000000000, 0.9238795325112867385, 1.000000000000000000, 0.9238795325112867385, 1.000000000000000000, 0.9238795325112905132, 0.9999999999999962252 ) ) 
 REPRESENTATION_ITEM ( '' )  );
#14116=CIRCLE ( 'NONE', #12565, 0.3119999999999999996 ) ;
#14117=CARTESIAN_POINT ( 'NONE',  ( 0.3038789596872260024, 3.809946929045645359, -0.08166725170457082850 ) ) ;
#14122=CARTESIAN_POINT ( 'NONE',  ( -0.1993543840281266910, 5.082027777853643791, -0.1993543840281266910 ) ) ;
#14124=ORIENTED_EDGE ( 'NONE', *, *, #2023, .F. ) ;
#14125=CARTESIAN_POINT ( 'NONE',  ( -0.001169892149794590427, 4.599422744928899576, -0.3120000010507765764 ) ) ;
#14128=CARTESIAN_POINT ( 'NONE',  ( 0.1292346314604057023, 0.5076388888888885287, 0.3119999999999998885 ) ) ;
#14129=CARTESIAN_POINT ( 'NONE',  ( -1.910449006669871087E-17, 4.870222222222222008, -0.3119999999999999996 ) ) ;
#14130=CARTESIAN_POINT ( 'NONE',  ( -0.1993543840281266355, 4.193138888964754507, 0.1993543840281267465 ) ) ;
#14131=CARTESIAN_POINT ( 'NONE',  ( -0.1167790944451423257, 3.911888888964754507, -0.2819296736111110424 ) ) ;
#14136=CARTESIAN_POINT ( 'NONE',  ( 0.2819296736111110979, 4.432722222298088433, 0.1167790944451422425 ) ) ;
#14138=CARTESIAN_POINT ( 'NONE',  ( -0.08608376305752644952, 4.490775599581271926, -0.3006775868009963215 ) ) ;
#14143=CARTESIAN_POINT ( 'NONE',  ( -0.2819296736111110979, 4.196611111186976828, -0.1167790944451422980 ) ) ;
#14145=CARTESIAN_POINT ( 'NONE',  ( -0.2206173157302027954, 0.3722222222222218990, -0.2206173157302028232 ) ) ;
#14149=CARTESIAN_POINT ( 'NONE',  ( -0.1167790944451424368, 0.01805555547968892838, 0.2819296736111110424 ) ) ;
#14151=CARTESIAN_POINT ( 'NONE',  ( -0.2206173157302027954, 0.09444444444444409503, -0.2206173157302028232 ) ) ;
#14157=LINE ( 'NONE', #12347, #9098 ) ;
#14158=CARTESIAN_POINT ( 'NONE',  ( -0.0003064590024795931108, 3.766063790100582231, -0.3119998596873261865 ) ) ;
#14160=CARTESIAN_POINT ( 'NONE',  ( 0.1993543840281266355, 0.3618055554796889006, 0.1993543840281267465 ) ) ;
#14161=CARTESIAN_POINT ( 'NONE',  ( 0.2819296736111110979, 4.005638888964754507, -3.452642723725051716E-17 ) ) ;
#14163=ORIENTED_EDGE ( 'NONE', *, *, #5739, .F. ) ;
#14164=CARTESIAN_POINT ( 'NONE',  ( -0.1167790944451423257, 4.634111111186976828, -0.2819296736111110424 ) ) ;
#14165=CARTESIAN_POINT ( 'NONE',  ( 0.2967394294427592727, 5.128870701040007418, 0.08104332260532720600 ) ) ;
#14166=CARTESIAN_POINT ( 'NONE',  ( 0.05669741369301228850, 5.090589713294394691, -0.3076489064292024511 ) ) ;
#14169=CARTESIAN_POINT ( 'NONE',  ( 0.1993543840281266633, 5.165361111186976828, -0.1993543840281266910 ) ) ;
#14171=CARTESIAN_POINT ( 'NONE',  ( 0.3126550460293563427, 4.197112280939127693, -0.01677631843042015625 ) ) ;
#14173=CARTESIAN_POINT ( 'NONE',  ( 0.2065212855157302352, 0.03242967361111054325, 0.1924695337126736405 ) ) ;
#14174=CARTESIAN_POINT ( 'NONE',  ( -1.726321361862525858E-17, 4.783416666742532186, -0.2819296736111110979 ) ) ;
#14176=ORIENTED_EDGE ( 'NONE', *, *, #10045, .T. ) ;
#14177=CARTESIAN_POINT ( 'NONE',  ( -0.1367999271637809766, 5.104340882757027131, -0.2793827907768540730 ) ) ;
#14179=CARTESIAN_POINT ( 'NONE',  ( -0.1167790944451422702, 0.3999999999241333759, -0.2819296736111110424 ) ) ;
#14183=CARTESIAN_POINT ( 'NONE',  ( 0.2968882310381912304, 4.082774378827750184, 0.09599610789069373817 ) ) ;
#14185=CARTESIAN_POINT ( 'NONE',  ( -0.1644747555172010878, 5.066690419149153080, 0.2661110666209607345 ) ) ;
#14188=CARTESIAN_POINT ( 'NONE',  ( -0.2819296736111110424, 4.703555555631421470, 0.1167790944451424923 ) ) ;
#14190=EDGE_CURVE ( 'NONE', #1934, #10834, #17425, .T. ) ;
#14192=CARTESIAN_POINT ( 'NONE',  ( -0.1993543840281266910, 3.734805555631421026, -0.1993543840281266910 ) ) ;
#14194=CARTESIAN_POINT ( 'NONE',  ( 0.07868793315885187767, 5.018292790751019972, 0.3026089890143150440 ) ) ;
#14195=CARTESIAN_POINT ( 'NONE',  ( 0.1989077834500278252, 5.073000000000000398, 0.2437966507032887920 ) ) ;
#14197=CARTESIAN_POINT ( 'NONE',  ( -0.2206173157302027676, 4.398000000151732536, 0.2206173157302028787 ) ) ;
#14198=EDGE_CURVE ( 'NONE', #5827, #16588, #4492, .T. ) ;
#14199=CARTESIAN_POINT ( 'NONE',  ( 5.178964085587577574E-17, 4.825083333409199149, 0.2819296736111110979 ) ) ;
#14202=CARTESIAN_POINT ( 'NONE',  ( -0.1167790944451423257, 4.009111111186976828, -0.2819296736111110424 ) ) ;
#14208=CARTESIAN_POINT ( 'NONE',  ( 1.145733547534701715E-12, 5.130222168000691418, 0.3067077167097377322 ) ) ;
#14210=CARTESIAN_POINT ( 'NONE',  ( 0.1292346314604056745, 0.1881944442927115102, -0.3119999999999999996 ) ) ;
#14211=CARTESIAN_POINT ( 'NONE',  ( -0.2707896025394566086, 4.386469429090337435, -0.1563191200470392395 ) ) ;
#14215=CARTESIAN_POINT ( 'NONE',  ( 0.3119999999999999996, 0.2368055554038226151, -0.1292346314604056468 ) ) ;
#14216=CARTESIAN_POINT ( 'NONE',  ( 1.726321361862525858E-17, 0.04930555547968892144, -0.2819296736111110979 ) ) ;
#14218=CARTESIAN_POINT ( 'NONE',  ( 0.1167790944451424368, 4.481333333409199149, 0.2819296736111110424 ) ) ;
#14223=CARTESIAN_POINT ( 'NONE',  ( 0.3119999999999999996, 3.967444444444443441, -3.820898013339742174E-17 ) ) ;
#14227=CARTESIAN_POINT ( 'NONE',  ( 0.3042924909783515930, 4.972423745096966385, 0.06982855329471476802 ) ) ;
#14234=CARTESIAN_POINT ( 'NONE',  ( 0.3120000192078950518, 3.808819556236046733, -0.04084196867937928827 ) ) ;
#14235=ADVANCED_FACE ( 'NONE', ( #15598 ), #22906, .F. ) ;
#14239=CARTESIAN_POINT ( 'NONE',  ( -5.178964085587577574E-17, 0.03541666659080003332, 0.2819296736111110979 ) ) ;
#14242=FACE_OUTER_BOUND ( 'NONE', #6897, .T. ) ;
#14245=CARTESIAN_POINT ( 'NONE',  ( -0.1749087105507561857, 4.604688012726042778, -0.2584107560775423806 ) ) ;
#14246=CARTESIAN_POINT ( 'NONE',  ( -0.3055012760687011442, 4.277984914513297099, -0.06818561754197617619 ) ) ;
#14249=CARTESIAN_POINT ( 'NONE',  ( -0.2206173157302028787, 0.4416666666666662633, 0.2206173157302027954 ) ) ;
#14250=CARTESIAN_POINT ( 'NONE',  ( 0.2206173157302027954, 4.752166666666665762, -0.2206173157302028232 ) ) ;
#14251=CARTESIAN_POINT ( 'NONE',  ( -0.2819296736111110424, 4.300777777853643791, 0.1167790944451424923 ) ) ;
#14258=CARTESIAN_POINT ( 'NONE',  ( 0.2819296736111110424, 4.606333333409200037, -0.1167790944451423396 ) ) ;
#14262=CYLINDRICAL_SURFACE ( 'NONE', #8794, 0.3119999999999999996 ) ;
#14264=CARTESIAN_POINT ( 'NONE',  ( 0.1167790944451422702, 4.182722222298088433, -0.2819296736111110979 ) ) ;
#14265=CARTESIAN_POINT ( 'NONE',  ( -0.0002601744550385995803, 4.821618687316853169, -0.3120000001095587505 ) ) ;
#14266=CARTESIAN_POINT ( 'NONE',  ( 5.731347020009612645E-17, 4.897999999999998799, 0.3119999999999999996 ) ) ;
#14270=CARTESIAN_POINT ( 'NONE',  ( 0.2819296736111110424, 0.03194444436857781650, 0.1167790944451424923 ) ) ;
#14272=DIRECTION ( 'NONE',  ( 0.000000000000000000, 0.000000000000000000, -1.000000000000000000 ) ) ;
#14279=CARTESIAN_POINT ( 'NONE',  ( -0.1167790944451422702, 0.3861111110352444808, -0.2819296736111110424 ) ) ;
#14280=CARTESIAN_POINT ( 'NONE',  ( 0.2819296736111110979, 3.950083333409199149, -3.452642723725051716E-17 ) ) ;
#14283=VERTEX_POINT ( 'NONE', #2553 ) ;
#14284=CARTESIAN_POINT ( 'NONE',  ( 0.1167790944451422702, 4.738277777853642903, -0.2819296736111110424 ) ) ;
#14287=DIRECTION ( 'NONE',  ( -0.000000000000000000, -1.000000000000000000, -0.000000000000000000 ) ) ;
#14290=CARTESIAN_POINT ( 'NONE',  ( -0.1167790944451423257, 5.064666666742533074, -0.2819296736111110424 ) ) ;
#14291=CARTESIAN_POINT ( 'NONE',  ( 0.04350585610265966102, 4.209263110863878055, -0.3090598294826615300 ) ) ;
#14295=CARTESIAN_POINT ( 'NONE',  ( 0.1334304699324121435, 5.206640035683670398, 0.2489627644214695845 ) ) ;
#14296=CARTESIAN_POINT ( 'NONE',  ( 0.2819296736111110979, 4.828555555631420582, -0.1167790944451423396 ) ) ;
#14298=ORIENTED_EDGE ( 'NONE', *, *, #17942, .T. ) ;
#14300=CARTESIAN_POINT ( 'NONE',  ( -0.1206839867636108760, 4.568140654558272118, 0.2884027983365602954 ) ) ;
#14302=CARTESIAN_POINT ( 'NONE',  ( 0.2819296736111110424, 0.2680555554796889561, 0.1167790944451424923 ) ) ;
#14304=CARTESIAN_POINT ( 'NONE',  ( -0.2819296736111110979, 0.02152777770191114520, -3.452642723725051716E-17 ) ) ;
#14305=CARTESIAN_POINT ( 'NONE',  ( -0.03900460988328559309, 4.737132092303641073, 0.3120000036723390435 ) ) ;
#14308=CARTESIAN_POINT ( 'NONE',  ( -0.2296592410380279836, 5.064312714222578116, 0.2111886365721926673 ) ) ;
#14309=CARTESIAN_POINT ( 'NONE',  ( 0.2206173157302028787, 4.182722222222221120, 0.2206173157302027954 ) ) ;
#14311=CARTESIAN_POINT ( 'NONE',  ( 0.2819296736111110424, 4.842444444520309865, -0.1167790944451423396 ) ) ;
#14313=CARTESIAN_POINT ( 'NONE',  ( 0.2811290616301844736, 4.525923312079648042, 0.1368482528082854699 ) ) ;
#14314=CARTESIAN_POINT ( 'NONE',  ( -0.2819296736111110424, 5.252166666742532186, -0.1167790944451423119 ) ) ;
#14316=CARTESIAN_POINT ( 'NONE',  ( -0.2922127367187743463, 0.05061570093428138795, -0.07118518849912422453 ) ) ;
#14320=CARTESIAN_POINT ( 'NONE',  ( -0.3119999999999998885, 4.283416666818398610, 0.1292346314604058410 ) ) ;
#14321=CARTESIAN_POINT ( 'NONE',  ( 0.2819296736111111534, 4.724388888964754507, 0.1167790944451422563 ) ) ;
#14322=CARTESIAN_POINT ( 'NONE',  ( 0.1167790944451422702, 3.891055555631421914, -0.2819296736111110424 ) ) ;
#14327=( BOUNDED_CURVE ( )  B_SPLINE_CURVE ( 2, ( #3, #16843, #20500, #7100, #7451, #11360, #20264, #22444, #14538 ),
 .UNSPECIFIED., .F., .F. ) 
 B_SPLINE_CURVE_WITH_KNOTS ( ( 3, 2, 2, 2, 3 ),
 ( 0.3541666666666666852, 0.3645833333333333148, 0.3750000000000000000, 0.3854166666666666852, 0.3958333333333333148 ),
 .UNSPECIFIED. ) 
 CURVE ( )  GEOMETRIC_REPRESENTATION_ITEM ( )  RATIONAL_B_SPLINE_CURVE ( ( 1.000000000000000000, 0.9238795325112867385, 1.000000000000000000, 0.9238795325112867385, 1.000000000000000000, 0.9238795325112867385, 1.000000000000000000, 0.9238795325112867385, 1.000000000000000000 ) ) 
 REPRESENTATION_ITEM ( '' )  );
#14331=CARTESIAN_POINT ( 'NONE',  ( -0.3119999999999999996, 0.2055555554038226151, -3.820898013339742174E-17 ) ) ;
#14332=CARTESIAN_POINT ( 'NONE',  ( -0.1913778543947200761, 4.399133461649255672, 0.2497584621283620854 ) ) ;
#14338=CARTESIAN_POINT ( 'NONE',  ( 0.1993543840281266355, 0.3618055554796889006, 0.1993543840281267465 ) ) ;
#14340=CARTESIAN_POINT ( 'NONE',  ( 5.178964085587577574E-17, 4.422305555631421470, 0.2819296736111110979 ) ) ;
#14344=CARTESIAN_POINT ( 'NONE',  ( 0.3119999999999999996, 4.075083333333332725, 0.1292346314604056190 ) ) ;
#14346=CARTESIAN_POINT ( 'NONE',  ( 0.3119999999999999996, 4.863277777929510215, -3.820898013339742174E-17 ) ) ;
#14348=VERTEX_POINT ( 'NONE', #17189 ) ;
#14349=CARTESIAN_POINT ( 'NONE',  ( 5.731347020009612645E-17, 4.842444444444443441, 0.3119999999999999996 ) ) ;
#14350=VERTEX_POINT ( 'NONE', #475 ) ;
#14351=CARTESIAN_POINT ( 'NONE',  ( -0.04081130781707435068, 4.903883588982272279, 0.3119999910883811123 ) ) ;
#14361=CARTESIAN_POINT ( 'NONE',  ( -0.2819296736111110979, 5.200083333409199149, 0.000000000000000000 ) ) ;
#14362=CARTESIAN_POINT ( 'NONE',  ( 0.2734354562523998444, 4.478980055100710622, -0.1527955304013648985 ) ) ;
#14364=CARTESIAN_POINT ( 'NONE',  ( -0.09885966046364118298, 4.602272359509021804, -0.2966034080420659746 ) ) ;
#14366=DIRECTION ( 'NONE',  ( 0.000000000000000000, 0.000000000000000000, 1.000000000000000000 ) ) ;
#14368=CARTESIAN_POINT ( 'NONE',  ( 0.3119999999999999996, 4.804249999999998799, -0.1292346314604056745 ) ) ;
#14370=CARTESIAN_POINT ( 'NONE',  ( 5.178964085587577574E-17, 3.922305555631421026, 0.2819296736111110979 ) ) ;
#14374=ORIENTED_EDGE ( 'NONE', *, *, #16191, .F. ) ;
#14375=AXIS2_PLACEMENT_3D ( 'NONE', #21320, #3380, #16312 ) ;
#14376=CARTESIAN_POINT ( 'NONE',  ( 0.1292346314604058410, 3.901472222222222008, 0.3119999999999998885 ) ) ;
#14377=CARTESIAN_POINT ( 'NONE',  ( 0.2819296736111110424, 4.495222222298087544, -0.1167790944451423396 ) ) ;
#14380=CARTESIAN_POINT ( 'NONE',  ( -0.2581348291378180448, 4.507463561769111671, 0.1754396708902748736 ) ) ;
#14382=EDGE_CURVE ( 'NONE', #16112, #6049, #19930, .T. ) ;
#14386=CARTESIAN_POINT ( 'NONE',  ( 0.1993543840281266633, 4.123694444520309865, -0.1993543840281266910 ) ) ;
#14387=CARTESIAN_POINT ( 'NONE',  ( 1.910449006669871087E-17, 0.3652777777777774237, -0.3119999999999999996 ) ) ;
#14388=EDGE_CURVE ( 'NONE', #20417, #8097, #11342, .T. ) ;
#14392=AXIS2_PLACEMENT_3D ( 'NONE', #2446, #3909, #15370 ) ;
#14393=B_SPLINE_CURVE_WITH_KNOTS ( 'NONE', 3,
 ( #882, #12361, #8672, #13941, #19536, #23537, #14295, #10286, #17709, #13284 ),
 .UNSPECIFIED., .F., .F.,
 ( 4, 2, 2, 2, 4 ),
 ( 0.005993913058028690378, 0.007327704144062629002, 0.008661495230096568493, 0.009995286316130507984, 0.01132907740216444574 ),
 .UNSPECIFIED. ) ;
#14394=CARTESIAN_POINT ( 'NONE',  ( 0.1993543840281266355, 0.02847222214635558926, 0.1993543840281267465 ) ) ;
#14396=CYLINDRICAL_SURFACE ( 'NONE', #275, 0.3119999999999999996 ) ;
#14400=ORIENTED_EDGE ( 'NONE', *, *, #10374, .T. ) ;
#14402=DIRECTION ( 'NONE',  ( 0.000000000000000000, 0.000000000000000000, -1.000000000000000000 ) ) ;
#14403=CARTESIAN_POINT ( 'NONE',  ( -0.3120000192244279935, 3.836597312062911325, 0.04084114088547415033 ) ) ;
#14404=CARTESIAN_POINT ( 'NONE',  ( -0.1167790944451424368, 0.5180555554796888451, 0.2819296736111110424 ) ) ;
#14405=CARTESIAN_POINT ( 'NONE',  ( -1.726321361862525858E-17, 3.797305555631421470, -0.2819296736111110979 ) ) ;
#14408=CARTESIAN_POINT ( 'NONE',  ( -0.1993543840281266910, 4.470916666742532186, -0.1993543840281266910 ) ) ;
#14412=ORIENTED_EDGE ( 'NONE', *, *, #18402, .F. ) ;
#14413=CARTESIAN_POINT ( 'NONE',  ( 3.820898013339742174E-17, 5.384999999999999787, 0.3119999999999999996 ) ) ;
#14414=CARTESIAN_POINT ( 'NONE',  ( -0.1167790944451423257, 5.120222222298088433, -0.2819296736111110424 ) ) ;
#14419=CARTESIAN_POINT ( 'NONE',  ( 0.1993543840281267465, 4.818138888964754507, 0.1993543840281266633 ) ) ;
#14426=CARTESIAN_POINT ( 'NONE',  ( -0.2819296736111110424, 0.3513888888130222155, -0.1167790944451423396 ) ) ;
#14427=CARTESIAN_POINT ( 'NONE',  ( -0.1167790944451424368, 0.08749999992413336203, 0.2819296736111110424 ) ) ;
#14428=DIRECTION ( 'NONE',  ( -0.000000000000000000, -1.000000000000000000, -0.000000000000000000 ) ) ;
#14431=CARTESIAN_POINT ( 'NONE',  ( 2.064578755398029967E-15, 5.043833333485014947, -0.3119999999999999996 ) ) ;
#14432=DIRECTION ( 'NONE',  ( -0.000000000000000000, -1.000000000000000000, -0.000000000000000000 ) ) ;
#14434=CARTESIAN_POINT ( 'NONE',  ( -0.1857019731761083148, 3.882747264168788792, -0.2515721468173275910 ) ) ;
#14437=CARTESIAN_POINT ( 'NONE',  ( -0.2819296736111110979, 4.422305555631421470, 0.000000000000000000 ) ) ;
#14439=CARTESIAN_POINT ( 'NONE',  ( 0.2122370167333460234, 4.522644990543859045, 0.2293254978506919506 ) ) ;
#14440=CARTESIAN_POINT ( 'NONE',  ( -0.2819296736111110424, 5.029944444520310753, -0.1167790944451423119 ) ) ;
#14442=DIRECTION ( 'NONE',  ( 0.000000000000000000, 0.000000000000000000, -1.000000000000000000 ) ) ;
#14446=CARTESIAN_POINT ( 'NONE',  ( 0.1292346314604058410, 4.408416666818399499, 0.3119999999999998885 ) ) ;
#14447=CARTESIAN_POINT ( 'NONE',  ( 0.1993543840281266633, 4.512583333409199149, -0.1993543840281266910 ) ) ;
#14448=CARTESIAN_POINT ( 'NONE',  ( -0.2819296736111110979, 3.908416666742532630, 0.000000000000000000 ) ) ;
#14451=AXIS2_PLACEMENT_3D ( 'NONE', #20464, #7421, #3761 ) ;
#14456=CARTESIAN_POINT ( 'NONE',  ( -0.1914089481446534236, 4.954695441720193827, 0.2497358724762595572 ) ) ;
#14457=FACE_OUTER_BOUND ( 'NONE', #2716, .T. ) ;
#14458=VERTEX_POINT ( 'NONE', #22280 ) ;
#14459=CARTESIAN_POINT ( 'NONE',  ( 0.1292346314604057023, 0.3340277776260448528, 0.3119999999999998885 ) ) ;
#14461=CARTESIAN_POINT ( 'NONE',  ( -0.07998601114778688959, 5.127656800766811074, 0.2972660808172664093 ) ) ;
#14464=ORIENTED_EDGE ( 'NONE', *, *, #19419, .F. ) ;
#14466=CARTESIAN_POINT ( 'NONE',  ( 0.2819296736111110424, 0.3097222221463555303, 0.1167790944451424923 ) ) ;
#14468=CARTESIAN_POINT ( 'NONE',  ( -0.1993543840281266355, 4.415361111186976828, 0.1993543840281267465 ) ) ;
#14469=DIRECTION ( 'NONE',  ( -0.000000000000000000, -1.000000000000000000, -0.000000000000000000 ) ) ;
#14471=CARTESIAN_POINT ( 'NONE',  ( -5.731347020009612645E-17, 0.3861111109593781676, 0.3119999999999999996 ) ) ;
#14472=CARTESIAN_POINT ( 'NONE',  ( 0.3119999999999999996, 4.134111111111110404, -3.820898013339742174E-17 ) ) ;
#14474=CARTESIAN_POINT ( 'NONE',  ( 0.3119999999999999996, 4.974388889040620931, -3.820898013339742174E-17 ) ) ;
#14475=CARTESIAN_POINT ( 'NONE',  ( 0.2206173157302027954, 4.863277777777777366, -0.2206173157302028232 ) ) ;
#14476=ORIENTED_EDGE ( 'NONE', *, *, #8866, .T. ) ;
#14483=CARTESIAN_POINT ( 'NONE',  ( -0.1993543840281267465, 0.3618055554796889006, 0.1993543840281266633 ) ) ;
#14485=CARTESIAN_POINT ( 'NONE',  ( -0.2819296736111110424, 5.252166666742532186, -0.1167790944451423119 ) ) ;
#14488=CARTESIAN_POINT ( 'NONE',  ( 5.731347020009612645E-17, 3.842444444444443441, 0.3119999999999999996 ) ) ;
#14490=CARTESIAN_POINT ( 'NONE',  ( 0.01770140881492013318, 4.876688247272896071, -0.3115197202295738044 ) ) ;
#14493=CARTESIAN_POINT ( 'NONE',  ( 0.1292346314604058410, 4.679249999999998799, 0.3119999999999998885 ) ) ;
#14494=CARTESIAN_POINT ( 'NONE',  ( 0.06933867596744393291, 5.200618429028261325, 0.2766904312229080953 ) ) ;
#14496=CARTESIAN_POINT ( 'NONE',  ( -0.1167790944451423535, 3.918833333409198705, 0.2819296736111110979 ) ) ;
#14497=CARTESIAN_POINT ( 'NONE',  ( -0.2819296736111110424, 3.752166666742533074, -0.1167790944451423119 ) ) ;
#14498=CARTESIAN_POINT ( 'NONE',  ( 0.06970122686329188744, 4.041909198427281247, -0.3046041375326968281 ) ) ;
#14501=CARTESIAN_POINT ( 'NONE',  ( -0.3119999999999999996, 4.550777777777777366, 0.000000000000000000 ) ) ;
#14502=CARTESIAN_POINT ( 'NONE',  ( -0.2819296736111110424, 4.467444444520308977, 0.1167790944451424923 ) ) ;
#14504=CARTESIAN_POINT ( 'NONE',  ( -0.3118796326775569172, 4.502940687055745350, 0.02682079161860434491 ) ) ;
#14509=CARTESIAN_POINT ( 'NONE',  ( -0.2819296736111110979, 3.811194444520310309, 0.000000000000000000 ) ) ;
#14512=CARTESIAN_POINT ( 'NONE',  ( 0.3119999999999999996, 0.07013888873715595773, -0.1292346314604056468 ) ) ;
#14514=CARTESIAN_POINT ( 'NONE',  ( -0.1993543840281267465, 0.3479166665908000611, 0.1993543840281266633 ) ) ;
#14521=VERTEX_POINT ( 'NONE', #11196 ) ;
#14523=CARTESIAN_POINT ( 'NONE',  ( -0.3038794317022511793, 3.833275345265239942, -0.08166550760139516807 ) ) ;
#14524=CARTESIAN_POINT ( 'NONE',  ( 0.3119999999999998885, 0.1256944444444441089, 0.1292346314604058410 ) ) ;
#14526=CARTESIAN_POINT ( 'NONE',  ( 0.2819296736111110424, 3.953555555631421914, -0.1167790944451423396 ) ) ;
#14529=CARTESIAN_POINT ( 'NONE',  ( -0.1167790944451423535, 4.488277777853644679, 0.2819296736111110424 ) ) ;
#14531=CARTESIAN_POINT ( 'NONE',  ( 5.731347020009612645E-17, 4.397999999999999687, 0.3119999999999999996 ) ) ;
#14534=CARTESIAN_POINT ( 'NONE',  ( 0.2819296736111110979, 5.154944444520308977, 0.1167790944451422425 ) ) ;
#14536=CARTESIAN_POINT ( 'NONE',  ( 0.02226199859978414408, 4.209868373251637763, -0.3112347022699947230 ) ) ;
#14538=CARTESIAN_POINT ( 'NONE',  ( -5.731347020009612645E-17, 0.2263888888888885564, 0.3119999999999999996 ) ) ;
#14539=CARTESIAN_POINT ( 'NONE',  ( -0.1167790944451423535, 4.863277777853642903, 0.2819296736111110979 ) ) ;
#14541=CARTESIAN_POINT ( 'NONE',  ( -0.1618391056162997999, 4.066759731312079573, 0.2668031243805282782 ) ) ;
#14543=CARTESIAN_POINT ( 'NONE',  ( -0.2206173157302027954, 0.4208333331816004330, -0.2206173157302028232 ) ) ;
#14545=CARTESIAN_POINT ( 'NONE',  ( 0.1993543840281266355, 0.2090277777019111383, 0.1993543840281267465 ) ) ;
#14546=ORIENTED_EDGE ( 'NONE', *, *, #10189, .F. ) ;
#14547=CARTESIAN_POINT ( 'NONE',  ( 1.726321361862525858E-17, 0.06319444436857780956, -0.2819296736111110979 ) ) ;
#14551=CARTESIAN_POINT ( 'NONE',  ( -0.3119999999999998885, 3.776472222222221564, 0.1292346314604058410 ) ) ;
#14552=EDGE_CURVE ( 'NONE', #23019, #10368, #8860, .T. ) ;
#14553=CARTESIAN_POINT ( 'NONE',  ( -0.2517964863178585588, 3.885433942164395305, -0.1842776042936377368 ) ) ;
#14554=CARTESIAN_POINT ( 'NONE',  ( 0.1993543840281266910, -0.01319444452031107509, -0.1993543840281266910 ) ) ;
#14556=CARTESIAN_POINT ( 'NONE',  ( 0.2819296736111110424, 4.620222222298088433, -0.1167790944451423396 ) ) ;
#14557=FACE_OUTER_BOUND ( 'NONE', #18695, .T. ) ;
#14558=CARTESIAN_POINT ( 'NONE',  ( 0.2060069779502269882, 4.537481089443112126, -0.2362988211741367806 ) ) ;
#14559=CARTESIAN_POINT ( 'NONE',  ( 5.178964085587577574E-17, 4.991750000075866112, 0.2819296736111110979 ) ) ;
#14560=CARTESIAN_POINT ( 'NONE',  ( -0.2993415042824079109, 0.05277108377353196406, 0.04638604691508683292 ) ) ;
#14561=CARTESIAN_POINT ( 'NONE',  ( 0.07147791734704542210, 3.764038038968208877, -0.3039139294749904074 ) ) ;
#14564=CARTESIAN_POINT ( 'NONE',  ( -1.910449006669871087E-17, 4.266055555707287894, -0.3119999999999999996 ) ) ;
#14567=CARTESIAN_POINT ( 'NONE',  ( -1.726321361862525858E-17, 4.519527777853643791, -0.2819296736111110979 ) ) ;
#14568=CARTESIAN_POINT ( 'NONE',  ( -0.1167790944451423535, 3.863277777853643791, 0.2819296736111110424 ) ) ;
#14570=VERTEX_POINT ( 'NONE', #22763 ) ;
#14572=CYLINDRICAL_SURFACE ( 'NONE', #9211, 0.3119999999999999996 ) ;
#14573=ADVANCED_FACE ( 'NONE', ( #16915 ), #569, .T. ) ;
#14574=CARTESIAN_POINT ( 'NONE',  ( -0.1572786115130385687, 4.937427088230124106, -0.2725414607716101223 ) ) ;
#14577=CARTESIAN_POINT ( 'NONE',  ( 1.910449006669871087E-17, 0.2472222220704892726, -0.3119999999999999996 ) ) ;
#14578=CARTESIAN_POINT ( 'NONE',  ( -0.2476943800122561878, 4.396861609578765595, 0.1908053648353139065 ) ) ;
#14584=ORIENTED_EDGE ( 'NONE', *, *, #7642, .T. ) ;
#14586=CARTESIAN_POINT ( 'NONE',  ( 0.1989253662351168350, 5.077772732731912875, 0.2405052583373312181 ) ) ;
#14588=CARTESIAN_POINT ( 'NONE',  ( -1.726321361862525858E-17, 4.116750000075865223, -0.2819296736111110979 ) ) ;
#14589=CARTESIAN_POINT ( 'NONE',  ( 0.1167790944451424506, 5.092444444520309865, 0.2819296736111110424 ) ) ;
#14592=CARTESIAN_POINT ( 'NONE',  ( -0.1292346314604056745, 3.984805555555554601, -0.3119999999999999996 ) ) ;
#14594=CARTESIAN_POINT ( 'NONE',  ( -0.1292346314604057023, 4.957027777929510215, 0.3119999999999998885 ) ) ;
#14596=CARTESIAN_POINT ( 'NONE',  ( 5.178964085587577574E-17, 5.158416666742532186, 0.2819296736111110979 ) ) ;
#14597=CARTESIAN_POINT ( 'NONE',  ( 0.3119999999999999996, 4.859805555555554157, -0.1292346314604056745 ) ) ;
#14600=CARTESIAN_POINT ( 'NONE',  ( -0.1331525752728061063, 0.05822810958904708900, 0.2781245439472574410 ) ) ;
#14607=CARTESIAN_POINT ( 'NONE',  ( 1.726321361862525858E-17, 0.3409722221463556413, -0.2819296736111110979 ) ) ;
#14609=CARTESIAN_POINT ( 'NONE',  ( 0.1167790944451424368, 5.106333333409198261, 0.2819296736111110424 ) ) ;
#14612=CARTESIAN_POINT ( 'NONE',  ( 0.1993543840281266633, 4.998694444520309865, -0.1993543840281266910 ) ) ;
#14614=CARTESIAN_POINT ( 'NONE',  ( 0.0001028783557116418908, 4.877163902639057191, -0.3119999876241853487 ) ) ;
#14615=CARTESIAN_POINT ( 'NONE',  ( 0.3120000000000000551, 4.575083333333332725, 0.1292346314604056190 ) ) ;
#14617=CARTESIAN_POINT ( 'NONE',  ( -0.3119999999999999996, 4.661888888888888083, 0.000000000000000000 ) ) ;
#14618=CARTESIAN_POINT ( 'NONE',  ( 0.1167790944451422702, 4.113277777853642903, -0.2819296736111110979 ) ) ;
#14619=CARTESIAN_POINT ( 'NONE',  ( -0.1993543840281266910, 3.748694444520310309, -0.1993543840281266910 ) ) ;
#14621=CARTESIAN_POINT ( 'NONE',  ( 0.2877648753177015628, 4.033457023929424956, -0.1207660770027009639 ) ) ;
#14622=CARTESIAN_POINT ( 'NONE',  ( -5.731347020009612645E-17, 0.3930555555555551583, 0.3119999999999999996 ) ) ;
#14624=VERTEX_POINT ( 'NONE', #19702 ) ;
#14627=CARTESIAN_POINT ( 'NONE',  ( 5.178964085587577574E-17, 4.255638888964754507, 0.2819296736111110979 ) ) ;
#14628=CARTESIAN_POINT ( 'NONE',  ( -0.2416764884589730211, 4.508252704873092043, 0.1973253190368417231 ) ) ;
#14638=CARTESIAN_POINT ( 'NONE',  ( 1.726321361862525858E-17, 0.2159722221463555858, -0.2819296736111110979 ) ) ;
#14639=CARTESIAN_POINT ( 'NONE',  ( 0.3120005064808646922, 3.864374921735875379, -0.04083496376970818104 ) ) ;
#14644=ORIENTED_EDGE ( 'NONE', *, *, #23553, .T. ) ;
#14646=DIRECTION ( 'NONE',  ( -0.000000000000000000, -1.000000000000000000, -0.000000000000000000 ) ) ;
#14647=CARTESIAN_POINT ( 'NONE',  ( -0.3119999999999999996, 4.713972222222221120, -0.1292346314604056468 ) ) ;
#14648=CARTESIAN_POINT ( 'NONE',  ( -0.1292346314604058410, 0.0006944444444441107535, 0.3119999999999998885 ) ) ;
#14649=CARTESIAN_POINT ( 'NONE',  ( -0.1167790944451423257, 3.856333333409198705, -0.2819296736111110424 ) ) ;
#14651=VECTOR ( 'NONE', #22511, 39.37007874015748143 ) ;
#14652=CARTESIAN_POINT ( 'NONE',  ( 0.1993543840281267465, 4.443138888964754507, 0.1993543840281266633 ) ) ;
#14653=DIRECTION ( 'NONE',  ( -0.000000000000000000, -1.000000000000000000, -0.000000000000000000 ) ) ;
#14656=CARTESIAN_POINT ( 'NONE',  ( 0.05907641261700106311, 4.375511868578897179, -0.3066178703699756758 ) ) ;
#14657=CARTESIAN_POINT ( 'NONE',  ( 0.1167790944451422702, 5.168833333409199149, -0.2819296736111110424 ) ) ;
#14660=( LENGTH_UNIT ( ) NAMED_UNIT ( * ) SI_UNIT ( $, .METRE. ) );
#14662=FACE_OUTER_BOUND ( 'NONE', #4086, .T. ) ;
#14664=CARTESIAN_POINT ( 'NONE',  ( 0.1993543840281266633, 4.665361111186976828, -0.1993543840281266910 ) ) ;
#14670=CARTESIAN_POINT ( 'NONE',  ( 0.1167790944451423257, 0.6152777777019110550, -0.2819296736111110424 ) ) ;
#14673=CARTESIAN_POINT ( 'NONE',  ( 0.1167790944451423257, 0.2819444443685777957, -0.2819296736111110424 ) ) ;
#14674=FACE_OUTER_BOUND ( 'NONE', #12155, .T. ) ;
#14680=CARTESIAN_POINT ( 'NONE',  ( 3.820898013339742174E-17, 5.384999999999999787, 0.3119999999999999996 ) ) ;
#14681=CARTESIAN_POINT ( 'NONE',  ( -0.1167790944451423257, 4.467444444520309865, -0.2819296736111110424 ) ) ;
#14682=CARTESIAN_POINT ( 'NONE',  ( -0.1993543840281267465, 0.01458333325746670114, 0.1993543840281266633 ) ) ;
#14683=CARTESIAN_POINT ( 'NONE',  ( -0.2819296736111110424, 4.585500000075865223, -0.1167790944451423119 ) ) ;
#14685=CARTESIAN_POINT ( 'NONE',  ( 0.02106394849456709809, 4.543234972684153661, -0.3113162720545575857 ) ) ;
#14686=CARTESIAN_POINT ( 'NONE',  ( -0.1167790944451423257, 5.023000000075867000, -0.2819296736111110424 ) ) ;
#14687=CARTESIAN_POINT ( 'NONE',  ( 0.1993543840281266633, 4.443138888964754507, -0.1993543840281266910 ) ) ;
#14688=CARTESIAN_POINT ( 'NONE',  ( 0.2902266206095440726, 3.748848065998740875, 0.1156229089065601984 ) ) ;
#14689=CARTESIAN_POINT ( 'NONE',  ( -0.3120000000000000551, 0.4868055554038225874, 0.1292346314604056190 ) ) ;
#14691=CARTESIAN_POINT ( 'NONE',  ( -3.345742422185251127E-06, 4.766055647721512578, -0.3119999999820609049 ) ) ;
#14692=CARTESIAN_POINT ( 'NONE',  ( -0.3119999999999999996, 4.220916666818398610, -0.1292346314604056468 ) ) ;
#14693=CARTESIAN_POINT ( 'NONE',  ( -0.1993543840281266355, 4.484805555631421470, 0.1993543840281267465 ) ) ;
#14694=CARTESIAN_POINT ( 'NONE',  ( 0.1993543840281266633, 3.832027777853643791, -0.1993543840281266910 ) ) ;
#14703=VERTEX_POINT ( 'NONE', #22838 ) ;
#14704=CARTESIAN_POINT ( 'NONE',  ( 0.3119999999999999996, 0.2333333331816004053, 0.000000000000000000 ) ) ;
#14706=CARTESIAN_POINT ( 'NONE',  ( -2.750539236387841874E-07, 4.266055563097283176, -0.3119999999998787632 ) ) ;
#14707=CARTESIAN_POINT ( 'NONE',  ( 5.731347020009612645E-17, 4.509111111111110404, 0.3119999999999999996 ) ) ;
#14716=CARTESIAN_POINT ( 'NONE',  ( 0.1167790944451422702, 4.224388888964755395, -0.2819296736111110424 ) ) ;
#14717=CARTESIAN_POINT ( 'NONE',  ( 0.1167790944451422702, 5.113277777853642903, -0.2819296736111110979 ) ) ;
#14719=CARTESIAN_POINT ( 'NONE',  ( -0.3036138212764256661, 4.226459472032660258, 0.07378917105941848464 ) ) ;
#14721=CARTESIAN_POINT ( 'NONE',  ( 0.3119999999999999996, 4.922305555707287006, -0.1292346314604056745 ) ) ;
#14722=CARTESIAN_POINT ( 'NONE',  ( -0.2082794372640225100, 5.206640035683668621, 0.1900105704308308607 ) ) ;
#14726=ORIENTED_EDGE ( 'NONE', *, *, #8866, .F. ) ;
#14728=CARTESIAN_POINT ( 'NONE',  ( -0.2194851440959312838, 0.05625703873743409522, 0.2130962475854012161 ) ) ;
#14729=ORIENTED_EDGE ( 'NONE', *, *, #12728, .T. ) ;
#14731=CARTESIAN_POINT ( 'NONE',  ( -0.1167790944451423257, 5.009111111186976828, -0.2819296736111110424 ) ) ;
#14737=CARTESIAN_POINT ( 'NONE',  ( -5.178964085587577574E-17, 0.3131944443685777957, 0.2819296736111110979 ) ) ;
#14739=CARTESIAN_POINT ( 'NONE',  ( 0.1167790944451424368, 4.939666666742532186, 0.2819296736111110424 ) ) ;
#14740=CARTESIAN_POINT ( 'NONE',  ( 0.01010037888641339247, 4.487987261627375268, -0.3119999999597998785 ) ) ;
#14742=CARTESIAN_POINT ( 'NONE',  ( -0.2819296736111110424, 4.967444444520310753, 0.1167790944451424923 ) ) ;
#14743=CARTESIAN_POINT ( 'NONE',  ( -0.1570231241692966462, 4.178164908778625453, 0.2726904212700292374 ) ) ;
#14747=CARTESIAN_POINT ( 'NONE',  ( 0.1292346314604058410, 4.623694444444443441, 0.3119999999999998885 ) ) ;
#14748=CARTESIAN_POINT ( 'NONE',  ( -0.1993543840281266910, 4.068138888964754507, -0.1993543840281266910 ) ) ;
#14749=CARTESIAN_POINT ( 'NONE',  ( 0.000000000000000000, 5.384999999999999787, -0.3119999999999999996 ) ) ;
#14750=CARTESIAN_POINT ( 'NONE',  ( 0.2972964765959422717, 4.032653405754279774, -0.09468309758334170212 ) ) ;
#14760=CARTESIAN_POINT ( 'NONE',  ( -1.910449006669871087E-17, 4.259111111111110404, -0.3119999999999999996 ) ) ;
#14764=CARTESIAN_POINT ( 'NONE',  ( -0.1993543840281266633, 0.2784722221463555858, -0.1993543840281266910 ) ) ;
#14771=( BOUNDED_CURVE ( )  B_SPLINE_CURVE ( 2, ( #8478, #15920, #12530, #5182, #19949, #17636, #3239, #8847, #7027 ),
 .UNSPECIFIED., .F., .T. ) 
 B_SPLINE_CURVE_WITH_KNOTS ( ( 3, 2, 2, 2, 3 ),
 ( 0.3125000000000000000, 0.3229166666666666852, 0.3333333333333333148, 0.3437500000000000000, 0.3541666666666666852 ),
 .UNSPECIFIED. ) 
 CURVE ( )  GEOMETRIC_REPRESENTATION_ITEM ( )  RATIONAL_B_SPLINE_CURVE ( ( 1.000000000000000000, 0.9238795325112867385, 1.000000000000000000, 0.9238795325112867385, 1.000000000000000000, 0.9238795325112867385, 1.000000000000000000, 0.9238795325112867385, 1.000000000000000000 ) ) 
 REPRESENTATION_ITEM ( '' )  );
#14772=CARTESIAN_POINT ( 'NONE',  ( -0.3083781185080407550, 5.106384284016617592, 0.03939064032742058130 ) ) ;
#14774=CARTESIAN_POINT ( 'NONE',  ( 0.1292346314604057023, 0.007638888888888556439, 0.3119999999999998885 ) ) ;
#14775=CARTESIAN_POINT ( 'NONE',  ( -0.2819296736111110424, 3.918833333409198705, -0.1167790944451423119 ) ) ;
#14778=CARTESIAN_POINT ( 'NONE',  ( -0.1167790944451423535, 4.377166666742532186, 0.2819296736111110424 ) ) ;
#14779=CARTESIAN_POINT ( 'NONE',  ( 0.2206173157302027676, 0.1152777776260448528, 0.2206173157302028787 ) ) ;
#14782=CARTESIAN_POINT ( 'NONE',  ( 0.2824780601149360915, 4.367251178688803748, -0.1354494196218661295 ) ) ;
#14783=CARTESIAN_POINT ( 'NONE',  ( -0.1993543840281266355, 4.859805555631421470, 0.1993543840281267465 ) ) ;
#14784=CARTESIAN_POINT ( 'NONE',  ( -0.2605107293023110615, 5.151385429156462692, -0.1530708234642420562 ) ) ;
#14787=DIRECTION ( 'NONE',  ( 0.000000000000000000, 0.000000000000000000, -1.000000000000000000 ) ) ;
#14788=CARTESIAN_POINT ( 'NONE',  ( 0.1993543840281267465, 4.762583333409199149, 0.1993543840281266633 ) ) ;
#14790=CARTESIAN_POINT ( 'NONE',  ( -0.1292346314604044810, 4.783416666666666650, 0.3120000000000012208 ) ) ;
#14791=CARTESIAN_POINT ( 'NONE',  ( 0.000000000000000000, 5.384999999999999787, 0.000000000000000000 ) ) ;
#14792=CARTESIAN_POINT ( 'NONE',  ( 0.1167790944451423257, 0.5041666665908002276, -0.2819296736111110424 ) ) ;
#14793=ORIENTED_EDGE ( 'NONE', *, *, #34, .T. ) ;
#14795=CARTESIAN_POINT ( 'NONE',  ( -0.2819296736111110979, 0.2437499999241333759, -3.452642723725051716E-17 ) ) ;
#14796=CARTESIAN_POINT ( 'NONE',  ( -0.2206173157302027676, 4.335499999999998799, 0.2206173157302028787 ) ) ;
#14797=CARTESIAN_POINT ( 'NONE',  ( -0.2838685103340625182, 5.200889060888042259, -0.02438439758188335263 ) ) ;
#14803=CARTESIAN_POINT ( 'NONE',  ( -0.1993543840281266910, 4.526472222298087544, -0.1993543840281266910 ) ) ;
#14805=CARTESIAN_POINT ( 'NONE',  ( 0.1281033428157181131, 4.540104105756370245, -0.2863062090479261412 ) ) ;
#14806=CARTESIAN_POINT ( 'NONE',  ( 5.178964085587577574E-17, 5.102861111186976828, 0.2819296736111110979 ) ) ;
#14807=CARTESIAN_POINT ( 'NONE',  ( 0.2819296736111110979, 4.380638888964754507, -3.452642723725051716E-17 ) ) ;
#14808=CARTESIAN_POINT ( 'NONE',  ( 0.1943347089597592114, 3.744229887717848815, 0.2454019012448671322 ) ) ;
#14811=CARTESIAN_POINT ( 'NONE',  ( 0.2450140762121532367, 3.912827427306669215, 0.1969830315022409462 ) ) ;
#14812=CARTESIAN_POINT ( 'NONE',  ( -0.2206173157302028232, 4.050777777929510215, -0.2206173157302028232 ) ) ;
#14813=CARTESIAN_POINT ( 'NONE',  ( -0.1993543840281266910, 4.526472222298087544, -0.1993543840281266910 ) ) ;
#14814=CARTESIAN_POINT ( 'NONE',  ( 0.1167790944451424368, 3.925777777853643347, 0.2819296736111110424 ) ) ;
#14816=ORIENTED_EDGE ( 'NONE', *, *, #23915, .F. ) ;
#14820=CARTESIAN_POINT ( 'NONE',  ( -4.760580627680044823E-09, 4.932722222506802368, -0.3119999999999999996 ) ) ;
#14822=ORIENTED_EDGE ( 'NONE', *, *, #21273, .F. ) ;
#14823=CARTESIAN_POINT ( 'NONE',  ( 1.910449006669871087E-17, 0.5249999998482670627, -0.3119999999999999996 ) ) ;
#14825=CARTESIAN_POINT ( 'NONE',  ( 4.422035572083168519E-06, 4.266055436896041719, -0.3120000000040196175 ) ) ;
#14828=CARTESIAN_POINT ( 'NONE',  ( 0.08160588755459347032, 3.962804008186619154, 0.3038914485545370359 ) ) ;
#14830=VERTEX_POINT ( 'NONE', #7723 ) ;
#14833=CARTESIAN_POINT ( 'NONE',  ( 0.2615970440521218077, 5.090933575972008462, -0.1701841655577382706 ) ) ;
#14835=CARTESIAN_POINT ( 'NONE',  ( -0.2819296736111110424, 4.182722222298087544, -0.1167790944451423119 ) ) ;
#14836=CARTESIAN_POINT ( 'NONE',  ( 0.2819296736111110979, 5.047305555631421470, -3.452642723725051716E-17 ) ) ;
#14839=CARTESIAN_POINT ( 'NONE',  ( -0.3118931856306824124, 4.223187597109412827, -0.04158228275762527321 ) ) ;
#14840=CARTESIAN_POINT ( 'NONE',  ( -0.3119999999999999996, 3.828555555555555046, 0.000000000000000000 ) ) ;
#14842=CARTESIAN_POINT ( 'NONE',  ( -0.3119999999999999996, 5.054250000151731648, -0.1292346314604056468 ) ) ;
#14843=CARTESIAN_POINT ( 'NONE',  ( 0.2065105149757635039, 4.800239184964532058, 0.2355781109500581227 ) ) ;
#14849=CARTESIAN_POINT ( 'NONE',  ( 0.2739954178377071448, 0.03290028280361406710, 0.07218012553276310916 ) ) ;
#14850=ORIENTED_EDGE ( 'NONE', *, *, #17076, .T. ) ;
#14852=CARTESIAN_POINT ( 'NONE',  ( 5.178964085587577574E-17, 5.144527777853643791, 0.2819296736111110979 ) ) ;
#14857=CARTESIAN_POINT ( 'NONE',  ( -5.178964085587577574E-17, 0.3687499999241333204, 0.2819296736111110979 ) ) ;
#14859=CARTESIAN_POINT ( 'NONE',  ( -0.1167790944451423535, 5.043833333409199149, 0.2819296736111110424 ) ) ;
#14860=CARTESIAN_POINT ( 'NONE',  ( 0.09811062177514703886, 4.485527722901675673, -0.2964682546474478597 ) ) ;
#14861=CARTESIAN_POINT ( 'NONE',  ( 0.2819296736111110979, 4.988277777853642903, 0.1167790944451422425 ) ) ;
#14867=CARTESIAN_POINT ( 'NONE',  ( -0.2206173157302027676, 4.446611111111110404, 0.2206173157302028787 ) ) ;
#14869=CARTESIAN_POINT ( 'NONE',  ( -0.1993543840281266910, 3.957027777853642903, -0.1993543840281266910 ) ) ;
#14871=CARTESIAN_POINT ( 'NONE',  ( 0.3092439325280461060, 4.031202289993226273, -0.04474935879389044247 ) ) ;
#14872=CARTESIAN_POINT ( 'NONE',  ( -0.1056007431694158949, 3.735235609415689773, 0.2935856185260024565 ) ) ;
#14873=CARTESIAN_POINT ( 'NONE',  ( -0.1292346314604081725, 4.561194444444443441, 0.3119999999999974460 ) ) ;
#14875=CARTESIAN_POINT ( 'NONE',  ( -0.1746005203414776330, 4.121880983008269439, 0.2585734667409969600 ) ) ;
#14876=CARTESIAN_POINT ( 'NONE',  ( 0.03061863295597656159, 4.154064737224905102, -0.3119999618532416918 ) ) ;
#14881=CARTESIAN_POINT ( 'NONE',  ( 1.726321361862525858E-17, 0.1604166665908000333, -0.2819296736111110979 ) ) ;
#14887=CARTESIAN_POINT ( 'NONE',  ( 0.000000000000000000, 5.384999999999999787, 0.000000000000000000 ) ) ;
#14888=CARTESIAN_POINT ( 'NONE',  ( -0.2206173157302027954, 0.03888888888888855644, -0.2206173157302028232 ) ) ;
#14889=CARTESIAN_POINT ( 'NONE',  ( 0.1292346314604056190, 5.255638888888888083, -0.3119999999999999996 ) ) ;
#14891=VERTEX_POINT ( 'NONE', #20358 ) ;
#14892=CARTESIAN_POINT ( 'NONE',  ( 0.2819296736111110979, 4.505638888964754507, -3.452642723725051716E-17 ) ) ;
#14894=DIRECTION ( 'NONE',  ( -0.000000000000000000, -1.000000000000000000, -0.000000000000000000 ) ) ;
#14896=CARTESIAN_POINT ( 'NONE',  ( -0.2819296736111110424, 5.023000000075864335, 0.1167790944451424923 ) ) ;
#14897=CARTESIAN_POINT ( 'NONE',  ( -0.2851947699491957922, 5.157899255522624848, 0.09432962184258192329 ) ) ;
#14900=CARTESIAN_POINT ( 'NONE',  ( 0.2819296736111111534, 4.766055555631421470, 0.1167790944451422563 ) ) ;
#14903=CARTESIAN_POINT ( 'NONE',  ( -0.3120000000000000551, 0.4312499998482670072, 0.1292346314604056190 ) ) ;
#14904=( BOUNDED_CURVE ( )  B_SPLINE_CURVE ( 2, ( #3840, #5900, #13008, #14941, #15065, #20304, #24067, #9326, #16766 ),
 .UNSPECIFIED., .F., .F. ) 
 B_SPLINE_CURVE_WITH_KNOTS ( ( 3, 2, 2, 2, 3 ),
 ( 0.7708333333333333703, 0.7812500000000000000, 0.7916666666666666297, 0.8020833333333333703, 0.8125000000000000000 ),
 .UNSPECIFIED. ) 
 CURVE ( )  GEOMETRIC_REPRESENTATION_ITEM ( )  RATIONAL_B_SPLINE_CURVE ( ( 1.000000000000000000, 0.9238795325112867385, 1.000000000000000000, 0.9238795325112867385, 1.000000000000000000, 0.9238795325112867385, 1.000000000000000000, 0.9238795325112867385, 1.000000000000000000 ) ) 
 REPRESENTATION_ITEM ( '' )  );
#14905=CARTESIAN_POINT ( 'NONE',  ( 0.1167790944451423535, 0.4833333332574667462, 0.2819296736111110424 ) ) ;
#14908=CARTESIAN_POINT ( 'NONE',  ( 0.1993543840281266910, 0.1673611110352444808, -0.1993543840281266910 ) ) ;
#14916=CARTESIAN_POINT ( 'NONE',  ( -0.2819296736111111534, 0.3444444443685778512, 0.1167790944451422563 ) ) ;
#14918=CARTESIAN_POINT ( 'NONE',  ( 0.1167790944451424368, 4.606333333409200037, 0.2819296736111110424 ) ) ;
#14921=CARTESIAN_POINT ( 'NONE',  ( 0.1993543840281267465, 5.165361111186976828, 0.1993543840281266633 ) ) ;
#14923=CARTESIAN_POINT ( 'NONE',  ( -0.2819296736111110979, 4.519527777853643791, 0.000000000000000000 ) ) ;
#14924=CARTESIAN_POINT ( 'NONE',  ( 0.03254485797104954281, 3.739221291613469500, 0.3108638213126159733 ) ) ;
#14926=CARTESIAN_POINT ( 'NONE',  ( 0.3119999999999999996, 4.088972222373953969, -0.1292346314604056745 ) ) ;
#14927=CARTESIAN_POINT ( 'NONE',  ( -0.1993543840281266910, 4.582027777853643791, -0.1993543840281266910 ) ) ;
#14934=CARTESIAN_POINT ( 'NONE',  ( -0.1246856373887775538, 4.845749071750494963, 0.2860203695084122533 ) ) ;
#14935=FACE_OUTER_BOUND ( 'NONE', #21672, .T. ) ;
#14937=CARTESIAN_POINT ( 'NONE',  ( 0.2206173157302027676, 0.5597222220704892726, 0.2206173157302028787 ) ) ;
#14941=CARTESIAN_POINT ( 'NONE',  ( -0.3119999999999999996, 0.4868055555555551583, -0.1292346314604056745 ) ) ;
#14944=VERTEX_POINT ( 'NONE', #7549 ) ;
#14950=CARTESIAN_POINT ( 'NONE',  ( -0.1167790944451423535, 4.252166666742533074, 0.2819296736111110424 ) ) ;
#14951=CARTESIAN_POINT ( 'NONE',  ( 0.2819296736111110979, 5.102861111186976828, -3.452642723725051716E-17 ) ) ;
#14954=CARTESIAN_POINT ( 'NONE',  ( -0.3119999999999999996, 3.936194444444443441, -0.1292346314604056468 ) ) ;
#14955=CARTESIAN_POINT ( 'NONE',  ( -0.3119999999999999996, 4.832027777929510215, -0.1292346314604056468 ) ) ;
#14956=CARTESIAN_POINT ( 'NONE',  ( 0.3010077053382372303, 4.805368180615793960, 0.08343459883119609677 ) ) ;
#14960=CARTESIAN_POINT ( 'NONE',  ( 0.2267002397118211554, 0.03806586609000491700, -0.1772890151010469983 ) ) ;
#14965=CARTESIAN_POINT ( 'NONE',  ( 0.1167790944451422702, 5.057722222298087544, -0.2819296736111110424 ) ) ;
#14966=CARTESIAN_POINT ( 'NONE',  ( 5.178964085587577574E-17, 3.769527777853644235, 0.2819296736111110979 ) ) ;
#14971=CARTESIAN_POINT ( 'NONE',  ( -0.1167790944451424506, 0.2541666665908000056, 0.2819296736111110424 ) ) ;
#14973=CARTESIAN_POINT ( 'NONE',  ( -0.1993543840281266355, 4.929250000075866112, 0.1993543840281267465 ) ) ;
#14976=CARTESIAN_POINT ( 'NONE',  ( 0.1167790944451424368, 4.981333333409198261, 0.2819296736111110424 ) ) ;
#14981=CARTESIAN_POINT ( 'NONE',  ( -0.1292346314604057023, 4.505638888888887195, 0.3119999999999998885 ) ) ;
#14984=CARTESIAN_POINT ( 'NONE',  ( 0.1292346314604057300, 0.3340277776260447418, 0.3119999999999998885 ) ) ;
#14985=CYLINDRICAL_SURFACE ( 'NONE', #14451, 0.3119999999999999996 ) ;
#14986=CARTESIAN_POINT ( 'NONE',  ( 0.07901360339605351113, 4.597109866223552110, -0.3045289936772480055 ) ) ;
#14989=CARTESIAN_POINT ( 'NONE',  ( -0.1607995357127989244, 4.122348446938056021, 0.2674091126109629513 ) ) ;
#14990=CARTESIAN_POINT ( 'NONE',  ( 6.388359114324787822E-07, 4.627192232271967853, 0.3119999999985919592 ) ) ;
#14992=EDGE_CURVE ( 'NONE', #2791, #21366, #1004, .T. ) ;
#14995=AXIS2_PLACEMENT_3D ( 'NONE', #21100, #9524, #13567 ) ;
#14997=CARTESIAN_POINT ( 'NONE',  ( 0.2993330080277241678, 5.144326520802546376, 0.05249542264811372927 ) ) ;
#15000=CARTESIAN_POINT ( 'NONE',  ( -0.1167790944451422702, 0.1638888888130222432, -0.2819296736111110424 ) ) ;
#15003=LINE ( 'NONE', #4014, #18326 ) ;
#15008=CARTESIAN_POINT ( 'NONE',  ( 0.2206173157302028787, 4.349388888888888083, 0.2206173157302027954 ) ) ;
#15010=CARTESIAN_POINT ( 'NONE',  ( -0.3119999999999999996, 0.1048611111111107663, 0.1292346314604056190 ) ) ;
#15011=CARTESIAN_POINT ( 'NONE',  ( 0.2206173157302028787, 5.127166666666665762, 0.2206173157302027954 ) ) ;
#15013=CARTESIAN_POINT ( 'NONE',  ( -0.1167790944451423535, 4.266055555631421470, 0.2819296736111110424 ) ) ;
#15016=ORIENTED_EDGE ( 'NONE', *, *, #15293, .T. ) ;
#15018=CARTESIAN_POINT ( 'NONE',  ( -1.726321361862525858E-17, 5.005638888964754507, -0.2819296736111110979 ) ) ;
#15019=CARTESIAN_POINT ( 'NONE',  ( -2.307748244742446386E-07, 4.182713274783838919, 0.3119999999998222528 ) ) ;
#15020=CARTESIAN_POINT ( 'NONE',  ( 0.1988756632394131918, 3.704359868413474199, -0.2404006459456452249 ) ) ;
#15022=CARTESIAN_POINT ( 'NONE',  ( -0.1167790944451423535, 4.696611111186976828, 0.2819296736111110979 ) ) ;
#15024=CARTESIAN_POINT ( 'NONE',  ( -0.3119999999999999996, 4.769527777777777366, -0.1292346314604056468 ) ) ;
#15025=FACE_OUTER_BOUND ( 'NONE', #18114, .T. ) ;
#15026=CARTESIAN_POINT ( 'NONE',  ( -0.1993543840281267465, 0.4173611110352444253, 0.1993543840281266633 ) ) ;
#15029=CARTESIAN_POINT ( 'NONE',  ( 0.1167790944451423535, 0.3166666665907999501, 0.2819296736111110424 ) ) ;
#15035=ADVANCED_FACE ( 'NONE', ( #13660 ), #4365, .T. ) ;
#15037=CARTESIAN_POINT ( 'NONE',  ( 0.000000000000000000, 5.384999999999999787, -0.3119999999999999996 ) ) ;
#15038=CARTESIAN_POINT ( 'NONE',  ( 0.1993543840281266910, 0.1534722221463555858, -0.1993543840281266910 ) ) ;
#15039=CARTESIAN_POINT ( 'NONE',  ( -0.1167790944451424368, 0.07361111103524446697, 0.2819296736111110424 ) ) ;
#15040=CARTESIAN_POINT ( 'NONE',  ( 0.1993543840281266633, 4.234805555631421470, -0.1993543840281266910 ) ) ;
#15043=CARTESIAN_POINT ( 'NONE',  ( 0.2819296736111110979, 4.835500000075866112, 0.1167790944451422425 ) ) ;
#15044=CARTESIAN_POINT ( 'NONE',  ( 0.1167790944451424506, 4.425777777853642903, 0.2819296736111110424 ) ) ;
#15047=EDGE_LOOP ( 'NONE', ( #313, #10664, #11574, #2389 ) ) ;
#15048=CARTESIAN_POINT ( 'NONE',  ( 0.03189102445560762500, 3.905830426954165269, 0.3119999985971984025 ) ) ;
#15049=CARTESIAN_POINT ( 'NONE',  ( -0.3119999999999999996, 3.998694444596176734, -0.1292346314604056468 ) ) ;
#15050=CARTESIAN_POINT ( 'NONE',  ( 0.1797083160605401908, 3.721720973846279534, -0.2172308955953379805 ) ) ;
#15059=ORIENTED_EDGE ( 'NONE', *, *, #7665, .T. ) ;
#15060=CARTESIAN_POINT ( 'NONE',  ( 1.910449006669871087E-17, 0.5805555554038225319, -0.3119999999999999996 ) ) ;
#15063=CARTESIAN_POINT ( 'NONE',  ( 0.03384475192914793845, 4.739198603489362505, 0.3119999968134716806 ) ) ;
#15065=CARTESIAN_POINT ( 'NONE',  ( -0.3119999999999999996, 0.4902777777777773682, -3.820898013339742174E-17 ) ) ;
#15070=CARTESIAN_POINT ( 'NONE',  ( -0.2934967222474210158, 4.665782234535950757, -0.1058913119755514193 ) ) ;
#15071=CARTESIAN_POINT ( 'NONE',  ( -0.1167790944451423535, 4.141055555631421470, 0.2819296736111110424 ) ) ;
#15074=CARTESIAN_POINT ( 'NONE',  ( -0.3119999999999998885, 3.832027777777777366, 0.1292346314604058410 ) ) ;
#15075=CARTESIAN_POINT ( 'NONE',  ( -0.1292346314604057023, 4.734805555707287894, 0.3119999999999998885 ) ) ;
#15076=CARTESIAN_POINT ( 'NONE',  ( 0.03717498437443090414, 4.794923932970774239, 0.3120000032159864767 ) ) ;
#15078=CARTESIAN_POINT ( 'NONE',  ( -0.1993543840281266910, 4.179250000075865223, -0.1993543840281266910 ) ) ;
#15083=CONICAL_SURFACE ( 'NONE', #2217, 0.3119999999999999996, 0.7853981633974450594 ) ;
#15087=CARTESIAN_POINT ( 'NONE',  ( -1.726321361862525858E-17, 5.061194444520309865, -0.2819296736111110979 ) ) ;
#15088=CARTESIAN_POINT ( 'NONE',  ( -1.726321361862525858E-17, 3.908416666742532630, -0.2819296736111110979 ) ) ;
#15089=CARTESIAN_POINT ( 'NONE',  ( 0.07516378717669286447, 4.407066051533294448, 0.3028153355424372806 ) ) ;
#15093=CARTESIAN_POINT ( 'NONE',  ( 0.2819296736111110979, 0.4937499999241333759, 0.000000000000000000 ) ) ;
#15095=CARTESIAN_POINT ( 'NONE',  ( -0.2819296736111110979, 4.866750000075866112, 0.000000000000000000 ) ) ;
#15097=CARTESIAN_POINT ( 'NONE',  ( 0.1993543840281266633, 4.943138888964754507, -0.1993543840281266910 ) ) ;
#15100=DIRECTION ( 'NONE',  ( -0.000000000000000000, -1.000000000000000000, -0.000000000000000000 ) ) ;
#15102=CARTESIAN_POINT ( 'NONE',  ( 0.3119999999999999996, 4.519527777777776478, 0.1292346314604056190 ) ) ;
#15105=CARTESIAN_POINT ( 'NONE',  ( 5.731347020009612645E-17, 4.231333333333332725, 0.3119999999999999996 ) ) ;
#15106=CARTESIAN_POINT ( 'NONE',  ( 0.04766631159125447187, 4.986907329414384193, -0.3085658132919876229 ) ) ;
#15107=CARTESIAN_POINT ( 'NONE',  ( -0.1053467703269967554, 3.735243447484689394, 0.2936768054724072097 ) ) ;
#15109=ORIENTED_EDGE ( 'NONE', *, *, #17465, .T. ) ;
#15110=CARTESIAN_POINT ( 'NONE',  ( -0.02675153519987890152, 4.126403458700751870, 0.3120000000339450130 ) ) ;
#15112=CARTESIAN_POINT ( 'NONE',  ( 0.2967562270154266435, 4.638299250765053117, 0.09806193730438493572 ) ) ;
#15113=B_SPLINE_CURVE_WITH_KNOTS ( 'NONE', 3,
 ( #5543, #1885, #2010, #7495, #1763, #18594, #11400, #16881, #18712, #172, #18832, #22362, #2127, #49, #5665, #14828, #17000, #10923 ),
 .UNSPECIFIED., .F., .F.,
 ( 4, 2, 2, 2, 2, 2, 2, 2, 4 ),
 ( 0.8132388816940862020, 0.8155224221455371625, 0.8178059625969880120, 0.8200895030484388615, 0.8223730434998898220, 0.8246565839513406715, 0.8269401244027916320, 0.8292236648542425925, 0.8315072053056934420 ),
 .UNSPECIFIED. ) ;
#15120=CARTESIAN_POINT ( 'NONE',  ( -0.1993543840281267465, 0.5145833332574667462, 0.1993543840281266633 ) ) ;
#15125=CARTESIAN_POINT ( 'NONE',  ( -0.3098116448389192645, 5.104813878284599760, -0.02126393433258285878 ) ) ;
#15127=CARTESIAN_POINT ( 'NONE',  ( -0.2206173157302028787, 0.2749999999999996891, 0.2206173157302027954 ) ) ;
#15128=CARTESIAN_POINT ( 'NONE',  ( 0.3119999999999999996, 5.241749999999997911, 0.1292346314604056190 ) ) ;
#15129=CARTESIAN_POINT ( 'NONE',  ( -0.2819296736111110424, 4.252166666742533074, -0.1167790944451423119 ) ) ;
#15130=CARTESIAN_POINT ( 'NONE',  ( -0.1292346314604032043, 3.818138888888887639, -0.3120000000000024420 ) ) ;
#15134=EDGE_CURVE ( 'NONE', #14458, #10194, #3335, .T. ) ;
#15136=CARTESIAN_POINT ( 'NONE',  ( -0.1167790944451423257, 4.898000000075866112, -0.2819296736111110424 ) ) ;
#15138=ADVANCED_FACE ( 'NONE', ( #712 ), #8140, .T. ) ;
#15140=CARTESIAN_POINT ( 'NONE',  ( 2.824051777240061223E-14, 3.849388889040854522, 0.3119999999999999996 ) ) ;
#15141=CARTESIAN_POINT ( 'NONE',  ( -0.2819296736111110424, 4.578555555631421470, 0.1167790944451424923 ) ) ;
#15142=CARTESIAN_POINT ( 'NONE',  ( -0.002064217775335610086, 4.043888859528191659, -0.3119941523652927096 ) ) ;
#15144=CARTESIAN_POINT ( 'NONE',  ( 0.1993543840281266910, 0.4451388888130222710, -0.1993543840281266910 ) ) ;
#15147=CARTESIAN_POINT ( 'NONE',  ( -5.178964085587577574E-17, 0.5354166665908000056, 0.2819296736111110979 ) ) ;
#15154=CARTESIAN_POINT ( 'NONE',  ( -0.1167790944451424506, 0.2958333332574667462, 0.2819296736111110424 ) ) ;
#15155=CARTESIAN_POINT ( 'NONE',  ( 0.2819296736111110424, 0.3097222221463555303, 0.1167790944451424923 ) ) ;
#15156=CARTESIAN_POINT ( 'NONE',  ( -0.1167790944451423257, 4.245222222298088433, -0.2819296736111110424 ) ) ;
#15158=CARTESIAN_POINT ( 'NONE',  ( -0.1167790944451423257, 4.967444444520310753, -0.2819296736111110424 ) ) ;
#15159=CARTESIAN_POINT ( 'NONE',  ( -1.726321361862525858E-17, 4.338972222298087544, -0.2819296736111110979 ) ) ;
#15163=CARTESIAN_POINT ( 'NONE',  ( 0.3119999999999999996, 4.033416666818398610, -0.1292346314604056745 ) ) ;
#15171=CARTESIAN_POINT ( 'NONE',  ( -0.08124123436041086332, 4.990575526692240693, -0.3039879947993704423 ) ) ;
#15173=CARTESIAN_POINT ( 'NONE',  ( 0.3119999999999998885, 0.4520833331816004885, 0.1292346314604058410 ) ) ;
#15175=DIRECTION ( 'NONE',  ( -0.000000000000000000, -1.000000000000000000, -0.000000000000000000 ) ) ;
#15177=CARTESIAN_POINT ( 'NONE',  ( 0.0003672435171428997994, 4.766045129345851450, -0.3119998398083521085 ) ) ;
#15184=CARTESIAN_POINT ( 'NONE',  ( -0.2819296736111110424, 3.904944444520309865, -0.1167790944451423119 ) ) ;
#15187=CARTESIAN_POINT ( 'NONE',  ( -0.3119999999999999996, 3.769527777777778255, -0.1292346314604056468 ) ) ;
#15188=CARTESIAN_POINT ( 'NONE',  ( 0.2206173157302027954, 4.814666666818398610, -0.2206173157302028232 ) ) ;
#15189=CARTESIAN_POINT ( 'NONE',  ( 0.2819296736111110979, 5.005638888964754507, -3.452642723725051716E-17 ) ) ;
#15190=EDGE_LOOP ( 'NONE', ( #24072, #22072, #16182, #168 ) ) ;
#15191=CARTESIAN_POINT ( 'NONE',  ( -0.1167790944451423535, 4.307722222298088433, 0.2819296736111110424 ) ) ;
#15200=CARTESIAN_POINT ( 'NONE',  ( -0.1993543840281266355, 5.193138888964753619, 0.1993543840281267465 ) ) ;
#15201=CARTESIAN_POINT ( 'NONE',  ( 0.2819296736111111534, 3.946611111186976828, 0.1167790944451422563 ) ) ;
#15202=CARTESIAN_POINT ( 'NONE',  ( 0.1079706958816955137, 4.429610341295819431, -0.2927247107414157612 ) ) ;
#15207=CARTESIAN_POINT ( 'NONE',  ( 0.2819296736111110979, 0.4381944443685778512, 0.000000000000000000 ) ) ;
#15209=CARTESIAN_POINT ( 'NONE',  ( 0.2819296736111110979, 5.061194444520310753, -3.452642723725051716E-17 ) ) ;
#15211=CARTESIAN_POINT ( 'NONE',  ( -0.1167790944451423257, 4.564666666742531298, -0.2819296736111110424 ) ) ;
#15219=CARTESIAN_POINT ( 'NONE',  ( -0.2206173157302027676, 4.613277777777776478, 0.2206173157302028787 ) ) ;
#15221=CARTESIAN_POINT ( 'NONE',  ( -0.2819296736111110424, 3.745222222298088433, 0.1167790944451424923 ) ) ;
#15222=CARTESIAN_POINT ( 'NONE',  ( 1.910449006669871087E-17, 0.3583333331816003775, -0.3119999999999999996 ) ) ;
#15226=CYLINDRICAL_SURFACE ( 'NONE', #11285, 0.3119999999999999996 ) ;
#15229=CARTESIAN_POINT ( 'NONE',  ( 0.04602711923241634834, 4.628539372138874342, 0.3120000069469925363 ) ) ;
#15232=CARTESIAN_POINT ( 'NONE',  ( 0.1569173507168480086, 4.298453709044838256, 0.2727343952408894379 ) ) ;
#15235=CARTESIAN_POINT ( 'NONE',  ( 0.1167790944451423257, 0.5458333332574666352, -0.2819296736111110424 ) ) ;
#15236=CARTESIAN_POINT ( 'NONE',  ( -0.2082794372640225100, 5.206640035683668621, 0.1900105704308308607 ) ) ;
#15240=DIRECTION ( 'NONE',  ( 1.224646799147353207E-16, 0.000000000000000000, -1.000000000000000000 ) ) ;
#15241=CARTESIAN_POINT ( 'NONE',  ( -0.2206173157302028787, 0.2194444444444441089, 0.2206173157302027954 ) ) ;
#15242=CARTESIAN_POINT ( 'NONE',  ( 0.3119999999999999996, 5.186194444444442553, 0.1292346314604056190 ) ) ;
#15244=CARTESIAN_POINT ( 'NONE',  ( -0.1167790944451423257, 4.134111111186977716, -0.2819296736111110424 ) ) ;
#15245=CARTESIAN_POINT ( 'NONE',  ( -0.1917964032624795701, 4.327441163112869305, -0.2494539190351865721 ) ) ;
#15247=DIRECTION ( 'NONE',  ( 0.000000000000000000, 0.000000000000000000, -1.000000000000000000 ) ) ;
#15249=CARTESIAN_POINT ( 'NONE',  ( -0.1167790944451423535, 4.918833333409199149, 0.2819296736111110424 ) ) ;
#15251=CARTESIAN_POINT ( 'NONE',  ( -0.009801821498707709301, 5.143598273731186943, -0.3039077880706267942 ) ) ;
#15252=( BOUNDED_CURVE ( )  B_SPLINE_CURVE ( 2, ( #253, #22568, #6096, #491, #616, #11725, #735, #8046, #18788 ),
 .UNSPECIFIED., .F., .T. ) 
 B_SPLINE_CURVE_WITH_KNOTS ( ( 3, 2, 2, 2, 3 ),
 ( 0.8958333333333333703, 0.9062500000000000000, 0.9166666666666666297, 0.9270833333333333703, 0.9375000000000000000 ),
 .UNSPECIFIED. ) 
 CURVE ( )  GEOMETRIC_REPRESENTATION_ITEM ( )  RATIONAL_B_SPLINE_CURVE ( ( 1.000000000000000000, 0.9238795325112867385, 1.000000000000000000, 0.9238795325112867385, 1.000000000000000000, 0.9238795325112867385, 1.000000000000000000, 0.9238795325112867385, 1.000000000000000000 ) ) 
 REPRESENTATION_ITEM ( '' )  );
#15254=CARTESIAN_POINT ( 'NONE',  ( 0.0005601723535045452463, 3.710484947398785316, -0.3119995287117768856 ) ) ;
#15256=CARTESIAN_POINT ( 'NONE',  ( -0.1993543840281266910, 4.359805555631421470, -0.1993543840281266910 ) ) ;
#15259=CARTESIAN_POINT ( 'NONE',  ( -0.1999482914134789180, 4.050008517921297013, -0.2395145290917104208 ) ) ;
#15265=CARTESIAN_POINT ( 'NONE',  ( -0.2819296736111110979, 0.4138888888130222155, 0.1167790944451422425 ) ) ;
#15272=CARTESIAN_POINT ( 'NONE',  ( 0.1993543840281266910, 0.3756944443685777957, -0.1993543840281266910 ) ) ;
#15273=CARTESIAN_POINT ( 'NONE',  ( -0.1167790944451422702, 0.3305555554796889561, -0.2819296736111110424 ) ) ;
#15274=CARTESIAN_POINT ( 'NONE',  ( 0.2819296736111110424, 4.342444444520311642, -0.1167790944451423396 ) ) ;
#15276=EDGE_CURVE ( 'NONE', #2366, #10939, #17890, .T. ) ;
#15277=CARTESIAN_POINT ( 'NONE',  ( 0.1993543840281267465, 4.887583333409199149, 0.1993543840281266633 ) ) ;
#15278=CARTESIAN_POINT ( 'NONE',  ( -0.2819296736111110424, 4.134111111186976828, 0.1167790944451424923 ) ) ;
#15281=CARTESIAN_POINT ( 'NONE',  ( 0.3119999999999999996, 4.137583333485066461, 0.1292346314604056190 ) ) ;
#15283=LINE ( 'NONE', #22599, #10700 ) ;
#15288=CARTESIAN_POINT ( 'NONE',  ( 0.000000000000000000, 5.384999999999999787, -0.3119999999999999996 ) ) ;
#15289=CARTESIAN_POINT ( 'NONE',  ( -0.3058731308713533159, 5.000420509829539562, -0.06261731312025432816 ) ) ;
#15291=CARTESIAN_POINT ( 'NONE',  ( 0.1292346314604057023, 0.4451388887371560688, 0.3119999999999998885 ) ) ;
#15293=EDGE_CURVE ( 'NONE', #20467, #787, #22558, .T. ) ;
#15296=DIRECTION ( 'NONE',  ( -0.000000000000000000, -1.000000000000000000, -0.000000000000000000 ) ) ;
#15299=CARTESIAN_POINT ( 'NONE',  ( 0.1789513046941397512, 5.185541748123438488, -0.2296687052981416510 ) ) ;
#15303=CARTESIAN_POINT ( 'NONE',  ( -0.2447627460273846534, 4.674789551421016043, 0.1936577326920176922 ) ) ;
#15305=CARTESIAN_POINT ( 'NONE',  ( -0.1993543840281266355, 3.970916666742532186, 0.1993543840281267465 ) ) ;
#15308=CARTESIAN_POINT ( 'NONE',  ( -0.1940754166076595899, 5.189177002903242020, 0.2157554602168622049 ) ) ;
#15309=CARTESIAN_POINT ( 'NONE',  ( 0.3119999999999999996, 4.644527777929510215, -0.1292346314604056745 ) ) ;
#15311=CARTESIAN_POINT ( 'NONE',  ( -0.2819296736111110979, 5.029944444520308977, -0.1167790944451422980 ) ) ;
#15313=CARTESIAN_POINT ( 'NONE',  ( -1.726321361862525858E-17, 4.338972222298087544, -0.2819296736111110979 ) ) ;
#15320=CARTESIAN_POINT ( 'NONE',  ( 0.1167790944451422702, 3.904944444520310309, -0.2819296736111110979 ) ) ;
#15322=CARTESIAN_POINT ( 'NONE',  ( 0.2450693591352816059, 4.424882274230782286, -0.1965390533656376226 ) ) ;
#15323=CARTESIAN_POINT ( 'NONE',  ( 0.3119999999999999996, 4.634111111111110404, -3.820898013339742174E-17 ) ) ;
#15326=CARTESIAN_POINT ( 'NONE',  ( -0.2819296736111111534, 0.5805555554796888451, 0.1167790944451422563 ) ) ;
#15328=ADVANCED_FACE ( 'NONE', ( #2971 ), #4917, .T. ) ;
#15330=CARTESIAN_POINT ( 'NONE',  ( 0.2819296736111110979, 4.668833333409200037, 0.1167790944451422425 ) ) ;
#15333=CARTESIAN_POINT ( 'NONE',  ( 0.1167790944451424368, 4.648000000075865223, 0.2819296736111110424 ) ) ;
#15334=CARTESIAN_POINT ( 'NONE',  ( -0.0001107979596245131973, 4.154947627944543420, -0.3120000001382827182 ) ) ;
#15338=CARTESIAN_POINT ( 'NONE',  ( -1.910449006669871087E-17, 4.481333333333331836, -0.3119999999999999996 ) ) ;
#15345=CARTESIAN_POINT ( 'NONE',  ( 0.2761937380445508849, 4.700912946670643855, -0.1452742419101630544 ) ) ;
#15346=CARTESIAN_POINT ( 'NONE',  ( 0.1171198219552221365, 4.651519741485643955, -0.2900815769309791348 ) ) ;
#15352=CARTESIAN_POINT ( 'NONE',  ( 0.1993543840281266910, 0.3756944443685777957, -0.1993543840281266910 ) ) ;
#15355=CARTESIAN_POINT ( 'NONE',  ( -5.731347020009612645E-17, 0.3861111109593781676, 0.3119999999999999996 ) ) ;
#15358=CARTESIAN_POINT ( 'NONE',  ( -0.2917190787933745533, 4.609974286260102971, -0.1140841330618171251 ) ) ;
#15361=CARTESIAN_POINT ( 'NONE',  ( -0.1292346314604058410, 0.1673611111111107941, 0.3119999999999998885 ) ) ;
#15362=CARTESIAN_POINT ( 'NONE',  ( -0.2206173157302027676, 5.168833333333332725, 0.2206173157302028787 ) ) ;
#15363=CARTESIAN_POINT ( 'NONE',  ( 0.2819296736111110979, 4.283416666742533074, -3.452642723725051716E-17 ) ) ;
#15364=CARTESIAN_POINT ( 'NONE',  ( 5.731347020009612645E-17, 3.842444444444443441, 0.3119999999999999996 ) ) ;
#15370=DIRECTION ( 'NONE',  ( 0.000000000000000000, 0.000000000000000000, 1.000000000000000000 ) ) ;
#15371=CARTESIAN_POINT ( 'NONE',  ( 0.1993543840281266633, 4.720916666742532186, -0.1993543840281266910 ) ) ;
#15374=CARTESIAN_POINT ( 'NONE',  ( -1.910449006669871087E-17, 4.092444444444444329, -0.3119999999999999996 ) ) ;
#15378=CARTESIAN_POINT ( 'NONE',  ( -0.2819296736111110979, 4.422305555631421470, 0.000000000000000000 ) ) ;
#15381=CARTESIAN_POINT ( 'NONE',  ( -0.3080870731862870859, 4.059453030256765516, 0.06306296359780783067 ) ) ;
#15385=CARTESIAN_POINT ( 'NONE',  ( 0.1167790944451423257, 0.5041666665908002276, -0.2819296736111110424 ) ) ;
#15387=DIRECTION ( 'NONE',  ( -0.000000000000000000, -1.000000000000000000, -0.000000000000000000 ) ) ;
#15390=CARTESIAN_POINT ( 'NONE',  ( 0.1292346314604058410, 3.957027777777776922, 0.3119999999999998885 ) ) ;
#15392=CARTESIAN_POINT ( 'NONE',  ( 0.2819296736111110979, 0.5909722221463555858, 0.000000000000000000 ) ) ;
#15393=CARTESIAN_POINT ( 'NONE',  ( 0.1167790944451423257, 0.2124999999241334314, -0.2819296736111110424 ) ) ;
#15395=CARTESIAN_POINT ( 'NONE',  ( 0.2819296736111110979, 4.338972222298087544, -3.452642723725051716E-17 ) ) ;
#15398=CARTESIAN_POINT ( 'NONE',  ( 0.2819296736111110424, 4.898000000075866112, -0.1167790944451423396 ) ) ;
#15399=CARTESIAN_POINT ( 'NONE',  ( -0.1167790944451423119, 4.120222222298087544, -0.2819296736111110979 ) ) ;
#15401=FACE_OUTER_BOUND ( 'NONE', #11457, .T. ) ;
#15402=CARTESIAN_POINT ( 'NONE',  ( -1.910449006669871087E-17, 3.821611111262843252, -0.3119999999999999996 ) ) ;
#15403=( BOUNDED_CURVE ( )  B_SPLINE_CURVE ( 2, ( #12953, #3780, #13068, #18772, #22068, #9509, #15008, #22429, #10989 ),
 .UNSPECIFIED., .F., .T. ) 
 B_SPLINE_CURVE_WITH_KNOTS ( ( 3, 2, 2, 2, 3 ),
 ( 0.5803571428571426827, 0.5848214285714283811, 0.5892857142857141906, 0.5937500000000000000, 0.5982142857142856984 ),
 .UNSPECIFIED. ) 
 CURVE ( )  GEOMETRIC_REPRESENTATION_ITEM ( )  RATIONAL_B_SPLINE_CURVE ( ( 1.000000000000003775, 0.9238795325112829637, 1.000000000000000000, 0.9238795325112867385, 1.000000000000000000, 0.9238795325112867385, 1.000000000000000000, 0.9238795325112867385, 1.000000000000000000 ) ) 
 REPRESENTATION_ITEM ( '' )  );
#15405=CARTESIAN_POINT ( 'NONE',  ( 0.3119999999999998885, 0.1256944444444441089, 0.1292346314604058410 ) ) ;
#15412=VERTEX_POINT ( 'NONE', #8691 ) ;
#15413=CARTESIAN_POINT ( 'NONE',  ( -0.2819296736111110979, 0.07708333325746669074, -3.452642723725051716E-17 ) ) ;
#15414=ORIENTED_EDGE ( 'NONE', *, *, #22341, .T. ) ;
#15415=CARTESIAN_POINT ( 'NONE',  ( 0.2839469674206308025, 4.255952816943617378, -0.1292989629763649229 ) ) ;
#15417=CARTESIAN_POINT ( 'NONE',  ( 0.1776117012215460422, 4.760747979974951249, -0.2606188829398497497 ) ) ;
#15419=CARTESIAN_POINT ( 'NONE',  ( 0.09457430736025282392, 5.187965616402109958, -0.2748785845271523032 ) ) ;
#15424=CARTESIAN_POINT ( 'NONE',  ( -1.910449006669871087E-17, 4.036888888888888083, -0.3119999999999999996 ) ) ;
#15425=CARTESIAN_POINT ( 'NONE',  ( -0.1993543840281266910, 4.012583333409198261, -0.1993543840281266910 ) ) ;
#15427=CARTESIAN_POINT ( 'NONE',  ( -0.09460153516617859915, 5.193837599247971504, 0.2723203693900976829 ) ) ;
#15429=CARTESIAN_POINT ( 'NONE',  ( -0.3119999999999999996, 4.554250000151733424, -0.1292346314604056468 ) ) ;
#15430=CARTESIAN_POINT ( 'NONE',  ( -0.1993543840281266910, 4.915361111186976828, -0.1993543840281266910 ) ) ;
#15433=CARTESIAN_POINT ( 'NONE',  ( -0.1993543840281266910, 4.234805555631421470, -0.1993543840281266910 ) ) ;
#15434=ORIENTED_EDGE ( 'NONE', *, *, #13694, .F. ) ;
#15443=CARTESIAN_POINT ( 'NONE',  ( 0.3119999999999999996, 0.01458333318160040526, -0.1292346314604056468 ) ) ;
#15445=CARTESIAN_POINT ( 'NONE',  ( 0.2928594795036059129, 4.415712943899434251, 0.1100155955557257648 ) ) ;
#15449=CARTESIAN_POINT ( 'NONE',  ( 0.1167790944451423535, 0.5388888888130223265, 0.2819296736111110979 ) ) ;
#15452=CARTESIAN_POINT ( 'NONE',  ( 0.2819296736111110979, 4.727861111186976828, -3.452642723725051716E-17 ) ) ;
#15454=CARTESIAN_POINT ( 'NONE',  ( -0.2819296736111110424, 4.682722222298087544, -0.1167790944451423119 ) ) ;
#15456=CARTESIAN_POINT ( 'NONE',  ( 0.1864576510852719859, 4.871607367807203381, -0.2512479716031276178 ) ) ;
#15459=CARTESIAN_POINT ( 'NONE',  ( -0.2206173157302028232, 4.210499999999999687, -0.2206173157302028232 ) ) ;
#15460=CARTESIAN_POINT ( 'NONE',  ( -0.1167790944451423119, 3.786888888964754063, -0.2819296736111110979 ) ) ;
#15466=CARTESIAN_POINT ( 'NONE',  ( 0.01239450642302288193, 4.710165812920179995, -0.3117901439589589874 ) ) ;
#15467=CARTESIAN_POINT ( 'NONE',  ( 0.1906193665221117550, 4.133011534993895175, 0.2469985270587236048 ) ) ;
#15469=CARTESIAN_POINT ( 'NONE',  ( 4.282505654011733572E-07, 3.932722210548942776, -0.3119999999997061790 ) ) ;
#15470=ORIENTED_EDGE ( 'NONE', *, *, #11530, .F. ) ;
#15473=CARTESIAN_POINT ( 'NONE',  ( 0.1167790944451423257, 0.4902777777019112215, -0.2819296736111110424 ) ) ;
#15479=CARTESIAN_POINT ( 'NONE',  ( -0.3125685445540615781, 4.612853974748221120, -0.01387924731082778793 ) ) ;
#15481=CARTESIAN_POINT ( 'NONE',  ( 0.3119999999999999996, 4.745222222222221120, -3.820898013339742174E-17 ) ) ;
#15482=CARTESIAN_POINT ( 'NONE',  ( -0.2206173157302027954, 0.2611111111111107386, -0.2206173157302028232 ) ) ;
#15483=CARTESIAN_POINT ( 'NONE',  ( 0.3119999999999999996, 4.859805555555554157, -0.1292346314604056745 ) ) ;
#15484=CARTESIAN_POINT ( 'NONE',  ( 5.178964085587577574E-17, 4.102861111186976828, 0.2819296736111110979 ) ) ;
#15485=CARTESIAN_POINT ( 'NONE',  ( -5.428794840643969700E-10, 4.321611111277808170, -0.3119999999999999996 ) ) ;
#15486=CARTESIAN_POINT ( 'NONE',  ( -0.3119999999999999996, 0.4798611109593782231, -0.1292346314604056745 ) ) ;
#15487=CARTESIAN_POINT ( 'NONE',  ( 0.2669940301182540665, 4.812622197162082394, -0.1675650707301165887 ) ) ;
#15488=ORIENTED_EDGE ( 'NONE', *, *, #8701, .T. ) ;
#15490=CARTESIAN_POINT ( 'NONE',  ( -0.2819296736111110979, 4.797305555631420582, 0.000000000000000000 ) ) ;
#15492=CARTESIAN_POINT ( 'NONE',  ( -0.1507708519810125880, 5.163359433834837198, 0.2585303382794060800 ) ) ;
#15494=EDGE_CURVE ( 'NONE', #23698, #12009, #19733, .T. ) ;
#15498=CARTESIAN_POINT ( 'NONE',  ( -0.2819296736111110979, 4.252166666742533074, -0.1167790944451422980 ) ) ;
#15500=CARTESIAN_POINT ( 'NONE',  ( 0.1292346314604031765, 4.311194444444443441, -0.3120000000000024420 ) ) ;
#15503=CARTESIAN_POINT ( 'NONE',  ( -0.2819296736111110979, 0.4694444443685777957, 0.1167790944451422425 ) ) ;
#15508=FACE_OUTER_BOUND ( 'NONE', #17866, .T. ) ;
#15510=CARTESIAN_POINT ( 'NONE',  ( 0.1167790944451423119, 0.4347222221463555858, -0.2819296736111110979 ) ) ;
#15511=CARTESIAN_POINT ( 'NONE',  ( 0.1167790944451423257, 0.2680555554796889561, -0.2819296736111110424 ) ) ;
#15513=CARTESIAN_POINT ( 'NONE',  ( -0.2819296736111110424, 4.252166666742533074, -0.1167790944451423119 ) ) ;
#15516=CARTESIAN_POINT ( 'NONE',  ( 0.1167790944451422702, 4.793833333409199149, -0.2819296736111110424 ) ) ;
#15519=EDGE_LOOP ( 'NONE', ( #4996, #8839, #2513, #21847 ) ) ;
#15521=CARTESIAN_POINT ( 'NONE',  ( -0.1292346314604057023, 3.957027777929510215, 0.3119999999999998885 ) ) ;
#15524=ORIENTED_EDGE ( 'NONE', *, *, #5591, .F. ) ;
#15528=CARTESIAN_POINT ( 'NONE',  ( -8.251178249108312710E-07, 5.016022433328296337, 0.3119999999976432181 ) ) ;
#15530=CARTESIAN_POINT ( 'NONE',  ( -5.178964085587577574E-17, 0.09097222214635558579, 0.2819296736111110979 ) ) ;
#15533=CARTESIAN_POINT ( 'NONE',  ( 0.08432056328971544723, 4.096951260793152194, -0.3033353371696297374 ) ) ;
#15536=ORIENTED_EDGE ( 'NONE', *, *, #5846, .T. ) ;
#15538=CARTESIAN_POINT ( 'NONE',  ( -0.3119999999999999996, 4.047305555555555046, -0.1292346314604056468 ) ) ;
#15539=EDGE_CURVE ( 'NONE', #10051, #9670, #16431, .T. ) ;
#15540=CARTESIAN_POINT ( 'NONE',  ( 0.2819296736111110979, 3.988277777853643347, 0.1167790944451422425 ) ) ;
#15543=CARTESIAN_POINT ( 'NONE',  ( 0.02891941893387090998, 5.043051531045750657, -0.3110769485290388325 ) ) ;
#15544=CARTESIAN_POINT ( 'NONE',  ( -0.06631323151226614643, 5.164881977199022423, -0.2908543057123224029 ) ) ;
#15546=CARTESIAN_POINT ( 'NONE',  ( 0.3119999999999999996, 4.529944444596176290, -3.820898013339742174E-17 ) ) ;
#15547=EDGE_CURVE ( 'NONE', #20545, #9930, #2924, .T. ) ;
#15548=CARTESIAN_POINT ( 'NONE',  ( 5.178964085587577574E-17, 4.991750000075866112, 0.2819296736111110979 ) ) ;
#15550=CARTESIAN_POINT ( 'NONE',  ( 0.1167790944451424368, 4.036888888964754507, 0.2819296736111110424 ) ) ;
#15551=EDGE_LOOP ( 'NONE', ( #3218, #15414, #9315, #23641 ) ) ;
#15556=CARTESIAN_POINT ( 'NONE',  ( -0.2819296736111110979, 3.755638888964754951, 0.000000000000000000 ) ) ;
#15559=CARTESIAN_POINT ( 'NONE',  ( 0.1849291740725004518, 5.155468161834985352, -0.2375778761813798490 ) ) ;
#15560=CARTESIAN_POINT ( 'NONE',  ( 0.1767089000523858477, 4.410255657018761433, 0.2583257397394467803 ) ) ;
#15567=CARTESIAN_POINT ( 'NONE',  ( 0.2819296736111110979, 4.835500000075866112, 0.1167790944451422425 ) ) ;
#15569=CARTESIAN_POINT ( 'NONE',  ( -0.2819296736111110424, 4.738277777853642903, -0.1167790944451423119 ) ) ;
#15570=CARTESIAN_POINT ( 'NONE',  ( -0.01779695850694028303, 4.155454319339479063, -0.3115646979797883076 ) ) ;
#15571=DIRECTION ( 'NONE',  ( -0.000000000000000000, -1.000000000000000000, -0.000000000000000000 ) ) ;
#15574=CARTESIAN_POINT ( 'NONE',  ( 0.1292346314604058410, 4.290361111111110404, 0.3119999999999998885 ) ) ;
#15575=CARTESIAN_POINT ( 'NONE',  ( 0.2206173157302027954, 5.092444444596176290, -0.2206173157302028232 ) ) ;
#15577=CARTESIAN_POINT ( 'NONE',  ( -5.731347020009612645E-17, 0.5527777776260448528, 0.3119999999999999996 ) ) ;
#15582=CARTESIAN_POINT ( 'NONE',  ( 0.0002156662915977773556, 4.710494205284167180, -0.3119999301816606674 ) ) ;
#15584=CARTESIAN_POINT ( 'NONE',  ( 0.2704457082507048526, 4.136385615343296074, 0.1578283642472184667 ) ) ;
#15589=AXIS2_PLACEMENT_3D ( 'NONE', #19484, #2666, #2778 ) ;
#15591=CARTESIAN_POINT ( 'NONE',  ( -0.1993543840281267465, 0.4034722221463555858, 0.1993543840281266633 ) ) ;
#15592=CARTESIAN_POINT ( 'NONE',  ( -0.01963737563095444699, 5.206640035683668621, 0.2814148482456156897 ) ) ;
#15596=VERTEX_POINT ( 'NONE', #19021 ) ;
#15598=FACE_OUTER_BOUND ( 'NONE', #16406, .T. ) ;
#15600=CARTESIAN_POINT ( 'NONE',  ( 0.1292346314604056745, 0.1395833333333330317, -0.3119999999999999996 ) ) ;
#15601=CARTESIAN_POINT ( 'NONE',  ( -0.2206173157302028232, 5.043833333333332725, -0.2206173157302028232 ) ) ;
#15603=CARTESIAN_POINT ( 'NONE',  ( 0.2819296736111110979, 3.891055555631421914, 0.1167790944451422425 ) ) ;
#15604=ADVANCED_FACE ( 'NONE', ( #6444 ), #22907, .T. ) ;
#15610=CARTESIAN_POINT ( 'NONE',  ( -0.08166533652539130494, 3.990609059424373051, -0.3038794758048473654 ) ) ;
#15611=CARTESIAN_POINT ( 'NONE',  ( 0.2819296736111110979, 4.654944444520309865, 0.1167790944451422425 ) ) ;
#15620=CARTESIAN_POINT ( 'NONE',  ( -0.1167790944451423119, 4.245222222298088433, -0.2819296736111110979 ) ) ;
#15621=CARTESIAN_POINT ( 'NONE',  ( -0.01840724122558156858, 4.044333937968741743, -0.3114566890697244017 ) ) ;
#15624=CARTESIAN_POINT ( 'NONE',  ( 0.1993543840281266355, 0.4868055554796889006, 0.1993543840281267465 ) ) ;
#15625=CARTESIAN_POINT ( 'NONE',  ( -0.3119999999999999996, 0.4347222222222218435, -3.820898013339742174E-17 ) ) ;
#15626=LINE ( 'NONE', #8293, #20655 ) ;
#15631=CARTESIAN_POINT ( 'NONE',  ( -0.2819296736111111534, 0.5111111110352445364, 0.1167790944451422563 ) ) ;
#15632=CARTESIAN_POINT ( 'NONE',  ( -0.2819296736111110979, 0.2854166665908000611, -3.452642723725051716E-17 ) ) ;
#15634=CARTESIAN_POINT ( 'NONE',  ( -0.2819296736111110424, 4.148000000075866112, 0.1167790944451424923 ) ) ;
#15636=CARTESIAN_POINT ( 'NONE',  ( 5.178964085587577574E-17, 4.547305555631421470, 0.2819296736111110979 ) ) ;
#15637=EDGE_CURVE ( 'NONE', #15596, #12509, #17617, .T. ) ;
#15639=EDGE_LOOP ( 'NONE', ( #11525, #17463, #579, #18458 ) ) ;
#15642=CARTESIAN_POINT ( 'NONE',  ( -0.3119999999999998885, 3.894527777929509771, 0.1292346314604058410 ) ) ;
#15647=CARTESIAN_POINT ( 'NONE',  ( -0.3032932187877268593, 5.000078586144176995, -0.07417139457035222538 ) ) ;
#15649=CARTESIAN_POINT ( 'NONE',  ( -0.2819296736111110979, 0.02152777770191114173, -3.452642723725051716E-17 ) ) ;
#15650=ORIENTED_EDGE ( 'NONE', *, *, #2331, .T. ) ;
#15651=CARTESIAN_POINT ( 'NONE',  ( 0.08155431767186305247, 4.240654305037732996, 0.3039018303971695034 ) ) ;
#15653=CARTESIAN_POINT ( 'NONE',  ( 0.1735223483235301123, 4.076898470827504894, 0.2600906113308195655 ) ) ;
#15655=CARTESIAN_POINT ( 'NONE',  ( 0.2010820074625671305, 5.184841366458968537, -0.2109359274478957158 ) ) ;
#15659=CARTESIAN_POINT ( 'NONE',  ( 0.2819296736111110424, 3.995222222298087544, -0.1167790944451423396 ) ) ;
#15661=CARTESIAN_POINT ( 'NONE',  ( -0.2841123412848098884, 5.182397235849433237, 0.07086212028873112301 ) ) ;
#15663=CARTESIAN_POINT ( 'NONE',  ( 0.2206173157302027954, 4.481333333485065573, -0.2206173157302028232 ) ) ;
#15664=CARTESIAN_POINT ( 'NONE',  ( 0.2819296736111110979, 4.898000000075865223, -0.1167790944451423396 ) ) ;
#15667=CARTESIAN_POINT ( 'NONE',  ( 0.2819296736111110979, 3.988277777853643347, 0.1167790944451422425 ) ) ;
#15676=CARTESIAN_POINT ( 'NONE',  ( 0.1292346314604057023, 0.05624999984826706961, 0.3119999999999998885 ) ) ;
#15677=CARTESIAN_POINT ( 'NONE',  ( 0.01998333260083862140, 5.130840972916198339, 0.3061013181601511257 ) ) ;
#15681=( BOUNDED_CURVE ( )  B_SPLINE_CURVE ( 2, ( #10710, #3383, #15829, #3028, #10475, #23727, #17905, #18021, #14488 ),
 .UNSPECIFIED., .F., .T. ) 
 B_SPLINE_CURVE_WITH_KNOTS ( ( 3, 2, 2, 2, 3 ),
 ( 0.9017857142857141906, 0.9062499999999998890, 0.9107142857142855874, 0.9151785714285713969, 0.9196428571428570953 ),
 .UNSPECIFIED. ) 
 CURVE ( )  GEOMETRIC_REPRESENTATION_ITEM ( )  RATIONAL_B_SPLINE_CURVE ( ( 1.000000000000001998, 0.9238795325112848511, 1.000000000000000000, 0.9238795325112867385, 1.000000000000000000, 0.9238795325112867385, 1.000000000000000000, 0.9238795325112867385, 1.000000000000000000 ) ) 
 REPRESENTATION_ITEM ( '' )  );
#15682=( BOUNDED_CURVE ( )  B_SPLINE_CURVE ( 1, ( #10127, #15724 ),
 .UNSPECIFIED., .F., .T. ) 
 B_SPLINE_CURVE_WITH_KNOTS ( ( 2, 2 ),
 ( 0.000000000000000000, 1.000000000000000000 ),
 .UNSPECIFIED. ) 
 CURVE ( )  GEOMETRIC_REPRESENTATION_ITEM ( )  RATIONAL_B_SPLINE_CURVE ( ( 0.9836823002065551158, 0.9836823002065551158 ) ) 
 REPRESENTATION_ITEM ( '' )  );
#15687=ORIENTED_EDGE ( 'NONE', *, *, #5537, .T. ) ;
#15689=AXIS2_PLACEMENT_3D ( 'NONE', #21297, #6416, #13870 ) ;
#15690=CARTESIAN_POINT ( 'NONE',  ( -0.1167790944451423257, 4.675777777853642903, -0.2819296736111110424 ) ) ;
#15695=CARTESIAN_POINT ( 'NONE',  ( 0.1292346314604058410, 4.345916666666665762, 0.3119999999999998885 ) ) ;
#15696=CARTESIAN_POINT ( 'NONE',  ( 0.2206173157302028787, 5.078555555707287006, 0.2206173157302027954 ) ) ;
#15697=CARTESIAN_POINT ( 'NONE',  ( 0.3095665875726216210, 4.973302152571846158, 0.03932295407607730442 ) ) ;
#15700=CARTESIAN_POINT ( 'NONE',  ( 4.589747744727345336E-07, 4.571629220806286753, 0.3119999999992840722 ) ) ;
#15702=CARTESIAN_POINT ( 'NONE',  ( 0.2841390510945954739, 4.700384098082350803, -0.1288870310084711535 ) ) ;
#15704=CARTESIAN_POINT ( 'NONE',  ( 0.03111664948054426727, 4.128053875489018587, 0.3119999999605160279 ) ) ;
#15709=CARTESIAN_POINT ( 'NONE',  ( 0.1167790944451423119, 0.1152777777019111383, -0.2819296736111110979 ) ) ;
#15715=CARTESIAN_POINT ( 'NONE',  ( -0.2905554862335017474, 4.616567866447413238, 0.1152557973630595062 ) ) ;
#15718=CARTESIAN_POINT ( 'NONE',  ( -0.3119999999999999996, 0.4312499999999996336, -0.1292346314604056745 ) ) ;
#15719=CARTESIAN_POINT ( 'NONE',  ( -0.3119999999999998885, 5.054249999999998799, 0.1292346314604058410 ) ) ;
#15720=B_SPLINE_CURVE_WITH_KNOTS ( 'NONE', 3,
 ( #16812, #93, #11204, #1925, #9490, #22407, #5708, #2051, #219, #20584, #11325, #7657, #18755, #15107, #14872, #22288, #11039, #3587, #12888, #20419, #16526, #16409, #3714, #18469, #23944, #47, #21883, #7493, #11163, #22242, #20182, #19940, #1883, #23695, #23817, #16764, #7375, #8835, #7260, #20302, #20060, #9324, #16284, #9205, #12642, #5174 ),
 .UNSPECIFIED., .F., .F.,
 ( 4, 2, 2, 2, 2, 1, 2, 2, 1, 1, 1, 1, 2, 2, 2, 2, 2, 2, 1, 1, 2, 2, 1, 2, 2, 2, 4 ),
 ( 0.9753616152418370655, 0.9766508353774531193, 0.9779400555130691730, 0.9792292756486852268, 0.9795515806825892957, 0.9797127331995412192, 0.9797177692156959772, 0.9797228052318507352, 0.9797328772641602512, 0.9797530213287792833, 0.9797933094580172364, 0.9798738857164932536, 0.9805184957843013915, 0.9830969360555337211, 0.9856753763267659396, 0.9882538165979982692, 0.9908322568692305987, 0.9914768669370387366, 0.9917991719709426945, 0.9918797482294187118, 0.9919200363586567759, 0.9919401804232758080, 0.9919603244878947290, 0.9921214770048467635, 0.9934106971404627062, 0.9946999172760787600, 0.9959891374116947027 ),
 .UNSPECIFIED. ) ;
#15722=CARTESIAN_POINT ( 'NONE',  ( 0.1167790944451422702, 4.071611111186977716, -0.2819296736111110424 ) ) ;
#15724=CARTESIAN_POINT ( 'NONE',  ( 0.1988756632394131918, 3.704359868413474199, -0.2404006459456452249 ) ) ;
#15726=ORIENTED_EDGE ( 'NONE', *, *, #670, .F. ) ;
#15728=CARTESIAN_POINT ( 'NONE',  ( -0.08166537602659873496, 4.013806181748617696, 0.3038794651914065725 ) ) ;
#15729=CARTESIAN_POINT ( 'NONE',  ( -0.1993543840281266355, 4.637583333409198261, 0.1993543840281267465 ) ) ;
#15731=CARTESIAN_POINT ( 'NONE',  ( -0.2206173157302027676, 4.113277777777777366, 0.2206173157302028787 ) ) ;
#15737=CARTESIAN_POINT ( 'NONE',  ( 0.2819296736111110979, 4.338972222298087544, -3.452642723725051716E-17 ) ) ;
#15742=CARTESIAN_POINT ( 'NONE',  ( -1.910449006669871087E-17, 4.870222222222222008, -0.3119999999999999996 ) ) ;
#15745=CARTESIAN_POINT ( 'NONE',  ( -0.1167790944451424368, 0.07361111103524446697, 0.2819296736111110424 ) ) ;
#15746=CARTESIAN_POINT ( 'NONE',  ( 1.910449006669871087E-17, 0.08749999999999966138, -0.3119999999999999996 ) ) ;
#15750=DIRECTION ( 'NONE',  ( 0.000000000000000000, 0.000000000000000000, -1.000000000000000000 ) ) ;
#15752=CARTESIAN_POINT ( 'NONE',  ( -0.2819296736111110979, 0.5076388888130222155, -3.452642723725051716E-17 ) ) ;
#15753=CARTESIAN_POINT ( 'NONE',  ( 0.1993543840281266910, 0.5423611110352445364, -0.1993543840281266910 ) ) ;
#15754=CARTESIAN_POINT ( 'NONE',  ( -0.1167790944451423535, 4.154944444520309865, 0.2819296736111110424 ) ) ;
#15756=CARTESIAN_POINT ( 'NONE',  ( 0.1993543840281266633, 4.568138888964755395, -0.1993543840281266910 ) ) ;
#15759=CARTESIAN_POINT ( 'NONE',  ( 0.2840431067139673749, 5.082267742700584456, -0.1295341344031159247 ) ) ;
#15760=CARTESIAN_POINT ( 'NONE',  ( 5.731347020009612645E-17, 4.786888888888888083, 0.3119999999999999996 ) ) ;
#15761=CARTESIAN_POINT ( 'NONE',  ( -0.1292346314604057023, 3.790361111262843252, 0.3119999999999998885 ) ) ;
#15765=( GEOMETRIC_REPRESENTATION_CONTEXT ( 3 ) GLOBAL_UNCERTAINTY_ASSIGNED_CONTEXT ( ( #13882 ) ) GLOBAL_UNIT_ASSIGNED_CONTEXT ( ( #12842, #2214, #3914 ) ) REPRESENTATION_CONTEXT ( 'NONE', 'WORKASPACE' ) );
#15767=ORIENTED_EDGE ( 'NONE', *, *, #10756, .F. ) ;
#15768=CARTESIAN_POINT ( 'NONE',  ( -0.2324876215537165225, 5.107993264127207667, -0.2053580284920872856 ) ) ;
#15769=CARTESIAN_POINT ( 'NONE',  ( -0.3133021733797068942, 4.558532991712811011, 0.02780185521819914310 ) ) ;
#15770=CARTESIAN_POINT ( 'NONE',  ( 0.3119999999999999996, 0.6222222220704892726, 0.000000000000000000 ) ) ;
#15772=CARTESIAN_POINT ( 'NONE',  ( 0.3120349077283414152, 4.253276283983363548, -0.04063966104624280873 ) ) ;
#15773=CARTESIAN_POINT ( 'NONE',  ( -0.07676069278406914831, 4.736058685955594427, 0.3046265517824304214 ) ) ;
#15774=CARTESIAN_POINT ( 'NONE',  ( 0.3105152002621879292, 4.084448063609871227, 0.03699839793702524443 ) ) ;
#15777=CARTESIAN_POINT ( 'NONE',  ( 0.2786832587059077659, 5.181255304933189088, -0.09125116685248849113 ) ) ;
#15780=CARTESIAN_POINT ( 'NONE',  ( -0.1993543840281266355, 3.748694444520309865, 0.1993543840281267465 ) ) ;
#15781=CARTESIAN_POINT ( 'NONE',  ( 1.910449006669871087E-17, 0.08055555540382261515, -0.3119999999999999996 ) ) ;
#15783=CARTESIAN_POINT ( 'NONE',  ( -0.03821718199043266234, 5.196224427665105061, 0.2847346366168296283 ) ) ;
#15785=CARTESIAN_POINT ( 'NONE',  ( -0.2206173157302027676, 4.620222222373953969, 0.2206173157302028787 ) ) ;
#15786=CARTESIAN_POINT ( 'NONE',  ( 0.1167790944451422702, 4.627166666742533074, -0.2819296736111110979 ) ) ;
#15787=EDGE_LOOP ( 'NONE', ( #14110, #6917, #12196, #5982 ) ) ;
#15788=CARTESIAN_POINT ( 'NONE',  ( -0.1993543840281266910, 4.012583333409198261, -0.1993543840281266910 ) ) ;
#15794=CARTESIAN_POINT ( 'NONE',  ( 0.1292346314604057300, 0.4520833333333329485, 0.3119999999999998885 ) ) ;
#15796=CARTESIAN_POINT ( 'NONE',  ( 0.1292346314604057023, 0.1118055554038226151, 0.3119999999999998885 ) ) ;
#15797=CARTESIAN_POINT ( 'NONE',  ( 0.04953945640252711835, 5.131792726399142524, 0.3025406458412410182 ) ) ;
#15801=CARTESIAN_POINT ( 'NONE',  ( 0.000000000000000000, 5.384999999999999787, 0.000000000000000000 ) ) ;
#15802=CARTESIAN_POINT ( 'NONE',  ( -0.2819296736111110979, 0.05972222214635559273, -0.1167790944451423396 ) ) ;
#15805=CARTESIAN_POINT ( 'NONE',  ( -0.2819296736111110424, 4.467444444520308977, 0.1167790944451424923 ) ) ;
#15809=CARTESIAN_POINT ( 'NONE',  ( 0.2206173157302027954, 4.196611111111110404, -0.2206173157302028232 ) ) ;
#15811=CARTESIAN_POINT ( 'NONE',  ( 0.1869076612972776497, 4.966140514420732899, 0.2519720605836450744 ) ) ;
#15818=CARTESIAN_POINT ( 'NONE',  ( 0.3065906244346884857, 4.142790625704452445, -0.06232558618896349295 ) ) ;
#15820=CARTESIAN_POINT ( 'NONE',  ( 0.2726203751773835227, 3.812261744675993214, -0.1571308155000509799 ) ) ;
#15823=CARTESIAN_POINT ( 'NONE',  ( 0.1167790944451423535, 0.09444444436857780956, 0.2819296736111110979 ) ) ;
#15829=CARTESIAN_POINT ( 'NONE',  ( 0.2206173157302027954, 3.863277777777777366, -0.2206173157302028232 ) ) ;
#15832=CARTESIAN_POINT ( 'NONE',  ( 0.2206173157302028232, 0.4138888888888885287, -0.2206173157302028232 ) ) ;
#15833=CARTESIAN_POINT ( 'NONE',  ( 0.3119999999999999996, 5.026472222222221120, -0.1292346314604056745 ) ) ;
#15836=CARTESIAN_POINT ( 'NONE',  ( -0.1167790944451423535, 4.196611111186976828, 0.2819296736111110979 ) ) ;
#15837=CARTESIAN_POINT ( 'NONE',  ( 0.1993543840281267465, 4.054250000075865223, 0.1993543840281266633 ) ) ;
#15838=CARTESIAN_POINT ( 'NONE',  ( -0.2206173157302027954, 0.5874999998482670627, -0.2206173157302028232 ) ) ;
#15842=ORIENTED_EDGE ( 'NONE', *, *, #19903, .T. ) ;
#15844=CARTESIAN_POINT ( 'NONE',  ( -0.1167790944451423535, 4.418833333409198261, 0.2819296736111110424 ) ) ;
#15847=CARTESIAN_POINT ( 'NONE',  ( -0.2268203959220264077, 5.160927072947055549, 0.1963408053746545645 ) ) ;
#15852=CARTESIAN_POINT ( 'NONE',  ( -0.1993543840281266355, 3.984805555631421470, 0.1993543840281267465 ) ) ;
#15853=CARTESIAN_POINT ( 'NONE',  ( -0.1292346314604056190, 0.3687499999999997446, -0.3119999999999999996 ) ) ;
#15854=CARTESIAN_POINT ( 'NONE',  ( -0.2206173157302027676, 4.891055555555555046, 0.2206173157302028787 ) ) ;
#15857=CARTESIAN_POINT ( 'NONE',  ( -0.1993543840281267465, 0.1256944443685777957, 0.1993543840281266633 ) ) ;
#15860=CARTESIAN_POINT ( 'NONE',  ( 3.820898013339742174E-17, 5.384999999999999787, 0.3119999999999999996 ) ) ;
#15864=CARTESIAN_POINT ( 'NONE',  ( 1.679791495769851560E-14, 3.793833333485275183, 0.3119999999999999996 ) ) ;
#15866=CARTESIAN_POINT ( 'NONE',  ( -0.1993543840281266633, 0.5562499999241333759, -0.1993543840281266910 ) ) ;
#15867=CARTESIAN_POINT ( 'NONE',  ( -0.2819296736111110979, 4.033416666742532186, 0.000000000000000000 ) ) ;
#15869=CARTESIAN_POINT ( 'NONE',  ( 0.2819296736111110424, 4.731333333409200925, -0.1167790944451423396 ) ) ;
#15870=CARTESIAN_POINT ( 'NONE',  ( 0.2871469936926860367, 5.133785134621813739, -0.1062893706155275259 ) ) ;
#15871=CARTESIAN_POINT ( 'NONE',  ( 0.2824505285658038822, 5.074643056359858129, 0.1332943695421338060 ) ) ;
#15872=ORIENTED_EDGE ( 'NONE', *, *, #11414, .T. ) ;
#15873=AXIS2_PLACEMENT_3D ( 'NONE', #14071, #2970, #12497 ) ;
#15874=CARTESIAN_POINT ( 'NONE',  ( 0.2206173157302027954, 4.807722222222221120, -0.2206173157302028232 ) ) ;
#15875=CARTESIAN_POINT ( 'NONE',  ( -0.2206173157302028232, 3.884111111262842808, -0.2206173157302028232 ) ) ;
#15876=EDGE_CURVE ( 'NONE', #11353, #12971, #8633, .T. ) ;
#15878=CARTESIAN_POINT ( 'NONE',  ( 0.000000000000000000, 0.000000000000000000, 0.000000000000000000 ) ) ;
#15880=CARTESIAN_POINT ( 'NONE',  ( -0.1167790944451423119, 4.842444444520309865, -0.2819296736111110979 ) ) ;
#15884=CARTESIAN_POINT ( 'NONE',  ( -1.853979398150703436E-06, 4.543833384706993606, -0.3119999999944916280 ) ) ;
#15885=ORIENTED_EDGE ( 'NONE', *, *, #20049, .T. ) ;
#15886=CARTESIAN_POINT ( 'NONE',  ( 1.726321361862525858E-17, 0.1187499999241333620, -0.2819296736111110979 ) ) ;
#15889=PLANE ( 'NONE',  #22833 ) ;
#15892=CARTESIAN_POINT ( 'NONE',  ( -0.2665248263244868743, 5.052834303660202586, -0.1630106687325746095 ) ) ;
#15895=CARTESIAN_POINT ( 'NONE',  ( -0.1167790944451423535, 3.807722222298087988, 0.2819296736111110424 ) ) ;
#15896=CARTESIAN_POINT ( 'NONE',  ( 0.2828027056401378747, 5.033810059304799189, -0.1317826061406767446 ) ) ;
#15898=CARTESIAN_POINT ( 'NONE',  ( -0.1876242985175622935, 4.771710133335938409, -0.2524446861021691912 ) ) ;
#15899=CARTESIAN_POINT ( 'NONE',  ( -1.910449006669871087E-17, 4.543833333485065573, -0.3119999999999999996 ) ) ;
#15900=CARTESIAN_POINT ( 'NONE',  ( -1.726321361862525858E-17, 4.797305555631421470, -0.2819296736111110979 ) ) ;
#15902=CARTESIAN_POINT ( 'NONE',  ( 0.2819296736111110979, 4.102861111186976828, -3.452642723725051716E-17 ) ) ;
#15903=AXIS2_PLACEMENT_3D ( 'NONE', #18824, #9200, #3709 ) ;
#15904=ORIENTED_EDGE ( 'NONE', *, *, #13957, .F. ) ;
#15908=CARTESIAN_POINT ( 'NONE',  ( 1.910449006669871087E-17, 0.4763888888888885287, -0.3119999999999999996 ) ) ;
#15910=CARTESIAN_POINT ( 'NONE',  ( -0.1568165683378916209, 4.400276573276943104, 0.2727880797438460569 ) ) ;
#15918=CARTESIAN_POINT ( 'NONE',  ( 0.000000000000000000, 5.384999999999999787, 0.000000000000000000 ) ) ;
#15919=CARTESIAN_POINT ( 'NONE',  ( -0.1993543840281266910, 4.401472222298088433, -0.1993543840281266910 ) ) ;
#15920=CARTESIAN_POINT ( 'NONE',  ( 0.1292346314604057300, 0.1743055555555551861, 0.3119999999999998885 ) ) ;
#15923=CARTESIAN_POINT ( 'NONE',  ( 0.3119999999999998885, 0.4520833331816005995, 0.1292346314604058410 ) ) ;
#15924=CARTESIAN_POINT ( 'NONE',  ( 0.2206173157302027954, 4.307722222222221120, -0.2206173157302028232 ) ) ;
#15926=CARTESIAN_POINT ( 'NONE',  ( -0.3119999999999999996, 5.113277777929509327, 0.000000000000000000 ) ) ;
#15928=CARTESIAN_POINT ( 'NONE',  ( 0.1444491956679451461, 4.964733462867917169, 0.2770352471482286361 ) ) ;
#15929=CARTESIAN_POINT ( 'NONE',  ( 0.2252755657635890640, 4.578756013223267196, 0.2171699826210613526 ) ) ;
#15930=ORIENTED_EDGE ( 'NONE', *, *, #19953, .T. ) ;
#15933=CARTESIAN_POINT ( 'NONE',  ( 0.2032514787282173330, 4.133466838173744939, 0.2368180772981753890 ) ) ;
#15936=CARTESIAN_POINT ( 'NONE',  ( 0.04084013455945455923, 3.794930617901433934, 0.3119999999999988338 ) ) ;
#15937=PRODUCT_DEFINITION_SHAPE ( 'NONE', 'NONE',  #9710 ) ;
#15939=CARTESIAN_POINT ( 'NONE',  ( -0.1993543840281267465, 0.08402777770191115214, 0.1993543840281266633 ) ) ;
#15942=CARTESIAN_POINT ( 'NONE',  ( 5.178964085587577574E-17, 5.102861111186976828, 0.2819296736111110979 ) ) ;
#15944=ORIENTED_EDGE ( 'NONE', *, *, #20051, .F. ) ;
#15947=CARTESIAN_POINT ( 'NONE',  ( -0.1474229253358168013, 4.289503790139332473, 0.2774834428915729512 ) ) ;
#15949=CARTESIAN_POINT ( 'NONE',  ( -5.731347020009612645E-17, 0.5041666666666663188, 0.3119999999999999996 ) ) ;
#15950=CARTESIAN_POINT ( 'NONE',  ( -0.1292346314604057023, 4.894527777777777366, 0.3119999999999998885 ) ) ;
#15952=CARTESIAN_POINT ( 'NONE',  ( 0.2819296736111110979, 4.325083333409198261, -3.452642723725051716E-17 ) ) ;
#15953=CARTESIAN_POINT ( 'NONE',  ( 5.178964085587577574E-17, 3.936194444520310309, 0.2819296736111110979 ) ) ;
#15955=CARTESIAN_POINT ( 'NONE',  ( -0.1292346314604081170, 3.873694444444442997, -0.3119999999999975016 ) ) ;
#15957=ORIENTED_EDGE ( 'NONE', *, *, #20209, .F. ) ;
#15960=CARTESIAN_POINT ( 'NONE',  ( 0.1993543840281267465, 4.540361111186976828, 0.1993543840281266633 ) ) ;
#15963=CARTESIAN_POINT ( 'NONE',  ( 0.1292346314604131963, 3.790361111111110404, 0.3119999999999925611 ) ) ;
#15967=EDGE_CURVE ( 'NONE', #9548, #5345, #7112, .T. ) ;
#15969=VECTOR ( 'NONE', #20630, 39.37007874015748143 ) ;
#15970=CARTESIAN_POINT ( 'NONE',  ( 0.1993543840281267465, 4.165361111186976828, 0.1993543840281266633 ) ) ;
#15972=CARTESIAN_POINT ( 'NONE',  ( -0.2952551624447684597, 4.838429752736293388, 0.1030155185898169040 ) ) ;
#15976=CARTESIAN_POINT ( 'NONE',  ( 0.2819296736111110424, 0.1430555554796889284, 0.1167790944451424923 ) ) ;
#15984=CARTESIAN_POINT ( 'NONE',  ( -0.01784808211855408791, 3.766536899369928637, -0.3115622909592437595 ) ) ;
#15986=CARTESIAN_POINT ( 'NONE',  ( -0.1993543840281266633, 0.3895833332574667462, -0.1993543840281266910 ) ) ;
#15987=CARTESIAN_POINT ( 'NONE',  ( 0.1167790944451422702, 4.016055555631422358, -0.2819296736111110424 ) ) ;
#15989=VERTEX_POINT ( 'NONE', #12679 ) ;
#15990=CARTESIAN_POINT ( 'NONE',  ( 0.1167790944451422702, 4.682722222298088433, -0.2819296736111110424 ) ) ;
#15991=CARTESIAN_POINT ( 'NONE',  ( 0.2309745581487958610, 5.136678346995997124, -0.2008515164670272302 ) ) ;
#15995=VECTOR ( 'NONE', #15387, 39.37007874015748143 ) ;
#15998=CARTESIAN_POINT ( 'NONE',  ( 0.1993543840281267465, 5.095916666742532186, 0.1993543840281266633 ) ) ;
#16002=CARTESIAN_POINT ( 'NONE',  ( -0.2819296736111110424, 4.967444444520310753, 0.1167790944451424923 ) ) ;
#16005=CARTESIAN_POINT ( 'NONE',  ( -0.1549461890638730299, 5.104977286800423286, -0.2696689821046959756 ) ) ;
#16006=CARTESIAN_POINT ( 'NONE',  ( -5.731347020009612645E-17, 0.2194444442927115380, 0.3119999999999999996 ) ) ;
#16007=ORIENTED_EDGE ( 'NONE', *, *, #21983, .T. ) ;
#16008=CARTESIAN_POINT ( 'NONE',  ( 0.1993543840281266910, 0.3895833332574667462, -0.1993543840281266910 ) ) ;
#16011=CYLINDRICAL_SURFACE ( 'NONE', #17921, 0.3119999999999999996 ) ;
#16015=CARTESIAN_POINT ( 'NONE',  ( -0.1649367396721517220, 5.048643163735372141, -0.2662506188672706386 ) ) ;
#16018=CARTESIAN_POINT ( 'NONE',  ( -0.1993543840281266910, 4.637583333409199149, -0.1993543840281266910 ) ) ;
#16019=CARTESIAN_POINT ( 'NONE',  ( 0.000000000000000000, 5.384999999999999787, 0.000000000000000000 ) ) ;
#16020=CARTESIAN_POINT ( 'NONE',  ( 0.2819296736111110424, 3.884111111186976384, -0.1167790944451423396 ) ) ;
#16021=CARTESIAN_POINT ( 'NONE',  ( -0.1516584850513022498, 0.04616102306513563541, -0.2545636604784221046 ) ) ;
#16022=CARTESIAN_POINT ( 'NONE',  ( 0.2824852782387745620, 5.033831851842247573, -0.1324622426912574757 ) ) ;
#16025=CARTESIAN_POINT ( 'NONE',  ( 0.3119999999999999996, 4.307722222373953969, -3.820898013339742174E-17 ) ) ;
#16026=CARTESIAN_POINT ( 'NONE',  ( 0.2819296736111110979, 4.727861111186976828, -3.452642723725051716E-17 ) ) ;
#16028=ADVANCED_FACE ( 'NONE', ( #6560 ), #2783, .T. ) ;
#16029=CARTESIAN_POINT ( 'NONE',  ( 0.1993543840281267465, 4.151472222298087544, 0.1993543840281266633 ) ) ;
#16036=EDGE_LOOP ( 'NONE', ( #23422, #8785, #19059, #4888 ) ) ;
#16037=( BOUNDED_CURVE ( )  B_SPLINE_CURVE ( 2, ( #21164, #1286, #13740, #17994, #17627, #8227, #19693, #4694, #8346 ),
 .UNSPECIFIED., .F., .F. ) 
 B_SPLINE_CURVE_WITH_KNOTS ( ( 3, 2, 2, 2, 3 ),
 ( 0.2291666666666666574, 0.2395833333333333426, 0.2500000000000000000, 0.2604166666666666852, 0.2708333333333333148 ),
 .UNSPECIFIED. ) 
 CURVE ( )  GEOMETRIC_REPRESENTATION_ITEM ( )  RATIONAL_B_SPLINE_CURVE ( ( 1.000000000000000000, 0.9238795325112867385, 1.000000000000000000, 0.9238795325112867385, 1.000000000000000000, 0.9238795325112867385, 1.000000000000000000, 0.9238795325112867385, 1.000000000000000000 ) ) 
 REPRESENTATION_ITEM ( '' )  );
#16041=CARTESIAN_POINT ( 'NONE',  ( 0.1292346314604056745, 0.3548611109593781676, -0.3119999999999999996 ) ) ;
#16042=CARTESIAN_POINT ( 'NONE',  ( -0.006901823634795379095, 4.377352498881602827, -0.3119347351468002572 ) ) ;
#16045=EDGE_CURVE ( 'NONE', #16588, #1106, #17110, .T. ) ;
#16048=CARTESIAN_POINT ( 'NONE',  ( 0.2819296736111110979, 0.03541666659080003332, 0.000000000000000000 ) ) ;
#16050=CARTESIAN_POINT ( 'NONE',  ( 0.1993543840281266633, 4.554250000075866112, -0.1993543840281266910 ) ) ;
#16054=CARTESIAN_POINT ( 'NONE',  ( 0.000000000000000000, 5.384999999999999787, 0.000000000000000000 ) ) ;
#16055=CARTESIAN_POINT ( 'NONE',  ( -0.2206173157302027676, 4.002166666666665762, 0.2206173157302028787 ) ) ;
#16056=CARTESIAN_POINT ( 'NONE',  ( 0.1292346314604056190, 5.095916666818398610, -0.3119999999999999996 ) ) ;
#16057=CARTESIAN_POINT ( 'NONE',  ( 0.3072865194369331920, 4.976230144801160549, -0.06581296942666983729 ) ) ;
#16058=EDGE_LOOP ( 'NONE', ( #13213, #23188, #19444, #4558 ) ) ;
#16063=DIRECTION ( 'NONE',  ( 0.000000000000000000, 0.000000000000000000, -1.000000000000000000 ) ) ;
#16064=EDGE_CURVE ( 'NONE', #10194, #12509, #14116, .T. ) ;
#16067=EDGE_CURVE ( 'NONE', #17157, #3183, #5459, .T. ) ;
#16070=CARTESIAN_POINT ( 'NONE',  ( 0.2819296736111110979, 0.1083333332574667046, -0.1167790944451422980 ) ) ;
#16073=CARTESIAN_POINT ( 'NONE',  ( -0.2819296736111110979, 5.144527777853643791, 0.000000000000000000 ) ) ;
#16075=ORIENTED_EDGE ( 'NONE', *, *, #17520, .F. ) ;
#16076=DIRECTION ( 'NONE',  ( 0.000000000000000000, 0.000000000000000000, -1.000000000000000000 ) ) ;
#16077=CARTESIAN_POINT ( 'NONE',  ( -0.2525534724708262124, 4.285549707882127635, 0.1860445849415660324 ) ) ;
#16078=CARTESIAN_POINT ( 'NONE',  ( 0.000000000000000000, 5.384999999999999787, -0.3119999999999999996 ) ) ;
#16079=CARTESIAN_POINT ( 'NONE',  ( 0.3119999999999999996, 0.4659722222222220100, -0.1292346314604056468 ) ) ;
#16080=CARTESIAN_POINT ( 'NONE',  ( -0.1292346314604056745, 4.818138888888888083, -0.3119999999999999996 ) ) ;
#16081=CARTESIAN_POINT ( 'NONE',  ( 0.2819296736111111534, 4.154944444520310753, 0.1167790944451422563 ) ) ;
#16082=CARTESIAN_POINT ( 'NONE',  ( -0.1993543840281266355, 3.929250000075865668, 0.1993543840281267465 ) ) ;
#16085=ORIENTED_EDGE ( 'NONE', *, *, #17414, .F. ) ;
#16088=CARTESIAN_POINT ( 'NONE',  ( 0.1993543840281267465, 4.429250000075865223, 0.1993543840281266633 ) ) ;
#16090=CARTESIAN_POINT ( 'NONE',  ( 5.731347020009612645E-17, 3.786888888888888527, 0.3119999999999999996 ) ) ;
#16092=CARTESIAN_POINT ( 'NONE',  ( 0.2206173157302027676, 0.06666666666666633267, 0.2206173157302028787 ) ) ;
#16094=CARTESIAN_POINT ( 'NONE',  ( -0.2819296736111110424, 4.092444444520309865, 0.1167790944451424923 ) ) ;
#16095=CARTESIAN_POINT ( 'NONE',  ( -0.008720534560302872079, 4.821864677000621491, -0.3118955259047569983 ) ) ;
#16096=CYLINDRICAL_SURFACE ( 'NONE', #1935, 0.3119999999999999996 ) ;
#16099=CARTESIAN_POINT ( 'NONE',  ( -0.1993543840281267465, 0.5840277777019110550, 0.1993543840281266633 ) ) ;
#16109=CARTESIAN_POINT ( 'NONE',  ( -0.1167790944451424368, 0.3513888888130222155, 0.2819296736111110424 ) ) ;
#16110=CARTESIAN_POINT ( 'NONE',  ( 0.2819296736111110424, 4.120222222298087544, -0.1167790944451423396 ) ) ;
#16112=VERTEX_POINT ( 'NONE', #18627 ) ;
#16113=CARTESIAN_POINT ( 'NONE',  ( 0.1993543840281266633, 4.679250000075866112, -0.1993543840281266910 ) ) ;
#16116=CARTESIAN_POINT ( 'NONE',  ( 0.2188935633852181206, 5.085427961609339853, -0.2224342940683537995 ) ) ;
#16119=CARTESIAN_POINT ( 'NONE',  ( 0.1988758185427091096, 3.704359862811034798, -0.2404005174681773382 ) ) ;
#16121=CARTESIAN_POINT ( 'NONE',  ( 0.1239654880878250376, 4.206901642129136754, -0.2877763507316923874 ) ) ;
#16124=VERTEX_POINT ( 'NONE', #9364 ) ;
#16125=CARTESIAN_POINT ( 'NONE',  ( 5.178964085587577574E-17, 4.977861111186976828, 0.2819296736111110979 ) ) ;
#16127=CARTESIAN_POINT ( 'NONE',  ( -0.2993836324830134732, 5.117341590464007162, 0.07846023516673897302 ) ) ;
#16128=CARTESIAN_POINT ( 'NONE',  ( -0.05332960504393493423, 4.570127177272008012, 0.3074086044673321472 ) ) ;
#16130=CARTESIAN_POINT ( 'NONE',  ( 0.1167790944451423535, 0.2055555554796889006, 0.2819296736111110424 ) ) ;
#16132=CARTESIAN_POINT ( 'NONE',  ( -0.1167790944451422702, 0.01111111103524448085, -0.2819296736111110424 ) ) ;
#16133=CARTESIAN_POINT ( 'NONE',  ( -0.2780745499956817079, 5.202872933541006439, 0.05779310355066207688 ) ) ;
#16135=CARTESIAN_POINT ( 'NONE',  ( -0.2368628722706440370, 5.064021184620441041, 0.2033160227223854977 ) ) ;
#16136=( BOUNDED_CURVE ( )  B_SPLINE_CURVE ( 2, ( #23908, #1616, #14796, #3682, #12854, #7228, #5264, #7344, #22211 ),
 .UNSPECIFIED., .F., .F. ) 
 B_SPLINE_CURVE_WITH_KNOTS ( ( 3, 2, 2, 2, 3 ),
 ( 0.5982142857142856984, 0.6026785714285713969, 0.6071428571428569843, 0.6116071428571427937, 0.6160714285714284921 ),
 .UNSPECIFIED. ) 
 CURVE ( )  GEOMETRIC_REPRESENTATION_ITEM ( )  RATIONAL_B_SPLINE_CURVE ( ( 1.000000000000000000, 0.9238795325112867385, 1.000000000000000000, 0.9238795325112867385, 1.000000000000000000, 0.9238795325112867385, 1.000000000000000000, 0.9238795325112886259, 0.9999999999999981126 ) ) 
 REPRESENTATION_ITEM ( '' )  );
#16139=CARTESIAN_POINT ( 'NONE',  ( -0.2819296736111110424, 4.759111111186978604, 0.1167790944451424923 ) ) ;
#16140=CARTESIAN_POINT ( 'NONE',  ( -0.1292346314604058410, 0.2715277776260448528, 0.3119999999999998885 ) ) ;
#16142=CARTESIAN_POINT ( 'NONE',  ( 0.1797087373818229139, 3.721720957026357191, -0.2172305470487487511 ) ) ;
#16143=CARTESIAN_POINT ( 'NONE',  ( -0.3013616091699982680, 0.05241076192755348556, 0.02684792332517318622 ) ) ;
#16149=CARTESIAN_POINT ( 'NONE',  ( 0.3119999999999999996, 4.255638889040621820, -0.1292346314604056745 ) ) ;
#16150=CARTESIAN_POINT ( 'NONE',  ( 0.1993543840281267465, 4.776472222298088433, 0.1993543840281266633 ) ) ;
#16151=ORIENTED_EDGE ( 'NONE', *, *, #7036, .T. ) ;
#16152=CARTESIAN_POINT ( 'NONE',  ( -0.2819296736111110424, 3.745222222298088433, 0.1167790944451424923 ) ) ;
#16160=CARTESIAN_POINT ( 'NONE',  ( 0.2206173157302028232, 0.2402777776260448528, -0.2206173157302028232 ) ) ;
#16161=CARTESIAN_POINT ( 'NONE',  ( -0.2537383668351042565, 4.385579815452747887, -0.1818392428212168843 ) ) ;
#16166=VERTEX_POINT ( 'NONE', #10838 ) ;
#16167=CARTESIAN_POINT ( 'NONE',  ( -0.1167790944451422702, 0.3305555554796889561, -0.2819296736111110979 ) ) ;
#16170=CARTESIAN_POINT ( 'NONE',  ( -0.1167790944451423257, 4.398000000075866112, -0.2819296736111110424 ) ) ;
#16176=CARTESIAN_POINT ( 'NONE',  ( -0.3119999999999998885, 3.998694444444443441, 0.1292346314604058410 ) ) ;
#16178=CARTESIAN_POINT ( 'NONE',  ( 0.3119999999999999996, 5.033416666818398610, -0.1292346314604056745 ) ) ;
#16181=DIRECTION ( 'NONE',  ( -0.000000000000000000, -1.000000000000000000, -0.000000000000000000 ) ) ;
#16182=ORIENTED_EDGE ( 'NONE', *, *, #6441, .T. ) ;
#16184=B_SPLINE_CURVE_WITH_KNOTS ( 'NONE', 3,
 ( #22888, #338, #14986, #5710, #13172, #22656, #4237, #13531, #8011, #5944, #20946, #20585, #13402, #3883, #20825, #11326, #11690, #9860, #17289, #13646, #11206, #18756, #22532, #9491, #221, #7658, #19587, #8128, #820, #15929, #1060, #701, #21183, #12057, #19469, #15700 ),
 .UNSPECIFIED., .F., .F.,
 ( 4, 2, 2, 2, 2, 1, 1, 1, 2, 2, 1, 2, 2, 2, 2, 2, 2, 2, 2, 4 ),
 ( 0.4111882619051633325, 0.4135300815769560323, 0.4158719012487487876, 0.4182137209205414874, 0.4205555405923341872, 0.4207019043218212517, 0.4207750861865647840, 0.4208116771189365224, 0.4208208248520294847, 0.4208299725851223916, 0.4208482680513083163, 0.4211409955102825009, 0.4217264504282308701, 0.4228973602641276086, 0.4240682701000244026, 0.4252391799359211411, 0.4264100897718179350, 0.4275809996077146735, 0.4287519094436114675, 0.4299228192795082060 ),
 .UNSPECIFIED. ) ;
#16186=CARTESIAN_POINT ( 'NONE',  ( -0.08160653437250413311, 4.902727489126108118, 0.3038913141772855986 ) ) ;
#16191=EDGE_CURVE ( 'NONE', #2780, #2366, #23929, .T. ) ;
#16193=CARTESIAN_POINT ( 'NONE',  ( 0.1993543840281266355, 0.1534722221463556135, 0.1993543840281267465 ) ) ;
#16195=CARTESIAN_POINT ( 'NONE',  ( 0.1167790944451424368, 5.161888888964753619, 0.2819296736111110424 ) ) ;
#16197=ORIENTED_EDGE ( 'NONE', *, *, #342, .T. ) ;
#16198=CARTESIAN_POINT ( 'NONE',  ( -0.2094324427062704830, 4.605912874362315002, -0.2317822580471521066 ) ) ;
#16199=CARTESIAN_POINT ( 'NONE',  ( -0.05039085684935192683, 4.267471303508200364, -0.3086620900824355029 ) ) ;
#16203=CARTESIAN_POINT ( 'NONE',  ( 0.2206173157302027954, 4.641055555555554157, -0.2206173157302028232 ) ) ;
#16204=CARTESIAN_POINT ( 'NONE',  ( 0.1167790944451422702, 3.946611111186976828, -0.2819296736111110979 ) ) ;
#16205=CARTESIAN_POINT ( 'NONE',  ( -0.1167790944451423535, 3.821611111186977272, 0.2819296736111110424 ) ) ;
#16207=CARTESIAN_POINT ( 'NONE',  ( 0.1292346314604056745, 0.5215277776260448528, -0.3119999999999999996 ) ) ;
#16211=CARTESIAN_POINT ( 'NONE',  ( 0.2819296736111110424, 4.550777777853643791, -0.1167790944451423396 ) ) ;
#16213=CARTESIAN_POINT ( 'NONE',  ( -0.04339772285640217109, 4.489528066591655708, -0.3091585257072999027 ) ) ;
#16218=CARTESIAN_POINT ( 'NONE',  ( 0.1167790944451424506, 4.050777777853643791, 0.2819296736111110424 ) ) ;
#16219=FACE_OUTER_BOUND ( 'NONE', #296, .T. ) ;
#16224=CARTESIAN_POINT ( 'NONE',  ( 0.1993543840281266910, 0.09791666659080001944, -0.1993543840281266910 ) ) ;
#16226=CARTESIAN_POINT ( 'NONE',  ( 5.731347020009612645E-17, 4.064666666666665762, 0.3119999999999999996 ) ) ;
#16230=ORIENTED_EDGE ( 'NONE', *, *, #15876, .F. ) ;
#16233=CARTESIAN_POINT ( 'NONE',  ( -0.1571291654308913377, 3.844849430847837368, 0.2726213298963375276 ) ) ;
#16234=CARTESIAN_POINT ( 'NONE',  ( -0.1993543840281267465, 0.5145833332574667462, 0.1993543840281266633 ) ) ;
#16235=CARTESIAN_POINT ( 'NONE',  ( -0.1167790944451423257, 3.800777777853643347, -0.2819296736111110424 ) ) ;
#16237=CARTESIAN_POINT ( 'NONE',  ( -0.1167790944451423535, 4.321611111186976828, 0.2819296736111110424 ) ) ;
#16238=CARTESIAN_POINT ( 'NONE',  ( -1.861236469537744314E-17, 5.143359825938298435, -0.3039629827691722741 ) ) ;
#16239=CARTESIAN_POINT ( 'NONE',  ( -0.3119999999999998885, 4.387583333333331836, 0.1292346314604058410 ) ) ;
#16241=CARTESIAN_POINT ( 'NONE',  ( -1.910449006669871087E-17, 4.703555555555555046, -0.3119999999999999996 ) ) ;
#16242=CARTESIAN_POINT ( 'NONE',  ( -0.3119999999999999996, 3.724388889040620931, 0.000000000000000000 ) ) ;
#16244=CARTESIAN_POINT ( 'NONE',  ( 0.007906488776360224083, 4.210275811275788094, -0.3119139767300507793 ) ) ;
#16245=AXIS2_PLACEMENT_3D ( 'NONE', #20359, #11096, #18527 ) ;
#16246=DIRECTION ( 'NONE',  ( 0.000000000000000000, 0.000000000000000000, -1.000000000000000000 ) ) ;
#16247=CARTESIAN_POINT ( 'NONE',  ( -1.726321361862525858E-17, 4.950083333409199149, -0.2819296736111110979 ) ) ;
#16251=CARTESIAN_POINT ( 'NONE',  ( -0.1535707713190125057, 4.548357062511502846, -0.2744944684223242781 ) ) ;
#16253=CARTESIAN_POINT ( 'NONE',  ( -0.1167790944451424368, 0.1986111110352444808, 0.2819296736111110424 ) ) ;
#16254=CARTESIAN_POINT ( 'NONE',  ( -0.2819296736111110979, 0.07708333325746669074, -3.452642723725051716E-17 ) ) ;
#16255=CARTESIAN_POINT ( 'NONE',  ( -0.3096848393397610977, 4.725704742377146772, 0.04818851133790161972 ) ) ;
#16256=CARTESIAN_POINT ( 'NONE',  ( 0.1797084794423411680, 3.735609856212664948, -0.2172307604343298448 ) ) ;
#16258=CARTESIAN_POINT ( 'NONE',  ( -0.3097076850518720170, 5.056434073990216049, -0.04707335161509815930 ) ) ;
#16259=CARTESIAN_POINT ( 'NONE',  ( 0.1292346314604058410, 4.179249999999998799, 0.3119999999999998885 ) ) ;
#16260=CARTESIAN_POINT ( 'NONE',  ( -3.268767525105149064E-07, 3.877166675600695722, -0.3119999999998287477 ) ) ;
#16262=CARTESIAN_POINT ( 'NONE',  ( -0.1167790944451423257, 4.523000000075867000, -0.2819296736111110424 ) ) ;
#16264=CARTESIAN_POINT ( 'NONE',  ( -0.2206173157302027954, 0.2541666665149337478, -0.2206173157302028232 ) ) ;
#16265=CARTESIAN_POINT ( 'NONE',  ( -0.1993543840281266910, 5.193138888964755395, -0.1993543840281266910 ) ) ;
#16266=CARTESIAN_POINT ( 'NONE',  ( -0.2445782993682861228, 0.05555107339308604231, 0.1825817229059248648 ) ) ;
#16267=CARTESIAN_POINT ( 'NONE',  ( 0.3067602754552773425, 3.750577552586075836, 0.05698053772913803244 ) ) ;
#16270=CARTESIAN_POINT ( 'NONE',  ( -0.1292346314604056745, 4.380638889040620931, -0.3119999999999999996 ) ) ;
#16271=CARTESIAN_POINT ( 'NONE',  ( 0.2819296736111110979, 4.675777777853643791, -0.1167790944451423396 ) ) ;
#16272=CARTESIAN_POINT ( 'NONE',  ( -0.1167790944451423257, 3.898000000075865668, -0.2819296736111110424 ) ) ;
#16280=CARTESIAN_POINT ( 'NONE',  ( -0.2206173157302027954, 0.1986111109593781676, -0.2206173157302028232 ) ) ;
#16282=CARTESIAN_POINT ( 'NONE',  ( -1.292110690191215982E-05, 4.377167013980166388, -0.3120000000056822875 ) ) ;
#16283=EDGE_CURVE ( 'NONE', #16613, #5468, #22764, .T. ) ;
#16284=CARTESIAN_POINT ( 'NONE',  ( -0.07209992989303458388, 3.712509909146093356, -0.3042198929050881073 ) ) ;
#16287=VERTEX_POINT ( 'NONE', #20699 ) ;
#16289=CARTESIAN_POINT ( 'NONE',  ( 0.1167790944451423119, 0.2680555554796889561, -0.2819296736111110979 ) ) ;
#16292=CARTESIAN_POINT ( 'NONE',  ( 0.2819296736111110979, 4.543833333409199149, 0.1167790944451422425 ) ) ;
#16295=CARTESIAN_POINT ( 'NONE',  ( -0.04307916566617576992, 4.237087336754088440, 0.3090125702873792735 ) ) ;
#16296=CARTESIAN_POINT ( 'NONE',  ( 0.1292346314604056190, 4.033416666666666650, -0.3119999999999999996 ) ) ;
#16298=CARTESIAN_POINT ( 'NONE',  ( 0.1292346314604058410, 5.019527777929509327, 0.3119999999999998885 ) ) ;
#16299=CARTESIAN_POINT ( 'NONE',  ( -0.2206173157302027676, 4.168833333333332725, 0.2206173157302028787 ) ) ;
#16301=CARTESIAN_POINT ( 'NONE',  ( -0.08612638745143788577, 4.879649618296496350, -0.3001248726556640101 ) ) ;
#16304=ADVANCED_FACE ( 'NONE', ( #7884 ), #9853, .T. ) ;
#16306=ORIENTED_EDGE ( 'NONE', *, *, #16922, .T. ) ;
#16309=CARTESIAN_POINT ( 'NONE',  ( 0.1167790944451423119, 0.2263888888130222710, -0.2819296736111110979 ) ) ;
#16311=CARTESIAN_POINT ( 'NONE',  ( 0.1993543840281266633, 5.234805555631421470, -0.1993543840281266910 ) ) ;
#16312=DIRECTION ( 'NONE',  ( 0.000000000000000000, 0.000000000000000000, -1.000000000000000000 ) ) ;
#16315=CARTESIAN_POINT ( 'NONE',  ( -0.1811091878839710123, 4.604899780125036202, -0.2541407697476306127 ) ) ;
#16317=DIRECTION ( 'NONE',  ( -0.000000000000000000, -1.000000000000000000, -0.000000000000000000 ) ) ;
#16319=CARTESIAN_POINT ( 'NONE',  ( -0.2206173157302027676, 4.724388888888888083, 0.2206173157302028787 ) ) ;
#16320=CARTESIAN_POINT ( 'NONE',  ( 0.2819296736111110979, 4.102861111186976828, -3.452642723725051716E-17 ) ) ;
#16321=CARTESIAN_POINT ( 'NONE',  ( -0.1993543840281266910, 3.859805555631421470, -0.1993543840281266910 ) ) ;
#16325=( BOUNDED_CURVE ( )  B_SPLINE_CURVE ( 2, ( #15105, #20823, #13169, #22653, #2049, #22285, #22528, #20703, #335 ),
 .UNSPECIFIED., .F., .T. ) 
 B_SPLINE_CURVE_WITH_KNOTS ( ( 3, 2, 2, 2, 3 ),
 ( 0.6696428571428570953, 0.6741071428571429047, 0.6785714285714286031, 0.6830357142857144126, 0.6875000000000001110 ),
 .UNSPECIFIED. ) 
 CURVE ( )  GEOMETRIC_REPRESENTATION_ITEM ( )  RATIONAL_B_SPLINE_CURVE ( ( 1.000000000000000000, 0.9238795325112867385, 1.000000000000000000, 0.9238795325112867385, 1.000000000000000000, 0.9238795325112867385, 1.000000000000000000, 0.9238795325112848511, 1.000000000000001998 ) ) 
 REPRESENTATION_ITEM ( '' )  );
#16329=CARTESIAN_POINT ( 'NONE',  ( -0.1167790944451423535, 4.474388888964753619, 0.2819296736111110424 ) ) ;
#16330=CARTESIAN_POINT ( 'NONE',  ( -0.1665361594110063848, 4.493262398435235561, -0.2674012144246484257 ) ) ;
#16336=CARTESIAN_POINT ( 'NONE',  ( -0.1993543840281266910, 4.082027777853643791, -0.1993543840281266910 ) ) ;
#16338=CARTESIAN_POINT ( 'NONE',  ( 0.03980666169698005713, 5.161137237538360623, -0.2968008138702253329 ) ) ;
#16342=CARTESIAN_POINT ( 'NONE',  ( 0.1993543840281266910, 0.3201388888130222710, -0.1993543840281266910 ) ) ;
#16344=CARTESIAN_POINT ( 'NONE',  ( 0.3119999999999999996, 0.5736111111111107386, 0.000000000000000000 ) ) ;
#16350=EDGE_LOOP ( 'NONE', ( #11641, #22887, #18581, #518 ) ) ;
#16353=CARTESIAN_POINT ( 'NONE',  ( -0.1292346314604058410, 0.1118055555555552139, 0.3119999999999998885 ) ) ;
#16354=CARTESIAN_POINT ( 'NONE',  ( -0.2819296736111110424, 3.863277777853644235, -0.1167790944451423119 ) ) ;
#16356=CARTESIAN_POINT ( 'NONE',  ( -0.2819296736111110979, 4.477861111186976828, 0.000000000000000000 ) ) ;
#16358=CARTESIAN_POINT ( 'NONE',  ( 0.1865217406463640371, 5.123621613869084435, 0.2451376668825187843 ) ) ;
#16360=ORIENTED_EDGE ( 'NONE', *, *, #13051, .T. ) ;
#16361=CARTESIAN_POINT ( 'NONE',  ( 0.2206173157302028787, 4.682722222222222008, 0.2206173157302027954 ) ) ;
#16362=CARTESIAN_POINT ( 'NONE',  ( 0.2819296736111110424, 5.217444444520309865, -0.1167790944451423396 ) ) ;
#16364=CARTESIAN_POINT ( 'NONE',  ( 0.2328681059028355482, 4.203070697174108972, -0.2076452145264223170 ) ) ;
#16367=CARTESIAN_POINT ( 'NONE',  ( -0.1292346314604069513, 5.005638888888888083, 0.3119999999999986673 ) ) ;
#16368=APPLICATION_CONTEXT ( 'configuration controlled 3d designs of mechanical parts and assemblies' ) ;
#16369=CARTESIAN_POINT ( 'NONE',  ( -0.2819296736111110979, 4.908416666742532186, 0.000000000000000000 ) ) ;
#16371=CARTESIAN_POINT ( 'NONE',  ( 5.731347020009612645E-17, 4.786888888888888083, 0.3119999999999999996 ) ) ;
#16372=CARTESIAN_POINT ( 'NONE',  ( 0.3119999999999999996, 4.915361111111110404, -0.1292346314604056745 ) ) ;
#16374=CARTESIAN_POINT ( 'NONE',  ( 0.2819296736111110424, 0.2749999999241333204, -0.1167790944451423119 ) ) ;
#16380=CARTESIAN_POINT ( 'NONE',  ( -0.1404473344439336469, 5.067469647815745049, 0.2805009585328055999 ) ) ;
#16384=CARTESIAN_POINT ( 'NONE',  ( -0.3084949655708456029, 3.892483775246653011, 0.05129296941314141767 ) ) ;
#16387=CARTESIAN_POINT ( 'NONE',  ( 0.2819296736111110979, 4.505638888964754507, -3.452642723725051716E-17 ) ) ;
#16390=CARTESIAN_POINT ( 'NONE',  ( 0.1993543840281267465, 4.998694444520309865, 0.1993543840281266633 ) ) ;
#16391=CARTESIAN_POINT ( 'NONE',  ( -0.2611519554406496191, 0.05500242899132112839, 0.1578457353328193979 ) ) ;
#16392=CARTESIAN_POINT ( 'NONE',  ( 0.08400942620796066074, 3.763674766651834425, -0.3008225317091856033 ) ) ;
#16395=CARTESIAN_POINT ( 'NONE',  ( -0.2206173157302028232, 4.328555555707287894, -0.2206173157302028232 ) ) ;
#16396=CARTESIAN_POINT ( 'NONE',  ( 0.1993543840281267465, 4.609805555631421470, 0.1993543840281266633 ) ) ;
#16397=CARTESIAN_POINT ( 'NONE',  ( -0.2819296736111110979, 3.797305555631421470, 0.000000000000000000 ) ) ;
#16406=EDGE_LOOP ( 'NONE', ( #15650, #13377 ) ) ;
#16407=CARTESIAN_POINT ( 'NONE',  ( -0.3119999999999999996, 0.2090277776260448250, 0.1292346314604056190 ) ) ;
#16408=CARTESIAN_POINT ( 'NONE',  ( -0.03266130754527781649, 4.378054373819415090, -0.3103992783048078463 ) ) ;
#16409=CARTESIAN_POINT ( 'NONE',  ( -0.2212700040550385772, 3.731355058608409880, 0.2247321557902158817 ) ) ;
#16410=CARTESIAN_POINT ( 'NONE',  ( -0.2206173157302028787, 0.2749999999999996891, 0.2206173157302027954 ) ) ;
#16412=EDGE_LOOP ( 'NONE', ( #9007, #19478, #9348, #19176 ) ) ;
#16413=ORIENTED_EDGE ( 'NONE', *, *, #12915, .T. ) ;
#16417=CARTESIAN_POINT ( 'NONE',  ( 0.2819296736111110979, 4.325083333409198261, -3.452642723725051716E-17 ) ) ;
#16418=CARTESIAN_POINT ( 'NONE',  ( -0.2819296736111110979, 5.016055555631420582, -0.1167790944451422980 ) ) ;
#16420=CARTESIAN_POINT ( 'NONE',  ( -0.3084396050889865459, 4.225691337356074051, 0.04700294603068136401 ) ) ;
#16421=CARTESIAN_POINT ( 'NONE',  ( -0.2206173157302027676, 4.057722222222221120, 0.2206173157302028787 ) ) ;
#16423=CARTESIAN_POINT ( 'NONE',  ( -0.2206173157302028232, 4.995222222373954857, -0.2206173157302028232 ) ) ;
#16424=CARTESIAN_POINT ( 'NONE',  ( 0.2556300033343845146, 4.802328034493535291, 0.1804581348862814294 ) ) ;
#16426=CARTESIAN_POINT ( 'NONE',  ( -0.2493665650958605817, 4.896940045553083820, 0.1919006865458766919 ) ) ;
#16430=CARTESIAN_POINT ( 'NONE',  ( -0.2819296736111110979, 5.241750000075865223, 0.000000000000000000 ) ) ;
#16431=B_SPLINE_CURVE_WITH_KNOTS ( 'NONE', 3,
 ( #18210, #23919, #22103, #9182, #3567, #8815, #12619, #1505, #7355, #14685, #3448, #11139, #23675, #23556, #14805, #16625, #14558, #6870, #12985, #10654, #8940, #21981, #5275, #12745, #20160, #1625, #18085, #14313, #1385, #20282, #6995, #14439, #22222, #21747, #9059, #5032, #7238, #5398, #5521 ),
 .UNSPECIFIED., .F., .F.,
 ( 4, 2, 1, 1, 1, 1, 1, 2, 2, 2, 2, 2, 2, 2, 2, 2, 2, 2, 2, 2, 2, 4 ),
 ( 0.4477383270978809171, 0.4477425025345394549, 0.4477466779711979927, 0.4477550288445150128, 0.4477717305911491641, 0.4478051340844174111, 0.4478719410709538495, 0.4480055550440267820, 0.4482727829901727024, 0.4488072388824644876, 0.4498761506670480581, 0.4509450624516316286, 0.4520139742362151991, 0.4530828860207987696, 0.4541517978053823401, 0.4552207095899659106, 0.4562896213745494811, 0.4573585331591330516, 0.4584274449437166221, 0.4605652685128837631, 0.4627030920820509041, 0.4648409156512180451 ),
 .UNSPECIFIED. ) ;
#16434=CARTESIAN_POINT ( 'NONE',  ( -5.178964085587577574E-17, 0.2020833332574667185, 0.2819296736111110979 ) ) ;
#16436=CARTESIAN_POINT ( 'NONE',  ( -0.1167790944451423257, 5.134111111186976828, -0.2819296736111110424 ) ) ;
#16437=CARTESIAN_POINT ( 'NONE',  ( 1.241811370555571286E-09, 4.488277777895108400, -0.3119999999999999996 ) ) ;
#16439=CARTESIAN_POINT ( 'NONE',  ( -0.1167790944451423257, 4.786888888964755395, -0.2819296736111110424 ) ) ;
#16440=CARTESIAN_POINT ( 'NONE',  ( -0.1916867731382111140, 4.177017067639016368, 0.2495446019803314319 ) ) ;
#16441=CARTESIAN_POINT ( 'NONE',  ( 0.001496851655420368583, 4.877126432010315149, -0.3119969275169424128 ) ) ;
#16444=CARTESIAN_POINT ( 'NONE',  ( 5.731347020009612645E-17, 4.675777777777777366, 0.3119999999999999996 ) ) ;
#16445=CARTESIAN_POINT ( 'NONE',  ( 0.1993543840281267465, 3.984805555631421470, 0.1993543840281266633 ) ) ;
#16446=CARTESIAN_POINT ( 'NONE',  ( -0.1167790944451423535, 3.766055555631421470, 0.2819296736111110424 ) ) ;
#16447=CARTESIAN_POINT ( 'NONE',  ( 0.2967651801959635405, 4.032702029939365218, -0.09630854978782486808 ) ) ;
#16448=CARTESIAN_POINT ( 'NONE',  ( 0.3119999999999999996, 0.5145833331816004330, -0.1292346314604056468 ) ) ;
#16451=CARTESIAN_POINT ( 'NONE',  ( -0.2819296736111110979, 4.352861111186976828, 0.000000000000000000 ) ) ;
#16452=CARTESIAN_POINT ( 'NONE',  ( -0.3093573145567999894, 4.501048372529125707, -0.04052794418377673319 ) ) ;
#16457=CARTESIAN_POINT ( 'NONE',  ( -0.08166535435460516024, 3.958181172869919440, 0.3038794725157443755 ) ) ;
#16461=CARTESIAN_POINT ( 'NONE',  ( -5.178964085587577574E-17, 0.3548611110352444808, 0.2819296736111110979 ) ) ;
#16466=B_SPLINE_CURVE_WITH_KNOTS ( 'NONE', 3,
 ( #4077, #2263, #11654, #6023, #13492, #20907, #19078, #6845, #16358, #23412, #1239, #1356, #6601, #10402, #19770, #3067, #6481, #2821, #14165, #12467, #23288, #14048, #21595, #4891, #1117, #17825, #2945, #15870, #21479, #3181, #4764, #15991, #19889, #18059, #6721, #12353, #10630, #17944, #12235, #10513, #6968, #8787, #16238 ),
 .UNSPECIFIED., .F., .F.,
 ( 4, 2, 2, 2, 2, 2, 2, 2, 2, 2, 2, 2, 1, 2, 2, 2, 2, 2, 2, 2, 2, 4 ),
 ( 0.04224588871235206156, 0.04377812836417232373, 0.04531036801599258590, 0.04684260766781284113, 0.04760872749372297569, 0.04837484731963310330, 0.04914096714554323092, 0.04990708697145335854, 0.05143932662327361377, 0.05297156627509387594, 0.05450380592691413117, 0.05526992575282425879, 0.05603604557873438641, 0.05680216540464452096, 0.05756828523055465552, 0.05910052488237491075, 0.06063276453419516598, 0.06216500418601542122, 0.06293112401192554883, 0.06369724383783567645, 0.06522948348965594556, 0.06676172314147620079 ),
 .UNSPECIFIED. ) ;
#16467=VERTEX_POINT ( 'NONE', #1296 ) ;
#16469=( BOUNDED_CURVE ( )  B_SPLINE_CURVE ( 2, ( #21054, #2645, #6173, #10094, #4344, #17514, #19220, #7769, #2527 ),
 .UNSPECIFIED., .F., .T. ) 
 B_SPLINE_CURVE_WITH_KNOTS ( ( 3, 2, 2, 2, 3 ),
 ( 0.3958333333333333148, 0.4062500000000000000, 0.4166666666666666852, 0.4270833333333333148, 0.4375000000000000000 ),
 .UNSPECIFIED. ) 
 CURVE ( )  GEOMETRIC_REPRESENTATION_ITEM ( )  RATIONAL_B_SPLINE_CURVE ( ( 1.000000000000000000, 0.9238795325112867385, 1.000000000000000000, 0.9238795325112867385, 1.000000000000000000, 0.9238795325112867385, 1.000000000000000000, 0.9238795325112867385, 1.000000000000000000 ) ) 
 REPRESENTATION_ITEM ( '' )  );
#16471=( BOUNDED_SURFACE ( )  B_SPLINE_SURFACE ( 1, 2, ( 
 ( #16430, #1064, #12420, #12542, #8492, #19835, #9591, #10944, #7756, #22386, #5688, #9230, #16791, #16667, #15200, #9350, #20444, #17023, #20323, #18615, #196, #1667, #20684, #5803, #3741, #9469, #1785, #3861, #14852, #18372, #13030, #73, #13151, #18735, #18857, #317, #3610, #24090, #2032, #7402, #11063, #2156, #11187, #11304, #16548, #22267, #7638, #16903, #9100, #5445, #1906, #7516, #15087, #14965, #22509, #20564, #3492, #5564, #5323, #13268, #3975, #11425, #12788, #20206, #18492, #23970, #7282, #14731, #22147, #12909, #14612, #12797, #20455, #14861, #1794, #14976, #10956, #16679, #22036, #14742, #3504, #83, #7527, #12922, #3750, #210, #15097, #13277, #5332, #11436, #1917, #9360, #20333, #11194, #3622, #18867, #13038, #24101, #20696, #23980, #22278, #3872, #20216, #7649, #9480, #7410, #13161, #5454, #22398, #18502, #18381, #5574, #18623, #16803, #5698, #22520, #3986, #7292, #11072, #20575, #9238, #22157, #5813, #11315, #18746, #1676, #2042, #16913, #8996, #9109, #16559, #16439, #23849, #7169, #13519, #22761, #11563, #18991, #22992, #2289, #11680, #8115, #13749, #19103, #8002, #15569, #13636, #450, #9850, #2644, #6296, #691, #9971, #17513, #21053, #8236, #22877, #2409, #20935, #23104, #17034, #15454, #808, #15690, #10093, #21294, #17279, #19219, #7881, #328, #4228, #15333, #567, #6053, #6172, #20814, #6413, #13392, #21173, #4343, #11795, #2526, #4104, #13867, #9724, #4463, #17160, #17398, #11927, #4588, #19346, #2170, #12047, #9603, #7768, #15211, #22646, #5934, #16050, #10686, #4701, #16292, #19460, #18120, #8719, #924, #23223, #6774, #1171, #12286, #1294, #21412, #3003, #8354, #1050, #13985, #10571, #18002, #23342, #14218, #1417, #8846, #23705, #15805, #21892, #12406, #19825, #6653, #21655, #14100, #5181, #23465, #10452, #7026, #10329, #8609, #14340, #6532, #14468, #19948, #17879, #23585, #15919, #16170, #4816, #12169, #4942, #3120, #6902, #21773, #2758, #10209, #17756, #21527, #5060, #19700, #8477, #17635, #12529, #3238, #19578, #2870, #7502, #16771, #16417, #12772, #3596, #11048, #7268, #23954, #9086, #22011, #5309, #9335, #20190, #22129, #18600, #55, #5430, #18477, #1892, #24075, #10930, #20312, #13136, #14950, #11172, #20429, #3845, #7384, #18718, #9215, #12896, #14716, #9453, #3358, #1770, #11290, #2017, #20549, #7620, #16654, #5549, #18358, #10810, #14835, #1651, #22253, #16535, #13014, #3725, #18238, #20070, #22369, #5671, #16887, #180, #15071, #22493, #12652, #1537, #8968, #23826, #7148, #14588, #3479, #17370, #22621, #18962, #17135, #21145, #4316, #17253, #780, #5907, #8210, #4434, #22965, #20905, #20667, #2618, #300, #422, #17484, #8088, #9574, #539, #13609, #20785, #4200, #7974, #2501, #9820, #9940, #15425, #661, #11652, #3962, #22734, #15659, #7856, #15540, #2384, #11900, #13490, #4075, #15305, #11531, #17007, #6266, #21024, #5788, #11406, #13724, #11771, #2261, #19076, #7740, #18839, #22853, #19319, #6021, #13364, #10061, #2135, #15184, #9695, #6142, #19191, #13252, #2843, #16020, #4918, #14073, #1021, #6510, #8583, #23437, #12501, #18086, #21501, #2733, #21268, #10184, #4790, #23557, #17975, #19922, #8452, #21625, #8330, #12257, #4560, #15895, #12020, #3096, #23317, #6747, #8816, #6625, #17853, #1266, #23199, #10304, #19672, #2973, #23078, #19433, #10428, #12382, #15780, #1144, #1386, #5033, #14192, #19798, #10541, #8692, #16142 ),
 ( #6871, #14314, #4677, #17607, #17726, #12145, #21748, #19553, #3209, #898, #10655, #13958, #6387, #21387, #13835, #3694, #18686, #11022, #16265, #9183, #12865, #7473, #25, #1626, #24046, #20283, #14921, #1506, #13107, #23676, #22340, #5522, #21864, #20039, #3568, #22104, #9060, #22223, #18212, #23921, #5155, #21984, #10785, #7356, #14806, #20161, #18446, #5643, #20520, #3818, #12621, #1988, #16627, #12986, #3449, #1743, #10900, #6996, #20401, #7240, #11261, #7119, #5399, #11140, #3327, #14440, #16743, #14686, #18570, #12746, #1860, #16507, #8941, #9302, #16390, #23798, #14559, #5276, #18330, #7712, #13336, #6115, #20758, #15158, #6237, #17104, #7942, #20636, #4048, #4289, #13584, #13225, #9544, #392, #7831, #11503, #18937, #5876, #18807, #2103, #20995, #16977, #2234, #15398, #11746, #9667, #15277, #22824, #20877, #22590, #22704, #9911, #5994, #17228, #13460, #635, #272, #13702, #9424, #8066, #19167, #15043, #3937, #4171, #11623, #19053, #2476, #11379, #2354, #22465, #9795, #510, #17343, #15516, #22940, #21119, #4409, #11873, #19288, #5765, #16863, #148, #7592, #6480, #14047, #13932, #5005, #6600, #17700, #14284, #17582, #15869, #21594, #23054, #17943, #3066, #993, #6720, #23170, #1116, #12117, #8181, #10277, #21478, #2944, #15990, #16113, #6844, #873, #21362, #23411, #4649, #8304, #23526, #8422, #8549, #13808, #19526, #4889, #14164, #6362, #2706, #23287, #4763, #2820, #12234, #19645, #11995, #19409, #12352, #10157, #10401, #19769, #10512, #17824, #1238, #8664, #21721, #15756, #12466, #2592, #10038, #17460, #753, #15636, #21245, #4533, #16476, #5244, #7088, #16713, #10629, #9034, #18538, #1828, #3661, #14892, #20130, #12835, #1476, #18058, #14529, #8914, #3421, #16356, #10871, #14408, #14681, #6967, #24016, #3296, #12589, #7326, #22311, #14652, #19888, #20253, #23888, #11107, #9272, #7444, #21831, #21951, #5609, #22193, #23648, #22073, #3540, #10751, #18300, #7207, #16596, #5368, #14778, #10993, #5491, #1599, #1354, #12716, #3180, #18419, #12957, #1712, #8786, #9151, #18182, #20371, #23767, #5123, #16237, #20010, #22910, #3785, #7912, #4137, #11348, #2205, #16835, #11229, #22673, #15363, #245, #5734, #22792, #1950, #15013, #18776, #17066, #7679, #15129, #16945, #5963, #19024, #4021, #22556, #20608, #13425, #20846, #2439, #8034, #11470, #119, #18657, #7561, #18903, #13552, #6086, #9882, #5847, #11593, #22435, #9636, #9395, #13309, #13193, #17194, #20724, #2320, #13073, #360, #7801, #20966, #3905, #15244, #9756, #480, #20489, #2072, #4261, #11711, #9513, #19134, #15484, #17309, #602, #842, #11963, #19492, #17549, #4375, #13671, #15722, #8271, #4617, #12082, #954, #15837, #19377, #17669, #19611, #23134, #14015, #12203, #1080, #17788, #23025, #2674, #6447, #21561, #4731, #8385, #1206, #6326, #8637, #4851, #23378, #21328, #21085, #8151, #10125, #10240, #13900, #2787, #23256, #6565, #2905, #21445, #10364, #13778, #8512, #15953, #19732, #16082, #6686, #10006, #11835, #17429, #14131, #12319, #3034, #10481, #17913, #6206, #15603, #19253, #2558, #722, #21206, #4498, #23734, #23857, #9246, #16321, #18270, #18388, #23619, #3266, #12683, #20101, #23495, #19853, #7058, #5340, #16205, #5210, #18509, #5465, #21920, #18151, #5090, #3390, #10717, #21687, #6810, #8880, #1446, #10842, #1567, #9002, #16446, #12558, #7178, #12804, #14497, #14619, #20223, #1683, #10963, #6933 ) ),
 .UNSPECIFIED., .F., .F., .F. ) 
 B_SPLINE_SURFACE_WITH_KNOTS ( ( 2, 2 ),
 ( 3, 2, 2, 2, 2, 2, 2, 2, 2, 2, 2, 2, 2, 2, 2, 2, 2, 2, 2, 2, 2, 2, 2, 2, 2, 2, 2, 2, 2, 2, 2, 2, 2, 2, 2, 2, 2, 2, 2, 2, 2, 2, 2, 2, 2, 2, 2, 2, 2, 2, 2, 2, 2, 2, 2, 2, 2, 2, 2, 2, 2, 2, 2, 2, 2, 2, 2, 2, 2, 2, 2, 2, 2, 2, 2, 2, 2, 2, 2, 2, 2, 2, 2, 2, 2, 2, 2, 2, 2, 2, 2, 2, 2, 2, 2, 2, 2, 2, 2, 2, 2, 2, 2, 2, 2, 2, 2, 2, 2, 2, 2, 2, 2, 2, 2, 2, 2, 2, 2, 2, 2, 2, 2, 2, 2, 2, 2, 2, 2, 2, 2, 2, 2, 2, 2, 2, 2, 2, 2, 2, 2, 2, 2, 2, 2, 2, 2, 2, 2, 2, 2, 2, 2, 2, 2, 2, 2, 2, 2, 2, 2, 2, 2, 2, 2, 2, 2, 2, 2, 2, 2, 2, 2, 2, 2, 2, 2, 2, 2, 2, 2, 2, 2, 2, 2, 2, 2, 2, 2, 2, 2, 2, 2, 2, 2, 2, 2, 2, 2, 2, 2, 2, 2, 2, 2, 2, 2, 2, 2, 2, 2, 2, 2, 2, 2, 2, 2, 2, 2, 3 ),
 ( 0.000000000000000000, 1.000000000000000000 ),
 ( 0.000000000000000000, 0.004464285714285714038, 0.008928571428571428076, 0.01339285714285714211, 0.01785714285714285615, 0.02232142857142857192, 0.02678571428571428423, 0.03125000000000000000, 0.03571428571428571230, 0.04017857142857143155, 0.04464285714285714385, 0.04910714285714285615, 0.05357142857142856845, 0.05803571428571428770, 0.06250000000000000000, 0.06696428571428571230, 0.07142857142857142461, 0.07589285714285713691, 0.08035714285714286309, 0.08482142857142857539, 0.08928571428571428770, 0.09375000000000000000, 0.09821428571428571230, 0.1026785714285714246, 0.1071428571428571369, 0.1116071428571428631, 0.1160714285714285754, 0.1205357142857142877, 0.1250000000000000000, 0.1294642857142857262, 0.1339285714285714246, 0.1383928571428571508, 0.1428571428571428492, 0.1473214285714285754, 0.1517857142857142738, 0.1562500000000000000, 0.1607142857142857262, 0.1651785714285714246, 0.1696428571428571508, 0.1741071428571428492, 0.1785714285714285754, 0.1830357142857142738, 0.1875000000000000000, 0.1919642857142857262, 0.1964285714285714246, 0.2008928571428571508, 0.2053571428571428492, 0.2098214285714285754, 0.2142857142857142738, 0.2187500000000000000, 0.2232142857142857262, 0.2276785714285714246, 0.2321428571428571508, 0.2366071428571428492, 0.2410714285714285754, 0.2455357142857142738, 0.2500000000000000000, 0.2544642857142856984, 0.2589285714285714524, 0.2633928571428571508, 0.2678571428571428492, 0.2723214285714285476, 0.2767857142857143016, 0.2812500000000000000, 0.2857142857142856984, 0.2901785714285714524, 0.2946428571428571508, 0.2991071428571428492, 0.3035714285714285476, 0.3080357142857143016, 0.3125000000000000000, 0.3169642857142856984, 0.3214285714285714524, 0.3258928571428571508, 0.3303571428571428492, 0.3348214285714285476, 0.3392857142857143016, 0.3437500000000000000, 0.3482142857142856984, 0.3526785714285714524, 0.3571428571428571508, 0.3616071428571428492, 0.3660714285714285476, 0.3705357142857143016, 0.3750000000000000000, 0.3794642857142856984, 0.3839285714285714524, 0.3883928571428571508, 0.3928571428571428492, 0.3973214285714285476, 0.4017857142857143016, 0.4062500000000000000, 0.4107142857142856984, 0.4151785714285714524, 0.4196428571428571508, 0.4241071428571428492, 0.4285714285714285476, 0.4330357142857143016, 0.4375000000000000000, 0.4419642857142856984, 0.4464285714285714524, 0.4508928571428571508, 0.4553571428571428492, 0.4598214285714285476, 0.4642857142857143016, 0.4687500000000000000, 0.4732142857142856984, 0.4776785714285714524, 0.4821428571428571508, 0.4866071428571428492, 0.4910714285714285476, 0.4955357142857143016, 0.5000000000000000000, 0.5044642857142856984, 0.5089285714285713969, 0.5133928571428570953, 0.5178571428571429047, 0.5223214285714286031, 0.5267857142857143016, 0.5312500000000000000, 0.5357142857142856984, 0.5401785714285713969, 0.5446428571428570953, 0.5491071428571429047, 0.5535714285714286031, 0.5580357142857143016, 0.5625000000000000000, 0.5669642857142856984, 0.5714285714285713969, 0.5758928571428570953, 0.5803571428571429047, 0.5848214285714286031, 0.5892857142857143016, 0.5937500000000000000, 0.5982142857142856984, 0.6026785714285713969, 0.6071428571428570953, 0.6116071428571429047, 0.6160714285714286031, 0.6205357142857143016, 0.6250000000000000000, 0.6294642857142856984, 0.6339285714285713969, 0.6383928571428570953, 0.6428571428571429047, 0.6473214285714286031, 0.6517857142857143016, 0.6562500000000000000, 0.6607142857142856984, 0.6651785714285713969, 0.6696428571428570953, 0.6741071428571429047, 0.6785714285714286031, 0.6830357142857143016, 0.6875000000000000000, 0.6919642857142856984, 0.6964285714285713969, 0.7008928571428570953, 0.7053571428571429047, 0.7098214285714286031, 0.7142857142857143016, 0.7187500000000000000, 0.7232142857142856984, 0.7276785714285713969, 0.7321428571428570953, 0.7366071428571429047, 0.7410714285714286031, 0.7455357142857143016, 0.7500000000000000000, 0.7544642857142856984, 0.7589285714285713969, 0.7633928571428570953, 0.7678571428571429047, 0.7723214285714286031, 0.7767857142857143016, 0.7812500000000000000, 0.7857142857142856984, 0.7901785714285713969, 0.7946428571428570953, 0.7991071428571429047, 0.8035714285714286031, 0.8080357142857143016, 0.8125000000000000000, 0.8169642857142856984, 0.8214285714285713969, 0.8258928571428570953, 0.8303571428571429047, 0.8348214285714286031, 0.8392857142857143016, 0.8437500000000000000, 0.8482142857142856984, 0.8526785714285713969, 0.8571428571428570953, 0.8616071428571429047, 0.8660714285714286031, 0.8705357142857143016, 0.8750000000000000000, 0.8794642857142856984, 0.8839285714285713969, 0.8883928571428570953, 0.8928571428571429047, 0.8973214285714286031, 0.9017857142857143016, 0.9062500000000000000, 0.9107142857142856984, 0.9151785714285713969, 0.9196428571428570953, 0.9241071428571429047, 0.9285714285714286031, 0.9330357142857143016, 0.9375000000000000000, 0.9419642857142856984, 0.9464285714285713969, 0.9508928571428570953, 0.9553571428571429047, 0.9598214285714286031, 0.9642857142857143016, 0.9687500000000000000, 0.9732142857142856984, 0.9771335416943486285 ),
 .UNSPECIFIED. ) 
 GEOMETRIC_REPRESENTATION_ITEM ( )  RATIONAL_B_SPLINE_SURFACE ( (
 ( 1.000000000000000000, 0.9238795325112867385, 1.000000000000000000, 0.9238795325112867385, 1.000000000000000000, 0.9238795325112867385, 1.000000000000000000, 0.9238795325112867385, 1.000000000000000000, 0.9238795325112867385, 1.000000000000000000, 0.9238795325112867385, 1.000000000000000000, 0.9238795325112867385, 1.000000000000000000, 0.9238795325112867385, 1.000000000000000000, 0.9238795325112867385, 1.000000000000000000, 0.9238795325112867385, 1.000000000000000000, 0.9238795325112867385, 1.000000000000000000, 0.9238795325112867385, 1.000000000000000000, 0.9238795325112867385, 1.000000000000000000, 0.9238795325112867385, 1.000000000000000000, 0.9238795325112867385, 1.000000000000000000, 0.9238795325112867385, 1.000000000000000000, 0.9238795325112867385, 1.000000000000000000, 0.9238795325112867385, 1.000000000000000000, 0.9238795325112867385, 1.000000000000000000, 0.9238795325112867385, 1.000000000000000000, 0.9238795325112867385, 1.000000000000000000, 0.9238795325112867385, 1.000000000000000000, 0.9238795325112867385, 1.000000000000000000, 0.9238795325112867385, 1.000000000000000000, 0.9238795325112867385, 1.000000000000000000, 0.9238795325112867385, 1.000000000000000000, 0.9238795325112867385, 1.000000000000000000, 0.9238795325112867385, 1.000000000000000000, 0.9238795325112867385, 1.000000000000000000, 0.9238795325112867385, 1.000000000000000000, 0.9238795325112867385, 1.000000000000000000, 0.9238795325112867385, 1.000000000000000000, 0.9238795325112867385, 1.000000000000000000, 0.9238795325112867385, 1.000000000000000000, 0.9238795325112867385, 1.000000000000000000, 0.9238795325112867385, 1.000000000000000000, 0.9238795325112867385, 1.000000000000000000, 0.9238795325112867385, 1.000000000000000000, 0.9238795325112867385, 1.000000000000000000, 0.9238795325112867385, 1.000000000000000000, 0.9238795325112867385, 1.000000000000000000, 0.9238795325112867385, 1.000000000000000000, 0.9238795325112867385, 1.000000000000000000, 0.9238795325112867385, 1.000000000000000000, 0.9238795325112867385, 1.000000000000000000, 0.9238795325112867385, 1.000000000000000000, 0.9238795325112867385, 1.000000000000000000, 0.9238795325112867385, 1.000000000000000000, 0.9238795325112867385, 1.000000000000000000, 0.9238795325112867385, 1.000000000000000000, 0.9238795325112867385, 1.000000000000000000, 0.9238795325112867385, 1.000000000000000000, 0.9238795325112867385, 1.000000000000000000, 0.9238795325112867385, 1.000000000000000000, 0.9238795325112867385, 1.000000000000000000, 0.9238795325112867385, 1.000000000000000000, 0.9238795325112867385, 1.000000000000000000, 0.9238795325112867385, 1.000000000000000000, 0.9238795325112867385, 1.000000000000000000, 0.9238795325112867385, 1.000000000000000000, 0.9238795325112867385, 1.000000000000000000, 0.9238795325112867385, 1.000000000000000000, 0.9238795325112867385, 1.000000000000000000, 0.9238795325112867385, 1.000000000000000000, 0.9238795325112867385, 1.000000000000000000, 0.9238795325112867385, 1.000000000000000000, 0.9238795325112867385, 1.000000000000000000, 0.9238795325112867385, 1.000000000000000000, 0.9238795325112867385, 1.000000000000000000, 0.9238795325112867385, 1.000000000000000000, 0.9238795325112867385, 1.000000000000000000, 0.9238795325112867385, 1.000000000000000000, 0.9238795325112867385, 1.000000000000000000, 0.9238795325112867385, 1.000000000000000000, 0.9238795325112867385, 1.000000000000000000, 0.9238795325112867385, 1.000000000000000000, 0.9238795325112867385, 1.000000000000000000, 0.9238795325112867385, 1.000000000000000000, 0.9238795325112867385, 1.000000000000000000, 0.9238795325112867385, 1.000000000000000000, 0.9238795325112867385, 1.000000000000000000, 0.9238795325112867385, 1.000000000000000000, 0.9238795325112867385, 1.000000000000000000, 0.9238795325112867385, 1.000000000000000000, 0.9238795325112867385, 1.000000000000000000, 0.9238795325112867385, 1.000000000000000000, 0.9238795325112867385, 1.000000000000000000, 0.9238795325112867385, 1.000000000000000000, 0.9238795325112867385, 1.000000000000000000, 0.9238795325112867385, 1.000000000000000000, 0.9238795325112867385, 1.000000000000000000, 0.9238795325112867385, 1.000000000000000000, 0.9238795325112867385, 1.000000000000000000, 0.9238795325112867385, 1.000000000000000000, 0.9238795325112867385, 1.000000000000000000, 0.9238795325112867385, 1.000000000000000000, 0.9238795325112867385, 1.000000000000000000, 0.9238795325112867385, 1.000000000000000000, 0.9238795325112867385, 1.000000000000000000, 0.9238795325112867385, 1.000000000000000000, 0.9238795325112867385, 1.000000000000000000, 0.9238795325112867385, 1.000000000000000000, 0.9238795325112867385, 1.000000000000000000, 0.9238795325112867385, 1.000000000000000000, 0.9238795325112867385, 1.000000000000000000, 0.9238795325112867385, 1.000000000000000000, 0.9238795325112867385, 1.000000000000000000, 0.9238795325112867385, 1.000000000000000000, 0.9238795325112867385, 1.000000000000000000, 0.9238795325112867385, 1.000000000000000000, 0.9238795325112867385, 1.000000000000000000, 0.9238795325112867385, 1.000000000000000000, 0.9238795325112867385, 1.000000000000000000, 0.9238795325112867385, 1.000000000000000000, 0.9238795325112867385, 1.000000000000000000, 0.9238795325112867385, 1.000000000000000000, 0.9238795325112867385, 1.000000000000000000, 0.9238795325112867385, 1.000000000000000000, 0.9238795325112867385, 1.000000000000000000, 0.9238795325112867385, 1.000000000000000000, 0.9238795325112867385, 1.000000000000000000, 0.9238795325112867385, 1.000000000000000000, 0.9238795325112867385, 1.000000000000000000, 0.9238795325112867385, 1.000000000000000000, 0.9238795325112867385, 1.000000000000000000, 0.9238795325112867385, 1.000000000000000000, 0.9238795325112867385, 1.000000000000000000, 0.9238795325112867385, 1.000000000000000000, 0.9238795325112867385, 1.000000000000000000, 0.9238795325112867385, 1.000000000000000000, 0.9238795325112867385, 1.000000000000000000, 0.9238795325112867385, 1.000000000000000000, 0.9238795325112867385, 1.000000000000000000, 0.9238795325112867385, 1.000000000000000000, 0.9238795325112867385, 1.000000000000000000, 0.9238795325112867385, 1.000000000000000000, 0.9238795325112867385, 1.000000000000000000, 0.9238795325112867385, 1.000000000000000000, 0.9238795325112867385, 1.000000000000000000, 0.9238795325112867385, 1.000000000000000000, 0.9238795325112867385, 1.000000000000000000, 0.9238795325112867385, 1.000000000000000000, 0.9238795325112867385, 1.000000000000000000, 0.9238795325112867385, 1.000000000000000000, 0.9238795325112867385, 1.000000000000000000, 0.9238795325112867385, 1.000000000000000000, 0.9238795325112867385, 1.000000000000000000, 0.9238795325112867385, 1.000000000000000000, 0.9238795325112867385, 1.000000000000000000, 0.9238795325112867385, 1.000000000000000000, 0.9238795325112867385, 1.000000000000000000, 0.9238795325112867385, 1.000000000000000000, 0.9238795325112867385, 1.000000000000000000, 0.9238795325112867385, 1.000000000000000000, 0.9238795325112867385, 1.000000000000000000, 0.9238795325112867385, 1.000000000000000000, 0.9238795325112867385, 1.000000000000000000, 0.9238795325112867385, 1.000000000000000000, 0.9238795325112867385, 1.000000000000000000, 0.9238795325112867385, 1.000000000000000000, 0.9238795325112867385, 1.000000000000000000, 0.9238795325112867385, 1.000000000000000000, 0.9238795325112867385, 1.000000000000000000, 0.9238795325112867385, 1.000000000000000000, 0.9238795325112867385, 1.000000000000000000, 0.9238795325112867385, 1.000000000000000000, 0.9238795325112867385, 1.000000000000000000, 0.9238795325112867385, 1.000000000000000000, 0.9238795325112867385, 1.000000000000000000, 0.9238795325112867385, 1.000000000000000000, 0.9238795325112867385, 1.000000000000000000, 0.9238795325112867385, 1.000000000000000000, 0.9238795325112867385, 1.000000000000000000, 0.9238795325112867385, 1.000000000000000000, 0.9238795325112867385, 1.000000000000000000, 0.9238795325112867385, 1.000000000000000000, 0.9238795325112867385, 1.000000000000000000, 0.9238795325112867385, 1.000000000000000000, 0.9238795325112867385, 1.000000000000000000, 0.9238795325112867385, 1.000000000000000000, 0.9238795325112867385, 1.000000000000000000, 0.9238795325112867385, 1.000000000000000000, 0.9238795325112867385, 1.000000000000000000, 0.9238795325112867385, 1.000000000000000000, 0.9238795325112867385, 1.000000000000000000, 0.9238795325112867385, 1.000000000000000000, 0.9238795325112867385, 1.000000000000000000, 0.9238795325112867385, 1.000000000000000000, 0.9238795325112867385, 1.000000000000000000, 0.9238795325112867385, 1.000000000000000000, 0.9238795325112867385, 1.000000000000000000, 0.9238795325112867385, 1.000000000000000000, 0.9238795325112867385, 1.000000000000000000, 0.9238795325112867385, 1.000000000000000000, 0.9238795325112867385, 1.000000000000000000, 0.9238795325112867385, 1.000000000000000000, 0.9238795325112867385, 1.000000000000000000, 0.9238795325112867385, 1.000000000000000000, 0.9238795325112867385, 1.000000000000000000, 0.9238795325112867385, 1.000000000000000000, 0.9238795325112867385, 1.000000000000000000, 0.9238795325112867385, 1.000000000000000000, 0.9238795325112867385, 1.000000000000000000, 0.9238795325112867385, 1.000000000000000000, 0.9238795325112867385, 1.000000000000000000, 0.9238795325112867385, 1.000000000000000000, 0.9238795325112867385, 1.000000000000000000, 0.9238795325112867385, 1.000000000000000000, 0.9238795325112867385, 1.000000000000000000, 0.9238795325112867385, 1.000000000000000000, 0.9238795325112867385, 1.000000000000000000, 0.9238795325112867385, 1.000000000000000000, 0.9238795325112867385, 1.000000000000000000, 0.9238795325112867385, 1.000000000000000000, 0.9238795325112867385, 1.000000000000000000, 0.9238795325112867385, 1.000000000000000000, 0.9238795325112867385, 1.000000000000000000, 0.9238795325112867385, 1.000000000000000000, 0.9331728261800869006, 0.9836825870399050764),
 ( 1.000000000000000000, 0.9238795325112867385, 1.000000000000000000, 0.9238795325112867385, 1.000000000000000000, 0.9238795325112867385, 1.000000000000000000, 0.9238795325112867385, 1.000000000000000000, 0.9238795325112867385, 1.000000000000000000, 0.9238795325112867385, 1.000000000000000000, 0.9238795325112867385, 1.000000000000000000, 0.9238795325112867385, 1.000000000000000000, 0.9238795325112867385, 1.000000000000000000, 0.9238795325112867385, 1.000000000000000000, 0.9238795325112867385, 1.000000000000000000, 0.9238795325112867385, 1.000000000000000000, 0.9238795325112867385, 1.000000000000000000, 0.9238795325112867385, 1.000000000000000000, 0.9238795325112867385, 1.000000000000000000, 0.9238795325112867385, 1.000000000000000000, 0.9238795325112867385, 1.000000000000000000, 0.9238795325112867385, 1.000000000000000000, 0.9238795325112867385, 1.000000000000000000, 0.9238795325112867385, 1.000000000000000000, 0.9238795325112867385, 1.000000000000000000, 0.9238795325112867385, 1.000000000000000000, 0.9238795325112867385, 1.000000000000000000, 0.9238795325112867385, 1.000000000000000000, 0.9238795325112867385, 1.000000000000000000, 0.9238795325112867385, 1.000000000000000000, 0.9238795325112867385, 1.000000000000000000, 0.9238795325112867385, 1.000000000000000000, 0.9238795325112867385, 1.000000000000000000, 0.9238795325112867385, 1.000000000000000000, 0.9238795325112867385, 1.000000000000000000, 0.9238795325112867385, 1.000000000000000000, 0.9238795325112867385, 1.000000000000000000, 0.9238795325112867385, 1.000000000000000000, 0.9238795325112867385, 1.000000000000000000, 0.9238795325112867385, 1.000000000000000000, 0.9238795325112867385, 1.000000000000000000, 0.9238795325112867385, 1.000000000000000000, 0.9238795325112867385, 1.000000000000000000, 0.9238795325112867385, 1.000000000000000000, 0.9238795325112867385, 1.000000000000000000, 0.9238795325112867385, 1.000000000000000000, 0.9238795325112867385, 1.000000000000000000, 0.9238795325112867385, 1.000000000000000000, 0.9238795325112867385, 1.000000000000000000, 0.9238795325112867385, 1.000000000000000000, 0.9238795325112867385, 1.000000000000000000, 0.9238795325112867385, 1.000000000000000000, 0.9238795325112867385, 1.000000000000000000, 0.9238795325112867385, 1.000000000000000000, 0.9238795325112867385, 1.000000000000000000, 0.9238795325112867385, 1.000000000000000000, 0.9238795325112867385, 1.000000000000000000, 0.9238795325112867385, 1.000000000000000000, 0.9238795325112867385, 1.000000000000000000, 0.9238795325112867385, 1.000000000000000000, 0.9238795325112867385, 1.000000000000000000, 0.9238795325112867385, 1.000000000000000000, 0.9238795325112867385, 1.000000000000000000, 0.9238795325112867385, 1.000000000000000000, 0.9238795325112867385, 1.000000000000000000, 0.9238795325112867385, 1.000000000000000000, 0.9238795325112867385, 1.000000000000000000, 0.9238795325112867385, 1.000000000000000000, 0.9238795325112867385, 1.000000000000000000, 0.9238795325112867385, 1.000000000000000000, 0.9238795325112867385, 1.000000000000000000, 0.9238795325112867385, 1.000000000000000000, 0.9238795325112867385, 1.000000000000000000, 0.9238795325112867385, 1.000000000000000000, 0.9238795325112867385, 1.000000000000000000, 0.9238795325112867385, 1.000000000000000000, 0.9238795325112867385, 1.000000000000000000, 0.9238795325112867385, 1.000000000000000000, 0.9238795325112867385, 1.000000000000000000, 0.9238795325112867385, 1.000000000000000000, 0.9238795325112867385, 1.000000000000000000, 0.9238795325112867385, 1.000000000000000000, 0.9238795325112867385, 1.000000000000000000, 0.9238795325112867385, 1.000000000000000000, 0.9238795325112867385, 1.000000000000000000, 0.9238795325112867385, 1.000000000000000000, 0.9238795325112867385, 1.000000000000000000, 0.9238795325112867385, 1.000000000000000000, 0.9238795325112867385, 1.000000000000000000, 0.9238795325112867385, 1.000000000000000000, 0.9238795325112867385, 1.000000000000000000, 0.9238795325112867385, 1.000000000000000000, 0.9238795325112867385, 1.000000000000000000, 0.9238795325112867385, 1.000000000000000000, 0.9238795325112867385, 1.000000000000000000, 0.9238795325112867385, 1.000000000000000000, 0.9238795325112867385, 1.000000000000000000, 0.9238795325112867385, 1.000000000000000000, 0.9238795325112867385, 1.000000000000000000, 0.9238795325112867385, 1.000000000000000000, 0.9238795325112867385, 1.000000000000000000, 0.9238795325112867385, 1.000000000000000000, 0.9238795325112867385, 1.000000000000000000, 0.9238795325112867385, 1.000000000000000000, 0.9238795325112867385, 1.000000000000000000, 0.9238795325112867385, 1.000000000000000000, 0.9238795325112867385, 1.000000000000000000, 0.9238795325112867385, 1.000000000000000000, 0.9238795325112867385, 1.000000000000000000, 0.9238795325112867385, 1.000000000000000000, 0.9238795325112867385, 1.000000000000000000, 0.9238795325112867385, 1.000000000000000000, 0.9238795325112867385, 1.000000000000000000, 0.9238795325112867385, 1.000000000000000000, 0.9238795325112867385, 1.000000000000000000, 0.9238795325112867385, 1.000000000000000000, 0.9238795325112867385, 1.000000000000000000, 0.9238795325112867385, 1.000000000000000000, 0.9238795325112867385, 1.000000000000000000, 0.9238795325112867385, 1.000000000000000000, 0.9238795325112867385, 1.000000000000000000, 0.9238795325112867385, 1.000000000000000000, 0.9238795325112867385, 1.000000000000000000, 0.9238795325112867385, 1.000000000000000000, 0.9238795325112867385, 1.000000000000000000, 0.9238795325112867385, 1.000000000000000000, 0.9238795325112867385, 1.000000000000000000, 0.9238795325112867385, 1.000000000000000000, 0.9238795325112867385, 1.000000000000000000, 0.9238795325112867385, 1.000000000000000000, 0.9238795325112867385, 1.000000000000000000, 0.9238795325112867385, 1.000000000000000000, 0.9238795325112867385, 1.000000000000000000, 0.9238795325112867385, 1.000000000000000000, 0.9238795325112867385, 1.000000000000000000, 0.9238795325112867385, 1.000000000000000000, 0.9238795325112867385, 1.000000000000000000, 0.9238795325112867385, 1.000000000000000000, 0.9238795325112867385, 1.000000000000000000, 0.9238795325112867385, 1.000000000000000000, 0.9238795325112867385, 1.000000000000000000, 0.9238795325112867385, 1.000000000000000000, 0.9238795325112867385, 1.000000000000000000, 0.9238795325112867385, 1.000000000000000000, 0.9238795325112867385, 1.000000000000000000, 0.9238795325112867385, 1.000000000000000000, 0.9238795325112867385, 1.000000000000000000, 0.9238795325112867385, 1.000000000000000000, 0.9238795325112867385, 1.000000000000000000, 0.9238795325112867385, 1.000000000000000000, 0.9238795325112867385, 1.000000000000000000, 0.9238795325112867385, 1.000000000000000000, 0.9238795325112867385, 1.000000000000000000, 0.9238795325112867385, 1.000000000000000000, 0.9238795325112867385, 1.000000000000000000, 0.9238795325112867385, 1.000000000000000000, 0.9238795325112867385, 1.000000000000000000, 0.9238795325112867385, 1.000000000000000000, 0.9238795325112867385, 1.000000000000000000, 0.9238795325112867385, 1.000000000000000000, 0.9238795325112867385, 1.000000000000000000, 0.9238795325112867385, 1.000000000000000000, 0.9238795325112867385, 1.000000000000000000, 0.9238795325112867385, 1.000000000000000000, 0.9238795325112867385, 1.000000000000000000, 0.9238795325112867385, 1.000000000000000000, 0.9238795325112867385, 1.000000000000000000, 0.9238795325112867385, 1.000000000000000000, 0.9238795325112867385, 1.000000000000000000, 0.9238795325112867385, 1.000000000000000000, 0.9238795325112867385, 1.000000000000000000, 0.9238795325112867385, 1.000000000000000000, 0.9238795325112867385, 1.000000000000000000, 0.9238795325112867385, 1.000000000000000000, 0.9238795325112867385, 1.000000000000000000, 0.9238795325112867385, 1.000000000000000000, 0.9238795325112867385, 1.000000000000000000, 0.9238795325112867385, 1.000000000000000000, 0.9238795325112867385, 1.000000000000000000, 0.9238795325112867385, 1.000000000000000000, 0.9238795325112867385, 1.000000000000000000, 0.9238795325112867385, 1.000000000000000000, 0.9238795325112867385, 1.000000000000000000, 0.9238795325112867385, 1.000000000000000000, 0.9238795325112867385, 1.000000000000000000, 0.9238795325112867385, 1.000000000000000000, 0.9238795325112867385, 1.000000000000000000, 0.9238795325112867385, 1.000000000000000000, 0.9238795325112867385, 1.000000000000000000, 0.9238795325112867385, 1.000000000000000000, 0.9238795325112867385, 1.000000000000000000, 0.9238795325112867385, 1.000000000000000000, 0.9238795325112867385, 1.000000000000000000, 0.9238795325112867385, 1.000000000000000000, 0.9238795325112867385, 1.000000000000000000, 0.9238795325112867385, 1.000000000000000000, 0.9238795325112867385, 1.000000000000000000, 0.9238795325112867385, 1.000000000000000000, 0.9238795325112867385, 1.000000000000000000, 0.9238795325112867385, 1.000000000000000000, 0.9238795325112867385, 1.000000000000000000, 0.9238795325112867385, 1.000000000000000000, 0.9238795325112867385, 1.000000000000000000, 0.9238795325112867385, 1.000000000000000000, 0.9238795325112867385, 1.000000000000000000, 0.9238795325112867385, 1.000000000000000000, 0.9238795325112867385, 1.000000000000000000, 0.9238795325112867385, 1.000000000000000000, 0.9238795325112867385, 1.000000000000000000, 0.9238795325112867385, 1.000000000000000000, 0.9238795325112867385, 1.000000000000000000, 0.9238795325112867385, 1.000000000000000000, 0.9238795325112867385, 1.000000000000000000, 0.9238795325112867385, 1.000000000000000000, 0.9238795325112867385, 1.000000000000000000, 0.9238795325112867385, 1.000000000000000000, 0.9238795325112867385, 1.000000000000000000, 0.9238795325112867385, 1.000000000000000000, 0.9238795325112867385, 1.000000000000000000, 0.9238795325112867385, 1.000000000000000000, 0.9238795325112867385, 1.000000000000000000, 0.9238795325112867385, 1.000000000000000000, 0.9331728261800869006, 0.9836825870399050764) ) ) 
 REPRESENTATION_ITEM ( '' )  SURFACE ( )  );
#16473=CARTESIAN_POINT ( 'NONE',  ( 0.1167790944451423257, 0.6013888888130223265, -0.2819296736111110424 ) ) ;
#16474=CARTESIAN_POINT ( 'NONE',  ( 0.1167790944451424368, 3.828555555631421470, 0.2819296736111110424 ) ) ;
#16476=CARTESIAN_POINT ( 'NONE',  ( -0.2819296736111110424, 4.536888888964754507, 0.1167790944451424923 ) ) ;
#16479=CARTESIAN_POINT ( 'NONE',  ( -0.2206173157302028232, 4.599388888888888083, -0.2206173157302028232 ) ) ;
#16484=CARTESIAN_POINT ( 'NONE',  ( -1.910449006669871087E-17, 3.710500000151732092, -0.3119999999999999996 ) ) ;
#16485=CARTESIAN_POINT ( 'NONE',  ( 0.3110561587738748246, 4.195609504020111125, 0.03575875776001819634 ) ) ;
#16487=CARTESIAN_POINT ( 'NONE',  ( -5.731347020009612645E-17, 0.5041666666666663188, 0.3119999999999999996 ) ) ;
#16489=CARTESIAN_POINT ( 'NONE',  ( -0.2819296736111110979, 4.630638888964754507, 0.000000000000000000 ) ) ;
#16491=VECTOR ( 'NONE', #21227, 39.37007874015748143 ) ;
#16492=CARTESIAN_POINT ( 'NONE',  ( -0.1292346314604068958, 4.762583333333332725, -0.3119999999999987228 ) ) ;
#16494=CARTESIAN_POINT ( 'NONE',  ( -0.1993543840281266633, 0.2368055554796889006, -0.1993543840281266910 ) ) ;
#16495=ORIENTED_EDGE ( 'NONE', *, *, #4185, .F. ) ;
#16496=CARTESIAN_POINT ( 'NONE',  ( -0.2819296736111110979, 0.1326388888130222710, -3.452642723725051716E-17 ) ) ;
#16497=CARTESIAN_POINT ( 'NONE',  ( -0.2549684922721914271, 5.198137420699272759, -0.1298580064688831803 ) ) ;
#16502=CARTESIAN_POINT ( 'NONE',  ( -0.2685268980859171206, 3.886276269974404229, -0.1597531070831219036 ) ) ;
#16503=CARTESIAN_POINT ( 'NONE',  ( -0.2819296736111110979, 0.06666666659080003332, 0.1167790944451422425 ) ) ;
#16504=CARTESIAN_POINT ( 'NONE',  ( 0.1167790944451422702, 4.460500000075867000, -0.2819296736111110424 ) ) ;
#16507=CARTESIAN_POINT ( 'NONE',  ( 0.2819296736111110424, 5.009111111186976828, -0.1167790944451423396 ) ) ;
#16509=CARTESIAN_POINT ( 'NONE',  ( 0.3027533619087663386, 3.750030080416155265, 0.07586331988550912286 ) ) ;
#16512=CARTESIAN_POINT ( 'NONE',  ( 0.3119999999999999996, 4.359805555707287894, 0.1292346314604056190 ) ) ;
#16514=CARTESIAN_POINT ( 'NONE',  ( -0.1993543840281266355, 4.540361111186976828, 0.1993543840281267465 ) ) ;
#16515=CARTESIAN_POINT ( 'NONE',  ( -0.2819296736111110424, 3.738277777853643347, -0.1167790944451423119 ) ) ;
#16522=DIRECTION ( 'NONE',  ( 0.000000000000000000, 0.000000000000000000, 1.000000000000000000 ) ) ;
#16524=CARTESIAN_POINT ( 'NONE',  ( -0.2206173157302028787, 0.3236111109593782231, 0.2206173157302027954 ) ) ;
#16526=CARTESIAN_POINT ( 'NONE',  ( -0.1852720301558682114, 3.732674766298908597, 0.2552238848127614257 ) ) ;
#16527=VECTOR ( 'NONE', #20936, 39.37007874015748143 ) ;
#16533=CARTESIAN_POINT ( 'NONE',  ( 0.2882303765580553900, 5.089197615778912720, -0.1187411923064577435 ) ) ;
#16535=CARTESIAN_POINT ( 'NONE',  ( -1.726321361862525858E-17, 4.172305555631420582, -0.2819296736111110979 ) ) ;
#16536=CARTESIAN_POINT ( 'NONE',  ( -0.2819296736111110979, 5.182722222298087544, -0.1167790944451422980 ) ) ;
#16537=LINE ( 'NONE', #20072, #11814 ) ;
#16538=CARTESIAN_POINT ( 'NONE',  ( -0.05810125945330829600, 4.236650434042510405, 0.3066015745271455373 ) ) ;
#16540=CARTESIAN_POINT ( 'NONE',  ( -1.910449006669871087E-17, 4.092444444444444329, -0.3119999999999999996 ) ) ;
#16541=CARTESIAN_POINT ( 'NONE',  ( -0.2206173157302027676, 4.898000000151732536, 0.2206173157302028787 ) ) ;
#16542=CARTESIAN_POINT ( 'NONE',  ( -0.2819296736111110979, 5.196611111186976828, -0.1167790944451422980 ) ) ;
#16548=CARTESIAN_POINT ( 'NONE',  ( 5.178964085587577574E-17, 5.088972222298087544, 0.2819296736111110979 ) ) ;
#16553=CARTESIAN_POINT ( 'NONE',  ( 0.1167790944451423535, 0.3722222221463555858, 0.2819296736111110979 ) ) ;
#16555=CARTESIAN_POINT ( 'NONE',  ( 0.2819296736111110979, 4.950083333409199149, -3.452642723725051716E-17 ) ) ;
#16556=CARTESIAN_POINT ( 'NONE',  ( 0.3052904481388406532, 4.472585030868217792, 0.06436050040701235542 ) ) ;
#16559=CARTESIAN_POINT ( 'NONE',  ( -0.1993543840281266910, 4.790361111186976828, -0.1993543840281266910 ) ) ;
#16560=CARTESIAN_POINT ( 'NONE',  ( -0.1914713219046094150, 4.160640935953036745, -0.2497021521199800087 ) ) ;
#16564=CARTESIAN_POINT ( 'NONE',  ( -0.3119999999999999996, 4.769527777777776478, -0.1292346314604056468 ) ) ;
#16565=CARTESIAN_POINT ( 'NONE',  ( 0.2819296736111111534, 4.043833333409200037, 0.1167790944451422563 ) ) ;
#16567=CARTESIAN_POINT ( 'NONE',  ( 0.1864095630950551863, 4.021751787035609205, 0.2501916434414996893 ) ) ;
#16571=VERTEX_POINT ( 'NONE', #19828 ) ;
#16578=CARTESIAN_POINT ( 'NONE',  ( -0.2726262432888192366, 4.442052030412000363, -0.1571209434472312649 ) ) ;
#16581=CARTESIAN_POINT ( 'NONE',  ( -5.178964085587577574E-17, 0.1881944443685778512, 0.2819296736111110979 ) ) ;
#16583=CARTESIAN_POINT ( 'NONE',  ( 0.3119999999999998885, 0.5701388888888886397, 0.1292346314604058410 ) ) ;
#16588=VERTEX_POINT ( 'NONE', #18122 ) ;
#16589=CARTESIAN_POINT ( 'NONE',  ( -0.3103325563594151459, 5.105850683298335468, 0.01916239243782727822 ) ) ;
#16591=CARTESIAN_POINT ( 'NONE',  ( -0.2206173157302027954, -0.01666666666666700297, -0.2206173157302028232 ) ) ;
#16592=CARTESIAN_POINT ( 'NONE',  ( -0.1167790944451423257, 3.745222222298088433, -0.2819296736111110424 ) ) ;
#16595=ADVANCED_FACE ( 'NONE', ( #8848 ), #1053, .T. ) ;
#16596=CARTESIAN_POINT ( 'NONE',  ( 0.1167790944451424368, 4.384111111186976828, 0.2819296736111110424 ) ) ;
#16597=CARTESIAN_POINT ( 'NONE',  ( 0.2206173157302027954, 4.974388888888888083, -0.2206173157302028232 ) ) ;
#16600=CARTESIAN_POINT ( 'NONE',  ( 0.2595622703492775907, 4.358042815605328357, 0.1731226536284558581 ) ) ;
#16601=CARTESIAN_POINT ( 'NONE',  ( -0.2819296736111110979, 4.852861111186976828, 0.000000000000000000 ) ) ;
#16605=CARTESIAN_POINT ( 'NONE',  ( 5.731347020009612645E-17, 5.009111111111110404, 0.3119999999999999996 ) ) ;
#16606=CARTESIAN_POINT ( 'NONE',  ( 0.1167790944451422702, 4.779944444520308977, -0.2819296736111110979 ) ) ;
#16609=( BOUNDED_CURVE ( )  B_SPLINE_CURVE ( 2, ( #11562, #11679, #18989, #2408, #2288, #9848, #22645, #5697, #327 ),
 .UNSPECIFIED., .F., .F. ) 
 B_SPLINE_CURVE_WITH_KNOTS ( ( 3, 2, 2, 2, 3 ),
 ( 0.8482142857142856984, 0.8526785714285713969, 0.8571428571428569843, 0.8616071428571427937, 0.8660714285714284921 ),
 .UNSPECIFIED. ) 
 CURVE ( )  GEOMETRIC_REPRESENTATION_ITEM ( )  RATIONAL_B_SPLINE_CURVE ( ( 1.000000000000000000, 0.9238795325112867385, 1.000000000000000000, 0.9238795325112867385, 1.000000000000000000, 0.9238795325112867385, 1.000000000000000000, 0.9238795325112886259, 0.9999999999999981126 ) ) 
 REPRESENTATION_ITEM ( '' )  );
#16610=CARTESIAN_POINT ( 'NONE',  ( 0.1167790944451423535, 0.4277777777019111105, 0.2819296736111110424 ) ) ;
#16612=ORIENTED_EDGE ( 'NONE', *, *, #22778, .T. ) ;
#16613=VERTEX_POINT ( 'NONE', #17759 ) ;
#16614=CARTESIAN_POINT ( 'NONE',  ( 0.2819296736111110979, 0.1604166665908000333, 0.000000000000000000 ) ) ;
#16616=CARTESIAN_POINT ( 'NONE',  ( -0.2778555843174162487, 5.199876218914782910, -0.06507818477629406795 ) ) ;
#16620=CARTESIAN_POINT ( 'NONE',  ( -0.2567736115681932274, 3.885679132990351281, -0.1772326254732079776 ) ) ;
#16622=CARTESIAN_POINT ( 'NONE',  ( -1.726321361862525858E-17, 4.463972222298087544, -0.2819296736111110979 ) ) ;
#16625=CARTESIAN_POINT ( 'NONE',  ( 0.1562950836073939143, 4.539213769334139670, -0.2717496176494637594 ) ) ;
#16627=CARTESIAN_POINT ( 'NONE',  ( -1.726321361862525858E-17, 5.075083333409198261, -0.2819296736111110979 ) ) ;
#16628=CARTESIAN_POINT ( 'NONE',  ( 0.1167790944451424506, 4.370222222298088433, 0.2819296736111110424 ) ) ;
#16629=CARTESIAN_POINT ( 'NONE',  ( 0.2151400685697778814, 3.744996934445992132, 0.2277764084372883857 ) ) ;
#16630=CARTESIAN_POINT ( 'NONE',  ( 3.820898013339742174E-17, 5.384999999999999787, 0.3119999999999999996 ) ) ;
#16633=CARTESIAN_POINT ( 'NONE',  ( 0.1292346314604058410, 4.130638889040620931, 0.3119999999999998885 ) ) ;
#16634=CARTESIAN_POINT ( 'NONE',  ( 0.2819296736111110979, 4.453555555631421470, -0.1167790944451423396 ) ) ;
#16635=CARTESIAN_POINT ( 'NONE',  ( 0.1167790944451422702, 3.946611111186976384, -0.2819296736111110424 ) ) ;
#16639=CARTESIAN_POINT ( 'NONE',  ( -0.3119999999999999996, 4.269527777777776478, -0.1292346314604056468 ) ) ;
#16644=CARTESIAN_POINT ( 'NONE',  ( 0.1292346314604056745, 0.5215277776260448528, -0.3119999999999999996 ) ) ;
#16648=CARTESIAN_POINT ( 'NONE',  ( 0.01934516033330287155, 5.167810441017906875, 0.2967713041391435991 ) ) ;
#16654=CARTESIAN_POINT ( 'NONE',  ( -0.1167790944451423535, 4.196611111186976828, 0.2819296736111110424 ) ) ;
#16655=CARTESIAN_POINT ( 'NONE',  ( 0.1993543840281267465, 5.151472222298087544, 0.1993543840281266633 ) ) ;
#16658=CARTESIAN_POINT ( 'NONE',  ( 0.1292346314604058410, 3.845916666666666206, 0.3119999999999998885 ) ) ;
#16659=CARTESIAN_POINT ( 'NONE',  ( -0.2206173157302027676, 5.009111111262843252, 0.2206173157302028787 ) ) ;
#16660=CARTESIAN_POINT ( 'NONE',  ( -0.1993543840281266910, 5.193138888964755395, -0.1993543840281266910 ) ) ;
#16664=CARTESIAN_POINT ( 'NONE',  ( 0.2043171450904766873, 0.03871863473645468373, -0.2036093692351375051 ) ) ;
#16667=CARTESIAN_POINT ( 'NONE',  ( -0.1167790944451423535, 5.196611111186976828, 0.2819296736111110424 ) ) ;
#16668=VERTEX_POINT ( 'NONE', #3846 ) ;
#16672=CARTESIAN_POINT ( 'NONE',  ( -0.2819296736111110979, 0.2402777777019112215, -0.1167790944451423396 ) ) ;
#16675=CARTESIAN_POINT ( 'NONE',  ( 0.2819296736111110979, 5.005638888964754507, -3.452642723725051716E-17 ) ) ;
#16676=CARTESIAN_POINT ( 'NONE',  ( 0.03527991335344082824, 4.487285812805300367, -0.3100400492211025094 ) ) ;
#16677=ORIENTED_EDGE ( 'NONE', *, *, #8493, .T. ) ;
#16679=CARTESIAN_POINT ( 'NONE',  ( -0.1167790944451423535, 4.974388888964754507, 0.2819296736111110424 ) ) ;
#16681=CARTESIAN_POINT ( 'NONE',  ( -0.009623778223146972621, 4.266321329850166322, -0.3120828329435257342 ) ) ;
#16682=DIRECTION ( 'NONE',  ( 0.000000000000000000, 0.000000000000000000, 1.000000000000000000 ) ) ;
#16685=CARTESIAN_POINT ( 'NONE',  ( -0.1292346314604057023, 4.394527777777777366, 0.3119999999999998885 ) ) ;
#16686=CARTESIAN_POINT ( 'NONE',  ( 0.1993543840281267465, 4.040361111186976828, 0.1993543840281266633 ) ) ;
#16688=CARTESIAN_POINT ( 'NONE',  ( 0.2994861972273289985, 4.032443608799596291, -0.08761480198954196830 ) ) ;
#16689=CARTESIAN_POINT ( 'NONE',  ( 0.2206173157302027676, 0.5041666665149336923, 0.2206173157302028787 ) ) ;
#16690=ORIENTED_EDGE ( 'NONE', *, *, #15494, .F. ) ;
#16693=LINE ( 'NONE', #6068, #11962 ) ;
#16696=CARTESIAN_POINT ( 'NONE',  ( -0.2494838521722312075, 4.452466089143981343, 0.1917547050432406863 ) ) ;
#16700=CARTESIAN_POINT ( 'NONE',  ( 0.1167790944451423257, 0.3236111110352444808, -0.2819296736111110424 ) ) ;
#16701=CARTESIAN_POINT ( 'NONE',  ( 0.001115507632757668918, 3.877136689224211175, -0.3119982913588789653 ) ) ;
#16702=FACE_OUTER_BOUND ( 'NONE', #12934, .T. ) ;
#16703=CARTESIAN_POINT ( 'NONE',  ( 5.731347020009612645E-17, 3.842444444444443441, 0.3119999999999999996 ) ) ;
#16706=ORIENTED_EDGE ( 'NONE', *, *, #24084, .F. ) ;
#16707=CARTESIAN_POINT ( 'NONE',  ( -0.2122204171184600696, 5.098494865722095426, -0.2275089404706317764 ) ) ;
#16709=CARTESIAN_POINT ( 'NONE',  ( -0.1292346314604058410, 0.05624999999999965444, 0.3119999999999998885 ) ) ;
#16710=CARTESIAN_POINT ( 'NONE',  ( 0.3119999999999999996, 5.082027777777776478, -0.1292346314604056745 ) ) ;
#16713=CARTESIAN_POINT ( 'NONE',  ( -0.1993543840281266910, 4.526472222298087544, -0.1993543840281266910 ) ) ;
#16715=CARTESIAN_POINT ( 'NONE',  ( -0.2206173157302027676, 4.391055555555555046, 0.2206173157302028787 ) ) ;
#16718=CARTESIAN_POINT ( 'NONE',  ( 0.2695900040198371261, 4.368010068071540353, -0.1590464363266536896 ) ) ;
#16719=CARTESIAN_POINT ( 'NONE',  ( -0.2819296736111110979, 5.019527777853642903, 0.000000000000000000 ) ) ;
#16720=CARTESIAN_POINT ( 'NONE',  ( -0.2990480016229275506, 5.156380186802008936, 0.03674222046541380376 ) ) ;
#16724=CARTESIAN_POINT ( 'NONE',  ( 0.2819296736111110979, 4.606333333409200037, -0.1167790944451423396 ) ) ;
#16728=CARTESIAN_POINT ( 'NONE',  ( 0.1167790944451423257, 0.5597222221463556968, -0.2819296736111110424 ) ) ;
#16731=CARTESIAN_POINT ( 'NONE',  ( 0.2819296736111110424, 0.2680555554796889561, 0.1167790944451424923 ) ) ;
#16732=CARTESIAN_POINT ( 'NONE',  ( -0.03785093491744839778, 4.711555345668029027, -0.3099667384353548827 ) ) ;
#16736=CARTESIAN_POINT ( 'NONE',  ( -0.3109939306932527070, 3.891914723735419912, 0.03129033405693151804 ) ) ;
#16737=CARTESIAN_POINT ( 'NONE',  ( -0.1167790944451422702, 0.1638888888130222432, -0.2819296736111110979 ) ) ;
#16739=CARTESIAN_POINT ( 'NONE',  ( 5.178964085587577574E-17, 4.602861111186976828, 0.2819296736111110979 ) ) ;
#16743=CARTESIAN_POINT ( 'NONE',  ( -0.1993543840281266910, 5.026472222298088433, -0.1993543840281266910 ) ) ;
#16744=CARTESIAN_POINT ( 'NONE',  ( -0.2819296736111110424, 4.356333333409198261, 0.1167790944451424923 ) ) ;
#16745=CARTESIAN_POINT ( 'NONE',  ( 1.519200945994765378E-06, 3.766055514889470324, -0.3119999999963013471 ) ) ;
#16749=CARTESIAN_POINT ( 'NONE',  ( 5.731347020009612645E-17, 4.182722222373953969, 0.3119999999999999996 ) ) ;
#16750=CARTESIAN_POINT ( 'NONE',  ( 0.2819296736111111534, 4.446611111186976828, 0.1167790944451422563 ) ) ;
#16756=EDGE_CURVE ( 'NONE', #23659, #23361, #16537, .T. ) ;
#16758=CARTESIAN_POINT ( 'NONE',  ( -0.1158813573290139315, 4.846026232838027248, 0.2897518779968182856 ) ) ;
#16760=EDGE_LOOP ( 'NONE', ( #8199, #16360, #15944, #20488, #20327 ) ) ;
#16761=CARTESIAN_POINT ( 'NONE',  ( -0.1292346314604056190, 0.4173611109593781676, -0.3119999999999999996 ) ) ;
#16763=DIRECTION ( 'NONE',  ( 0.000000000000000000, 0.000000000000000000, -1.000000000000000000 ) ) ;
#16764=CARTESIAN_POINT ( 'NONE',  ( -0.2005194665486881855, 3.716698251689450672, -0.2390317579944993553 ) ) ;
#16766=CARTESIAN_POINT ( 'NONE',  ( -5.731347020009612645E-17, 0.5041666666666663188, 0.3119999999999999996 ) ) ;
#16767=VERTEX_POINT ( 'NONE', #5551 ) ;
#16771=CARTESIAN_POINT ( 'NONE',  ( 0.2819296736111110424, 4.328555555631420582, -0.1167790944451423396 ) ) ;
#16772=CARTESIAN_POINT ( 'NONE',  ( 0.1167790944451422702, 5.168833333409199149, -0.2819296736111110979 ) ) ;
#16775=CARTESIAN_POINT ( 'NONE',  ( 0.2206173157302028787, 3.904944444444443885, 0.2206173157302027954 ) ) ;
#16776=CARTESIAN_POINT ( 'NONE',  ( 5.731347020009612645E-17, 4.849388889040620931, 0.3119999999999999996 ) ) ;
#16777=CARTESIAN_POINT ( 'NONE',  ( -1.726321361862525858E-17, 5.186194444520309865, -0.2819296736111110979 ) ) ;
#16778=( BOUNDED_CURVE ( )  B_SPLINE_CURVE ( 2, ( #3649, #5110, #20242, #16583, #16344, #23875, #3531, #24121, #9261 ),
 .UNSPECIFIED., .F., .T. ) 
 B_SPLINE_CURVE_WITH_KNOTS ( ( 3, 2, 2, 2, 3 ),
 ( 0.8958333333333333703, 0.9062500000000000000, 0.9166666666666666297, 0.9270833333333333703, 0.9375000000000000000 ),
 .UNSPECIFIED. ) 
 CURVE ( )  GEOMETRIC_REPRESENTATION_ITEM ( )  RATIONAL_B_SPLINE_CURVE ( ( 1.000000000000000000, 0.9238795325112867385, 1.000000000000000000, 0.9238795325112867385, 1.000000000000000000, 0.9238795325112867385, 1.000000000000000000, 0.9238795325112867385, 1.000000000000000000 ) ) 
 REPRESENTATION_ITEM ( '' )  );
#16779=AXIS2_PLACEMENT_3D ( 'NONE', #17419, #7901, #4250 ) ;
#16784=CARTESIAN_POINT ( 'NONE',  ( 0.3119999999999999996, 0.4104166666666663188, -0.1292346314604056468 ) ) ;
#16787=CARTESIAN_POINT ( 'NONE',  ( 0.2658661084243346684, 0.03242967361111057795, 0.09380593400082704036 ) ) ;
#16791=CARTESIAN_POINT ( 'NONE',  ( 5.178964085587577574E-17, 5.200083333409199149, 0.2819296736111110979 ) ) ;
#16792=CARTESIAN_POINT ( 'NONE',  ( 0.2819296736111111534, 3.779944444520309865, 0.1167790944451422563 ) ) ;
#16798=CARTESIAN_POINT ( 'NONE',  ( -0.1993543840281266633, 0.3479166665908000056, -0.1993543840281266910 ) ) ;
#16800=CARTESIAN_POINT ( 'NONE',  ( -0.2819296736111110424, 5.029944444520310753, -0.1167790944451423119 ) ) ;
#16803=CARTESIAN_POINT ( 'NONE',  ( -0.2819296736111110424, 4.849388888964755395, -0.1167790944451423119 ) ) ;
#16804=DIRECTION ( 'NONE',  ( 0.000000000000000000, 0.000000000000000000, -1.000000000000000000 ) ) ;
#16808=CARTESIAN_POINT ( 'NONE',  ( 0.2206173157302027954, 4.585499999999999687, -0.2206173157302028232 ) ) ;
#16809=CARTESIAN_POINT ( 'NONE',  ( 5.178964085587577574E-17, 3.866750000075865668, 0.2819296736111110979 ) ) ;
#16811=CARTESIAN_POINT ( 'NONE',  ( 0.1888842787674890333, 4.021839019550402128, 0.2483332517396733830 ) ) ;
#16812=CARTESIAN_POINT ( 'NONE',  ( 2.570936052289255124E-07, 3.738287934957344127, 0.3119999999997750129 ) ) ;
#16815=CARTESIAN_POINT ( 'NONE',  ( -0.07559737730188846594, 4.101573950995675233, -0.3050544060259108292 ) ) ;
#16818=CARTESIAN_POINT ( 'NONE',  ( 0.3018713704988151836, 4.638800393405135836, 0.08078439495390804526 ) ) ;
#16825=CARTESIAN_POINT ( 'NONE',  ( -0.1167790944451424368, 0.2958333332574667462, 0.2819296736111110424 ) ) ;
#16826=CARTESIAN_POINT ( 'NONE',  ( 0.3119994934711425860, 3.862180426189363303, 0.04084270294850755878 ) ) ;
#16831=CARTESIAN_POINT ( 'NONE',  ( -0.3119999999999999996, 4.717444444444443441, 0.000000000000000000 ) ) ;
#16832=CARTESIAN_POINT ( 'NONE',  ( -0.2206173157302027954, 0.09444444444444409503, -0.2206173157302028232 ) ) ;
#16833=CARTESIAN_POINT ( 'NONE',  ( 5.731347020009612645E-17, 5.175777777777777366, 0.3119999999999999996 ) ) ;
#16835=CARTESIAN_POINT ( 'NONE',  ( 0.1167790944451422702, 4.293833333409199149, -0.2819296736111110424 ) ) ;
#16836=CARTESIAN_POINT ( 'NONE',  ( 0.000000000000000000, 5.384999999999999787, 0.000000000000000000 ) ) ;
#16838=ORIENTED_EDGE ( 'NONE', *, *, #23894, .F. ) ;
#16839=CARTESIAN_POINT ( 'NONE',  ( 0.04809061687855835376, 4.375824664982923551, -0.3084196734384360150 ) ) ;
#16840=CARTESIAN_POINT ( 'NONE',  ( 0.2819296736111110979, 5.043833333409199149, 0.1167790944451422425 ) ) ;
#16841=CARTESIAN_POINT ( 'NONE',  ( -0.2911615289334776868, 5.153441331032047046, -0.08051819117923980640 ) ) ;
#16843=CARTESIAN_POINT ( 'NONE',  ( -0.1292346314604056190, 0.2020833333333329207, -0.3119999999999999996 ) ) ;
#16844=CARTESIAN_POINT ( 'NONE',  ( -0.1993543840281266355, 4.637583333409198261, 0.1993543840281267465 ) ) ;
#16848=CARTESIAN_POINT ( 'NONE',  ( -0.1993543840281267465, 0.5840277777019110550, 0.1993543840281266633 ) ) ;
#16850=CARTESIAN_POINT ( 'NONE',  ( 0.2819296736111110424, 0.2194444443685777957, -0.1167790944451423119 ) ) ;
#16859=CARTESIAN_POINT ( 'NONE',  ( 0.1993543840281266355, 0.3062499999241333759, 0.1993543840281267465 ) ) ;
#16860=CARTESIAN_POINT ( 'NONE',  ( -5.178964085587577574E-17, 0.07708333325746669074, 0.2819296736111110979 ) ) ;
#16861=CARTESIAN_POINT ( 'NONE',  ( -1.726321361862525858E-17, 4.186194444520309865, -0.2819296736111110979 ) ) ;
#16863=CARTESIAN_POINT ( 'NONE',  ( 5.178964085587577574E-17, 4.769527777853643791, 0.2819296736111110979 ) ) ;
#16864=CARTESIAN_POINT ( 'NONE',  ( -0.1993543840281266355, 4.470916666742532186, 0.1993543840281267465 ) ) ;
#16866=CARTESIAN_POINT ( 'NONE',  ( -1.910449006669871087E-17, 5.036888888888888971, -0.3119999999999999996 ) ) ;
#16868=CARTESIAN_POINT ( 'NONE',  ( -0.1292346314604057023, 4.179250000151731648, 0.3119999999999998885 ) ) ;
#16870=EDGE_LOOP ( 'NONE', ( #11166, #12625, #18253, #22049 ) ) ;
#16871=ORIENTED_EDGE ( 'NONE', *, *, #4976, .T. ) ;
#16877=CARTESIAN_POINT ( 'NONE',  ( -0.2206173157302027954, 0.5319444442927114824, -0.2206173157302028232 ) ) ;
#16879=CARTESIAN_POINT ( 'NONE',  ( 0.1358625382851928742, 4.742203176482449933, 0.2831117945823172222 ) ) ;
#16881=CARTESIAN_POINT ( 'NONE',  ( 0.3039879257364922482, 3.976659419480376823, -0.08128067288674797886 ) ) ;
#16882=ORIENTED_EDGE ( 'NONE', *, *, #3305, .F. ) ;
#16885=CARTESIAN_POINT ( 'NONE',  ( -0.2206173157302027676, 4.057722222222221120, 0.2206173157302028787 ) ) ;
#16887=CARTESIAN_POINT ( 'NONE',  ( 0.1167790944451424368, 4.148000000075866112, 0.2819296736111110424 ) ) ;
#16890=CARTESIAN_POINT ( 'NONE',  ( 0.3119999999999999996, 3.797305555555555046, 0.1292346314604056190 ) ) ;
#16891=CARTESIAN_POINT ( 'NONE',  ( 0.2206173157302028787, 4.800777777929509327, 0.2206173157302027954 ) ) ;
#16893=CARTESIAN_POINT ( 'NONE',  ( 5.178964085587577574E-17, 5.102861111186976828, 0.2819296736111110979 ) ) ;
#16894=CARTESIAN_POINT ( 'NONE',  ( 0.2819296736111110424, 4.328555555631420582, -0.1167790944451423396 ) ) ;
#16895=CARTESIAN_POINT ( 'NONE',  ( 0.3119999999999999996, 0.4069444444444440534, 0.000000000000000000 ) ) ;
#16896=ORIENTED_EDGE ( 'NONE', *, *, #6639, .F. ) ;
#16898=CARTESIAN_POINT ( 'NONE',  ( 0.1792189426095378846, 0.03935871358545873361, -0.2268249990278165540 ) ) ;
#16903=CARTESIAN_POINT ( 'NONE',  ( -0.2819296736111110424, 5.078555555631420582, 0.1167790944451424923 ) ) ;
#16904=CARTESIAN_POINT ( 'NONE',  ( 5.178964085587577574E-17, 3.936194444520310309, 0.2819296736111110979 ) ) ;
#16905=CARTESIAN_POINT ( 'NONE',  ( 0.06940672806685913021, 4.406896202175514254, 0.3041826934043310171 ) ) ;
#16907=EDGE_CURVE ( 'NONE', #6119, #2426, #7765, .T. ) ;
#16909=CARTESIAN_POINT ( 'NONE',  ( -0.1993543840281267465, 0.4729166665907999501, 0.1993543840281266633 ) ) ;
#16911=CARTESIAN_POINT ( 'NONE',  ( -0.1167790944451423257, 4.967444444520310753, -0.2819296736111110424 ) ) ;
#16913=CARTESIAN_POINT ( 'NONE',  ( -0.2819296736111110424, 4.800777777853643791, 0.1167790944451424923 ) ) ;
#16914=CARTESIAN_POINT ( 'NONE',  ( -0.04072741636813891064, 4.181569250771618229, 0.3099999491876047619 ) ) ;
#16915=FACE_OUTER_BOUND ( 'NONE', #16870, .T. ) ;
#16918=CARTESIAN_POINT ( 'NONE',  ( 0.1292346314604058410, 4.512583333333332725, 0.3119999999999998885 ) ) ;
#16919=CARTESIAN_POINT ( 'NONE',  ( -1.726321361862525858E-17, 3.838972222298087544, -0.2819296736111110979 ) ) ;
#16922=EDGE_CURVE ( 'NONE', #19560, #6274, #9804, .T. ) ;
#16923=CARTESIAN_POINT ( 'NONE',  ( 0.005285943416724413202, 4.988126182262142549, -0.3119616049321576323 ) ) ;
#16924=DIRECTION ( 'NONE',  ( -0.000000000000000000, -1.000000000000000000, -0.000000000000000000 ) ) ;
#16928=CARTESIAN_POINT ( 'NONE',  ( -0.2854338313968505791, 4.109616874731887748, -0.1273923718972508889 ) ) ;
#16929=CARTESIAN_POINT ( 'NONE',  ( 0.005393248022499976500, 4.654789771038872814, -0.3119600307737797618 ) ) ;
#16936=CARTESIAN_POINT ( 'NONE',  ( -0.2819296736111110424, 0.5041666665908000056, -0.1167790944451423396 ) ) ;
#16941=CARTESIAN_POINT ( 'NONE',  ( -0.2466418311916984407, 5.099818558436279403, -0.1902706867175692762 ) ) ;
#16943=CARTESIAN_POINT ( 'NONE',  ( 0.3119999999999999996, 0.2437499999999996891, -0.1292346314604056468 ) ) ;
#16944=CARTESIAN_POINT ( 'NONE',  ( -1.910449006669871087E-17, 5.147999999999998799, -0.3119999999999999996 ) ) ;
#16945=CARTESIAN_POINT ( 'NONE',  ( -0.1993543840281266910, 4.248694444520310753, -0.1993543840281266910 ) ) ;
#16950=ORIENTED_EDGE ( 'NONE', *, *, #15637, .T. ) ;
#16951=DIRECTION ( 'NONE',  ( 0.000000000000000000, 0.000000000000000000, -1.000000000000000000 ) ) ;
#16952=CARTESIAN_POINT ( 'NONE',  ( 5.178964085587577574E-17, 4.977861111186976828, 0.2819296736111110979 ) ) ;
#16956=CARTESIAN_POINT ( 'NONE',  ( 0.08877758875623015244, 3.708028241517439927, -0.2996422185575408070 ) ) ;
#16959=CARTESIAN_POINT ( 'NONE',  ( -0.2819296736111110979, 4.741750000075865223, 0.000000000000000000 ) ) ;
#16961=CARTESIAN_POINT ( 'NONE',  ( 0.3119999999999999996, 4.300777777777777366, -3.820898013339742174E-17 ) ) ;
#16963=CARTESIAN_POINT ( 'NONE',  ( 0.2819296736111110979, 0.4381944443685778512, 0.000000000000000000 ) ) ;
#16964=ORIENTED_EDGE ( 'NONE', *, *, #20049, .F. ) ;
#16965=CARTESIAN_POINT ( 'NONE',  ( -0.1993543840281267465, 0.1951388888130222710, 0.1993543840281266633 ) ) ;
#16967=CARTESIAN_POINT ( 'NONE',  ( -0.2082794372640225100, 5.206640035683668621, 0.1900105704308308607 ) ) ;
#16972=CARTESIAN_POINT ( 'NONE',  ( -5.178964085587577574E-17, 0.2993055554796889561, 0.2819296736111110979 ) ) ;
#16973=CARTESIAN_POINT ( 'NONE',  ( -0.1167790944451422702, 0.2194444443685777957, -0.2819296736111110424 ) ) ;
#16974=CARTESIAN_POINT ( 'NONE',  ( -0.2819296736111110424, 4.259111111186976828, 0.1167790944451424923 ) ) ;
#16976=EDGE_CURVE ( 'NONE', #9142, #9842, #580, .T. ) ;
#16977=CARTESIAN_POINT ( 'NONE',  ( 0.1167790944451422702, 4.904944444520311642, -0.2819296736111110424 ) ) ;
#16979=CARTESIAN_POINT ( 'NONE',  ( -1.726321361862525858E-17, 4.505638888964754507, -0.2819296736111110979 ) ) ;
#16980=FACE_OUTER_BOUND ( 'NONE', #15639, .T. ) ;
#16984=DIRECTION ( 'NONE',  ( -0.000000000000000000, -1.000000000000000000, -0.000000000000000000 ) ) ;
#16985=CARTESIAN_POINT ( 'NONE',  ( -0.2206173157302028232, 4.106333333485065573, -0.2206173157302028232 ) ) ;
#16988=ORIENTED_EDGE ( 'NONE', *, *, #12930, .T. ) ;
#16991=DIRECTION ( 'NONE',  ( 0.000000000000000000, 0.7071067811865497932, 0.7071067811865452413 ) ) ;
#16994=CARTESIAN_POINT ( 'NONE',  ( -0.2206173157302028787, 0.5458333331816004330, 0.2206173157302027954 ) ) ;
#16997=CARTESIAN_POINT ( 'NONE',  ( 0.000000000000000000, 5.384999999999999787, -0.3119999999999999996 ) ) ;
#16998=CARTESIAN_POINT ( 'NONE',  ( 0.001301388441426008921, 4.766018610250637444, -0.3119976773732344166 ) ) ;
#17000=CARTESIAN_POINT ( 'NONE',  ( 0.04081095154783396378, 3.961648846695317250, 0.3119999993940247851 ) ) ;
#17001=ORIENTED_EDGE ( 'NONE', *, *, #2306, .F. ) ;
#17007=CARTESIAN_POINT ( 'NONE',  ( -0.2819296736111110979, 3.963972222298087544, 0.000000000000000000 ) ) ;
#17008=CARTESIAN_POINT ( 'NONE',  ( 0.1857303984225210092, 5.038301444411008134, -0.2517477023668195923 ) ) ;
#17009=CARTESIAN_POINT ( 'NONE',  ( -4.974594353761572974E-07, 4.738258141874186258, 0.3119999999991586170 ) ) ;
#17010=CARTESIAN_POINT ( 'NONE',  ( -0.2206173157302027676, 3.779944444444443441, 0.2206173157302028787 ) ) ;
#17011=CARTESIAN_POINT ( 'NONE',  ( -1.910449006669871087E-17, 4.821611111262843252, -0.3119999999999999996 ) ) ;
#17012=CARTESIAN_POINT ( 'NONE',  ( 0.2819296736111111534, 4.891055555631421470, 0.1167790944451422563 ) ) ;
#17014=CARTESIAN_POINT ( 'NONE',  ( 0.1993543840281266633, 4.220916666742532186, -0.1993543840281266910 ) ) ;
#17015=CARTESIAN_POINT ( 'NONE',  ( -0.2568804798144080914, 3.896411533234364732, 0.1790538691666017646 ) ) ;
#17023=CARTESIAN_POINT ( 'NONE',  ( -0.2819296736111110424, 5.182722222298088433, -0.1167790944451423119 ) ) ;
#17024=CARTESIAN_POINT ( 'NONE',  ( 5.178964085587577574E-17, 3.825083333409199149, 0.2819296736111110979 ) ) ;
#17026=ADVANCED_FACE ( 'NONE', ( #12259 ), #21388, .T. ) ;
#17030=CARTESIAN_POINT ( 'NONE',  ( 0.2819296736111110979, 0.6048611110352445364, 0.000000000000000000 ) ) ;
#17032=CARTESIAN_POINT ( 'NONE',  ( 0.2819296736111110979, 5.057722222298088433, 0.1167790944451422425 ) ) ;
#17034=CARTESIAN_POINT ( 'NONE',  ( -0.2819296736111110979, 4.686194444520309865, 0.000000000000000000 ) ) ;
#17036=CARTESIAN_POINT ( 'NONE',  ( 0.1059882155383018582, 4.852523979370922724, 0.2940631531866885195 ) ) ;
#17038=DIRECTION ( 'NONE',  ( -0.000000000000000000, -1.000000000000000000, -0.000000000000000000 ) ) ;
#17039=CARTESIAN_POINT ( 'NONE',  ( 0.3119999999999999996, 4.575083333333332725, 0.1292346314604056190 ) ) ;
#17041=CARTESIAN_POINT ( 'NONE',  ( 0.1167790944451424506, 3.870222222298087988, 0.2819296736111110424 ) ) ;
#17042=CARTESIAN_POINT ( 'NONE',  ( 0.09330201573823466987, 4.985571540157835102, -0.2986323972303005503 ) ) ;
#17049=CARTESIAN_POINT ( 'NONE',  ( 0.2131833129333350341, 4.648326027883385336, -0.2316251136011019396 ) ) ;
#17052=CARTESIAN_POINT ( 'NONE',  ( -5.428794840643969700E-10, 4.321611111277808170, -0.3119999999999999996 ) ) ;
#17053=EDGE_CURVE ( 'NONE', #12392, #789, #17352, .T. ) ;
#17054=CARTESIAN_POINT ( 'NONE',  ( 0.2934357671952408375, 5.143311997241705846, 0.08181467001294073782 ) ) ;
#17057=CARTESIAN_POINT ( 'NONE',  ( 0.1167790944451423535, 0.5805555554796888451, 0.2819296736111110424 ) ) ;
#17060=LINE ( 'NONE', #5483, #1963 ) ;
#17064=CARTESIAN_POINT ( 'NONE',  ( 0.1292346314604057023, 0.1743055555555551861, 0.3119999999999998885 ) ) ;
#17065=CARTESIAN_POINT ( 'NONE',  ( 5.731347020009612645E-17, 5.120222222222221120, 0.3119999999999999996 ) ) ;
#17066=CARTESIAN_POINT ( 'NONE',  ( -0.2819296736111110424, 4.259111111186976828, 0.1167790944451424923 ) ) ;
#17067=CARTESIAN_POINT ( 'NONE',  ( -0.1570450868762801044, 4.344718169250874062, 0.2726662231104447498 ) ) ;
#17068=ADVANCED_FACE ( 'NONE', ( #20286 ), #5525, .T. ) ;
#17069=CARTESIAN_POINT ( 'NONE',  ( 0.000000000000000000, 5.384999999999999787, 0.000000000000000000 ) ) ;
#17071=ORIENTED_EDGE ( 'NONE', *, *, #7661, .F. ) ;
#17074=CARTESIAN_POINT ( 'NONE',  ( 0.1167790944451422702, 5.057722222298087544, -0.2819296736111110424 ) ) ;
#17076=EDGE_CURVE ( 'NONE', #15412, #10865, #23168, .T. ) ;
#17077=CARTESIAN_POINT ( 'NONE',  ( -0.3003886044924828358, 5.154938911184799188, -0.02224241330659365926 ) ) ;
#17083=CARTESIAN_POINT ( 'NONE',  ( 0.2819296736111110979, 4.283416666742533074, -3.452642723725051716E-17 ) ) ;
#17085=ADVANCED_FACE ( 'NONE', ( #16980 ), #20998, .T. ) ;
#17086=CARTESIAN_POINT ( 'NONE',  ( 1.910449006669871087E-17, 0.6361111109593781121, -0.3119999999999999996 ) ) ;
#17089=B_SPLINE_CURVE_WITH_KNOTS ( 'NONE', 3,
 ( #19676, #23562, #12505, #10433, #12386, #6877, #19802, #8455, #19926, #10659, #3213, #8822, #7002, #5160, #17611, #901, #6513, #13961, #12261, #21391, #4680, #12150, #19556, #1024, #15898, #6628, #154, #21988, #14691 ),
 .UNSPECIFIED., .F., .F.,
 ( 4, 2, 1, 1, 1, 2, 2, 2, 2, 2, 2, 2, 2, 2, 2, 4 ),
 ( 0.2837225594813787555, 0.2840009242586815086, 0.2841401066473329129, 0.2842096978416585595, 0.2842444934388214106, 0.2842618912374028639, 0.2842792890359842617, 0.2848360185905898234, 0.2859494776998008359, 0.2881763959182229717, 0.2904033141366450521, 0.2926302323550671880, 0.2948571505734892684, 0.2970840687919114043, 0.2993109870103335401, 0.3015379052287556205 ),
 .UNSPECIFIED. ) ;
#17090=CARTESIAN_POINT ( 'NONE',  ( -0.2819296736111110979, 0.5215277777019110550, -3.452642723725051716E-17 ) ) ;
#17092=ORIENTED_EDGE ( 'NONE', *, *, #21035, .T. ) ;
#17093=CARTESIAN_POINT ( 'NONE',  ( 0.2819296736111110424, 0.5527777777019111660, -0.1167790944451423119 ) ) ;
#17094=CARTESIAN_POINT ( 'NONE',  ( 5.731347020009612645E-17, 4.120222222222221120, 0.3119999999999999996 ) ) ;
#17100=CARTESIAN_POINT ( 'NONE',  ( 0.1167790944451423535, 0.5805555554796890672, 0.2819296736111110979 ) ) ;
#17101=CARTESIAN_POINT ( 'NONE',  ( -0.2819296736111110424, 0.1152777777019111521, -0.1167790944451423396 ) ) ;
#17102=CARTESIAN_POINT ( 'NONE',  ( 0.1167790944451422702, 4.349388888964754507, -0.2819296736111110424 ) ) ;
#17104=CARTESIAN_POINT ( 'NONE',  ( 0.1167790944451422702, 4.960500000075865223, -0.2819296736111110424 ) ) ;
#17105=CARTESIAN_POINT ( 'NONE',  ( -1.726321361862525858E-17, 4.450083333409198261, -0.2819296736111110979 ) ) ;
#17108=CARTESIAN_POINT ( 'NONE',  ( -1.910449006669871087E-17, 4.536888888888888083, -0.3119999999999999996 ) ) ;
#17109=CARTESIAN_POINT ( 'NONE',  ( 0.3119999999999999996, 4.026472222373954857, 0.1292346314604056190 ) ) ;
#17110=( BOUNDED_CURVE ( )  B_SPLINE_CURVE ( 2, ( #7530, #20458, #11197, #10959, #18384, #14615, #22160, #12800, #3385 ),
 .UNSPECIFIED., .F., .T. ) 
 B_SPLINE_CURVE_WITH_KNOTS ( ( 3, 2, 2, 2, 3 ),
 ( 0.4375000000000000555, 0.4419642857142857539, 0.4464285714285715079, 0.4508928571428572618, 0.4553571428571429602 ),
 .UNSPECIFIED. ) 
 CURVE ( )  GEOMETRIC_REPRESENTATION_ITEM ( )  RATIONAL_B_SPLINE_CURVE ( ( 0.9999999999999990008, 0.9238795325112877377, 1.000000000000000000, 0.9238795325112867385, 1.000000000000000000, 0.9238795325112867385, 1.000000000000000000, 0.9238795325112848511, 1.000000000000001998 ) ) 
 REPRESENTATION_ITEM ( '' )  );
#17122=CARTESIAN_POINT ( 'NONE',  ( 0.3119999999999999996, 0.3999999998482670627, 0.000000000000000000 ) ) ;
#17123=ORIENTED_EDGE ( 'NONE', *, *, #18094, .T. ) ;
#17124=CARTESIAN_POINT ( 'NONE',  ( 0.3119648635814757931, 4.250952432720125351, 0.04117389441842130016 ) ) ;
#17126=CARTESIAN_POINT ( 'NONE',  ( 1.910449006669871087E-17, 0.5319444444444439979, -0.3119999999999999996 ) ) ;
#17128=CARTESIAN_POINT ( 'NONE',  ( 0.09437171819121717431, 5.169739643388256312, 0.2818761894294421477 ) ) ;
#17135=CARTESIAN_POINT ( 'NONE',  ( 0.2819296736111110979, 4.099388888964754507, 0.1167790944451422425 ) ) ;
#17139=CARTESIAN_POINT ( 'NONE',  ( -0.2206173157302028232, 4.717444444596176290, -0.2206173157302028232 ) ) ;
#17140=CARTESIAN_POINT ( 'NONE',  ( -0.1993543840281266910, 5.026472222298088433, -0.1993543840281266910 ) ) ;
#17142=CARTESIAN_POINT ( 'NONE',  ( -0.1993543840281266355, 4.304250000075865223, 0.1993543840281267465 ) ) ;
#17150=CARTESIAN_POINT ( 'NONE',  ( -0.1167790944451423535, 3.877166666742532186, 0.2819296736111110979 ) ) ;
#17151=FACE_OUTER_BOUND ( 'NONE', #1996, .T. ) ;
#17152=CARTESIAN_POINT ( 'NONE',  ( -1.910449006669871087E-17, 4.647999999999998799, -0.3119999999999999996 ) ) ;
#17155=CARTESIAN_POINT ( 'NONE',  ( -0.1993543840281266633, 0.4590277777019111105, -0.1993543840281266910 ) ) ;
#17157=VERTEX_POINT ( 'NONE', #5878 ) ;
#17158=CARTESIAN_POINT ( 'NONE',  ( -0.1167790944451423535, 4.766055555631421470, 0.2819296736111110424 ) ) ;
#17160=CARTESIAN_POINT ( 'NONE',  ( 0.1993543840281267465, 4.595916666742532186, 0.1993543840281266633 ) ) ;
#17164=CARTESIAN_POINT ( 'NONE',  ( 0.2093153376853872927, 4.855910065012234433, 0.2313697181335848119 ) ) ;
#17166=CYLINDRICAL_SURFACE ( 'NONE', #9644, 0.3119999999999999996 ) ;
#17167=CARTESIAN_POINT ( 'NONE',  ( -0.2206173157302027676, 4.502166666666665762, 0.2206173157302028787 ) ) ;
#17170=CARTESIAN_POINT ( 'NONE',  ( -0.1993543840281266355, 3.804250000075865223, 0.1993543840281267465 ) ) ;
#17173=CARTESIAN_POINT ( 'NONE',  ( 0.000000000000000000, 5.384999999999999787, 0.000000000000000000 ) ) ;
#17177=CARTESIAN_POINT ( 'NONE',  ( 0.2206238289344933934, 4.703650875443257107, -0.2218057234084611085 ) ) ;
#17181=ORIENTED_EDGE ( 'NONE', *, *, #11553, .F. ) ;
#17183=CARTESIAN_POINT ( 'NONE',  ( 0.2819296736111110424, 0.5388888888130223265, -0.1167790944451423119 ) ) ;
#17184=CARTESIAN_POINT ( 'NONE',  ( -0.1802044324038121481, 5.206640035683668621, 0.2176895457663558520 ) ) ;
#17188=CARTESIAN_POINT ( 'NONE',  ( -0.1858657769656070491, 4.621489086676496605, 0.2509059806342907595 ) ) ;
#17189=CARTESIAN_POINT ( 'NONE',  ( -1.910449006669871087E-17, 4.370222222222221120, -0.3119999999999999996 ) ) ;
#17191=CARTESIAN_POINT ( 'NONE',  ( -0.3119999999999999996, 0.3201388888888885287, -0.1292346314604056745 ) ) ;
#17192=CARTESIAN_POINT ( 'NONE',  ( -0.3119999999999998885, 5.109805555555555046, 0.1292346314604058410 ) ) ;
#17194=CARTESIAN_POINT ( 'NONE',  ( 0.1167790944451424368, 4.161888888964755395, 0.2819296736111110424 ) ) ;
#17196=CARTESIAN_POINT ( 'NONE',  ( 5.731347020009612645E-17, 3.786888888888888527, 0.3119999999999999996 ) ) ;
#17201=CARTESIAN_POINT ( 'NONE',  ( -0.1167790944451423257, 4.786888888964755395, -0.2819296736111110424 ) ) ;
#17202=EDGE_CURVE ( 'NONE', #11875, #13964, #18939, .T. ) ;
#17208=CARTESIAN_POINT ( 'NONE',  ( -0.1167790944451423535, 4.266055555631421470, 0.2819296736111110979 ) ) ;
#17210=CARTESIAN_POINT ( 'NONE',  ( -0.1803192683449008904, 4.049281307906420047, -0.2549174622237436738 ) ) ;
#17213=CARTESIAN_POINT ( 'NONE',  ( 0.1167790944451423535, 0.3722222221463555858, 0.2819296736111110424 ) ) ;
#17215=CARTESIAN_POINT ( 'NONE',  ( -0.2427785569044363101, 5.205301948546705582, 0.1471746161278502940 ) ) ;
#17221=CARTESIAN_POINT ( 'NONE',  ( 0.1993543840281266910, 0.4312499999241333759, -0.1993543840281266910 ) ) ;
#17222=CARTESIAN_POINT ( 'NONE',  ( -0.2819296736111110979, 0.1187499999241333620, -3.452642723725051716E-17 ) ) ;
#17223=EDGE_LOOP ( 'NONE', ( #16677, #16197, #11884, #12367 ) ) ;
#17226=CARTESIAN_POINT ( 'NONE',  ( -1.726321361862525858E-17, 4.352861111186976828, -0.2819296736111110979 ) ) ;
#17228=CARTESIAN_POINT ( 'NONE',  ( -0.2819296736111110424, 4.863277777853643791, -0.1167790944451423119 ) ) ;
#17229=CARTESIAN_POINT ( 'NONE',  ( -0.2819296736111110424, 4.189666666742533074, 0.1167790944451424923 ) ) ;
#17230=DIRECTION ( 'NONE',  ( 0.000000000000000000, 0.000000000000000000, -1.000000000000000000 ) ) ;
#17232=CARTESIAN_POINT ( 'NONE',  ( -1.910449006669871087E-17, 3.766055555707287450, -0.3119999999999999996 ) ) ;
#17235=VERTEX_POINT ( 'NONE', #9547 ) ;
#17237=AXIS2_PLACEMENT_3D ( 'NONE', #8507, #16317, #14010 ) ;
#17239=CARTESIAN_POINT ( 'NONE',  ( -0.2284039324571512375, 5.008807737987557296, 0.2125498346988052012 ) ) ;
#17242=CARTESIAN_POINT ( 'NONE',  ( 0.1167790944451423257, 0.05972222214635558579, -0.2819296736111110424 ) ) ;
#17246=CARTESIAN_POINT ( 'NONE',  ( -5.731347020009612645E-17, 0.5597222222222218990, 0.3119999999999999996 ) ) ;
#17248=CARTESIAN_POINT ( 'NONE',  ( 0.2930505947314048787, 5.179336701705883783, -0.01581200851164489551 ) ) ;
#17253=CARTESIAN_POINT ( 'NONE',  ( 5.178964085587577574E-17, 4.088972222298087544, 0.2819296736111110979 ) ) ;
#17254=( BOUNDED_CURVE ( )  B_SPLINE_CURVE ( 2, ( #13862, #23220, #16048, #10450, #17876, #6651, #14216, #10326, #21652, #15802, #17752, #1168, #23101, #19456, #2639, #23461, #4583, #1291, #6529, #8607, #6410, #21290, #22986, #19342, #6291, #13744, #21169, #4458, #11922, #17508, #12043, #13981, #10206, #21409, #4698, #12165, #15038, #20516, #7023, #16737, #9539, #22461, #3932, #20631, #1414, #21890, #20397, #268, #7587, #3811, #4044, #8842, #11497, #7707, #2098, #19, #23582, #5869, #3232, #3688, #20753, #5517, #9297, #12980, #7467, #10683, #13331, #19946, #13220, #16289, #23702, #11375, #18932, #11257, #8717, #1983, #5638, #15154, #16972, #18564, #16859, #14466, #11135, #1853, #18117, #18803, #144, #16167, #6899, #22584, #5760, #14916, #22335, #13103, #18682, #9420, #14338, #21770, #5057, #12527, #15272, #21114, #17577, #8300, #6474, #7826, #4645, #19281, #2588, #6110, #13697, #13579, #12112, #6232, #17338, #13927, #17221, #15510, #21238, #22700, #867, #4528, #23164, #11740, #749, #11616, #8062, #387, #19162, #5990, #6357, #2469, #10034, #2230, #4404, #22936, #8177, #11867, #15752, #15631, #21357, #20872, #505, #17456, #13454, #4166, #7938, #23049, #20989, #4285, #9906, #13804, #11991, #631, #19403, #9790, #2701, #10153, #9662, #17100, #19048, #2350, #15392, #22820, #10746, #20006, #10507 ),
 .UNSPECIFIED., .F., .T. ) 
 B_SPLINE_CURVE_WITH_KNOTS ( ( 3, 2, 2, 2, 2, 2, 2, 2, 2, 2, 2, 2, 2, 2, 2, 2, 2, 2, 2, 2, 2, 2, 2, 2, 2, 2, 2, 2, 2, 2, 2, 2, 2, 2, 2, 2, 2, 2, 2, 2, 2, 2, 2, 2, 2, 2, 2, 2, 2, 2, 2, 2, 2, 2, 2, 2, 2, 2, 2, 2, 2, 2, 2, 2, 2, 2, 2, 2, 2, 2, 2, 2, 2, 2, 2, 2, 2, 2, 2, 2, 2, 2, 2, 3 ),
 ( 0.07882564326583262060, 0.08333333333333332871, 0.09375000000000000000, 0.1041666666666666713, 0.1145833333333333287, 0.1250000000000000000, 0.1354166666666666574, 0.1458333333333333426, 0.1562500000000000000, 0.1666666666666666574, 0.1770833333333333426, 0.1875000000000000000, 0.1979166666666666574, 0.2083333333333333703, 0.2187500000000000000, 0.2291666666666666852, 0.2395833333333333703, 0.2500000000000000000, 0.2604166666666666852, 0.2708333333333333148, 0.2812500000000000000, 0.2916666666666666852, 0.3020833333333333148, 0.3125000000000000000, 0.3229166666666666297, 0.3333333333333333148, 0.3437500000000000000, 0.3541666666666666852, 0.3645833333333333148, 0.3750000000000000555, 0.3854166666666666852, 0.3958333333333333148, 0.4062500000000000000, 0.4166666666666666852, 0.4270833333333333148, 0.4375000000000000000, 0.4479166666666666297, 0.4583333333333333148, 0.4687500000000000000, 0.4791666666666666852, 0.4895833333333333148, 0.5000000000000000000, 0.5104166666666666297, 0.5208333333333333703, 0.5312500000000000000, 0.5416666666666666297, 0.5520833333333333703, 0.5625000000000000000, 0.5729166666666666297, 0.5833333333333333703, 0.5937500000000000000, 0.6041666666666666297, 0.6145833333333333703, 0.6250000000000000000, 0.6354166666666666297, 0.6458333333333333703, 0.6562500000000000000, 0.6666666666666666297, 0.6770833333333333703, 0.6875000000000000000, 0.6979166666666667407, 0.7083333333333333703, 0.7187500000000000000, 0.7291666666666666297, 0.7395833333333333703, 0.7500000000000000000, 0.7604166666666666297, 0.7708333333333332593, 0.7812500000000000000, 0.7916666666666666297, 0.8020833333333333703, 0.8125000000000000000, 0.8229166666666666297, 0.8333333333333333703, 0.8437499999999998890, 0.8541666666666666297, 0.8645833333333333703, 0.8750000000000000000, 0.8854166666666666297, 0.8958333333333333703, 0.9062500000000000000, 0.9166666666666667407, 0.9270833333333333703, 0.9375000000000000000 ),
 .UNSPECIFIED. ) 
 CURVE ( )  GEOMETRIC_REPRESENTATION_ITEM ( )  RATIONAL_B_SPLINE_CURVE ( ( 0.9626285260900118157, 0.9670597623776912011, 1.000000000000000000, 0.9238795325112867385, 1.000000000000000000, 0.9238795325112867385, 1.000000000000000000, 0.9238795325112867385, 1.000000000000000000, 0.9238795325112867385, 1.000000000000000000, 0.9238795325112867385, 1.000000000000000000, 0.9238795325112867385, 1.000000000000000000, 0.9238795325112867385, 1.000000000000000000, 0.9238795325112867385, 1.000000000000000000, 0.9238795325112867385, 1.000000000000000000, 0.9238795325112867385, 1.000000000000000000, 0.9238795325112867385, 1.000000000000000000, 0.9238795325112867385, 1.000000000000000000, 0.9238795325112867385, 1.000000000000000000, 0.9238795325112867385, 1.000000000000000000, 0.9238795325112867385, 1.000000000000000000, 0.9238795325112867385, 1.000000000000000000, 0.9238795325112867385, 1.000000000000000000, 0.9238795325112867385, 1.000000000000000000, 0.9238795325112867385, 1.000000000000000000, 0.9238795325112867385, 1.000000000000000000, 0.9238795325112867385, 1.000000000000000000, 0.9238795325112867385, 1.000000000000000000, 0.9238795325112867385, 1.000000000000000000, 0.9238795325112867385, 1.000000000000000000, 0.9238795325112867385, 1.000000000000000000, 0.9238795325112867385, 1.000000000000000000, 0.9238795325112867385, 1.000000000000000000, 0.9238795325112867385, 1.000000000000000000, 0.9238795325112867385, 1.000000000000000000, 0.9238795325112867385, 1.000000000000000000, 0.9238795325112867385, 1.000000000000000000, 0.9238795325112867385, 1.000000000000000000, 0.9238795325112867385, 1.000000000000000000, 0.9238795325112867385, 1.000000000000000000, 0.9238795325112867385, 1.000000000000000000, 0.9238795325112867385, 1.000000000000000000, 0.9238795325112867385, 1.000000000000000000, 0.9238795325112867385, 1.000000000000000000, 0.9238795325112867385, 1.000000000000000000, 0.9238795325112867385, 1.000000000000000000, 0.9238795325112867385, 1.000000000000000000, 0.9238795325112867385, 1.000000000000000000, 0.9238795325112867385, 1.000000000000000000, 0.9238795325112867385, 1.000000000000000000, 0.9238795325112867385, 1.000000000000000000, 0.9238795325112867385, 1.000000000000000000, 0.9238795325112867385, 1.000000000000000000, 0.9238795325112867385, 1.000000000000000000, 0.9238795325112867385, 1.000000000000000000, 0.9238795325112867385, 1.000000000000000000, 0.9238795325112867385, 1.000000000000000000, 0.9238795325112867385, 1.000000000000000000, 0.9238795325112867385, 1.000000000000000000, 0.9238795325112867385, 1.000000000000000000, 0.9238795325112867385, 1.000000000000000000, 0.9238795325112867385, 1.000000000000000000, 0.9238795325112867385, 1.000000000000000000, 0.9238795325112867385, 1.000000000000000000, 0.9238795325112867385, 1.000000000000000000, 0.9238795325112867385, 1.000000000000000000, 0.9238795325112867385, 1.000000000000000000, 0.9238795325112867385, 1.000000000000000000, 0.9238795325112867385, 1.000000000000000000, 0.9238795325112867385, 1.000000000000000000, 0.9238795325112867385, 1.000000000000000000, 0.9238795325112867385, 1.000000000000000000, 0.9238795325112867385, 1.000000000000000000, 0.9238795325112867385, 1.000000000000000000, 0.9238795325112867385, 1.000000000000000000, 0.9238795325112867385, 1.000000000000000000, 0.9238795325112867385, 1.000000000000000000, 0.9238795325112867385, 1.000000000000000000, 0.9238795325112867385, 1.000000000000000000, 0.9238795325112867385, 1.000000000000000000, 0.9238795325112867385, 1.000000000000000000, 0.9238795325112867385, 1.000000000000000000, 0.9238795325112867385, 1.000000000000000000, 0.9238795325112867385, 1.000000000000000000, 0.9238795325112867385, 1.000000000000000000, 0.9238795325112867385, 1.000000000000000000, 0.9238795325112867385, 1.000000000000000000, 0.9238795325112867385, 1.000000000000000000 ) ) 
 REPRESENTATION_ITEM ( '' )  );
#17257=CARTESIAN_POINT ( 'NONE',  ( -0.07569519822120913954, 5.165236573017851995, -0.2884437376132976683 ) ) ;
#17258=CARTESIAN_POINT ( 'NONE',  ( 0.1292346314604058410, 4.741750000151731648, 0.3119999999999998885 ) ) ;
#17260=CARTESIAN_POINT ( 'NONE',  ( -0.2819296736111110979, 4.922305555631420582, 0.000000000000000000 ) ) ;
#17262=CARTESIAN_POINT ( 'NONE',  ( -0.2819296736111110424, 4.182722222298087544, -0.1167790944451423119 ) ) ;
#17266=VERTEX_POINT ( 'NONE', #274 ) ;
#17270=CARTESIAN_POINT ( 'NONE',  ( 0.2819296736111111534, 3.835500000075866112, 0.1167790944451422563 ) ) ;
#17271=CARTESIAN_POINT ( 'NONE',  ( 0.3141711261733516891, 4.418235456225991342, 0.02406080032727062751 ) ) ;
#17275=CARTESIAN_POINT ( 'NONE',  ( -0.2819296736111111534, 0.4138888888130222155, 0.1167790944451422563 ) ) ;
#17278=CARTESIAN_POINT ( 'NONE',  ( 0.2819296736111110979, 4.838972222298088433, -3.452642723725051716E-17 ) ) ;
#17279=CARTESIAN_POINT ( 'NONE',  ( 0.1993543840281266633, 4.665361111186976828, -0.1993543840281266910 ) ) ;
#17281=CARTESIAN_POINT ( 'NONE',  ( 0.2683590975675059220, 4.868055150729749592, -0.1597197667041882485 ) ) ;
#17284=CARTESIAN_POINT ( 'NONE',  ( 0.2206173157302027954, 4.363277777777777366, -0.2206173157302028232 ) ) ;
#17285=CARTESIAN_POINT ( 'NONE',  ( 0.1993543840281267465, 3.762583333409198705, 0.1993543840281266633 ) ) ;
#17286=EDGE_CURVE ( 'NONE', #9562, #18946, #23717, .T. ) ;
#17289=CARTESIAN_POINT ( 'NONE',  ( 0.3107418810063447556, 4.584733417854850224, 0.02800694585020104335 ) ) ;
#17290=ORIENTED_EDGE ( 'NONE', *, *, #20167, .T. ) ;
#17291=CARTESIAN_POINT ( 'NONE',  ( 0.04619135323477931848, 4.683997901097691319, 0.3085712561171880530 ) ) ;
#17294=CARTESIAN_POINT ( 'NONE',  ( -0.0005581460392713915100, 3.932738050107600802, -0.3119995721350460882 ) ) ;
#17295=ORIENTED_EDGE ( 'NONE', *, *, #11414, .F. ) ;
#17297=CARTESIAN_POINT ( 'NONE',  ( 0.1993543840281266910, 0.4312499999241333759, -0.1993543840281266910 ) ) ;
#17304=CARTESIAN_POINT ( 'NONE',  ( -0.1511513228892870098, 4.622670932816259182, 0.2729428619954094581 ) ) ;
#17307=CARTESIAN_POINT ( 'NONE',  ( 0.1292346314604057023, 0.2854166666666662633, 0.3119999999999998885 ) ) ;
#17308=CARTESIAN_POINT ( 'NONE',  ( 0.2206173157302027954, 4.863277777777777366, -0.2206173157302028232 ) ) ;
#17309=CARTESIAN_POINT ( 'NONE',  ( -0.1167790944451423535, 4.099388888964754507, 0.2819296736111110424 ) ) ;
#17315=CARTESIAN_POINT ( 'NONE',  ( 0.000000000000000000, 5.384999999999999787, 0.000000000000000000 ) ) ;
#17316=CARTESIAN_POINT ( 'NONE',  ( -1.726321361862525858E-17, 4.838972222298088433, -0.2819296736111110979 ) ) ;
#17318=CARTESIAN_POINT ( 'NONE',  ( -0.1089525909866506520, 4.512992428746574802, 0.2955693577741866918 ) ) ;
#17323=CARTESIAN_POINT ( 'NONE',  ( -0.1993543840281266910, 4.415361111186976828, -0.1993543840281266910 ) ) ;
#17325=B_SPLINE_CURVE_WITH_KNOTS ( 'NONE', 3,
 ( #12246, #8679, #4664, #1132, #17595, #19660, #8317, #23543, #17839, #16128, #5138, #8565, #4904, #14300, #19540, #23302, #21734, #5019, #2719, #15769, #12484, #3193, #23187, #2832, #8800, #16251, #23661, #6980, #15884 ),
 .UNSPECIFIED., .F., .F.,
 ( 4, 2, 1, 1, 1, 2, 2, 2, 2, 2, 2, 2, 2, 2, 2, 4 ),
 ( 0.4299228192795082060, 0.4302011865891702813, 0.4303403702440012912, 0.4304099620714167962, 0.4304447579851246042, 0.4304621559419784527, 0.4304795538988323567, 0.4310362885181565074, 0.4321497577568047532, 0.4343766962341013560, 0.4366036347113979588, 0.4388305731886945615, 0.4410575116659911643, 0.4432844501432877116, 0.4455113886205843143, 0.4477383270978809171 ),
 .UNSPECIFIED. ) ;
#17326=CARTESIAN_POINT ( 'NONE',  ( 0.3120000000000000551, 4.297305555555554157, 0.1292346314604056190 ) ) ;
#17330=CARTESIAN_POINT ( 'NONE',  ( -0.2819296736111110424, 0.4069444443685779067, -0.1167790944451423396 ) ) ;
#17336=CARTESIAN_POINT ( 'NONE',  ( 0.1292346314604007063, 3.977861111111111292, -0.3120000000000049400 ) ) ;
#17338=CARTESIAN_POINT ( 'NONE',  ( 0.2819296736111110979, 0.4243055554796889006, 0.000000000000000000 ) ) ;
#17339=CARTESIAN_POINT ( 'NONE',  ( -0.1167790944451422702, 0.2749999999241333204, -0.2819296736111110424 ) ) ;
#17340=CARTESIAN_POINT ( 'NONE',  ( -0.1167790944451423535, 4.210500000075866112, 0.2819296736111110424 ) ) ;
#17342=VECTOR ( 'NONE', #19062, 39.37007874015748143 ) ;
#17343=CARTESIAN_POINT ( 'NONE',  ( -1.726321361862525858E-17, 4.797305555631421470, -0.2819296736111110979 ) ) ;
#17346=CARTESIAN_POINT ( 'NONE',  ( 0.3119999999999999996, 3.755638889040621375, -0.1292346314604056745 ) ) ;
#17351=EDGE_CURVE ( 'NONE', #11042, #13964, #2154, .T. ) ;
#17352=B_SPLINE_CURVE_WITH_KNOTS ( 'NONE', 3,
 ( #2975, #11024, #13109, #18088, #22225, #18448, #1509, #12748, #5157, #20164, #5402, #5645, #21866, #18215, #12867, #23923, #21986, #1388, #22343, #10657 ),
 .UNSPECIFIED., .F., .F.,
 ( 4, 2, 2, 2, 2, 2, 2, 2, 2, 4 ),
 ( 0.1918878366009665604, 0.1930301452378265503, 0.1941724538746865680, 0.1964570711484065479, 0.1987416884221265556, 0.2010263056958465633, 0.2033109229695665710, 0.2055955402432865509, 0.2078801575170065585, 0.2101647747907265662 ),
 .UNSPECIFIED. ) ;
#17356=CARTESIAN_POINT ( 'NONE',  ( -0.2306026292281220802, 5.008719013999844094, 0.2101591525671422378 ) ) ;
#17358=CARTESIAN_POINT ( 'NONE',  ( -0.2819296736111110979, 0.08055555547968892838, 0.1167790944451422425 ) ) ;
#17361=LINE ( 'NONE', #16997, #17842 ) ;
#17362=CARTESIAN_POINT ( 'NONE',  ( 0.01044473586599018768, 4.765759009506619570, -0.3118501016267402060 ) ) ;
#17364=CARTESIAN_POINT ( 'NONE',  ( 0.04801364120717823564, 5.189167739831288984, -0.2857187088061001190 ) ) ;
#17369=CARTESIAN_POINT ( 'NONE',  ( -0.2338143246629017236, 4.675255141077020227, 0.2066237434125970107 ) ) ;
#17370=CARTESIAN_POINT ( 'NONE',  ( 0.1993543840281266633, 4.109805555631420582, -0.1993543840281266910 ) ) ;
#17371=CARTESIAN_POINT ( 'NONE',  ( -5.308788303787306404E-17, 0.03949697488198145034, 0.2889969748819818385 ) ) ;
#17374=CARTESIAN_POINT ( 'NONE',  ( -0.3119999999999999996, 4.446611111262843252, 0.000000000000000000 ) ) ;
#17375=CARTESIAN_POINT ( 'NONE',  ( 0.2819296736111110979, 4.894527777853643791, -3.452642723725051716E-17 ) ) ;
#17377=CARTESIAN_POINT ( 'NONE',  ( -1.726321361862525858E-17, 4.005638888964754507, -0.2819296736111110979 ) ) ;
#17379=EDGE_CURVE ( 'NONE', #14283, #5468, #4771, .T. ) ;
#17380=EDGE_CURVE ( 'NONE', #4599, #16588, #21308, .T. ) ;
#17381=VERTEX_POINT ( 'NONE', #5007 ) ;
#17386=CARTESIAN_POINT ( 'NONE',  ( -0.1292346314604056190, 0.08402777762604483891, -0.3119999999999999996 ) ) ;
#17388=CARTESIAN_POINT ( 'NONE',  ( 0.08315995787118272975, 4.407302845992192353, 0.3007856028562817530 ) ) ;
#17393=CARTESIAN_POINT ( 'NONE',  ( 0.1993543840281266910, 0.3895833332574667462, -0.1993543840281266910 ) ) ;
#17396=CARTESIAN_POINT ( 'NONE',  ( -0.1993543840281266355, 4.818138888964754507, 0.1993543840281267465 ) ) ;
#17398=CARTESIAN_POINT ( 'NONE',  ( 0.1167790944451424368, 4.592444444520309865, 0.2819296736111110424 ) ) ;
#17403=CARTESIAN_POINT ( 'NONE',  ( -0.3119999999999999996, 4.328555555555554157, 0.000000000000000000 ) ) ;
#17404=B_SPLINE_CURVE_WITH_KNOTS ( 'NONE', 3,
 ( #10561, #12399, #22001, #15910, #14332, #23816, #14578, #8961, #10919, #1285, #18109, #6765, #23332, #19816, #14211, #16161, #21644, #23577, #19691, #5301, #12275, #5051, #3349, #12520, #10803, #6892, #6644, #17993, #1041, #3113, #21882, #21765, #16408, #19939, #23456, #3227, #16042, #2995, #18231, #8834, #8470, #10445, #1406, #16282, #7017 ),
 .UNSPECIFIED., .F., .F.,
 ( 4, 2, 2, 2, 2, 2, 2, 2, 2, 1, 1, 2, 2, 2, 2, 2, 2, 2, 2, 1, 1, 1, 1, 1, 2, 4 ),
 ( 0.5391066853785936308, 0.5413919047289608155, 0.5436771240793280002, 0.5448197337545115371, 0.5459623434296951849, 0.5482475627800622586, 0.5505327821304294433, 0.5516753918056130912, 0.5522466966432048041, 0.5525323490620007716, 0.5526037621666997079, 0.5526394687190492316, 0.5526751752713986443, 0.5528180014807966280, 0.5539606111559801649, 0.5551032208311637017, 0.5562458305063472386, 0.5568171353439390625, 0.5571027877627349190, 0.5572456139721327917, 0.5573170270768318391, 0.5573527336291812517, 0.5573705869053560136, 0.5573795135434433945, 0.5573839768624870850, 0.5573884401815307754 ),
 .UNSPECIFIED. ) ;
#17405=CARTESIAN_POINT ( 'NONE',  ( -0.1292346314604056745, 5.158416666818399499, -0.3119999999999999996 ) ) ;
#17406=CARTESIAN_POINT ( 'NONE',  ( -0.3119999999999999996, 3.995222222222221120, 0.000000000000000000 ) ) ;
#17412=CARTESIAN_POINT ( 'NONE',  ( 0.05857570580426915696, 4.128840535618094165, 0.3073945904191558998 ) ) ;
#17414=EDGE_CURVE ( 'NONE', #21824, #2780, #3542, .T. ) ;
#17415=CARTESIAN_POINT ( 'NONE',  ( -0.2494959594970509731, 3.940827237094480573, -0.1917387026992011523 ) ) ;
#17418=CARTESIAN_POINT ( 'NONE',  ( -0.2819296736111110979, 0.3965277777019111660, -3.452642723725051716E-17 ) ) ;
#17419=CARTESIAN_POINT ( 'NONE',  ( 0.000000000000000000, 5.384999999999999787, 0.000000000000000000 ) ) ;
#17424=CARTESIAN_POINT ( 'NONE',  ( -0.08034884895360394630, 5.116190661212350221, 0.2985391448300075967 ) ) ;
#17425=LINE ( 'NONE', #8267, #17535 ) ;
#17426=DIRECTION ( 'NONE',  ( 1.224646799147353207E-16, 0.000000000000000000, -1.000000000000000000 ) ) ;
#17427=CARTESIAN_POINT ( 'NONE',  ( -0.3119999999999999996, 0.3270833333333330040, 0.1292346314604056190 ) ) ;
#17428=CARTESIAN_POINT ( 'NONE',  ( -0.1292346314604057023, 4.838972222222222008, 0.3119999999999998885 ) ) ;
#17429=CARTESIAN_POINT ( 'NONE',  ( -0.1993543840281266910, 3.915361111186976384, -0.1993543840281266910 ) ) ;
#17430=CARTESIAN_POINT ( 'NONE',  ( -0.08169358551447852834, 4.323948374030631925, -0.3038737831921874410 ) ) ;
#17432=CARTESIAN_POINT ( 'NONE',  ( 0.3108775578575657672, 4.806999315166346598, 0.02644136358318530111 ) ) ;
#17433=ORIENTED_EDGE ( 'NONE', *, *, #16064, .T. ) ;
#17434=CARTESIAN_POINT ( 'NONE',  ( -0.3120000026603148569, 4.003392929080275664, 0.04084068248537378598 ) ) ;
#17435=CARTESIAN_POINT ( 'NONE',  ( -0.2819296736111110979, 4.686194444520309865, 0.000000000000000000 ) ) ;
#17437=CARTESIAN_POINT ( 'NONE',  ( -0.1292346314604081170, 4.095916666666666650, -0.3119999999999975016 ) ) ;
#17443=CARTESIAN_POINT ( 'NONE',  ( -0.1993543840281266355, 4.262583333409199149, 0.1993543840281267465 ) ) ;
#17445=CARTESIAN_POINT ( 'NONE',  ( -0.1405978645015776851, 4.047927364732167632, -0.2794846453526392827 ) ) ;
#17448=CARTESIAN_POINT ( 'NONE',  ( 0.1167790944451423257, 0.4486111110352444808, -0.2819296736111110424 ) ) ;
#17453=ORIENTED_EDGE ( 'NONE', *, *, #19594, .F. ) ;
#17455=CARTESIAN_POINT ( 'NONE',  ( 0.000000000000000000, 5.384999999999999787, -0.3119999999999999996 ) ) ;
#17456=CARTESIAN_POINT ( 'NONE',  ( 0.1167790944451423535, 0.5249999999241333759, 0.2819296736111110979 ) ) ;
#17457=CARTESIAN_POINT ( 'NONE',  ( -0.1993543840281266633, 0.1673611110352444808, -0.1993543840281266910 ) ) ;
#17458=CARTESIAN_POINT ( 'NONE',  ( 0.2819296736111110979, 4.172305555631421470, -3.452642723725051716E-17 ) ) ;
#17460=CARTESIAN_POINT ( 'NONE',  ( 0.1993543840281267465, 4.554250000075866112, 0.1993543840281266633 ) ) ;
#17462=ORIENTED_EDGE ( 'NONE', *, *, #4937, .F. ) ;
#17463=ORIENTED_EDGE ( 'NONE', *, *, #5875, .T. ) ;
#17465=EDGE_CURVE ( 'NONE', #16467, #14348, #23775, .T. ) ;
#17466=CARTESIAN_POINT ( 'NONE',  ( -0.2206173157302027676, 3.786888889040620931, 0.2206173157302028787 ) ) ;
#17470=CARTESIAN_POINT ( 'NONE',  ( 0.2335501899993391861, 0.03242967361111066815, 0.1585748220631333916 ) ) ;
#17476=CARTESIAN_POINT ( 'NONE',  ( -0.2819296736111110424, 0.07361111103524449473, -0.1167790944451423396 ) ) ;
#17477=ORIENTED_EDGE ( 'NONE', *, *, #6913, .T. ) ;
#17478=CARTESIAN_POINT ( 'NONE',  ( 0.2785718490593341867, 4.256318101036998591, -0.1406648866877419080 ) ) ;
#17480=CARTESIAN_POINT ( 'NONE',  ( 0.3019181685026062767, 4.083273234461733736, 0.07867355378959554890 ) ) ;
#17482=CARTESIAN_POINT ( 'NONE',  ( 0.2910291928836289399, 5.177951985364569687, 0.04151328995014030854 ) ) ;
#17484=CARTESIAN_POINT ( 'NONE',  ( 0.2819296736111110424, 4.050777777853642903, -0.1167790944451423396 ) ) ;
#17490=CARTESIAN_POINT ( 'NONE',  ( 5.731347020009612645E-17, 4.571611111262843252, 0.3119999999999999996 ) ) ;
#17491=CARTESIAN_POINT ( 'NONE',  ( -0.1167790944451423119, 4.911888888964754507, -0.2819296736111110979 ) ) ;
#17493=CARTESIAN_POINT ( 'NONE',  ( -0.1167790944451423257, 3.953555555631421914, -0.2819296736111110424 ) ) ;
#17499=ORIENTED_EDGE ( 'NONE', *, *, #6670, .T. ) ;
#17501=CARTESIAN_POINT ( 'NONE',  ( -5.731347020009612645E-17, 0.1638888887371559577, 0.3119999999999999996 ) ) ;
#17503=CARTESIAN_POINT ( 'NONE',  ( 0.2283503518066058724, 5.138631362716698625, 0.2031935853610007670 ) ) ;
#17504=CARTESIAN_POINT ( 'NONE',  ( -1.910449006669871087E-17, 3.759111111111109960, -0.3119999999999999996 ) ) ;
#17507=CARTESIAN_POINT ( 'NONE',  ( 0.3119999999999998885, 0.2298611109593781954, 0.1292346314604058410 ) ) ;
#17508=CARTESIAN_POINT ( 'NONE',  ( -0.1167790944451424506, 0.1291666665908000611, 0.2819296736111110424 ) ) ;
#17511=CARTESIAN_POINT ( 'NONE',  ( 0.1167790944451424368, 4.661888888964754507, 0.2819296736111110424 ) ) ;
#17512=CARTESIAN_POINT ( 'NONE',  ( 1.726321361862525858E-17, 0.6048611110352445364, -0.2819296736111110979 ) ) ;
#17513=CARTESIAN_POINT ( 'NONE',  ( 0.2819296736111110979, 4.710500000075865223, 0.1167790944451422425 ) ) ;
#17514=CARTESIAN_POINT ( 'NONE',  ( 0.3119999999999999996, 0.2923611109593781676, -0.1292346314604056468 ) ) ;
#17519=CARTESIAN_POINT ( 'NONE',  ( -0.3119999999999998885, 4.276472222222222008, 0.1292346314604058410 ) ) ;
#17520=EDGE_CURVE ( 'NONE', #5177, #16467, #20373, .T. ) ;
#17521=CARTESIAN_POINT ( 'NONE',  ( 0.3119999999999999996, 5.085500000151732536, -3.820898013339742174E-17 ) ) ;
#17522=CARTESIAN_POINT ( 'NONE',  ( 0.3124206838852614521, 4.975230585218538337, -0.02986472433748768238 ) ) ;
#17530=CARTESIAN_POINT ( 'NONE',  ( 0.1675047463445451801, 4.705591268795053850, -0.2640365305035814458 ) ) ;
#17532=CARTESIAN_POINT ( 'NONE',  ( 0.1823287098769104386, 4.132714727220042406, 0.2533747461830617720 ) ) ;
#17535=VECTOR ( 'NONE', #4017, 39.37007874015748143 ) ;
#17541=CYLINDRICAL_SURFACE ( 'NONE', #15589, 0.3119999999999999996 ) ;
#17544=CARTESIAN_POINT ( 'NONE',  ( -0.06071790806472386615, 5.116734183609173314, 0.3033984148421727811 ) ) ;
#17546=DIRECTION ( 'NONE',  ( 0.000000000000000000, 0.000000000000000000, -1.000000000000000000 ) ) ;
#17547=CARTESIAN_POINT ( 'NONE',  ( -0.1292346314604056190, 0.4798611111111107386, -0.3119999999999999996 ) ) ;
#17548=CARTESIAN_POINT ( 'NONE',  ( -0.3119999999999998885, 4.887583333333331836, 0.1292346314604058410 ) ) ;
#17549=CARTESIAN_POINT ( 'NONE',  ( -0.1993543840281266910, 4.082027777853643791, -0.1993543840281266910 ) ) ;
#17550=CARTESIAN_POINT ( 'NONE',  ( -0.1292346314604058410, 0.6048611109593781121, 0.3119999999999998885 ) ) ;
#17553=ORIENTED_EDGE ( 'NONE', *, *, #19139, .T. ) ;
#17554=ORIENTED_EDGE ( 'NONE', *, *, #5096, .F. ) ;
#17556=CARTESIAN_POINT ( 'NONE',  ( 0.1167790944451424368, 4.814666666742533074, 0.2819296736111110424 ) ) ;
#17559=CARTESIAN_POINT ( 'NONE',  ( -0.01976297047192629441, 5.166874033658601206, 0.2975431225754354148 ) ) ;
#17564=CARTESIAN_POINT ( 'NONE',  ( 0.1167790944451422702, 4.404944444520309865, -0.2819296736111110979 ) ) ;
#17570=CARTESIAN_POINT ( 'NONE',  ( -0.1993543840281267465, 0.4173611110352444808, 0.1993543840281266633 ) ) ;
#17576=DIRECTION ( 'NONE',  ( -0.000000000000000000, -1.000000000000000000, -0.000000000000000000 ) ) ;
#17577=CARTESIAN_POINT ( 'NONE',  ( 1.726321361862525858E-17, 0.3826388888130222710, -0.2819296736111110979 ) ) ;
#17578=CARTESIAN_POINT ( 'NONE',  ( 0.2819296736111110424, 0.3722222221463555858, -0.1167790944451423119 ) ) ;
#17580=CARTESIAN_POINT ( 'NONE',  ( 0.1167790944451424368, 4.050777777853643791, 0.2819296736111110424 ) ) ;
#17582=CARTESIAN_POINT ( 'NONE',  ( 0.1993543840281266633, 4.734805555631421470, -0.1993543840281266910 ) ) ;
#17584=CARTESIAN_POINT ( 'NONE',  ( 0.3119999999999999996, 0.4034722220704893281, -0.1292346314604056468 ) ) ;
#17587=CARTESIAN_POINT ( 'NONE',  ( 0.2206173157302028787, 3.856333333485065573, 0.2206173157302027954 ) ) ;
#17590=CARTESIAN_POINT ( 'NONE',  ( 0.1745307416045020210, 0.03242967361111057101, 0.2218791675890348369 ) ) ;
#17595=CARTESIAN_POINT ( 'NONE',  ( -0.03821557678642730632, 4.570560848383669494, 0.3097108463167145276 ) ) ;
#17598=CARTESIAN_POINT ( 'NONE',  ( -0.1167790944451422702, 0.01111111103524447911, -0.2819296736111110424 ) ) ;
#17599=CARTESIAN_POINT ( 'NONE',  ( 0.2755167264257329940, 4.256510519907095613, -0.1465522358712102458 ) ) ;
#17601=CARTESIAN_POINT ( 'NONE',  ( 1.910449006669871087E-17, 0.3097222222222218435, -0.3119999999999999996 ) ) ;
#17602=CARTESIAN_POINT ( 'NONE',  ( 0.2933236148087240980, 4.082464510228600574, 0.1065868417401308055 ) ) ;
#17604=CARTESIAN_POINT ( 'NONE',  ( 0.2929506655323979580, 5.178423916424801376, 0.02240466457521756924 ) ) ;
#17607=CARTESIAN_POINT ( 'NONE',  ( -0.1167790944451423257, 5.245222222298087544, -0.2819296736111110424 ) ) ;
#17609=CARTESIAN_POINT ( 'NONE',  ( 0.009843460600206053318, 5.016272758367148477, 0.3119999979945484725 ) ) ;
#17610=CARTESIAN_POINT ( 'NONE',  ( -0.03815311363224990066, 5.163840424806421581, -0.2966550781246561908 ) ) ;
#17611=CARTESIAN_POINT ( 'NONE',  ( -0.1742279429200807583, 4.788667672295877864, 0.2618698547778107177 ) ) ;
#17612=CARTESIAN_POINT ( 'NONE',  ( -0.3119999999999999996, 4.443138889040621820, -0.1292346314604056468 ) ) ;
#17613=CARTESIAN_POINT ( 'NONE',  ( -1.726321361862525858E-17, 4.630638888964754507, -0.2819296736111110979 ) ) ;
#17615=CARTESIAN_POINT ( 'NONE',  ( 0.2819296736111110424, 4.161888888964755395, -0.1167790944451423396 ) ) ;
#17617=CIRCLE ( 'NONE', #99, 0.3119999999999999996 ) ;
#17625=CARTESIAN_POINT ( 'NONE',  ( -0.3119999999999999996, 0.03888888873715596467, -3.820898013339742174E-17 ) ) ;
#17627=CARTESIAN_POINT ( 'NONE',  ( 0.3119999999999999996, 0.1777777776260448250, 0.000000000000000000 ) ) ;
#17629=CARTESIAN_POINT ( 'NONE',  ( 0.2206173157302028232, 0.2402777776260448528, -0.2206173157302028232 ) ) ;
#17635=CARTESIAN_POINT ( 'NONE',  ( -0.2819296736111110424, 4.349388888964754507, -0.1167790944451423119 ) ) ;
#17636=CARTESIAN_POINT ( 'NONE',  ( 0.3119999999999999996, 0.1881944444444441367, -0.1292346314604056468 ) ) ;
#17640=CARTESIAN_POINT ( 'NONE',  ( 0.3119999999999999996, 4.241749999999999687, 0.1292346314604056190 ) ) ;
#17641=CARTESIAN_POINT ( 'NONE',  ( 0.2530624153226711526, 5.072996518863750026, 0.1824922298374807572 ) ) ;
#17642=CARTESIAN_POINT ( 'NONE',  ( 0.3119169361980965727, 4.974168473823462833, 0.008358547176593882772 ) ) ;
#17645=CARTESIAN_POINT ( 'NONE',  ( 0.07785856030076440670, 4.708349163112260705, -0.3026912953658169037 ) ) ;
#17648=CARTESIAN_POINT ( 'NONE',  ( 0.1899549616143030306, 4.132987843917230286, 0.2475100817204148873 ) ) ;
#17653=ORIENTED_EDGE ( 'NONE', *, *, #16045, .T. ) ;
#17655=CARTESIAN_POINT ( 'NONE',  ( 0.2819296736111110424, 0.5944444443685777957, -0.1167790944451423119 ) ) ;
#17660=ADVANCED_FACE ( 'NONE', ( #13428 ), #2207, .T. ) ;
#17662=CARTESIAN_POINT ( 'NONE',  ( -0.1487971286937952997, 4.622748527369191507, 0.2742326603549272157 ) ) ;
#17665=CARTESIAN_POINT ( 'NONE',  ( 0.1292346314604056745, 0.3618055555555552694, -0.3119999999999999996 ) ) ;
#17666=CARTESIAN_POINT ( 'NONE',  ( 0.2206173157302027954, 5.029944444444443441, -0.2206173157302028232 ) ) ;
#17667=CARTESIAN_POINT ( 'NONE',  ( -0.1993543840281266355, 4.304250000075865223, 0.1993543840281267465 ) ) ;
#17668=AXIS2_PLACEMENT_3D ( 'NONE', #19046, #2699, #15750 ) ;
#17669=CARTESIAN_POINT ( 'NONE',  ( 5.178964085587577574E-17, 4.047305555631421470, 0.2819296736111110979 ) ) ;
#17676=CARTESIAN_POINT ( 'NONE',  ( 0.2819296736111110979, 4.766055555631421470, 0.1167790944451422425 ) ) ;
#17679=CARTESIAN_POINT ( 'NONE',  ( -0.2060199298796748235, 5.161632575040133730, 0.2171178220200643549 ) ) ;
#17682=CARTESIAN_POINT ( 'NONE',  ( 5.178964085587577574E-17, 3.991750000075865223, 0.2819296736111110979 ) ) ;
#17683=CARTESIAN_POINT ( 'NONE',  ( -0.3109191470435612170, 4.834790615471364461, -0.02595519365989059843 ) ) ;
#17687=CARTESIAN_POINT ( 'NONE',  ( 0.1167790944451423257, -0.009722222298088854797, -0.2819296736111110424 ) ) ;
#17689=CARTESIAN_POINT ( 'NONE',  ( -0.3120000000000000551, 0.4381944444444440534, 0.1292346314604056190 ) ) ;
#17691=CARTESIAN_POINT ( 'NONE',  ( -1.910449006669871087E-17, 3.814666666666665762, -0.3119999999999999996 ) ) ;
#17697=CARTESIAN_POINT ( 'NONE',  ( -0.2819296736111110979, 0.3999999999241333759, 0.1167790944451422425 ) ) ;
#17698=CARTESIAN_POINT ( 'NONE',  ( 0.1993543840281267465, 4.054250000075865223, 0.1993543840281266633 ) ) ;
#17700=CARTESIAN_POINT ( 'NONE',  ( -1.726321361862525858E-17, 4.741750000075866112, -0.2819296736111110979 ) ) ;
#17701=CARTESIAN_POINT ( 'NONE',  ( 3.820898013339742174E-17, 5.384999999999999787, 0.3119999999999999996 ) ) ;
#17702=( BOUNDED_CURVE ( )  B_SPLINE_CURVE ( 2, ( #18584, #7253, #18226, #161, #1522, #16639, #1637, #3581, #5655 ),
 .UNSPECIFIED., .F., .F. ) 
 B_SPLINE_CURVE_WITH_KNOTS ( ( 3, 2, 2, 2, 3 ),
 ( 0.6339285714285713969, 0.6383928571428570953, 0.6428571428571429047, 0.6473214285714286031, 0.6517857142857143016 ),
 .UNSPECIFIED. ) 
 CURVE ( )  GEOMETRIC_REPRESENTATION_ITEM ( )  RATIONAL_B_SPLINE_CURVE ( ( 1.000000000000000000, 0.9238795325112867385, 1.000000000000000000, 0.9238795325112867385, 1.000000000000000000, 0.9238795325112867385, 1.000000000000000000, 0.9238795325112867385, 1.000000000000000000 ) ) 
 REPRESENTATION_ITEM ( '' )  );
#17703=EDGE_LOOP ( 'NONE', ( #10592, #3197, #12997, #11403 ) ) ;
#17705=CARTESIAN_POINT ( 'NONE',  ( 0.1292346314604058410, 3.908416666818398610, 0.3119999999999998885 ) ) ;
#17708=CYLINDRICAL_SURFACE ( 'NONE', #9985, 0.3119999999999999996 ) ;
#17709=CARTESIAN_POINT ( 'NONE',  ( 0.1770636233842524665, 5.206640035683666845, 0.2200907654775672573 ) ) ;
#17711=CARTESIAN_POINT ( 'NONE',  ( 0.2819296736111110979, 4.991750000075866112, -3.452642723725051716E-17 ) ) ;
#17714=CARTESIAN_POINT ( 'NONE',  ( 0.3119999999999998885, 0.2368055555555552416, 0.1292346314604058410 ) ) ;
#17716=CARTESIAN_POINT ( 'NONE',  ( -0.1993543840281266633, 0.07013888881302225708, -0.1993543840281266910 ) ) ;
#17717=CARTESIAN_POINT ( 'NONE',  ( -0.1167790944451422702, 0.06666666659080003332, -0.2819296736111110424 ) ) ;
#17719=CARTESIAN_POINT ( 'NONE',  ( -0.1453203959029216452, 4.733977942634502334, 0.2785166467954151570 ) ) ;
#17720=CARTESIAN_POINT ( 'NONE',  ( 0.09474597157417177784, 4.074405454342402422, 0.2981878519710033371 ) ) ;
#17723=CARTESIAN_POINT ( 'NONE',  ( -0.3109654920464638983, 5.058820495826127583, 0.03608335268173962912 ) ) ;
#17726=CARTESIAN_POINT ( 'NONE',  ( -1.726321361862525858E-17, 5.241750000075865223, -0.2819296736111110979 ) ) ;
#17727=CARTESIAN_POINT ( 'NONE',  ( 0.2823059351267606654, 5.033844105951821746, -0.1328440314189146265 ) ) ;
#17731=CARTESIAN_POINT ( 'NONE',  ( 0.2206173157302028787, 4.523000000151732536, 0.2206173157302027954 ) ) ;
#17732=CARTESIAN_POINT ( 'NONE',  ( 0.2819296736111111534, 4.613277777853643791, 0.1167790944451422563 ) ) ;
#17734=CARTESIAN_POINT ( 'NONE',  ( -0.1993543840281266355, 3.970916666742532186, 0.1993543840281267465 ) ) ;
#17743=CARTESIAN_POINT ( 'NONE',  ( 0.3119999999999999996, 0.4659722222222220100, -0.1292346314604056468 ) ) ;
#17745=CARTESIAN_POINT ( 'NONE',  ( -0.3119999999999999996, 0.1499999998482670627, -3.820898013339742174E-17 ) ) ;
#17746=CARTESIAN_POINT ( 'NONE',  ( 0.09752043859265088765, 5.133419670135086044, 0.2908335107427428845 ) ) ;
#17752=CARTESIAN_POINT ( 'NONE',  ( -0.2819296736111110979, 0.06319444436857780956, -3.452642723725051716E-17 ) ) ;
#17755=CONICAL_SURFACE ( 'NONE', #224, 0.3119999999999999996, 0.7853981633974450594 ) ;
#17756=CARTESIAN_POINT ( 'NONE',  ( 5.178964085587577574E-17, 4.366750000075866112, 0.2819296736111110979 ) ) ;
#17757=FACE_OUTER_BOUND ( 'NONE', #153, .T. ) ;
#17759=CARTESIAN_POINT ( 'NONE',  ( -5.731347020009612645E-17, 0.1708333333333330040, 0.3119999999999999996 ) ) ;
#17761=CARTESIAN_POINT ( 'NONE',  ( -0.2206173157302027676, 4.335499999999998799, 0.2206173157302028787 ) ) ;
#17762=CARTESIAN_POINT ( 'NONE',  ( 0.3119999999999999996, 5.144527777929510215, -0.1292346314604056745 ) ) ;
#17763=CARTESIAN_POINT ( 'NONE',  ( -0.2206173157302027676, 4.668833333333332725, 0.2206173157302028787 ) ) ;
#17767=CARTESIAN_POINT ( 'NONE',  ( -0.1963885513477411360, 4.883221008867676183, -0.2424500834866318566 ) ) ;
#17770=CARTESIAN_POINT ( 'NONE',  ( 0.1544305202402338206, 4.131765882334033968, 0.2716318344387808614 ) ) ;
#17775=CARTESIAN_POINT ( 'NONE',  ( -0.1167790944451422702, 0.1222222221463555997, -0.2819296736111110979 ) ) ;
#17781=CARTESIAN_POINT ( 'NONE',  ( -0.1920931035936397357, 4.605286123663857367, -0.2458545860066076727 ) ) ;
#17782=CARTESIAN_POINT ( 'NONE',  ( -0.03359205281520610126, 4.266996909436898022, -0.3104188874939881049 ) ) ;
#17784=CARTESIAN_POINT ( 'NONE',  ( 0.1292346314604057023, 0.3965277777777773682, 0.3119999999999998885 ) ) ;
#17785=CARTESIAN_POINT ( 'NONE',  ( 5.731347020009612645E-17, 4.897999999999998799, 0.3119999999999999996 ) ) ;
#17787=CARTESIAN_POINT ( 'NONE',  ( 0.2819296736111110979, 4.217444444520309865, -0.1167790944451423396 ) ) ;
#17788=CARTESIAN_POINT ( 'NONE',  ( -0.1993543840281266910, 4.026472222298087544, -0.1993543840281266910 ) ) ;
#17790=DIRECTION ( 'NONE',  ( -0.000000000000000000, -1.000000000000000000, -0.000000000000000000 ) ) ;
#17793=EDGE_LOOP ( 'NONE', ( #16871, #17123, #6241, #8619 ) ) ;
#17795=CARTESIAN_POINT ( 'NONE',  ( -0.2819296736111110979, 4.408416666742532186, 0.000000000000000000 ) ) ;
#17797=CARTESIAN_POINT ( 'NONE',  ( 0.3120000000000000551, 3.797305555555555046, 0.1292346314604056190 ) ) ;
#17800=CARTESIAN_POINT ( 'NONE',  ( 0.1988756463526800689, 5.384999999999999787, -0.2404006599154913104 ) ) ;
#17803=CARTESIAN_POINT ( 'NONE',  ( 5.178964085587577574E-17, 4.047305555631421470, 0.2819296736111110979 ) ) ;
#17809=CARTESIAN_POINT ( 'NONE',  ( 0.1993543840281266355, 0.1395833332574667185, 0.1993543840281267465 ) ) ;
#17818=CARTESIAN_POINT ( 'NONE',  ( -0.1917427225863750362, 3.788106276551002072, 0.2494930344764286489 ) ) ;
#17820=CARTESIAN_POINT ( 'NONE',  ( 0.2819296736111110979, 0.3687499999241333759, 0.000000000000000000 ) ) ;
#17821=CARTESIAN_POINT ( 'NONE',  ( 0.1167790944451422702, 4.071611111186977716, -0.2819296736111110424 ) ) ;
#17824=CARTESIAN_POINT ( 'NONE',  ( -0.1993543840281266910, 4.582027777853643791, -0.1993543840281266910 ) ) ;
#17825=CARTESIAN_POINT ( 'NONE',  ( 0.2963689254433287124, 5.132984698410943736, -0.07753672115038566515 ) ) ;
#17826=CARTESIAN_POINT ( 'NONE',  ( -1.906863420619159052E-17, 5.092106365077719410, -0.3114144293598434809 ) ) ;
#17831=CARTESIAN_POINT ( 'NONE',  ( 0.3119999999999999996, 4.804249999999998799, -0.1292346314604056745 ) ) ;
#17832=CARTESIAN_POINT ( 'NONE',  ( -0.2206173157302027676, 3.731333333485065129, 0.2206173157302028787 ) ) ;
#17836=CARTESIAN_POINT ( 'NONE',  ( -0.1167790944451423119, 4.786888888964754507, -0.2819296736111110979 ) ) ;
#17839=CARTESIAN_POINT ( 'NONE',  ( -0.05311512559760463159, 4.570133353518549768, 0.3074461305437241609 ) ) ;
#17840=ORIENTED_EDGE ( 'NONE', *, *, #10975, .F. ) ;
#17841=CARTESIAN_POINT ( 'NONE',  ( 0.2819296736111110979, 0.3826388888130222710, 0.000000000000000000 ) ) ;
#17842=VECTOR ( 'NONE', #15296, 39.37007874015748143 ) ;
#17844=CARTESIAN_POINT ( 'NONE',  ( 0.000000000000000000, 5.384999999999999787, 0.000000000000000000 ) ) ;
#17845=CYLINDRICAL_SURFACE ( 'NONE', #11550, 0.3119999999999999996 ) ;
#17848=CARTESIAN_POINT ( 'NONE',  ( -0.3131335442325084983, 5.058051426742139256, 0.009062785932360829452 ) ) ;
#17853=CARTESIAN_POINT ( 'NONE',  ( -1.726321361862525858E-17, 3.783416666742532186, -0.2819296736111110979 ) ) ;
#17855=CARTESIAN_POINT ( 'NONE',  ( 0.3121171848235045343, 5.031039829910873173, -0.04005612972654293974 ) ) ;
#17858=CARTESIAN_POINT ( 'NONE',  ( 0.3119999999999999996, 4.474388889040620931, -3.820898013339742174E-17 ) ) ;
#17859=CARTESIAN_POINT ( 'NONE',  ( -0.2819296736111110979, 4.700083333409199149, 0.000000000000000000 ) ) ;
#17861=CARTESIAN_POINT ( 'NONE',  ( -0.1167790944451423535, 4.141055555631421470, 0.2819296736111110424 ) ) ;
#17866=EDGE_LOOP ( 'NONE', ( #1007, #21514, #1874, #16706 ) ) ;
#17870=CARTESIAN_POINT ( 'NONE',  ( -0.1292346314604056190, 0.3062499998482670627, -0.3119999999999999996 ) ) ;
#17876=CARTESIAN_POINT ( 'NONE',  ( 0.1993543840281266910, 0.04236111103524448085, -0.1993543840281266910 ) ) ;
#17879=CARTESIAN_POINT ( 'NONE',  ( -0.2819296736111110979, 4.408416666742532186, 0.000000000000000000 ) ) ;
#17884=CARTESIAN_POINT ( 'NONE',  ( -0.1292346314604057023, 4.061194444444443441, 0.3119999999999998885 ) ) ;
#17885=CARTESIAN_POINT ( 'NONE',  ( -1.910449006669871087E-17, 5.099388889040620931, -0.3119999999999999996 ) ) ;
#17886=CARTESIAN_POINT ( 'NONE',  ( -0.2206173157302028232, 4.654944444444443441, -0.2206173157302028232 ) ) ;
#17890=( BOUNDED_CURVE ( )  B_SPLINE_CURVE ( 2, ( #299, #20665, #16885, #536, #9819, #15538, #3844, #7973, #15424 ),
 .UNSPECIFIED., .F., .T. ) 
 B_SPLINE_CURVE_WITH_KNOTS ( ( 3, 2, 2, 2, 3 ),
 ( 0.7767857142857145236, 0.7812500000000001110, 0.7857142857142858094, 0.7901785714285713969, 0.7946428571428569843 ),
 .UNSPECIFIED. ) 
 CURVE ( )  GEOMETRIC_REPRESENTATION_ITEM ( )  RATIONAL_B_SPLINE_CURVE ( ( 0.9999999999999962252, 0.9238795325112905132, 1.000000000000000000, 0.9238795325112867385, 1.000000000000000000, 0.9238795325112867385, 1.000000000000000000, 0.9238795325112886259, 0.9999999999999981126 ) ) 
 REPRESENTATION_ITEM ( '' )  );
#17891=CARTESIAN_POINT ( 'NONE',  ( -0.2498007881920322748, 4.885330436945963584, -0.1913351078665916638 ) ) ;
#17892=AXIS2_PLACEMENT_3D ( 'NONE', #1481, #20375, #7448 ) ;
#17894=CYLINDRICAL_SURFACE ( 'NONE', #11268, 0.3119999999999999996 ) ;
#17898=CARTESIAN_POINT ( 'NONE',  ( -0.1993543840281266633, 0.07013888881302225708, -0.1993543840281266910 ) ) ;
#17902=CARTESIAN_POINT ( 'NONE',  ( -1.726321361862525858E-17, 5.075083333409198261, -0.2819296736111110979 ) ) ;
#17905=CARTESIAN_POINT ( 'NONE',  ( 0.2206173157302028787, 3.849388888888888083, 0.2206173157302027954 ) ) ;
#17906=CARTESIAN_POINT ( 'NONE',  ( -0.03916966384476119195, 4.292719081527837766, 0.3096853047877550780 ) ) ;
#17908=CARTESIAN_POINT ( 'NONE',  ( -0.1292346314604056190, 0.4243055555555552139, -0.3119999999999999996 ) ) ;
#17909=CARTESIAN_POINT ( 'NONE',  ( -0.1292346314604057023, 4.616749999999998799, 0.3119999999999998885 ) ) ;
#17912=CARTESIAN_POINT ( 'NONE',  ( 0.2819296736111110979, 4.213972222298087544, -3.452642723725051716E-17 ) ) ;
#17913=CARTESIAN_POINT ( 'NONE',  ( 0.2819296736111110424, 3.898000000075866112, -0.1167790944451423396 ) ) ;
#17917=CARTESIAN_POINT ( 'NONE',  ( -0.1993543840281266355, 4.582027777853642903, 0.1993543840281267465 ) ) ;
#17918=CARTESIAN_POINT ( 'NONE',  ( -0.2472039951646029798, 4.507996249098253472, 0.1903866923103891273 ) ) ;
#17921=AXIS2_PLACEMENT_3D ( 'NONE', #17844, #12369, #23546 ) ;
#17923=CARTESIAN_POINT ( 'NONE',  ( -0.2819296736111110979, 4.033416666742532186, 0.000000000000000000 ) ) ;
#17924=CARTESIAN_POINT ( 'NONE',  ( -0.3018196487929861171, 4.837821592016447347, 0.08216582023643356769 ) ) ;
#17928=CARTESIAN_POINT ( 'NONE',  ( -0.1993543840281267465, 0.01458333325746670114, 0.1993543840281266633 ) ) ;
#17939=CARTESIAN_POINT ( 'NONE',  ( -0.1993543840281266633, 0.5006944443685777957, -0.1993543840281266910 ) ) ;
#17940=CARTESIAN_POINT ( 'NONE',  ( -0.2819296736111110979, 3.977861111186976828, 0.000000000000000000 ) ) ;
#17942=EDGE_CURVE ( 'NONE', #18493, #19908, #18476, .T. ) ;
#17943=CARTESIAN_POINT ( 'NONE',  ( 0.1993543840281267465, 4.720916666742533074, 0.1993543840281266633 ) ) ;
#17944=CARTESIAN_POINT ( 'NONE',  ( 0.1265266518300305620, 5.140004865470651829, -0.2773898234840398436 ) ) ;
#17950=CARTESIAN_POINT ( 'NONE',  ( -0.2819296736111110979, 5.186194444520309865, 0.000000000000000000 ) ) ;
#17952=CARTESIAN_POINT ( 'NONE',  ( 0.05766389498127402063, 0.03242967361111055019, 0.2763512717206497160 ) ) ;
#17953=CARTESIAN_POINT ( 'NONE',  ( 0.1993543840281267465, 4.873694444520309865, 0.1993543840281266633 ) ) ;
#17956=CARTESIAN_POINT ( 'NONE',  ( -0.2992172847943166403, 5.112391783004748724, -0.08165418766530285755 ) ) ;
#17957=CARTESIAN_POINT ( 'NONE',  ( -0.3119999999999999996, 0.2020833331816004053, -0.1292346314604056745 ) ) ;
#17959=CARTESIAN_POINT ( 'NONE',  ( -0.2819296736111110979, 0.3548611110352444808, -3.452642723725051716E-17 ) ) ;
#17960=EDGE_CURVE ( 'NONE', #14458, #10504, #3075, .T. ) ;
#17963=ORIENTED_EDGE ( 'NONE', *, *, #538, .T. ) ;
#17964=CARTESIAN_POINT ( 'NONE',  ( -0.1993543840281266633, 0.01458333325746670114, -0.1993543840281266910 ) ) ;
#17966=CARTESIAN_POINT ( 'NONE',  ( 0.3017093057370441866, 4.083250499197780492, 0.07947025837465231113 ) ) ;
#17971=CARTESIAN_POINT ( 'NONE',  ( 5.178964085587577574E-17, 4.825083333409199149, 0.2819296736111110979 ) ) ;
#17975=CARTESIAN_POINT ( 'NONE',  ( 0.1993543840281266633, 3.832027777853643791, -0.1993543840281266910 ) ) ;
#17977=CARTESIAN_POINT ( 'NONE',  ( 0.2666101000349533900, 5.034820359779531351, -0.1625958559946468762 ) ) ;
#17980=CARTESIAN_POINT ( 'NONE',  ( 0.2206173157302028787, 4.189666666818398610, 0.2206173157302027954 ) ) ;
#17981=CARTESIAN_POINT ( 'NONE',  ( 0.1167790944451424506, 4.661888888964753619, 0.2819296736111110424 ) ) ;
#17983=CARTESIAN_POINT ( 'NONE',  ( -0.2819296736111110424, 3.911888888964754507, 0.1167790944451424923 ) ) ;
#17985=ORIENTED_EDGE ( 'NONE', *, *, #16283, .T. ) ;
#17986=ADVANCED_FACE ( 'NONE', ( #13856 ), #10564, .T. ) ;
#17989=CARTESIAN_POINT ( 'NONE',  ( 0.3120000000000000551, 4.241749999999999687, 0.1292346314604056190 ) ) ;
#17991=ORIENTED_EDGE ( 'NONE', *, *, #20167, .F. ) ;
#17992=CARTESIAN_POINT ( 'NONE',  ( -0.3119999999999999996, 0.3166666665149337478, -3.820898013339742174E-17 ) ) ;
#17993=CARTESIAN_POINT ( 'NONE',  ( -0.1441205229031398416, 4.381327590240017500, -0.2776377754592725955 ) ) ;
#17994=CARTESIAN_POINT ( 'NONE',  ( 0.3119999999999998885, 0.1743055554038226151, 0.1292346314604058410 ) ) ;
#17998=CARTESIAN_POINT ( 'NONE',  ( 0.2206173157302027676, 0.2263888887371559577, 0.2206173157302028787 ) ) ;
#18002=CARTESIAN_POINT ( 'NONE',  ( 0.2819296736111110979, 4.488277777853643791, 0.1167790944451422425 ) ) ;
#18005=CARTESIAN_POINT ( 'NONE',  ( -0.08153216764024100172, 4.212811476589685356, -0.3039061551226592273 ) ) ;
#18006=CARTESIAN_POINT ( 'NONE',  ( -0.1292346314604056745, 4.151472222222222008, -0.3119999999999999996 ) ) ;
#18007=CARTESIAN_POINT ( 'NONE',  ( 0.3119999999999999996, 4.918833333485065573, -3.820898013339742174E-17 ) ) ;
#18010=ORIENTED_EDGE ( 'NONE', *, *, #21983, .F. ) ;
#18017=CARTESIAN_POINT ( 'NONE',  ( -0.1167790944451423257, 5.189666666742533074, -0.2819296736111110424 ) ) ;
#18021=CARTESIAN_POINT ( 'NONE',  ( 0.1292346314604058410, 3.845916666666666206, 0.3119999999999998885 ) ) ;
#18022=CARTESIAN_POINT ( 'NONE',  ( -0.004324734472469597517, 4.293710590358529977, 0.3119743139031605494 ) ) ;
#18024=CARTESIAN_POINT ( 'NONE',  ( 0.1292346314604057023, 0.4520833333333330040, 0.3119999999999998885 ) ) ;
#18025=CARTESIAN_POINT ( 'NONE',  ( -0.3119999999999999996, 4.825083333333331836, -0.1292346314604056468 ) ) ;
#18026=CARTESIAN_POINT ( 'NONE',  ( 0.2819296736111111534, 4.321611111186976828, 0.1167790944451422563 ) ) ;
#18029=CARTESIAN_POINT ( 'NONE',  ( -5.731347020009612645E-17, 0.3374999999999996336, 0.3119999999999999996 ) ) ;
#18031=( BOUNDED_CURVE ( )  B_SPLINE_CURVE ( 2, ( #472, #22425, #9388, #20718, #110, #237, #4130, #11587, #7903 ),
 .UNSPECIFIED., .F., .F. ) 
 B_SPLINE_CURVE_WITH_KNOTS ( ( 3, 2, 2, 2, 3 ),
 ( 0.2708333333333333148, 0.2812500000000000000, 0.2916666666666666852, 0.3020833333333333148, 0.3125000000000000000 ),
 .UNSPECIFIED. ) 
 CURVE ( )  GEOMETRIC_REPRESENTATION_ITEM ( )  RATIONAL_B_SPLINE_CURVE ( ( 1.000000000000000000, 0.9238795325112867385, 1.000000000000000000, 0.9238795325112867385, 1.000000000000000000, 0.9238795325112867385, 1.000000000000000000, 0.9238795325112867385, 1.000000000000000000 ) ) 
 REPRESENTATION_ITEM ( '' )  );
#18033=CARTESIAN_POINT ( 'NONE',  ( 0.1993543840281266633, 4.554250000075866112, -0.1993543840281266910 ) ) ;
#18035=CARTESIAN_POINT ( 'NONE',  ( -0.2536818300626839662, 4.507685682728529208, 0.1817722763046524526 ) ) ;
#18037=LINE ( 'NONE', #19862, #4136 ) ;
#18039=CARTESIAN_POINT ( 'NONE',  ( 0.2819296736111110979, 4.120222222298087544, -0.1167790944451423396 ) ) ;
#18040=CARTESIAN_POINT ( 'NONE',  ( -0.3104648678880025936, 4.836571241263951215, 0.03818230244409723251 ) ) ;
#18041=CARTESIAN_POINT ( 'NONE',  ( 0.000000000000000000, 5.384999999999999787, 0.000000000000000000 ) ) ;
#18045=CARTESIAN_POINT ( 'NONE',  ( -5.178964085587577574E-17, 0.07708333325746669074, 0.2819296736111110979 ) ) ;
#18055=CARTESIAN_POINT ( 'NONE',  ( -0.2819296736111110979, 0.5076388888130222155, -3.452642723725051716E-17 ) ) ;
#18056=CARTESIAN_POINT ( 'NONE',  ( 0.1993543840281267465, 3.943138888964754951, 0.1993543840281266633 ) ) ;
#18058=CARTESIAN_POINT ( 'NONE',  ( 5.178964085587577574E-17, 4.491750000075866112, 0.2819296736111110979 ) ) ;
#18059=CARTESIAN_POINT ( 'NONE',  ( 0.1871732423712090254, 5.138164441764971890, -0.2418006535867516238 ) ) ;
#18061=CARTESIAN_POINT ( 'NONE',  ( -0.1167790944451423535, 5.196611111186976828, 0.2819296736111110424 ) ) ;
#18063=ADVANCED_FACE ( 'NONE', ( #8169 ), #11731, .T. ) ;
#18066=FACE_OUTER_BOUND ( 'NONE', #16058, .T. ) ;
#18067=CARTESIAN_POINT ( 'NONE',  ( -0.1167790944451423119, 4.953555555631421470, -0.2819296736111110979 ) ) ;
#18071=CARTESIAN_POINT ( 'NONE',  ( -0.01006672540870686382, 5.100353940687614163, -0.3107987198613663127 ) ) ;
#18072=CARTESIAN_POINT ( 'NONE',  ( 0.1292346314604057300, 0.2298611111111107941, 0.3119999999999998885 ) ) ;
#18073=ORIENTED_EDGE ( 'NONE', *, *, #4979, .F. ) ;
#18074=CARTESIAN_POINT ( 'NONE',  ( -5.178964085587577574E-17, 0.3131944443685777957, 0.2819296736111110979 ) ) ;
#18075=ORIENTED_EDGE ( 'NONE', *, *, #646, .F. ) ;
#18076=CARTESIAN_POINT ( 'NONE',  ( 0.1993543840281266910, 0.0006944443685778138933, -0.1993543840281266910 ) ) ;
#18080=CARTESIAN_POINT ( 'NONE',  ( -0.2291390410192159499, 5.064333695668232771, 0.2117534099777545753 ) ) ;
#18082=DIRECTION ( 'NONE',  ( -0.000000000000000000, -1.000000000000000000, -0.000000000000000000 ) ) ;
#18084=CARTESIAN_POINT ( 'NONE',  ( 0.2819296736111110424, 4.453555555631421470, -0.1167790944451423396 ) ) ;
#18085=CARTESIAN_POINT ( 'NONE',  ( 0.2899264469942640088, 4.526525690781284972, 0.1173681943709265485 ) ) ;
#18086=CARTESIAN_POINT ( 'NONE',  ( -0.2819296736111110424, 3.856333333409198705, 0.1167790944451424923 ) ) ;
#18088=CARTESIAN_POINT ( 'NONE',  ( 0.08111133061092308527, 4.930371998486145380, -0.3019672302974793499 ) ) ;
#18092=CARTESIAN_POINT ( 'NONE',  ( 0.3119999999999999996, 4.304250000151731648, 0.1292346314604056190 ) ) ;
#18093=CARTESIAN_POINT ( 'NONE',  ( 0.1167790944451424506, 4.773000000075866112, 0.2819296736111110424 ) ) ;
#18094=EDGE_CURVE ( 'NONE', #848, #22975, #2459, .T. ) ;
#18096=CARTESIAN_POINT ( 'NONE',  ( -0.1167790944451423257, 3.731333333409198261, -0.2819296736111110424 ) ) ;
#18105=CARTESIAN_POINT ( 'NONE',  ( -0.04076013556702704627, 4.959297389055183025, 0.3120000044509055326 ) ) ;
#18108=CARTESIAN_POINT ( 'NONE',  ( -0.3119999999999999996, 0.3201388887371559577, 0.1292346314604056190 ) ) ;
#18109=CARTESIAN_POINT ( 'NONE',  ( -0.3119502584613883522, 4.392308377792550900, 0.04130061492316871447 ) ) ;
#18110=CARTESIAN_POINT ( 'NONE',  ( -0.1802073857353792830, 5.124029362565509338, 0.2497371168007535003 ) ) ;
#18114=EDGE_LOOP ( 'NONE', ( #13945, #4572, #13385, #19313 ) ) ;
#18116=CARTESIAN_POINT ( 'NONE',  ( 0.1569830666613089287, 5.095142424218626509, -0.2688941244208343795 ) ) ;
#18117=CARTESIAN_POINT ( 'NONE',  ( 0.1993543840281266910, 0.3201388888130222710, -0.1993543840281266910 ) ) ;
#18120=CARTESIAN_POINT ( 'NONE',  ( 0.1167790944451424368, 4.536888888964754507, 0.2819296736111110424 ) ) ;
#18122=CARTESIAN_POINT ( 'NONE',  ( -1.910449006669871087E-17, 4.592444444444443441, -0.3119999999999999996 ) ) ;
#18124=CARTESIAN_POINT ( 'NONE',  ( 0.1292346314604058410, 4.123694444444445217, 0.3119999999999998885 ) ) ;
#18125=CARTESIAN_POINT ( 'NONE',  ( 0.3119999999999999996, 5.026472222373954857, 0.1292346314604056190 ) ) ;
#18131=CARTESIAN_POINT ( 'NONE',  ( -0.1740286758623957597, 4.882424925759353052, -0.2591414521710017071 ) ) ;
#18135=EDGE_LOOP ( 'NONE', ( #12852, #11352, #4844, #3660 ) ) ;
#18139=CARTESIAN_POINT ( 'NONE',  ( -0.2819296736111110979, 0.3513888888130222155, -0.1167790944451423396 ) ) ;
#18141=CARTESIAN_POINT ( 'NONE',  ( 0.2819296736111110979, 5.116750000075866112, -3.452642723725051716E-17 ) ) ;
#18142=CARTESIAN_POINT ( 'NONE',  ( 0.3047585109715561513, 4.472512657067983177, 0.06683305890437241104 ) ) ;
#18143=EDGE_LOOP ( 'NONE', ( #13410, #12893, #2006, #11446 ) ) ;
#18144=CARTESIAN_POINT ( 'NONE',  ( -0.1901414604034510070, 4.605216824736812598, -0.2473673753929898356 ) ) ;
#18147=DIRECTION ( 'NONE',  ( -1.000000000000000000, 0.000000000000000000, 0.000000000000000000 ) ) ;
#18149=CARTESIAN_POINT ( 'NONE',  ( 5.731347020009612645E-17, 4.786888888888888083, 0.3119999999999999996 ) ) ;
#18150=CARTESIAN_POINT ( 'NONE',  ( -0.2819296736111110424, 4.023000000075866112, 0.1167790944451424923 ) ) ;
#18151=CARTESIAN_POINT ( 'NONE',  ( -0.1993543840281266910, 3.804250000075865668, -0.1993543840281266910 ) ) ;
#18154=VECTOR ( 'NONE', #1092, 39.37007874015748143 ) ;
#18155=CARTESIAN_POINT ( 'NONE',  ( -0.3119999999999999996, 4.547305555555554157, -0.1292346314604056468 ) ) ;
#18156=CARTESIAN_POINT ( 'NONE',  ( -1.726321361862525858E-17, 4.505638888964754507, -0.2819296736111110979 ) ) ;
#18157=CARTESIAN_POINT ( 'NONE',  ( -0.3077250951222398334, 4.500723898767198250, -0.05197174156527661210 ) ) ;
#18161=CARTESIAN_POINT ( 'NONE',  ( -0.1993543840281266910, 4.026472222298087544, -0.1993543840281266910 ) ) ;
#18162=CARTESIAN_POINT ( 'NONE',  ( -0.2685085545779261063, 4.830739561115536596, -0.1638191573221950137 ) ) ;
#18163=CARTESIAN_POINT ( 'NONE',  ( -0.2726119996617456520, 4.451313226511029342, 0.1571456554947538165 ) ) ;
#18164=CARTESIAN_POINT ( 'NONE',  ( 0.3119999999999998885, 0.06466217752329557478, 0.07460622607702992182 ) ) ;
#18167=CARTESIAN_POINT ( 'NONE',  ( -0.2819296736111110979, 0.06666666659080003332, 0.1167790944451422425 ) ) ;
#18177=( BOUNDED_CURVE ( )  B_SPLINE_CURVE ( 2, ( #23137, #11965, #8153, #8514, #12205, #6812, #11837, #15955, #19614 ),
 .UNSPECIFIED., .F., .F. ) 
 B_SPLINE_CURVE_WITH_KNOTS ( ( 3, 2, 2, 2, 3 ),
 ( 0.8839285714285713969, 0.8883928571428570953, 0.8928571428571427937, 0.8973214285714284921, 0.9017857142857141906 ),
 .UNSPECIFIED. ) 
 CURVE ( )  GEOMETRIC_REPRESENTATION_ITEM ( )  RATIONAL_B_SPLINE_CURVE ( ( 1.000000000000000000, 0.9238795325112867385, 1.000000000000000000, 0.9238795325112867385, 1.000000000000000000, 0.9238795325112867385, 1.000000000000000000, 0.9238795325112886259, 0.9999999999999981126 ) ) 
 REPRESENTATION_ITEM ( '' )  );
#18179=CARTESIAN_POINT ( 'NONE',  ( -0.1292346314604056190, 0.09097222222222188515, -0.3119999999999999996 ) ) ;
#18180=CARTESIAN_POINT ( 'NONE',  ( 0.1167790944451424368, 3.884111111186977272, 0.2819296736111110424 ) ) ;
#18182=CARTESIAN_POINT ( 'NONE',  ( 0.2819296736111110979, 4.335500000075866112, 0.1167790944451422425 ) ) ;
#18186=CARTESIAN_POINT ( 'NONE',  ( 0.2406838310274923010, 4.369438628241273825, -0.2001145488402920614 ) ) ;
#18187=CARTESIAN_POINT ( 'NONE',  ( 0.1993543840281267465, 5.207027777853642903, 0.1993543840281266633 ) ) ;
#18189=CARTESIAN_POINT ( 'NONE',  ( 0.2309108437718781492, 4.203151657608736436, -0.2098260001596312652 ) ) ;
#18191=CARTESIAN_POINT ( 'NONE',  ( -0.2819296736111110979, 4.904944444520309865, -0.1167790944451422980 ) ) ;
#18194=CARTESIAN_POINT ( 'NONE',  ( -0.1539433478974299718, 4.067022932034428884, 0.2713770215894354965 ) ) ;
#18197=CARTESIAN_POINT ( 'NONE',  ( -0.1993543840281267465, 0.2506944443685777957, 0.1993543840281266633 ) ) ;
#18199=CARTESIAN_POINT ( 'NONE',  ( 0.1993543840281266910, 0.05624999992413336897, -0.1993543840281266910 ) ) ;
#18200=CARTESIAN_POINT ( 'NONE',  ( -0.01200529352568108395, 4.710829466525995102, -0.3120383712586302649 ) ) ;
#18203=CARTESIAN_POINT ( 'NONE',  ( -0.3119999999999998885, 4.498694444444443441, 0.1292346314604058410 ) ) ;
#18204=CARTESIAN_POINT ( 'NONE',  ( -0.2206173157302027676, 3.779944444444443441, 0.2206173157302028787 ) ) ;
#18207=CARTESIAN_POINT ( 'NONE',  ( -0.1993543840281266910, 4.470916666742532186, -0.1993543840281266910 ) ) ;
#18210=CARTESIAN_POINT ( 'NONE',  ( -1.853979398150703436E-06, 4.543833384706993606, -0.3119999999944916280 ) ) ;
#18212=CARTESIAN_POINT ( 'NONE',  ( 0.1993543840281266633, 5.123694444520309865, -0.1993543840281266910 ) ) ;
#18213=CARTESIAN_POINT ( 'NONE',  ( -0.009820766461577611073, 0.04330690836666935273, -0.2928069083666697825 ) ) ;
#18214=B_SPLINE_CURVE_WITH_KNOTS ( 'NONE', 3,
 ( #20777, #20543, #15177, #8082, #16998, #530, #18955, #17362, #13356, #7731, #22613, #13243, #9445, #7965, #15417, #5663, #3838, #22845, #6134, #4067, #11522, #170, #11280, #18710, #2008, #16879, #7611, #15063, #22485 ),
 .UNSPECIFIED., .F., .F.,
 ( 4, 2, 1, 1, 1, 1, 1, 2, 2, 2, 2, 2, 2, 2, 2, 2, 4 ),
 ( 0.3015379052287556205, 0.3015433052825606808, 0.3015487053363657965, 0.3015595054439759726, 0.3015811056591962691, 0.3016243060896369177, 0.3017107069505182704, 0.3018835086722808647, 0.3022291121158061644, 0.3029203190028567083, 0.3043027327769577961, 0.3056851465510588839, 0.3070675603251599717, 0.3084499740992610040, 0.3098323878733620917, 0.3112148016474631795, 0.3125972154215642673 ),
 .UNSPECIFIED. ) ;
#18215=CARTESIAN_POINT ( 'NONE',  ( 0.2725341921420746383, 4.914269569154003037, 0.1572748026637361685 ) ) ;
#18217=CARTESIAN_POINT ( 'NONE',  ( -0.2206173157302027676, 4.286888889040620931, 0.2206173157302028787 ) ) ;
#18218=EDGE_CURVE ( 'NONE', #1526, #4444, #13445, .T. ) ;
#18219=CARTESIAN_POINT ( 'NONE',  ( -0.2819296736111110424, 4.536888888964754507, 0.1167790944451424923 ) ) ;
#18220=CARTESIAN_POINT ( 'NONE',  ( -1.726321361862525858E-17, 3.838972222298087544, -0.2819296736111110979 ) ) ;
#18224=ORIENTED_EDGE ( 'NONE', *, *, #11828, .F. ) ;
#18226=CARTESIAN_POINT ( 'NONE',  ( -0.2206173157302027676, 4.279944444444443441, 0.2206173157302028787 ) ) ;
#18228=CARTESIAN_POINT ( 'NONE',  ( -5.731347020009612645E-17, 0.4486111111111107386, 0.3119999999999999996 ) ) ;
#18230=CARTESIAN_POINT ( 'NONE',  ( 0.2206173157302027676, 0.2263888887371559577, 0.2206173157302028787 ) ) ;
#18231=CARTESIAN_POINT ( 'NONE',  ( -0.001713203249405378893, 4.377212721013385988, -0.3119959714558495079 ) ) ;
#18232=CARTESIAN_POINT ( 'NONE',  ( -0.2258242712019069010, 5.122164547046700100, 0.2098372851225053237 ) ) ;
#18236=CARTESIAN_POINT ( 'NONE',  ( 0.2517364957946364168, 5.079917474983905556, 0.1844428286663916672 ) ) ;
#18238=CARTESIAN_POINT ( 'NONE',  ( 0.2819296736111110424, 4.161888888964755395, -0.1167790944451423396 ) ) ;
#18239=CARTESIAN_POINT ( 'NONE',  ( -0.1167790944451423119, 5.175777777853643791, -0.2819296736111110979 ) ) ;
#18242=CARTESIAN_POINT ( 'NONE',  ( -0.3119999999999999996, 4.106333333333332725, 0.000000000000000000 ) ) ;
#18244=CARTESIAN_POINT ( 'NONE',  ( -0.3119999999999999996, 5.002166666818398610, 0.000000000000000000 ) ) ;
#18246=CARTESIAN_POINT ( 'NONE',  ( -0.1993543840281266355, 5.095916666742533074, 0.1993543840281267465 ) ) ;
#18249=CARTESIAN_POINT ( 'NONE',  ( -0.2137897711831445446, 4.883875763723968255, -0.2274687474526748132 ) ) ;
#18253=ORIENTED_EDGE ( 'NONE', *, *, #11988, .T. ) ;
#18258=CARTESIAN_POINT ( 'NONE',  ( 0.1167790944451423535, 0.2055555554796889006, 0.2819296736111110979 ) ) ;
#18260=CARTESIAN_POINT ( 'NONE',  ( -1.726321361862525858E-17, 5.186194444520309865, -0.2819296736111110979 ) ) ;
#18261=CARTESIAN_POINT ( 'NONE',  ( 0.000000000000000000, 5.384999999999999787, -0.3119999999999999996 ) ) ;
#18263=CARTESIAN_POINT ( 'NONE',  ( -8.106877718569361257E-06, 3.766055773525306627, -0.3120000000431728537 ) ) ;
#18264=DIRECTION ( 'NONE',  ( 0.000000000000000000, 0.000000000000000000, -1.000000000000000000 ) ) ;
#18265=CARTESIAN_POINT ( 'NONE',  ( 0.0003703964654298149100, 4.877156714020134842, -0.3119998122762405734 ) ) ;
#18267=CARTESIAN_POINT ( 'NONE',  ( 0.3119999999999999996, 0.5701388887371559022, -0.1292346314604056468 ) ) ;
#18268=CARTESIAN_POINT ( 'NONE',  ( -1.910449006669871087E-17, 4.703555555555555046, -0.3119999999999999996 ) ) ;
#18269=CARTESIAN_POINT ( 'NONE',  ( -0.2819296736111110979, 4.075083333409199149, 0.000000000000000000 ) ) ;
#18270=CARTESIAN_POINT ( 'NONE',  ( -0.1167790944451423257, 3.856333333409198705, -0.2819296736111110424 ) ) ;
#18272=CARTESIAN_POINT ( 'NONE',  ( 0.3079291438910055634, 4.028372153496735386, 0.05528882331475011569 ) ) ;
#18273=DIRECTION ( 'NONE',  ( -1.000000000000000000, 0.000000000000000000, 0.000000000000000000 ) ) ;
#18277=CARTESIAN_POINT ( 'NONE',  ( 0.1167790944451424368, 4.536888888964754507, 0.2819296736111110424 ) ) ;
#18278=CARTESIAN_POINT ( 'NONE',  ( -0.3028095456829690835, 4.500036060564890583, -0.07595219160868893482 ) ) ;
#18281=CARTESIAN_POINT ( 'NONE',  ( 0.2819296736111110979, 3.783416666742532186, -3.452642723725051716E-17 ) ) ;
#18287=CARTESIAN_POINT ( 'NONE',  ( -0.1167790944451424368, 0.2402777777019111660, 0.2819296736111110424 ) ) ;
#18296=CARTESIAN_POINT ( 'NONE',  ( -1.910449006669871087E-17, 4.703555555555555046, -0.3119999999999999996 ) ) ;
#18297=CARTESIAN_POINT ( 'NONE',  ( -0.1292346314604056190, -0.02013888888888922327, -0.3119999999999999996 ) ) ;
#18298=CARTESIAN_POINT ( 'NONE',  ( -0.2819296736111110424, 3.925777777853644235, 0.1167790944451424923 ) ) ;
#18300=CARTESIAN_POINT ( 'NONE',  ( 0.2819296736111110979, 4.391055555631421470, 0.1167790944451422425 ) ) ;
#18303=CARTESIAN_POINT ( 'NONE',  ( -0.3119999999999998885, 4.609805555555555046, 0.1292346314604058410 ) ) ;
#18305=CARTESIAN_POINT ( 'NONE',  ( 0.3119999999999999996, 4.689666666666665762, -3.820898013339742174E-17 ) ) ;
#18306=CARTESIAN_POINT ( 'NONE',  ( 0.2819296736111110424, 5.106333333409198261, -0.1167790944451423396 ) ) ;
#18308=CARTESIAN_POINT ( 'NONE',  ( 0.2416695147500300678, 4.202697174923091694, -0.1973961377565022768 ) ) ;
#18311=CARTESIAN_POINT ( 'NONE',  ( 0.000000000000000000, 5.384999999999999787, 0.000000000000000000 ) ) ;
#18312=CARTESIAN_POINT ( 'NONE',  ( -0.2819296736111110979, 4.627166666742532186, -0.1167790944451422980 ) ) ;
#18314=CARTESIAN_POINT ( 'NONE',  ( -0.2246295819815997963, 4.064464186035761095, 0.2174240014552116795 ) ) ;
#18316=CARTESIAN_POINT ( 'NONE',  ( 0.2819296736111110424, 0.3236111110352444808, 0.1167790944451424923 ) ) ;
#18317=CARTESIAN_POINT ( 'NONE',  ( -0.2819296736111110979, 0.2472222221463555580, 0.1167790944451422425 ) ) ;
#18319=CARTESIAN_POINT ( 'NONE',  ( 4.312521114635084752E-13, 5.190332509204934830, -0.2890970118899086061 ) ) ;
#18322=CARTESIAN_POINT ( 'NONE',  ( -0.3119999999999999996, 3.772999999999999243, 0.000000000000000000 ) ) ;
#18324=CARTESIAN_POINT ( 'NONE',  ( -0.007226626051191389552, 3.877360830121420854, -0.3119999924289658666 ) ) ;
#18326=VECTOR ( 'NONE', #2312, 39.37007874015748143 ) ;
#18327=CARTESIAN_POINT ( 'NONE',  ( 0.1993543840281266633, 4.512583333409199149, -0.1993543840281266910 ) ) ;
#18329=CARTESIAN_POINT ( 'NONE',  ( 1.910449006669871087E-17, 0.2472222220704892726, -0.3119999999999999996 ) ) ;
#18330=CARTESIAN_POINT ( 'NONE',  ( -0.1993543840281266355, 4.984805555631421470, 0.1993543840281267465 ) ) ;
#18333=CARTESIAN_POINT ( 'NONE',  ( 0.3078657136106562886, 3.750759388707112230, 0.05066613946664001722 ) ) ;
#18334=CARTESIAN_POINT ( 'NONE',  ( -0.3119999999999999996, 0.4833333331816003775, -3.820898013339742174E-17 ) ) ;
#18335=CARTESIAN_POINT ( 'NONE',  ( -2.336494862270849996E-07, 3.904935224540334815, 0.3119999999998144258 ) ) ;
#18336=CARTESIAN_POINT ( 'NONE',  ( 0.2206173157302028787, 4.245222222373954857, 0.2206173157302027954 ) ) ;
#18337=CARTESIAN_POINT ( 'NONE',  ( 5.178964085587577574E-17, 4.491750000075866112, 0.2819296736111110979 ) ) ;
#18338=CARTESIAN_POINT ( 'NONE',  ( 0.2819296736111110979, 3.821611111186975940, 0.1167790944451422425 ) ) ;
#18341=ORIENTED_EDGE ( 'NONE', *, *, #9519, .F. ) ;
#18344=CARTESIAN_POINT ( 'NONE',  ( -0.2722860045487212055, 4.951277928273133178, 0.1577204527339934603 ) ) ;
#18347=CARTESIAN_POINT ( 'NONE',  ( -0.1292346314604056190, 0.1951388887371559855, -0.3119999999999999996 ) ) ;
#18349=CARTESIAN_POINT ( 'NONE',  ( -0.09970838333114330487, 5.126982898110991727, 0.2913680866046736151 ) ) ;
#18354=ORIENTED_EDGE ( 'NONE', *, *, #20764, .T. ) ;
#18356=CARTESIAN_POINT ( 'NONE',  ( 0.3091021031802769214, 5.086905331102652639, -0.04453840733622199677 ) ) ;
#18358=CARTESIAN_POINT ( 'NONE',  ( -0.2819296736111110424, 4.189666666742533074, 0.1167790944451424923 ) ) ;
#18359=CARTESIAN_POINT ( 'NONE',  ( -0.2819296736111110979, 5.186194444520309865, 0.000000000000000000 ) ) ;
#18361=CARTESIAN_POINT ( 'NONE',  ( -0.2804485321785814000, 4.228482938243210754, 0.1413885024074663377 ) ) ;
#18362=CARTESIAN_POINT ( 'NONE',  ( -1.910449006669871087E-17, 4.147999999999998799, -0.3119999999999999996 ) ) ;
#18363=CARTESIAN_POINT ( 'NONE',  ( -0.3119999999999999996, 4.946611111262843252, 0.000000000000000000 ) ) ;
#18364=CARTESIAN_POINT ( 'NONE',  ( 0.2819296736111110979, 5.061194444520310753, -3.452642723725051716E-17 ) ) ;
#18366=CARTESIAN_POINT ( 'NONE',  ( 0.1292346314604007063, 4.866749999999998799, -0.3120000000000049400 ) ) ;
#18369=CARTESIAN_POINT ( 'NONE',  ( 0.1962369407262708754, 0.03892726110517438776, -0.2116860911888880925 ) ) ;
#18370=ORIENTED_EDGE ( 'NONE', *, *, #4979, .T. ) ;
#18372=CARTESIAN_POINT ( 'NONE',  ( -0.1167790944451423535, 5.141055555631421470, 0.2819296736111110424 ) ) ;
#18375=LINE ( 'NONE', #1670, #903 ) ;
#18376=CARTESIAN_POINT ( 'NONE',  ( 0.1167790944451423119, 0.1708333332574666907, -0.2819296736111110979 ) ) ;
#18378=CARTESIAN_POINT ( 'NONE',  ( 0.2819296736111110979, 5.172305555631421470, -3.452642723725051716E-17 ) ) ;
#18381=CARTESIAN_POINT ( 'NONE',  ( -0.1993543840281266355, 4.859805555631421470, 0.1993543840281267465 ) ) ;
#18382=CARTESIAN_POINT ( 'NONE',  ( -0.3037999168084053458, 4.166440789197388028, -0.08196366530100891723 ) ) ;
#18384=CARTESIAN_POINT ( 'NONE',  ( 0.3119999999999999996, 4.578555555555555046, -3.820898013339742174E-17 ) ) ;
#18386=CARTESIAN_POINT ( 'NONE',  ( 0.1292346314604056190, 4.644527777777776478, -0.3119999999999999996 ) ) ;
#18387=CARTESIAN_POINT ( 'NONE',  ( 0.2819296736111110979, 3.991750000075865223, -3.452642723725051716E-17 ) ) ;
#18388=CARTESIAN_POINT ( 'NONE',  ( -1.726321361862525858E-17, 3.852861111186976828, -0.2819296736111110979 ) ) ;
#18389=CARTESIAN_POINT ( 'NONE',  ( 0.2274761419923447270, 4.036699467566920774, -0.2150353765082197166 ) ) ;
#18392=CARTESIAN_POINT ( 'NONE',  ( 3.820898013339742174E-17, 5.384999999999999787, 0.3119999999999999996 ) ) ;
#18394=CARTESIAN_POINT ( 'NONE',  ( -0.1167790944451423257, 4.342444444520310753, -0.2819296736111110424 ) ) ;
#18395=CARTESIAN_POINT ( 'NONE',  ( 7.699581739047377146E-15, 4.099388889040679551, -0.3119999999999999996 ) ) ;
#18398=VECTOR ( 'NONE', #12433, 39.37007874015748143 ) ;
#18401=CARTESIAN_POINT ( 'NONE',  ( -0.3119999857123673670, 3.945456803481290908, -0.04084082312690016925 ) ) ;
#18402=EDGE_CURVE ( 'NONE', #14350, #9142, #18375, .T. ) ;
#18403=CARTESIAN_POINT ( 'NONE',  ( -0.1917433973171703554, 4.438561529983626741, -0.2494925429433268727 ) ) ;
#18406=CARTESIAN_POINT ( 'NONE',  ( 0.1993543840281266355, 0.2506944443685777957, 0.1993543840281267465 ) ) ;
#18414=CARTESIAN_POINT ( 'NONE',  ( -0.3119999999999998885, 4.720916666666666650, 0.1292346314604058410 ) ) ;
#18415=CARTESIAN_POINT ( 'NONE',  ( -0.2819296736111110424, 0.5597222221463555858, -0.1167790944451423396 ) ) ;
#18416=CARTESIAN_POINT ( 'NONE',  ( 0.1993543840281266633, 3.790361111186977272, -0.1993543840281266910 ) ) ;
#18419=CARTESIAN_POINT ( 'NONE',  ( -1.726321361862525858E-17, 4.352861111186976828, -0.2819296736111110979 ) ) ;
#18424=CARTESIAN_POINT ( 'NONE',  ( 0.2612248564553516506, 4.358128745886941324, 0.1706105875377467718 ) ) ;
#18425=CARTESIAN_POINT ( 'NONE',  ( -0.1167790944451423535, 4.863277777853642903, 0.2819296736111110424 ) ) ;
#18426=CARTESIAN_POINT ( 'NONE',  ( 0.001983654329502046367, 4.210443755940678656, -0.3119945956041611512 ) ) ;
#18428=CARTESIAN_POINT ( 'NONE',  ( -0.1167790944451423119, 4.564666666742532186, -0.2819296736111110979 ) ) ;
#18436=CARTESIAN_POINT ( 'NONE',  ( 0.1993543840281266355, 0.3201388888130222710, 0.1993543840281267465 ) ) ;
#18441=CARTESIAN_POINT ( 'NONE',  ( -0.09537969278195178313, 3.879872140107286871, -0.2974432100491698483 ) ) ;
#18443=CARTESIAN_POINT ( 'NONE',  ( 0.2819296736111110979, 4.502166666742532186, 0.1167790944451422425 ) ) ;
#18446=CARTESIAN_POINT ( 'NONE',  ( -0.1993543840281266355, 5.095916666742533074, 0.1993543840281267465 ) ) ;
#18447=CARTESIAN_POINT ( 'NONE',  ( 0.1167790944451422702, 4.502166666742532186, -0.2819296736111110979 ) ) ;
#18448=CARTESIAN_POINT ( 'NONE',  ( 0.1575217432702256393, 4.928054411463135054, -0.2724113156736405750 ) ) ;
#18450=CARTESIAN_POINT ( 'NONE',  ( -0.1292346314604058410, 0.4937499998482670627, 0.3119999999999998885 ) ) ;
#18451=B_SPLINE_CURVE_WITH_KNOTS ( 'NONE', 3,
 ( #9375, #4002, #2186, #7895, #13535, #16929, #22293, #24114, #5588, #9496, #19004, #20829, #15346, #225, #17049, #18637, #7662, #9741, #343, #1807, #7428, #22773, #4241, #16818, #15112, #22538, #20472, #18517, #9252, #13292, #15229, #14990 ),
 .UNSPECIFIED., .F., .F.,
 ( 4, 2, 1, 1, 1, 1, 2, 2, 2, 2, 2, 2, 2, 2, 2, 2, 2, 4 ),
 ( 0.3746381435405087279, 0.3746563456430798134, 0.3746745477456508988, 0.3747109519507930697, 0.3747837603610774670, 0.3749293771816462062, 0.3752206108227836290, 0.3758030781050585301, 0.3769680126696083322, 0.3792978817987079920, 0.3816277509278076518, 0.3839576200569072562, 0.3845400873391821572, 0.3851225546214570583, 0.3862874891860069160, 0.3886173583151065203, 0.3909472274442061801, 0.3932770965733057844 ),
 .UNSPECIFIED. ) ;
#18452=CARTESIAN_POINT ( 'NONE',  ( 0.06495106723445233377, 3.906766557144303764, 0.3070669447693011866 ) ) ;
#18453=CARTESIAN_POINT ( 'NONE',  ( -0.2206173157302028232, 4.384111111262843252, -0.2206173157302028232 ) ) ;
#18455=CARTESIAN_POINT ( 'NONE',  ( 0.1167790944451422702, 4.460500000075867000, -0.2819296736111110979 ) ) ;
#18456=CARTESIAN_POINT ( 'NONE',  ( 0.2819296736111110979, 3.936194444520309865, -3.452642723725051716E-17 ) ) ;
#18457=EDGE_LOOP ( 'NONE', ( #8559, #5299, #2982, #6498 ) ) ;
#18458=ORIENTED_EDGE ( 'NONE', *, *, #9010, .F. ) ;
#18460=EDGE_CURVE ( 'NONE', #22975, #3340, #5713, .T. ) ;
#18462=CARTESIAN_POINT ( 'NONE',  ( 0.000000000000000000, 5.384999999999999787, 0.000000000000000000 ) ) ;
#18464=CARTESIAN_POINT ( 'NONE',  ( 0.1292346314604058410, 4.234805555555554157, 0.3119999999999998885 ) ) ;
#18467=CARTESIAN_POINT ( 'NONE',  ( 0.3119999999999999996, 0.5111111109593782231, 0.000000000000000000 ) ) ;
#18469=CARTESIAN_POINT ( 'NONE',  ( -0.2962237115742567539, 3.727440431103998808, 0.1082426406064014301 ) ) ;
#18472=ORIENTED_EDGE ( 'NONE', *, *, #3343, .F. ) ;
#18474=CARTESIAN_POINT ( 'NONE',  ( 0.1816571697360684357, 5.094271231115367726, -0.2535119103260691786 ) ) ;
#18476=B_SPLINE_CURVE_WITH_KNOTS ( 'NONE', 3,
 ( #19736, #11838, #21209, #2790, #12085, #10128, #15487, #3365, #21088, #4378, #10244, #10009, #19615, #8388, #2908, #725, #10366, #6689, #21564, #17432, #9222, #24083, #5677, #7154, #2022, #11295, #1777, #14956, #7274, #9341, #20318, #16424, #18483, #14843, #11178, #64, #185, #15076, #9092 ),
 .UNSPECIFIED., .F., .F.,
 ( 4, 2, 2, 2, 2, 2, 1, 1, 1, 1, 2, 2, 1, 2, 2, 2, 2, 2, 2, 2, 2, 4 ),
 ( 0.2649879068747749700, 0.2673297384506001517, 0.2696715700264253890, 0.2720134016022505707, 0.2731843173901631894, 0.2743552331780757525, 0.2745015976515648437, 0.2745747798883093616, 0.2746113710066816482, 0.2746205187862747477, 0.2746250926760712696, 0.2746296665658677916, 0.2746479621250539349, 0.2749406910720321173, 0.2755261489659885932, 0.2766970647539014894, 0.2778679805418143300, 0.2790388963297272262, 0.2802098121176401224, 0.2813807279055530186, 0.2825516436934658593, 0.2837225594813787555 ),
 .UNSPECIFIED. ) ;
#18477=CARTESIAN_POINT ( 'NONE',  ( 0.2819296736111110424, 4.273000000075865223, -0.1167790944451423396 ) ) ;
#18478=CARTESIAN_POINT ( 'NONE',  ( 0.1993543840281266633, 5.054250000075865223, -0.1993543840281266910 ) ) ;
#18480=CARTESIAN_POINT ( 'NONE',  ( -0.3120253914852480492, 4.224625367392181197, 0.009383917684771203582 ) ) ;
#18481=CARTESIAN_POINT ( 'NONE',  ( -1.910449006669871087E-17, 3.814666666666665762, -0.3119999999999999996 ) ) ;
#18482=CARTESIAN_POINT ( 'NONE',  ( -0.3119999999999999996, 4.891055555707287894, 0.000000000000000000 ) ) ;
#18483=CARTESIAN_POINT ( 'NONE',  ( 0.2252594654730211976, 4.800977599731078627, 0.2171865793878193507 ) ) ;
#18489=CARTESIAN_POINT ( 'NONE',  ( 0.2839242323463955775, 0.03423162783098992329, 0.004826162406255454784 ) ) ;
#18492=CARTESIAN_POINT ( 'NONE',  ( -0.2819296736111110979, 5.019527777853642903, 0.000000000000000000 ) ) ;
#18493=VERTEX_POINT ( 'NONE', #7761 ) ;
#18496=CARTESIAN_POINT ( 'NONE',  ( 0.1167790944451423119, 0.3374999999241333759, -0.2819296736111110979 ) ) ;
#18498=CARTESIAN_POINT ( 'NONE',  ( 0.1993543840281266633, 4.957027777853642903, -0.1993543840281266910 ) ) ;
#18500=AXIS2_PLACEMENT_3D ( 'NONE', #2889, #6548, #10347 ) ;
#18501=ORIENTED_EDGE ( 'NONE', *, *, #4976, .F. ) ;
#18502=CARTESIAN_POINT ( 'NONE',  ( -0.1167790944451423535, 4.863277777853642903, 0.2819296736111110424 ) ) ;
#18506=CARTESIAN_POINT ( 'NONE',  ( -5.731347020009612645E-17, 0.5527777776260448528, 0.3119999999999999996 ) ) ;
#18507=CARTESIAN_POINT ( 'NONE',  ( 0.3119999999999999996, 4.467444444444443441, -3.820898013339742174E-17 ) ) ;
#18508=CARTESIAN_POINT ( 'NONE',  ( 0.1167790944451424506, 3.981333333409199593, 0.2819296736111110424 ) ) ;
#18509=CARTESIAN_POINT ( 'NONE',  ( -0.2819296736111110424, 3.814666666742532630, 0.1167790944451424923 ) ) ;
#18510=CARTESIAN_POINT ( 'NONE',  ( 0.08174725030332795350, 4.018423240896470183, 0.3038629659492873003 ) ) ;
#18511=CYLINDRICAL_SURFACE ( 'NONE', #22998, 0.3119999999999999996 ) ;
#18517=CARTESIAN_POINT ( 'NONE',  ( 0.2022309808788627650, 4.633432797117196245, 0.2408951298654545825 ) ) ;
#18520=CARTESIAN_POINT ( 'NONE',  ( -0.1571332995722349857, 4.437395902338867160, -0.2726191217874048278 ) ) ;
#18525=CARTESIAN_POINT ( 'NONE',  ( 0.2819296736111110979, 0.3131944443685777957, 0.000000000000000000 ) ) ;
#18527=DIRECTION ( 'NONE',  ( 0.000000000000000000, 0.000000000000000000, 1.000000000000000000 ) ) ;
#18532=DIRECTION ( 'NONE',  ( 1.000000000000000000, -0.000000000000000000, 1.224646799147353207E-16 ) ) ;
#18534=CARTESIAN_POINT ( 'NONE',  ( -0.1292346314604056190, 0.03541666666666633267, -0.3119999999999999996 ) ) ;
#18535=CARTESIAN_POINT ( 'NONE',  ( -0.2819296736111110424, 3.870222222298087988, 0.1167790944451424923 ) ) ;
#18538=CARTESIAN_POINT ( 'NONE',  ( 0.1167790944451422702, 4.516055555631421470, -0.2819296736111110424 ) ) ;
#18543=CARTESIAN_POINT ( 'NONE',  ( -0.2819296736111110424, 4.849388888964755395, -0.1167790944451423119 ) ) ;
#18544=EDGE_CURVE ( 'NONE', #11560, #14570, #23681, .T. ) ;
#18545=CARTESIAN_POINT ( 'NONE',  ( -0.3008913205206853458, 5.155183786276188229, -0.01229715577229057756 ) ) ;
#18550=CARTESIAN_POINT ( 'NONE',  ( -0.1167790944451423535, 4.752166666742531298, 0.2819296736111110979 ) ) ;
#18552=CARTESIAN_POINT ( 'NONE',  ( 0.1292346314604000956, 4.922305555555555046, -0.3120000000000054952 ) ) ;
#18553=CARTESIAN_POINT ( 'NONE',  ( 1.726321361862525858E-17, 0.5076388888130222155, -0.2819296736111110979 ) ) ;
#18556=CARTESIAN_POINT ( 'NONE',  ( 0.1993543840281266910, 0.2784722221463555858, -0.1993543840281266910 ) ) ;
#18558=CARTESIAN_POINT ( 'NONE',  ( -0.02753534767366182245, 5.190979356084988616, -0.2888344835192422910 ) ) ;
#18564=CARTESIAN_POINT ( 'NONE',  ( 0.1167790944451423535, 0.3027777777019111105, 0.2819296736111110979 ) ) ;
#18565=CARTESIAN_POINT ( 'NONE',  ( -0.2819296736111110979, 0.01111111103524447911, 0.1167790944451422425 ) ) ;
#18567=CARTESIAN_POINT ( 'NONE',  ( -1.726321361862525858E-17, 4.519527777853643791, -0.2819296736111110979 ) ) ;
#18570=CARTESIAN_POINT ( 'NONE',  ( -1.726321361862525858E-17, 5.019527777853643791, -0.2819296736111110979 ) ) ;
#18571=CARTESIAN_POINT ( 'NONE',  ( -0.2819296736111110979, 4.404944444520309865, -0.1167790944451422980 ) ) ;
#18572=CARTESIAN_POINT ( 'NONE',  ( 0.08942137597415596162, 3.740864561460785165, 0.2997242127448243032 ) ) ;
#18575=CARTESIAN_POINT ( 'NONE',  ( 0.02489560895761679105, 3.932016240302184773, -0.3119999658293151068 ) ) ;
#18576=CARTESIAN_POINT ( 'NONE',  ( -0.3119999999999999996, 4.002166666818398610, 0.000000000000000000 ) ) ;
#18577=EDGE_CURVE ( 'NONE', #1519, #16287, #12146, .T. ) ;
#18578=CARTESIAN_POINT ( 'NONE',  ( -0.1167790944451423535, 4.599388888964754507, 0.2819296736111110979 ) ) ;
#18581=ORIENTED_EDGE ( 'NONE', *, *, #5929, .F. ) ;
#18582=VERTEX_POINT ( 'NONE', #21744 ) ;
#18584=CARTESIAN_POINT ( 'NONE',  ( 5.731347020009612645E-17, 4.286888888888888083, 0.3119999999999999996 ) ) ;
#18585=CARTESIAN_POINT ( 'NONE',  ( -0.09230038814513606693, 4.846752338702703611, 0.2982970817797798713 ) ) ;
#18587=ORIENTED_EDGE ( 'NONE', *, *, #22918, .F. ) ;
#18588=CARTESIAN_POINT ( 'NONE',  ( 0.3119999999999999996, 0.4555555554038225874, 0.000000000000000000 ) ) ;
#18590=EDGE_LOOP ( 'NONE', ( #14051, #2113, #21122, #9613 ) ) ;
#18591=DIRECTION ( 'NONE',  ( -0.000000000000000000, -1.000000000000000000, -0.000000000000000000 ) ) ;
#18594=CARTESIAN_POINT ( 'NONE',  ( 0.2496703805607334292, 3.980133472758900393, -0.1915199933392999210 ) ) ;
#18598=CARTESIAN_POINT ( 'NONE',  ( 0.03852881856483229839, 5.098954151918542621, -0.3091372944403406042 ) ) ;
#18600=CARTESIAN_POINT ( 'NONE',  ( -1.726321361862525858E-17, 4.283416666742532186, -0.2819296736111110979 ) ) ;
#18601=CARTESIAN_POINT ( 'NONE',  ( 0.1993543840281266633, 5.109805555631420582, -0.1993543840281266910 ) ) ;
#18603=CARTESIAN_POINT ( 'NONE',  ( 0.3119999999999999996, 3.804249999999999243, -0.1292346314604056745 ) ) ;
#18605=CARTESIAN_POINT ( 'NONE',  ( -0.3119999999999999996, 4.720916666818398610, -0.1292346314604056468 ) ) ;
#18606=CARTESIAN_POINT ( 'NONE',  ( -0.2819296736111110979, 5.141055555631421470, -0.1167790944451422980 ) ) ;
#18615=CARTESIAN_POINT ( 'NONE',  ( -0.1167790944451423257, 5.175777777853644679, -0.2819296736111110424 ) ) ;
#18618=AXIS2_PLACEMENT_3D ( 'NONE', #13288, #575, #3994 ) ;
#18619=CARTESIAN_POINT ( 'NONE',  ( 0.1167790944451423535, 0.3166666665908000056, 0.2819296736111110979 ) ) ;
#18621=CARTESIAN_POINT ( 'NONE',  ( -0.1993543840281266910, 4.970916666742532186, -0.1993543840281266910 ) ) ;
#18622=LINE ( 'NONE', #18261, #18655 ) ;
#18623=CARTESIAN_POINT ( 'NONE',  ( -0.2819296736111110979, 4.852861111186976828, 0.000000000000000000 ) ) ;
#18624=CYLINDRICAL_SURFACE ( 'NONE', #23127, 0.3119999999999999996 ) ;
#18625=( BOUNDED_SURFACE ( )  B_SPLINE_SURFACE ( 1, 2, ( 
 ( #22218, #20278, #14554, #5272, #7351, #3564, #5518, #12981, #3689, #18565, #14682, #20398, #22336, #11018, #20, #5639, #18683, #20517, #9056, #22099, #11136, #7588, #1984, #1854, #3933, #16503, #11376, #15039, #16860, #22462, #12742, #13221, #3445, #20632, #8937, #10896, #23914, #7235, #5395, #17101, #17222, #13580, #22937, #6111, #6233, #20990, #13698, #506, #269, #19049, #11992, #13456, #21115, #22821, #17457, #9791, #388, #20873, #7827, #13332, #4405, #9907, #2099, #2589, #9540, #8178, #8063, #15393, #5870, #16973, #11741, #11868, #4167, #18933, #19282, #6358, #19163, #7939, #10035, #11617, #2351, #5991, #2470, #15511, #4286, #17339, #750, #632, #15632, #21239, #2231, #4529, #23050, #13805, #7708, #15155, #22585, #20754, #4045, #11498, #9663, #15273, #22701, #3061, #10272, #10397, #6715, #16109, #23407, #23522, #14160, #6839, #17820, #17578, #12230, #5118, #6596, #14279, #15986, #10626, #2939, #17697, #14044, #989, #6475, #21717, #10508, #19404, #19883, #2703, #1351, #1235, #8544, #23165, #10154, #4883, #5000, #21475, #12113, #12462, #23644, #12348, #1110, #3176, #4758, #19640, #23282, #19765, #8660, #21590, #17939, #2816, #18055, #8782, #16234, #14404, #6963, #13928, #868, #21358, #21828, #8301, #15753, #4646, #19523, #8418, #15866, #18415, #3781, #12954, #20007, #1472, #12830, #20366, #22430, #5365, #7323, #7441, #12712, #16473, #1709 ),
 ( #9148, #7557, #18653, #10990, #7202, #18297, #16591, #23883, #10747, #3293, #22069, #14648, #24013, #14774, #22189, #5488, #1595, #3657, #1824, #20249, #11104, #18534, #14888, #24126, #5240, #9030, #9269, #16709, #3418, #3537, #22307, #5605, #13070, #20485, #11225, #1946, #9392, #18179, #16832, #12584, #115, #15010, #8909, #16353, #23764, #10868, #7085, #14524, #21947, #20126, #13550, #15600, #6203, #13190, #11831, #11709, #19022, #9510, #20604, #15361, #600, #17064, #22553, #8031, #10003, #22790, #20844, #2436, #357, #7798, #9634, #6083, #19132, #4134, #15241, #13307, #20964, #4258, #19250, #720, #11591, #16943, #3901, #242, #2317, #13669, #15482, #2556, #22671, #9878, #15127, #9754, #21083, #17307, #11346, #18773, #5960, #22908, #5731, #13422, #477, #4373, #5844, #17191, #7909, #17427, #2069, #7677, #8148, #20722, #4018, #11468, #18901, #2201, #21442, #17665, #4615, #12200, #10237, #21203, #6324, #8382, #951, #4728, #19607, #17784, #8508, #12077, #10361, #12316, #15832, #6683, #4848, #17908, #10478, #15718, #19490, #23251, #14249, #21557, #1077, #18024, #23132, #1321, #21684, #16079, #14011, #13776, #19848, #17547, #6561, #10596, #1203, #2672, #8634, #10122, #15949, #14128, #13897, #2902, #23375, #19728, #3031, #23491, #6807, #4967, #12434, #4495, #3146, #8746, #23023, #11960, #19375, #840, #8269, #21326, #6445, #2784, #3262, #3626, #23985 ) ),
 .UNSPECIFIED., .F., .F., .F. ) 
 B_SPLINE_SURFACE_WITH_KNOTS ( ( 2, 2 ),
 ( 3, 2, 2, 2, 2, 2, 2, 2, 2, 2, 2, 2, 2, 2, 2, 2, 2, 2, 2, 2, 2, 2, 2, 2, 2, 2, 2, 2, 2, 2, 2, 2, 2, 2, 2, 2, 2, 2, 2, 2, 2, 2, 2, 2, 2, 2, 2, 2, 2, 2, 2, 2, 2, 2, 2, 2, 2, 2, 2, 2, 2, 2, 2, 2, 2, 2, 2, 2, 2, 2, 2, 2, 2, 2, 2, 2, 2, 2, 2, 2, 2, 2, 2, 2, 2, 2, 2, 2, 2, 2, 3 ),
 ( 0.000000000000000000, 1.000000000000000000 ),
 ( 0.000000000000000000, 0.01041666666666666609, 0.02083333333333333218, 0.03125000000000000000, 0.04166666666666666435, 0.05208333333333333565, 0.06250000000000000000, 0.07291666666666667129, 0.08333333333333332871, 0.09375000000000000000, 0.1041666666666666713, 0.1145833333333333287, 0.1250000000000000000, 0.1354166666666666574, 0.1458333333333333426, 0.1562500000000000000, 0.1666666666666666574, 0.1770833333333333426, 0.1875000000000000000, 0.1979166666666666574, 0.2083333333333333426, 0.2187500000000000000, 0.2291666666666666574, 0.2395833333333333426, 0.2500000000000000000, 0.2604166666666666852, 0.2708333333333333148, 0.2812500000000000000, 0.2916666666666666852, 0.3020833333333333148, 0.3125000000000000000, 0.3229166666666666852, 0.3333333333333333148, 0.3437500000000000000, 0.3541666666666666852, 0.3645833333333333148, 0.3750000000000000000, 0.3854166666666666852, 0.3958333333333333148, 0.4062500000000000000, 0.4166666666666666852, 0.4270833333333333148, 0.4375000000000000000, 0.4479166666666666852, 0.4583333333333333148, 0.4687500000000000000, 0.4791666666666666852, 0.4895833333333333148, 0.5000000000000000000, 0.5104166666666666297, 0.5208333333333333703, 0.5312500000000000000, 0.5416666666666666297, 0.5520833333333333703, 0.5625000000000000000, 0.5729166666666666297, 0.5833333333333333703, 0.5937500000000000000, 0.6041666666666666297, 0.6145833333333333703, 0.6250000000000000000, 0.6354166666666666297, 0.6458333333333333703, 0.6562500000000000000, 0.6666666666666666297, 0.6770833333333333703, 0.6875000000000000000, 0.6979166666666666297, 0.7083333333333333703, 0.7187500000000000000, 0.7291666666666666297, 0.7395833333333333703, 0.7500000000000000000, 0.7604166666666666297, 0.7708333333333333703, 0.7812500000000000000, 0.7916666666666666297, 0.8020833333333333703, 0.8125000000000000000, 0.8229166666666666297, 0.8333333333333333703, 0.8437500000000000000, 0.8541666666666666297, 0.8645833333333333703, 0.8750000000000000000, 0.8854166666666666297, 0.8958333333333333703, 0.9062500000000000000, 0.9166666666666666297, 0.9270833333333333703, 0.9375000000000000000 ),
 .UNSPECIFIED. ) 
 GEOMETRIC_REPRESENTATION_ITEM ( )  RATIONAL_B_SPLINE_SURFACE ( (
 ( 1.000000000000000000, 0.9238795325112867385, 1.000000000000000000, 0.9238795325112867385, 1.000000000000000000, 0.9238795325112867385, 1.000000000000000000, 0.9238795325112867385, 1.000000000000000000, 0.9238795325112867385, 1.000000000000000000, 0.9238795325112867385, 1.000000000000000000, 0.9238795325112867385, 1.000000000000000000, 0.9238795325112867385, 1.000000000000000000, 0.9238795325112867385, 1.000000000000000000, 0.9238795325112867385, 1.000000000000000000, 0.9238795325112867385, 1.000000000000000000, 0.9238795325112867385, 1.000000000000000000, 0.9238795325112867385, 1.000000000000000000, 0.9238795325112867385, 1.000000000000000000, 0.9238795325112867385, 1.000000000000000000, 0.9238795325112867385, 1.000000000000000000, 0.9238795325112867385, 1.000000000000000000, 0.9238795325112867385, 1.000000000000000000, 0.9238795325112867385, 1.000000000000000000, 0.9238795325112867385, 1.000000000000000000, 0.9238795325112867385, 1.000000000000000000, 0.9238795325112867385, 1.000000000000000000, 0.9238795325112867385, 1.000000000000000000, 0.9238795325112867385, 1.000000000000000000, 0.9238795325112867385, 1.000000000000000000, 0.9238795325112867385, 1.000000000000000000, 0.9238795325112867385, 1.000000000000000000, 0.9238795325112867385, 1.000000000000000000, 0.9238795325112867385, 1.000000000000000000, 0.9238795325112867385, 1.000000000000000000, 0.9238795325112867385, 1.000000000000000000, 0.9238795325112867385, 1.000000000000000000, 0.9238795325112867385, 1.000000000000000000, 0.9238795325112867385, 1.000000000000000000, 0.9238795325112867385, 1.000000000000000000, 0.9238795325112867385, 1.000000000000000000, 0.9238795325112867385, 1.000000000000000000, 0.9238795325112867385, 1.000000000000000000, 0.9238795325112867385, 1.000000000000000000, 0.9238795325112867385, 1.000000000000000000, 0.9238795325112867385, 1.000000000000000000, 0.9238795325112867385, 1.000000000000000000, 0.9238795325112867385, 1.000000000000000000, 0.9238795325112867385, 1.000000000000000000, 0.9238795325112867385, 1.000000000000000000, 0.9238795325112867385, 1.000000000000000000, 0.9238795325112867385, 1.000000000000000000, 0.9238795325112867385, 1.000000000000000000, 0.9238795325112867385, 1.000000000000000000, 0.9238795325112867385, 1.000000000000000000, 0.9238795325112867385, 1.000000000000000000, 0.9238795325112867385, 1.000000000000000000, 0.9238795325112867385, 1.000000000000000000, 0.9238795325112867385, 1.000000000000000000, 0.9238795325112867385, 1.000000000000000000, 0.9238795325112867385, 1.000000000000000000, 0.9238795325112867385, 1.000000000000000000, 0.9238795325112867385, 1.000000000000000000, 0.9238795325112867385, 1.000000000000000000, 0.9238795325112867385, 1.000000000000000000, 0.9238795325112867385, 1.000000000000000000, 0.9238795325112867385, 1.000000000000000000, 0.9238795325112867385, 1.000000000000000000, 0.9238795325112867385, 1.000000000000000000, 0.9238795325112867385, 1.000000000000000000, 0.9238795325112867385, 1.000000000000000000, 0.9238795325112867385, 1.000000000000000000, 0.9238795325112867385, 1.000000000000000000, 0.9238795325112867385, 1.000000000000000000, 0.9238795325112867385, 1.000000000000000000, 0.9238795325112867385, 1.000000000000000000, 0.9238795325112867385, 1.000000000000000000, 0.9238795325112867385, 1.000000000000000000, 0.9238795325112867385, 1.000000000000000000, 0.9238795325112867385, 1.000000000000000000, 0.9238795325112867385, 1.000000000000000000, 0.9238795325112867385, 1.000000000000000000, 0.9238795325112867385, 1.000000000000000000, 0.9238795325112867385, 1.000000000000000000, 0.9238795325112867385, 1.000000000000000000, 0.9238795325112867385, 1.000000000000000000, 0.9238795325112867385, 1.000000000000000000, 0.9238795325112867385, 1.000000000000000000, 0.9238795325112867385, 1.000000000000000000, 0.9238795325112867385, 1.000000000000000000, 0.9238795325112867385, 1.000000000000000000, 0.9238795325112867385, 1.000000000000000000, 0.9238795325112867385, 1.000000000000000000, 0.9238795325112867385, 1.000000000000000000, 0.9238795325112867385, 1.000000000000000000),
 ( 1.000000000000000000, 0.9238795325112867385, 1.000000000000000000, 0.9238795325112867385, 1.000000000000000000, 0.9238795325112867385, 1.000000000000000000, 0.9238795325112867385, 1.000000000000000000, 0.9238795325112867385, 1.000000000000000000, 0.9238795325112867385, 1.000000000000000000, 0.9238795325112867385, 1.000000000000000000, 0.9238795325112867385, 1.000000000000000000, 0.9238795325112867385, 1.000000000000000000, 0.9238795325112867385, 1.000000000000000000, 0.9238795325112867385, 1.000000000000000000, 0.9238795325112867385, 1.000000000000000000, 0.9238795325112867385, 1.000000000000000000, 0.9238795325112867385, 1.000000000000000000, 0.9238795325112867385, 1.000000000000000000, 0.9238795325112867385, 1.000000000000000000, 0.9238795325112867385, 1.000000000000000000, 0.9238795325112867385, 1.000000000000000000, 0.9238795325112867385, 1.000000000000000000, 0.9238795325112867385, 1.000000000000000000, 0.9238795325112867385, 1.000000000000000000, 0.9238795325112867385, 1.000000000000000000, 0.9238795325112867385, 1.000000000000000000, 0.9238795325112867385, 1.000000000000000000, 0.9238795325112867385, 1.000000000000000000, 0.9238795325112867385, 1.000000000000000000, 0.9238795325112867385, 1.000000000000000000, 0.9238795325112867385, 1.000000000000000000, 0.9238795325112867385, 1.000000000000000000, 0.9238795325112867385, 1.000000000000000000, 0.9238795325112867385, 1.000000000000000000, 0.9238795325112867385, 1.000000000000000000, 0.9238795325112867385, 1.000000000000000000, 0.9238795325112867385, 1.000000000000000000, 0.9238795325112867385, 1.000000000000000000, 0.9238795325112867385, 1.000000000000000000, 0.9238795325112867385, 1.000000000000000000, 0.9238795325112867385, 1.000000000000000000, 0.9238795325112867385, 1.000000000000000000, 0.9238795325112867385, 1.000000000000000000, 0.9238795325112867385, 1.000000000000000000, 0.9238795325112867385, 1.000000000000000000, 0.9238795325112867385, 1.000000000000000000, 0.9238795325112867385, 1.000000000000000000, 0.9238795325112867385, 1.000000000000000000, 0.9238795325112867385, 1.000000000000000000, 0.9238795325112867385, 1.000000000000000000, 0.9238795325112867385, 1.000000000000000000, 0.9238795325112867385, 1.000000000000000000, 0.9238795325112867385, 1.000000000000000000, 0.9238795325112867385, 1.000000000000000000, 0.9238795325112867385, 1.000000000000000000, 0.9238795325112867385, 1.000000000000000000, 0.9238795325112867385, 1.000000000000000000, 0.9238795325112867385, 1.000000000000000000, 0.9238795325112867385, 1.000000000000000000, 0.9238795325112867385, 1.000000000000000000, 0.9238795325112867385, 1.000000000000000000, 0.9238795325112867385, 1.000000000000000000, 0.9238795325112867385, 1.000000000000000000, 0.9238795325112867385, 1.000000000000000000, 0.9238795325112867385, 1.000000000000000000, 0.9238795325112867385, 1.000000000000000000, 0.9238795325112867385, 1.000000000000000000, 0.9238795325112867385, 1.000000000000000000, 0.9238795325112867385, 1.000000000000000000, 0.9238795325112867385, 1.000000000000000000, 0.9238795325112867385, 1.000000000000000000, 0.9238795325112867385, 1.000000000000000000, 0.9238795325112867385, 1.000000000000000000, 0.9238795325112867385, 1.000000000000000000, 0.9238795325112867385, 1.000000000000000000, 0.9238795325112867385, 1.000000000000000000, 0.9238795325112867385, 1.000000000000000000, 0.9238795325112867385, 1.000000000000000000, 0.9238795325112867385, 1.000000000000000000, 0.9238795325112867385, 1.000000000000000000, 0.9238795325112867385, 1.000000000000000000, 0.9238795325112867385, 1.000000000000000000, 0.9238795325112867385, 1.000000000000000000, 0.9238795325112867385, 1.000000000000000000, 0.9238795325112867385, 1.000000000000000000, 0.9238795325112867385, 1.000000000000000000, 0.9238795325112867385, 1.000000000000000000, 0.9238795325112867385, 1.000000000000000000, 0.9238795325112867385, 1.000000000000000000, 0.9238795325112867385, 1.000000000000000000, 0.9238795325112867385, 1.000000000000000000, 0.9238795325112867385, 1.000000000000000000, 0.9238795325112867385, 1.000000000000000000) ) ) 
 REPRESENTATION_ITEM ( '' )  SURFACE ( )  );
#18627=CARTESIAN_POINT ( 'NONE',  ( -8.379073922441706732E-07, 4.293833316950179224, 0.3119999999988748440 ) ) ;
#18629=CARTESIAN_POINT ( 'NONE',  ( -0.3119999999999999996, 4.602861111111111292, -0.1292346314604056468 ) ) ;
#18630=CARTESIAN_POINT ( 'NONE',  ( 0.1993543840281267465, 3.818138888964754507, 0.1993543840281266633 ) ) ;
#18637=CARTESIAN_POINT ( 'NONE',  ( 0.2667111700250733852, 4.645955859489413697, -0.1672198252236019589 ) ) ;
#18645=CARTESIAN_POINT ( 'NONE',  ( -0.2819296736111110979, 0.2854166665908000611, -3.452642723725051716E-17 ) ) ;
#18646=CARTESIAN_POINT ( 'NONE',  ( 0.1571321947316088596, 3.872627114028808659, -0.2726197584672552243 ) ) ;
#18649=CARTESIAN_POINT ( 'NONE',  ( 1.726321361862525858E-17, 0.6048611110352445364, -0.2819296736111110979 ) ) ;
#18652=DIRECTION ( 'NONE',  ( -0.000000000000000000, -1.000000000000000000, -0.000000000000000000 ) ) ;
#18653=CARTESIAN_POINT ( 'NONE',  ( 0.2206173157302028232, -0.03055555555555588762, -0.2206173157302028232 ) ) ;
#18654=CARTESIAN_POINT ( 'NONE',  ( 0.1292346314604058410, 5.068138888888887195, 0.3119999999999998885 ) ) ;
#18655=VECTOR ( 'NONE', #10707, 39.37007874015748143 ) ;
#18657=CARTESIAN_POINT ( 'NONE',  ( -0.1993543840281266355, 4.207027777853643791, 0.1993543840281267465 ) ) ;
#18658=CARTESIAN_POINT ( 'NONE',  ( 0.3119999999999999996, 0.1222222220704892864, 0.000000000000000000 ) ) ;
#18661=LINE ( 'NONE', #14413, #7380 ) ;
#18662=CARTESIAN_POINT ( 'NONE',  ( 0.2819296736111110424, 5.050777777853643791, -0.1167790944451423396 ) ) ;
#18663=CARTESIAN_POINT ( 'NONE',  ( -0.2854617896337424132, 5.152931539520130499, -0.09929655918317221996 ) ) ;
#18668=CARTESIAN_POINT ( 'NONE',  ( -1.726321361862525858E-17, 4.616750000075865223, -0.2819296736111110979 ) ) ;
#18671=CARTESIAN_POINT ( 'NONE',  ( -1.910449006669871087E-17, 4.925777777777777366, -0.3119999999999999996 ) ) ;
#18672=CARTESIAN_POINT ( 'NONE',  ( -0.2819296736111110979, 0.5770833332574666352, -3.452642723725051716E-17 ) ) ;
#18674=CARTESIAN_POINT ( 'NONE',  ( -0.1993543840281267465, 0.3062499999241333759, 0.1993543840281266633 ) ) ;
#18682=CARTESIAN_POINT ( 'NONE',  ( -5.178964085587577574E-17, 0.3548611110352444808, 0.2819296736111110979 ) ) ;
#18683=CARTESIAN_POINT ( 'NONE',  ( 0.2819296736111110979, 0.03541666659080003332, 0.000000000000000000 ) ) ;
#18684=CARTESIAN_POINT ( 'NONE',  ( -0.1993543840281266910, 4.193138888964754507, -0.1993543840281266910 ) ) ;
#18686=CARTESIAN_POINT ( 'NONE',  ( -0.2819296736111110979, 5.200083333409199149, 0.000000000000000000 ) ) ;
#18687=CARTESIAN_POINT ( 'NONE',  ( 5.178964085587577574E-17, 4.477861111186976828, 0.2819296736111110979 ) ) ;
#18692=CARTESIAN_POINT ( 'NONE',  ( 0.1831830759718832136, 3.927233054027901460, -0.2570004728143698847 ) ) ;
#18693=CARTESIAN_POINT ( 'NONE',  ( 0.2206173157302027954, 4.148000000151731648, -0.2206173157302028232 ) ) ;
#18694=CARTESIAN_POINT ( 'NONE',  ( 0.000000000000000000, 0.06249999999999967387, 0.3119999999999999996 ) ) ;
#18695=EDGE_LOOP ( 'NONE', ( #21944, #15488, #17499, #19172 ) ) ;
#18697=EDGE_CURVE ( 'NONE', #6276, #1106, #8810, .T. ) ;
#18703=CARTESIAN_POINT ( 'NONE',  ( -0.1378975025881151173, 4.845326366584603583, 0.2798720040862737735 ) ) ;
#18707=CARTESIAN_POINT ( 'NONE',  ( -0.3119999999999999996, 0.4312499998482670627, 0.1292346314604056190 ) ) ;
#18710=CARTESIAN_POINT ( 'NONE',  ( 0.2262030867566338643, 4.745356984526616806, 0.2181069733381811870 ) ) ;
#18712=CARTESIAN_POINT ( 'NONE',  ( 0.3120465040799779710, 3.975505242139018680, -0.04045383393106066761 ) ) ;
#18717=CARTESIAN_POINT ( 'NONE',  ( -0.3115938335747658328, 4.668094915020961189, -0.02818765380693593822 ) ) ;
#18718=CARTESIAN_POINT ( 'NONE',  ( -0.1993543840281266910, 4.234805555631421470, -0.1993543840281266910 ) ) ;
#18721=CARTESIAN_POINT ( 'NONE',  ( -0.3119999999999999996, 3.880638888888887639, -0.1292346314604056468 ) ) ;
#18723=CARTESIAN_POINT ( 'NONE',  ( 0.3119999999999999996, 4.641055555707287006, -3.820898013339742174E-17 ) ) ;
#18724=CARTESIAN_POINT ( 'NONE',  ( -0.2819296736111110424, 5.148000000075865223, 0.1167790944451424923 ) ) ;
#18730=CARTESIAN_POINT ( 'NONE',  ( 0.1702787520999720638, 0.03957802798364115637, -0.2338844550317653315 ) ) ;
#18731=EDGE_CURVE ( 'NONE', #11776, #2004, #8190, .T. ) ;
#18735=CARTESIAN_POINT ( 'NONE',  ( -0.2819296736111110424, 5.127166666742532186, -0.1167790944451423119 ) ) ;
#18736=CARTESIAN_POINT ( 'NONE',  ( 0.1167790944451424506, 3.884111111186977272, 0.2819296736111110424 ) ) ;
#18737=CARTESIAN_POINT ( 'NONE',  ( 0.1551925990475264694, 4.409532269935922066, 0.2718825043972741828 ) ) ;
#18742=CARTESIAN_POINT ( 'NONE',  ( -5.178964085587577574E-17, 0.5909722221463555858, 0.2819296736111110979 ) ) ;
#18744=CARTESIAN_POINT ( 'NONE',  ( 0.2819296736111110979, 4.891055555631421470, 0.1167790944451422425 ) ) ;
#18746=CARTESIAN_POINT ( 'NONE',  ( 5.178964085587577574E-17, 4.811194444520309865, 0.2819296736111110979 ) ) ;
#18747=DIRECTION ( 'NONE',  ( -0.000000000000000000, -1.000000000000000000, -0.000000000000000000 ) ) ;
#18748=CARTESIAN_POINT ( 'NONE',  ( 5.731347020009612645E-17, 5.064666666666665762, 0.3119999999999999996 ) ) ;
#18751=CARTESIAN_POINT ( 'NONE',  ( 0.1292346314604058410, 4.457027777777777366, 0.3119999999999998885 ) ) ;
#18755=CARTESIAN_POINT ( 'NONE',  ( -0.1052696321117038564, 3.735245827680147013, 0.2937044510672804365 ) ) ;
#18756=CARTESIAN_POINT ( 'NONE',  ( 0.3091804297555219017, 4.584330404083684307, 0.04228285750231519646 ) ) ;
#18758=CARTESIAN_POINT ( 'NONE',  ( -0.1179188671565439273, 4.123723453325901289, 0.2893754189311016356 ) ) ;
#18762=CARTESIAN_POINT ( 'NONE',  ( 0.3010013639763466919, 5.147262939741143128, -0.03641029953439574307 ) ) ;
#18766=CARTESIAN_POINT ( 'NONE',  ( 0.2819296736111110979, 0.3687499999241333759, 0.000000000000000000 ) ) ;
#18767=CARTESIAN_POINT ( 'NONE',  ( 0.3038812257567455322, 3.865502245511798662, -0.08165866421004353004 ) ) ;
#18772=CARTESIAN_POINT ( 'NONE',  ( 0.3119999999999999996, 4.359805555555555046, -0.1292346314604056745 ) ) ;
#18773=CARTESIAN_POINT ( 'NONE',  ( 0.3119999999999998885, 0.2923611111111107386, 0.1292346314604058410 ) ) ;
#18774=CARTESIAN_POINT ( 'NONE',  ( -0.3119999999999999996, 5.217444444444443441, 0.000000000000000000 ) ) ;
#18776=CARTESIAN_POINT ( 'NONE',  ( -0.1993543840281266355, 4.262583333409199149, 0.1993543840281267465 ) ) ;
#18779=ORIENTED_EDGE ( 'NONE', *, *, #18402, .T. ) ;
#18782=CARTESIAN_POINT ( 'NONE',  ( 0.2819296736111110424, 4.995222222298087544, -0.1167790944451423396 ) ) ;
#18788=CARTESIAN_POINT ( 'NONE',  ( 1.910449006669871087E-17, 0.6361111109593781121, -0.3119999999999999996 ) ) ;
#18789=CARTESIAN_POINT ( 'NONE',  ( -0.1167790944451423119, 4.731333333409199149, -0.2819296736111110979 ) ) ;
#18791=CARTESIAN_POINT ( 'NONE',  ( -0.1926153850652713162, 4.049733122821375098, -0.2454647334727473040 ) ) ;
#18793=CARTESIAN_POINT ( 'NONE',  ( -5.178964085587577574E-17, 0.4798611110352444253, 0.2819296736111110979 ) ) ;
#18795=CARTESIAN_POINT ( 'NONE',  ( 0.1993543840281266910, 0.2229166665908000333, -0.1993543840281266910 ) ) ;
#18803=CARTESIAN_POINT ( 'NONE',  ( 0.1167790944451423119, 0.3236111110352444808, -0.2819296736111110979 ) ) ;
#18805=CARTESIAN_POINT ( 'NONE',  ( -0.1993543840281266910, 4.304250000075866112, -0.1993543840281266910 ) ) ;
#18807=CARTESIAN_POINT ( 'NONE',  ( -0.1993543840281266910, 4.915361111186976828, -0.1993543840281266910 ) ) ;
#18808=CARTESIAN_POINT ( 'NONE',  ( -0.1167790944451423535, 4.474388888964753619, 0.2819296736111110979 ) ) ;
#18812=CARTESIAN_POINT ( 'NONE',  ( 0.2206173157302027954, 3.981333333485065573, -0.2206173157302028232 ) ) ;
#18814=( BOUNDED_CURVE ( )  B_SPLINE_CURVE ( 2, ( #10163, #21248, #12356, #19775, #23531, #21726, #12473, #19893, #3184 ),
 .UNSPECIFIED., .F., .F. ) 
 B_SPLINE_CURVE_WITH_KNOTS ( ( 3, 2, 2, 2, 3 ),
 ( 0.7946428571428569843, 0.7991071428571429047, 0.8035714285714286031, 0.8080357142857144126, 0.8125000000000002220 ),
 .UNSPECIFIED. ) 
 CURVE ( )  GEOMETRIC_REPRESENTATION_ITEM ( )  RATIONAL_B_SPLINE_CURVE ( ( 1.000000000000001998, 0.9238795325112848511, 1.000000000000000000, 0.9238795325112867385, 1.000000000000000000, 0.9238795325112867385, 1.000000000000000000, 0.9238795325112829637, 1.000000000000003775 ) ) 
 REPRESENTATION_ITEM ( '' )  );
#18823=CARTESIAN_POINT ( 'NONE',  ( 6.614309848781084774E-13, 0.03242967361111062652, 0.2819296736111109869 ) ) ;
#18824=CARTESIAN_POINT ( 'NONE',  ( 0.000000000000000000, 5.072999999999999510, 0.000000000000000000 ) ) ;
#18826=CARTESIAN_POINT ( 'NONE',  ( -0.1292346314604058410, 0.4937499998482670627, 0.3119999999999998885 ) ) ;
#18832=CARTESIAN_POINT ( 'NONE',  ( 0.3037978522088217725, 3.972042276961438745, 0.08195363556016189988 ) ) ;
#18836=DIRECTION ( 'NONE',  ( -0.000000000000000000, -1.000000000000000000, -0.000000000000000000 ) ) ;
#18837=CARTESIAN_POINT ( 'NONE',  ( -0.2297610394007475187, 4.675419736397950388, 0.2110789231160656865 ) ) ;
#18839=CARTESIAN_POINT ( 'NONE',  ( 0.1993543840281267465, 3.929250000075865668, 0.1993543840281266633 ) ) ;
#18840=CARTESIAN_POINT ( 'NONE',  ( 0.1311301917775922199, 5.040099063258902667, -0.2838626894904294207 ) ) ;
#18841=CARTESIAN_POINT ( 'NONE',  ( -0.3119999999999999996, 4.828555555555555046, 0.000000000000000000 ) ) ;
#18842=CARTESIAN_POINT ( 'NONE',  ( -0.1292346314604056745, 3.929249999999998799, -0.3119999999999999996 ) ) ;
#18844=CARTESIAN_POINT ( 'NONE',  ( 5.731347020009612645E-17, 4.793833333485065573, 0.3119999999999999996 ) ) ;
#18845=CARTESIAN_POINT ( 'NONE',  ( 0.1993543840281266633, 4.901472222298088433, -0.1993543840281266910 ) ) ;
#18847=CARTESIAN_POINT ( 'NONE',  ( -1.726321361862525858E-17, 4.394527777853643791, -0.2819296736111110979 ) ) ;
#18853=ORIENTED_EDGE ( 'NONE', *, *, #8254, .F. ) ;
#18857=CARTESIAN_POINT ( 'NONE',  ( -0.1993543840281266910, 5.123694444520309865, -0.1993543840281266910 ) ) ;
#18858=CARTESIAN_POINT ( 'NONE',  ( -0.1993543840281266910, 3.915361111186976384, -0.1993543840281266910 ) ) ;
#18860=CARTESIAN_POINT ( 'NONE',  ( 0.1054935783943683481, 4.429683660412986335, -0.2936247782397201633 ) ) ;
#18861=DIRECTION ( 'NONE',  ( -0.000000000000000000, -1.000000000000000000, -0.000000000000000000 ) ) ;
#18863=CARTESIAN_POINT ( 'NONE',  ( 0.1993543840281266355, 0.5979166665908001166, 0.1993543840281267465 ) ) ;
#18865=CARTESIAN_POINT ( 'NONE',  ( -1.726321361862525858E-17, 4.852861111186976828, -0.2819296736111110979 ) ) ;
#18867=CARTESIAN_POINT ( 'NONE',  ( -0.2819296736111110424, 4.911888888964754507, 0.1167790944451424923 ) ) ;
#18868=DIRECTION ( 'NONE',  ( 0.000000000000000000, 0.000000000000000000, -1.000000000000000000 ) ) ;
#18870=DIRECTION ( 'NONE',  ( 0.000000000000000000, 0.000000000000000000, -1.000000000000000000 ) ) ;
#18874=CARTESIAN_POINT ( 'NONE',  ( 0.2206173157302027954, 4.529944444444443441, -0.2206173157302028232 ) ) ;
#18876=CARTESIAN_POINT ( 'NONE',  ( -1.726321361862525858E-17, 3.783416666742532186, -0.2819296736111110979 ) ) ;
#18881=CARTESIAN_POINT ( 'NONE',  ( -0.1292346314604032043, 4.540361111111110404, -0.3120000000000024420 ) ) ;
#18884=CARTESIAN_POINT ( 'NONE',  ( -0.1733018972839396876, 4.121925556977420690, 0.2594426199919281917 ) ) ;
#18889=CARTESIAN_POINT ( 'NONE',  ( 0.2288853704217172214, 5.153467588116631859, -0.1971701303957707208 ) ) ;
#18890=ORIENTED_EDGE ( 'NONE', *, *, #5096, .T. ) ;
#18892=CARTESIAN_POINT ( 'NONE',  ( -0.1167790944451424368, 0.5736111110352444253, 0.2819296736111110424 ) ) ;
#18895=DIRECTION ( 'NONE',  ( -0.000000000000000000, -1.000000000000000000, -0.000000000000000000 ) ) ;
#18898=CARTESIAN_POINT ( 'NONE',  ( -0.3078090614149728288, 5.104275867521749888, -0.04150825043530404629 ) ) ;
#18901=CARTESIAN_POINT ( 'NONE',  ( 0.3119999999999999996, 0.3513888888888885287, 0.000000000000000000 ) ) ;
#18902=CARTESIAN_POINT ( 'NONE',  ( 0.2206173157302028787, 5.182722222222221120, 0.2206173157302027954 ) ) ;
#18903=CARTESIAN_POINT ( 'NONE',  ( -0.2819296736111110979, 4.200083333409199149, 0.000000000000000000 ) ) ;
#18907=ADVANCED_FACE ( 'NONE', ( #15508 ), #19519, .T. ) ;
#18908=CARTESIAN_POINT ( 'NONE',  ( 0.2819296736111110424, 4.884111111186975940, -0.1167790944451423396 ) ) ;
#18912=CARTESIAN_POINT ( 'NONE',  ( -0.2262210652167811753, 5.149889715124365885, -0.2008809606663144176 ) ) ;
#18915=CYLINDRICAL_SURFACE ( 'NONE', #14995, 0.3119999999999999996 ) ;
#18916=CARTESIAN_POINT ( 'NONE',  ( 0.1993543840281266633, 4.234805555631421470, -0.1993543840281266910 ) ) ;
#18921=CARTESIAN_POINT ( 'NONE',  ( 0.1993543840281266910, 0.6118055554796889561, -0.1993543840281266910 ) ) ;
#18924=CARTESIAN_POINT ( 'NONE',  ( 1.726321361862525858E-17, 0.4520833332574667462, -0.2819296736111110979 ) ) ;
#18925=CARTESIAN_POINT ( 'NONE',  ( -1.910449006669871087E-17, 4.147999999999998799, -0.3119999999999999996 ) ) ;
#18932=CARTESIAN_POINT ( 'NONE',  ( -0.1993543840281266633, 0.2784722221463555858, -0.1993543840281266910 ) ) ;
#18933=CARTESIAN_POINT ( 'NONE',  ( -0.2819296736111110979, 0.2333333332574667185, 0.1167790944451422425 ) ) ;
#18935=CARTESIAN_POINT ( 'NONE',  ( -0.1167790944451423535, 4.377166666742532186, 0.2819296736111110424 ) ) ;
#18937=CARTESIAN_POINT ( 'NONE',  ( -0.2819296736111110979, 4.922305555631420582, 0.000000000000000000 ) ) ;
#18938=CARTESIAN_POINT ( 'NONE',  ( -1.726321361862525858E-17, 4.394527777853643791, -0.2819296736111110979 ) ) ;
#18939=LINE ( 'NONE', #7595, #7518 ) ;
#18943=CARTESIAN_POINT ( 'NONE',  ( 0.2206173157302028787, 4.023000000151731648, 0.2206173157302027954 ) ) ;
#18946=VERTEX_POINT ( 'NONE', #2348 ) ;
#18948=CARTESIAN_POINT ( 'NONE',  ( -0.07866760015732025824, 0.03242967361111055713, 0.2712073892435483691 ) ) ;
#18951=CARTESIAN_POINT ( 'NONE',  ( 0.3119999999999999996, 0.4034722220704893281, -0.1292346314604056468 ) ) ;
#18952=ORIENTED_EDGE ( 'NONE', *, *, #7562, .F. ) ;
#18953=CARTESIAN_POINT ( 'NONE',  ( -1.903245722532910002E-17, 5.100068075568266579, -0.3108236144263021861 ) ) ;
#18954=DIRECTION ( 'NONE',  ( -0.000000000000000000, -1.000000000000000000, -0.000000000000000000 ) ) ;
#18955=CARTESIAN_POINT ( 'NONE',  ( 0.005222582290261976699, 4.765907289028824323, -0.3119625414449602729 ) ) ;
#18957=CARTESIAN_POINT ( 'NONE',  ( 0.2782785630874277660, 5.176493536591711297, 0.09777844860489284806 ) ) ;
#18961=CARTESIAN_POINT ( 'NONE',  ( -0.2300903070655175853, 4.675406423759836727, 0.2107194894688067810 ) ) ;
#18962=CARTESIAN_POINT ( 'NONE',  ( 0.2819296736111110979, 4.102861111186976828, -3.452642723725051716E-17 ) ) ;
#18964=( BOUNDED_CURVE ( )  B_SPLINE_CURVE ( 2, ( #16241, #23176, #6486, #1604, #18305, #3426, #16361, #23772, #3665 ),
 .UNSPECIFIED., .F., .T. ) 
 B_SPLINE_CURVE_WITH_KNOTS ( ( 3, 2, 2, 2, 3 ),
 ( 0.3660714285714285476, 0.3705357142857143016, 0.3750000000000000000, 0.3794642857142856429, 0.3839285714285713969 ),
 .UNSPECIFIED. ) 
 CURVE ( )  GEOMETRIC_REPRESENTATION_ITEM ( )  RATIONAL_B_SPLINE_CURVE ( ( 1.000000000000000000, 0.9238795325112867385, 1.000000000000000000, 0.9238795325112867385, 1.000000000000000000, 0.9238795325112867385, 1.000000000000000000, 0.9238795325112877377, 0.9999999999999990008 ) ) 
 REPRESENTATION_ITEM ( '' )  );
#18967=CARTESIAN_POINT ( 'NONE',  ( 1.910449006669871087E-17, 0.5874999999999996891, -0.3119999999999999996 ) ) ;
#18968=CARTESIAN_POINT ( 'NONE',  ( 0.2206173157302028787, 4.689666666818398610, 0.2206173157302027954 ) ) ;
#18969=CARTESIAN_POINT ( 'NONE',  ( 0.2819296736111110979, 4.950083333409199149, -3.452642723725051716E-17 ) ) ;
#18971=CARTESIAN_POINT ( 'NONE',  ( 0.1167790944451424368, 4.370222222298088433, 0.2819296736111110424 ) ) ;
#18979=CARTESIAN_POINT ( 'NONE',  ( -0.1167790944451423119, 3.967444444520310309, -0.2819296736111110979 ) ) ;
#18983=ORIENTED_EDGE ( 'NONE', *, *, #20260, .F. ) ;
#18985=CARTESIAN_POINT ( 'NONE',  ( -0.1167790944451424506, 0.5319444443685777957, 0.2819296736111110424 ) ) ;
#18988=CARTESIAN_POINT ( 'NONE',  ( 0.2819296736111110979, 4.946611111186976828, 0.1167790944451422425 ) ) ;
#18989=CARTESIAN_POINT ( 'NONE',  ( -0.2206173157302027676, 3.946611111111110404, 0.2206173157302028787 ) ) ;
#18990=EDGE_CURVE ( 'NONE', #10051, #16767, #20987, .T. ) ;
#18991=CARTESIAN_POINT ( 'NONE',  ( 0.2819296736111110979, 4.766055555631421470, 0.1167790944451422425 ) ) ;
#18992=CARTESIAN_POINT ( 'NONE',  ( -0.0003173656412832901504, 4.154953562412278423, -0.3119998790825884716 ) ) ;
#18993=CARTESIAN_POINT ( 'NONE',  ( 0.2613201277241708476, 4.868437831976468289, -0.1709465549858873445 ) ) ;
#18996=CARTESIAN_POINT ( 'NONE',  ( -0.3119999999999999996, 4.491749999999999687, -0.1292346314604056468 ) ) ;
#18998=CARTESIAN_POINT ( 'NONE',  ( -0.1993543840281266910, 3.734805555631421026, -0.1993543840281266910 ) ) ;
#19002=ORIENTED_EDGE ( 'NONE', *, *, #7661, .T. ) ;
#19003=CARTESIAN_POINT ( 'NONE',  ( 0.1857256452555779147, 4.704968275741245876, -0.2517511420527552835 ) ) ;
#19004=CARTESIAN_POINT ( 'NONE',  ( 0.06044521969078997525, 4.653203224452946429, -0.3063190883922444208 ) ) ;
#19010=CARTESIAN_POINT ( 'NONE',  ( -0.05085398167855915974, 3.934169838589318235, -0.3079969485113711603 ) ) ;
#19013=CARTESIAN_POINT ( 'NONE',  ( -0.1167790944451422702, 0.5527777777019111660, -0.2819296736111110424 ) ) ;
#19014=CARTESIAN_POINT ( 'NONE',  ( 2.824051777240061223E-14, 3.849388889040854522, 0.3119999999999999996 ) ) ;
#19019=CARTESIAN_POINT ( 'NONE',  ( -0.1504314248901025552, 4.622694688059741708, 0.2733394608957197547 ) ) ;
#19021=CARTESIAN_POINT ( 'NONE',  ( 4.312521114635084752E-13, 5.190332509204934830, -0.2890970118899086061 ) ) ;
#19022=CARTESIAN_POINT ( 'NONE',  ( -0.3119999999999999996, 0.1569444444444440812, -3.820898013339742174E-17 ) ) ;
#19023=CARTESIAN_POINT ( 'NONE',  ( 0.2206173157302027954, 5.141055555555555046, -0.2206173157302028232 ) ) ;
#19024=CARTESIAN_POINT ( 'NONE',  ( -1.726321361862525858E-17, 4.241750000075866112, -0.2819296736111110979 ) ) ;
#19028=ORIENTED_EDGE ( 'NONE', *, *, #6476, .T. ) ;
#19030=CARTESIAN_POINT ( 'NONE',  ( 0.3119999999999999996, 0.3548611111111107386, -0.1292346314604056468 ) ) ;
#19031=CARTESIAN_POINT ( 'NONE',  ( 0.2819296736111110424, 4.661888888964754507, -0.1167790944451423396 ) ) ;
#19035=CARTESIAN_POINT ( 'NONE',  ( -0.1167790944451423535, 4.210500000075866112, 0.2819296736111110979 ) ) ;
#19037=CARTESIAN_POINT ( 'NONE',  ( -0.02453107547806535407, 4.044502971429987603, -0.3110395951528659442 ) ) ;
#19041=CARTESIAN_POINT ( 'NONE',  ( 0.1993543840281266910, 0.5562499999241333759, -0.1993543840281266910 ) ) ;
#19046=CARTESIAN_POINT ( 'NONE',  ( 0.000000000000000000, 5.384999999999999787, 0.000000000000000000 ) ) ;
#19047=CARTESIAN_POINT ( 'NONE',  ( -8.183246661411124563E-08, 3.960496777434589610, 0.3119999999999772400 ) ) ;
#19048=CARTESIAN_POINT ( 'NONE',  ( 0.1993543840281266355, 0.5840277777019111660, 0.1993543840281267465 ) ) ;
#19049=CARTESIAN_POINT ( 'NONE',  ( 0.2819296736111110424, 0.1499999999241333482, -0.1167790944451423119 ) ) ;
#19051=CARTESIAN_POINT ( 'NONE',  ( 0.1993543840281267465, 4.387583333409199149, 0.1993543840281266633 ) ) ;
#19053=CARTESIAN_POINT ( 'NONE',  ( -0.1167790944451423535, 4.821611111186976828, 0.2819296736111110424 ) ) ;
#19054=CARTESIAN_POINT ( 'NONE',  ( 0.1993543840281266633, 4.332027777853642903, -0.1993543840281266910 ) ) ;
#19055=CARTESIAN_POINT ( 'NONE',  ( 0.2206173157302027954, 4.529944444444443441, -0.2206173157302028232 ) ) ;
#19056=CARTESIAN_POINT ( 'NONE',  ( 0.3119999999999999996, 3.918833333485065129, -3.820898013339742174E-17 ) ) ;
#19059=ORIENTED_EDGE ( 'NONE', *, *, #6472, .F. ) ;
#19062=DIRECTION ( 'NONE',  ( -0.000000000000000000, -1.000000000000000000, -0.000000000000000000 ) ) ;
#19063=CARTESIAN_POINT ( 'NONE',  ( -0.2491081030224410742, 4.996314154494937654, -0.1922342116985285287 ) ) ;
#19065=CARTESIAN_POINT ( 'NONE',  ( -0.1167790944451422702, 0.1222222221463555858, -0.2819296736111110424 ) ) ;
#19068=DIRECTION ( 'NONE',  ( 0.000000000000000000, 0.000000000000000000, -1.000000000000000000 ) ) ;
#19071=CARTESIAN_POINT ( 'NONE',  ( 0.2842222223090039024, 5.180769402414656000, -0.07294254692603430179 ) ) ;
#19076=CARTESIAN_POINT ( 'NONE',  ( 0.2819296736111110979, 3.936194444520309865, -3.452642723725051716E-17 ) ) ;
#19078=CARTESIAN_POINT ( 'NONE',  ( 0.1533040153457264076, 5.122559226553594414, 0.2679359661953843452 ) ) ;
#19079=CARTESIAN_POINT ( 'NONE',  ( -0.1781879481744626514, 5.169505967695794624, -0.2374271584184740325 ) ) ;
#19080=CARTESIAN_POINT ( 'NONE',  ( -0.3119999999999998885, 4.783416666818398610, 0.1292346314604058410 ) ) ;
#19081=CARTESIAN_POINT ( 'NONE',  ( 0.1167790944451422702, 5.016055555631420582, -0.2819296736111110979 ) ) ;
#19082=EDGE_LOOP ( 'NONE', ( #16075, #8905, #22468, #7898 ) ) ;
#19083=CARTESIAN_POINT ( 'NONE',  ( -0.1167790944451423535, 4.196611111186976828, 0.2819296736111110424 ) ) ;
#19088=ORIENTED_EDGE ( 'NONE', *, *, #24094, .T. ) ;
#19092=CARTESIAN_POINT ( 'NONE',  ( -0.1993543840281266910, 3.970916666742532186, -0.1993543840281266910 ) ) ;
#19093=CYLINDRICAL_SURFACE ( 'NONE', #10750, 0.3119999999999999996 ) ;
#19098=CARTESIAN_POINT ( 'NONE',  ( -0.2819296736111111534, 0.5249999999241332649, 0.1167790944451422563 ) ) ;
#19101=CARTESIAN_POINT ( 'NONE',  ( -0.2819296736111110424, 4.696611111186977716, -0.1167790944451423119 ) ) ;
#19103=CARTESIAN_POINT ( 'NONE',  ( -0.2819296736111110424, 4.745222222298088433, 0.1167790944451424923 ) ) ;
#19104=CARTESIAN_POINT ( 'NONE',  ( 0.000000000000000000, 5.384999999999999787, -0.3119999999999999996 ) ) ;
#19108=CARTESIAN_POINT ( 'NONE',  ( -5.731347020009612645E-17, 0.2194444442927115380, 0.3119999999999999996 ) ) ;
#19109=CARTESIAN_POINT ( 'NONE',  ( 0.1292346314604056190, 4.366749999999998799, -0.3119999999999999996 ) ) ;
#19112=FACE_OUTER_BOUND ( 'NONE', #15047, .T. ) ;
#19116=CARTESIAN_POINT ( 'NONE',  ( 0.2596173626562791603, 4.701861296690032610, -0.1735006093349389100 ) ) ;
#19121=CARTESIAN_POINT ( 'NONE',  ( -0.1005310964907748239, 3.935617334977024928, -0.2960650091076030277 ) ) ;
#19122=EDGE_LOOP ( 'NONE', ( #4735, #6112, #6072, #22677 ) ) ;
#19124=CARTESIAN_POINT ( 'NONE',  ( 0.1993543840281266910, 0.4868055554796889561, -0.1993543840281266910 ) ) ;
#19129=CARTESIAN_POINT ( 'NONE',  ( -0.2637094125609521500, 5.109987496479720726, 0.1629003720249567189 ) ) ;
#19132=CARTESIAN_POINT ( 'NONE',  ( -0.3119999999999999996, 0.2124999999999996336, -3.820898013339742174E-17 ) ) ;
#19133=CARTESIAN_POINT ( 'NONE',  ( -0.1292346314604057023, 5.172305555555555046, 0.3119999999999998885 ) ) ;
#19134=CARTESIAN_POINT ( 'NONE',  ( 0.1167790944451424368, 4.106333333409199149, 0.2819296736111110424 ) ) ;
#19135=CARTESIAN_POINT ( 'NONE',  ( -0.2206173157302028232, 3.821611111111110404, -0.2206173157302028232 ) ) ;
#19139=EDGE_CURVE ( 'NONE', #21365, #22483, #7280, .T. ) ;
#19141=CARTESIAN_POINT ( 'NONE',  ( 0.1993543840281266633, 4.665361111186976828, -0.1993543840281266910 ) ) ;
#19143=CARTESIAN_POINT ( 'NONE',  ( -0.04381235360356670883, 4.514848399031694548, 0.3091263664638504438 ) ) ;
#19148=CARTESIAN_POINT ( 'NONE',  ( -0.1167790944451423119, 4.300777777853643791, -0.2819296736111110979 ) ) ;
#19150=CARTESIAN_POINT ( 'NONE',  ( 0.3119999999999999996, 4.304249999999999687, -0.1292346314604056745 ) ) ;
#19152=DIRECTION ( 'NONE',  ( -0.000000000000000000, -1.000000000000000000, -0.000000000000000000 ) ) ;
#19153=ORIENTED_EDGE ( 'NONE', *, *, #11438, .T. ) ;
#19154=CARTESIAN_POINT ( 'NONE',  ( -0.1167790944451424368, 0.4763888888130222710, 0.2819296736111110424 ) ) ;
#19157=CARTESIAN_POINT ( 'NONE',  ( 3.820898013339742174E-17, 5.384999999999999787, 0.3119999999999999996 ) ) ;
#19162=CARTESIAN_POINT ( 'NONE',  ( 0.1993543840281266355, 0.4729166665908000611, 0.1993543840281267465 ) ) ;
#19163=CARTESIAN_POINT ( 'NONE',  ( -5.178964085587577574E-17, 0.2437499999241333204, 0.2819296736111110979 ) ) ;
#19165=CARTESIAN_POINT ( 'NONE',  ( 0.1993543840281267465, 4.220916666742532186, 0.1993543840281266633 ) ) ;
#19167=CARTESIAN_POINT ( 'NONE',  ( 0.2819296736111110979, 4.838972222298088433, -3.452642723725051716E-17 ) ) ;
#19168=CARTESIAN_POINT ( 'NONE',  ( -0.2819296736111110424, 4.245222222298087544, 0.1167790944451424923 ) ) ;
#19172=ORIENTED_EDGE ( 'NONE', *, *, #4852, .F. ) ;
#19173=CARTESIAN_POINT ( 'NONE',  ( 0.1292346314604080892, 4.533416666666665762, -0.3119999999999975016 ) ) ;
#19174=CARTESIAN_POINT ( 'NONE',  ( 0.1292346314604056190, 3.762583333485065573, -0.3119999999999999996 ) ) ;
#19176=ORIENTED_EDGE ( 'NONE', *, *, #5129, .F. ) ;
#19180=CARTESIAN_POINT ( 'NONE',  ( -0.2499270801673589282, 5.007890031258386720, 0.1869623468028804858 ) ) ;
#19182=CARTESIAN_POINT ( 'NONE',  ( 1.726321361862525858E-17, 0.1743055554796889284, -0.2819296736111110979 ) ) ;
#19183=CARTESIAN_POINT ( 'NONE',  ( 0.01790655108702505355, 4.265571681436381546, -0.3115083198477991422 ) ) ;
#19187=CARTESIAN_POINT ( 'NONE',  ( 0.2635902294012452129, 5.175512519792486721, 0.1331235142709102925 ) ) ;
#19188=ORIENTED_EDGE ( 'NONE', *, *, #23255, .T. ) ;
#19190=CARTESIAN_POINT ( 'NONE',  ( -0.07935600121137664775, 4.680387721508536103, 0.3045026414546517235 ) ) ;
#19191=CARTESIAN_POINT ( 'NONE',  ( -1.726321361862525858E-17, 3.894527777853643347, -0.2819296736111110979 ) ) ;
#19192=CARTESIAN_POINT ( 'NONE',  ( -0.06362248101067675965, 0.03486971683296733598, 0.2776287047131382191 ) ) ;
#19193=CARTESIAN_POINT ( 'NONE',  ( -0.2135870376730847342, 5.171211814165030063, -0.2053538857893718594 ) ) ;
#19194=CARTESIAN_POINT ( 'NONE',  ( 0.1292346314604056190, 4.429250000151731648, -0.3119999999999999996 ) ) ;
#19196=CARTESIAN_POINT ( 'NONE',  ( -0.2819296736111110979, 4.918833333409199149, -0.1167790944451422980 ) ) ;
#19198=CARTESIAN_POINT ( 'NONE',  ( 0.1167790944451424368, 4.314666666742532186, 0.2819296736111110424 ) ) ;
#19201=ADVANCED_FACE ( 'NONE', ( #3291 ), #4881, .T. ) ;
#19208=CARTESIAN_POINT ( 'NONE',  ( 0.3119999999999999996, 0.06666666651493373397, 0.000000000000000000 ) ) ;
#19210=CARTESIAN_POINT ( 'NONE',  ( 0.07064684460510516073, 4.406932727029926333, 0.3038970684541104084 ) ) ;
#19214=CARTESIAN_POINT ( 'NONE',  ( -0.1993543840281267465, 0.4173611110352444253, 0.1993543840281266633 ) ) ;
#19217=CARTESIAN_POINT ( 'NONE',  ( 0.1993543840281267465, 4.665361111186976828, 0.1993543840281266633 ) ) ;
#19219=CARTESIAN_POINT ( 'NONE',  ( 0.2819296736111110424, 4.661888888964754507, -0.1167790944451423396 ) ) ;
#19220=CARTESIAN_POINT ( 'NONE',  ( 0.2206173157302028232, 0.2958333331816003775, -0.2206173157302028232 ) ) ;
#19222=DIRECTION ( 'NONE',  ( -0.000000000000000000, -1.000000000000000000, -0.000000000000000000 ) ) ;
#19223=CARTESIAN_POINT ( 'NONE',  ( 0.000000000000000000, 5.384999999999999787, 0.000000000000000000 ) ) ;
#19224=CARTESIAN_POINT ( 'NONE',  ( 0.3119999999999999996, 4.189666666666665762, -3.820898013339742174E-17 ) ) ;
#19226=CARTESIAN_POINT ( 'NONE',  ( -0.2206173157302028232, 5.161888889040620931, -0.2206173157302028232 ) ) ;
#19227=CARTESIAN_POINT ( 'NONE',  ( -0.1292346314604105872, 3.984805555555555046, -0.3119999999999950591 ) ) ;
#19229=ORIENTED_EDGE ( 'NONE', *, *, #24084, .T. ) ;
#19233=CARTESIAN_POINT ( 'NONE',  ( 0.1902844741700089604, 4.688494737640487742, 0.2506308059723901249 ) ) ;
#19238=VERTEX_POINT ( 'NONE', #23881 ) ;
#19241=CARTESIAN_POINT ( 'NONE',  ( 0.2819296736111110979, 0.5354166665908000056, 0.000000000000000000 ) ) ;
#19246=ORIENTED_EDGE ( 'NONE', *, *, #18731, .T. ) ;
#19247=CARTESIAN_POINT ( 'NONE',  ( -0.09000656359012888796, 4.624632385561261216, 0.3024265629511137532 ) ) ;
#19250=CARTESIAN_POINT ( 'NONE',  ( 0.2206173157302027676, 0.2333333333333330040, 0.2206173157302028787 ) ) ;
#19251=CARTESIAN_POINT ( 'NONE',  ( 5.731347020009612645E-17, 4.842444444444443441, 0.3119999999999999996 ) ) ;
#19253=CARTESIAN_POINT ( 'NONE',  ( 0.1993543840281267465, 3.887583333409199149, 0.1993543840281266633 ) ) ;
#19258=VERTEX_POINT ( 'NONE', #7200 ) ;
#19260=CARTESIAN_POINT ( 'NONE',  ( 0.1993543840281266633, 4.776472222298087544, -0.1993543840281266910 ) ) ;
#19267=CARTESIAN_POINT ( 'NONE',  ( -0.1167790944451423535, 4.377166666742532186, 0.2819296736111110979 ) ) ;
#19268=CARTESIAN_POINT ( 'NONE',  ( -0.2437001351828723128, 4.051746529912200856, -0.1987809944906386850 ) ) ;
#19271=CARTESIAN_POINT ( 'NONE',  ( 3.820898013339742174E-17, 5.384999999999999787, 0.3119999999999999996 ) ) ;
#19273=CARTESIAN_POINT ( 'NONE',  ( -5.178964085587577574E-17, 0.4798611110352444253, 0.2819296736111110979 ) ) ;
#19274=CARTESIAN_POINT ( 'NONE',  ( 0.3119999999999999996, 4.134111111111110404, -3.820898013339742174E-17 ) ) ;
#19281=CARTESIAN_POINT ( 'NONE',  ( -0.2819296736111111534, 0.3999999999241333204, 0.1167790944451422563 ) ) ;
#19282=CARTESIAN_POINT ( 'NONE',  ( -0.1993543840281267465, 0.2368055554796889561, 0.1993543840281266633 ) ) ;
#19284=CARTESIAN_POINT ( 'NONE',  ( -0.1167790944451423257, 4.134111111186977716, -0.2819296736111110424 ) ) ;
#19288=CARTESIAN_POINT ( 'NONE',  ( 0.1993543840281267465, 4.776472222298088433, 0.1993543840281266633 ) ) ;
#19292=CARTESIAN_POINT ( 'NONE',  ( 5.731347020009612645E-17, 3.960500000151731648, 0.3119999999999999996 ) ) ;
#19302=CARTESIAN_POINT ( 'NONE',  ( -0.2648550963346621434, 5.007173855133585150, 0.1658120503390664024 ) ) ;
#19304=CARTESIAN_POINT ( 'NONE',  ( 0.2819296736111110424, 0.1083333332574667046, -0.1167790944451423119 ) ) ;
#19307=CARTESIAN_POINT ( 'NONE',  ( 0.1308302654899865247, 4.262330775219983714, -0.2839942560154425921 ) ) ;
#19311=CARTESIAN_POINT ( 'NONE',  ( 0.2549033356607801060, 5.182729380544451203, -0.1438613240065718113 ) ) ;
#19312=( BOUNDED_CURVE ( )  B_SPLINE_CURVE ( 2, ( #10134, #23264, #15731, #12211, #6575, #2567, #13681, #17437, #15374 ),
 .UNSPECIFIED., .F., .T. ) 
 B_SPLINE_CURVE_WITH_KNOTS ( ( 3, 2, 2, 2, 3 ),
 ( 0.7410714285714286031, 0.7455357142857143016, 0.7500000000000000000, 0.7544642857142855874, 0.7589285714285712858 ),
 .UNSPECIFIED. ) 
 CURVE ( )  GEOMETRIC_REPRESENTATION_ITEM ( )  RATIONAL_B_SPLINE_CURVE ( ( 1.000000000000000000, 0.9238795325112867385, 1.000000000000000000, 0.9238795325112867385, 1.000000000000000000, 0.9238795325112867385, 1.000000000000000000, 0.9238795325112886259, 0.9999999999999981126 ) ) 
 REPRESENTATION_ITEM ( '' )  );
#19313=ORIENTED_EDGE ( 'NONE', *, *, #11828, .T. ) ;
#19318=EDGE_CURVE ( 'NONE', #7560, #14944, #14157, .T. ) ;
#19319=CARTESIAN_POINT ( 'NONE',  ( 5.178964085587577574E-17, 3.922305555631421026, 0.2819296736111110979 ) ) ;
#19321=CARTESIAN_POINT ( 'NONE',  ( -0.2000768274382927203, 5.170541012004494341, -0.2188383321351891897 ) ) ;
#19324=CARTESIAN_POINT ( 'NONE',  ( -0.1292346314604056745, 4.602861111262843252, -0.3119999999999999996 ) ) ;
#19325=CARTESIAN_POINT ( 'NONE',  ( -1.726321361862525858E-17, 4.963972222298088433, -0.2819296736111110979 ) ) ;
#19326=ORIENTED_EDGE ( 'NONE', *, *, #10045, .F. ) ;
#19327=CARTESIAN_POINT ( 'NONE',  ( -0.2819296736111110424, 3.960500000075865668, -0.1167790944451423119 ) ) ;
#19334=CARTESIAN_POINT ( 'NONE',  ( 0.3119999999999998885, 0.2923611111111107386, 0.1292346314604058410 ) ) ;
#19335=CARTESIAN_POINT ( 'NONE',  ( 0.2206173157302027676, 0.1152777776260448528, 0.2206173157302028787 ) ) ;
#19337=CARTESIAN_POINT ( 'NONE',  ( 0.1998324900780631963, 5.137374311756707890, 0.2310110508733242141 ) ) ;
#19342=CARTESIAN_POINT ( 'NONE',  ( -0.1167790944451422702, 0.1083333332574667046, -0.2819296736111110979 ) ) ;
#19345=CARTESIAN_POINT ( 'NONE',  ( -1.726321361862525858E-17, 4.741750000075866112, -0.2819296736111110979 ) ) ;
#19346=CARTESIAN_POINT ( 'NONE',  ( -0.1993543840281266355, 4.582027777853642903, 0.1993543840281267465 ) ) ;
#19348=CARTESIAN_POINT ( 'NONE',  ( 0.02327375635197577106, 4.850116391403974880, 0.3120000040497944993 ) ) ;
#19351=CARTESIAN_POINT ( 'NONE',  ( 0.3119999999999999996, 4.356333333333332725, -3.820898013339742174E-17 ) ) ;
#19352=CARTESIAN_POINT ( 'NONE',  ( 0.2206173157302028787, 5.134111111262843252, 0.2206173157302027954 ) ) ;
#19353=CARTESIAN_POINT ( 'NONE',  ( 0.06225566914758315362, 4.962242484901489448, 0.3057257872088504635 ) ) ;
#19358=CARTESIAN_POINT ( 'NONE',  ( 0.2823011957516836645, 4.700511095951428686, -0.1328541025166166123 ) ) ;
#19359=CARTESIAN_POINT ( 'NONE',  ( 0.1903147850440313482, 4.133000686346171015, 0.2472334505447376096 ) ) ;
#19362=CARTESIAN_POINT ( 'NONE',  ( -0.08089596400723292335, 3.935038355344236738, -0.3020212475751637982 ) ) ;
#19372=CARTESIAN_POINT ( 'NONE',  ( 1.679791495769851560E-14, 3.793833333485275183, 0.3119999999999999996 ) ) ;
#19375=CARTESIAN_POINT ( 'NONE',  ( -5.731347020009612645E-17, 0.5597222222222218990, 0.3119999999999999996 ) ) ;
#19376=CARTESIAN_POINT ( 'NONE',  ( 0.1292346314604058410, 4.901472222222222008, 0.3119999999999998885 ) ) ;
#19377=CARTESIAN_POINT ( 'NONE',  ( 0.1167790944451424368, 4.050777777853643791, 0.2819296736111110424 ) ) ;
#19378=DIRECTION ( 'NONE',  ( -0.000000000000000000, -1.000000000000000000, -0.000000000000000000 ) ) ;
#19383=DIRECTION ( 'NONE',  ( -0.000000000000000000, -1.000000000000000000, -0.000000000000000000 ) ) ;
#19384=CARTESIAN_POINT ( 'NONE',  ( -0.1167790944451423535, 4.641055555631422358, 0.2819296736111110424 ) ) ;
#19387=VECTOR ( 'NONE', #13074, 39.37007874015748143 ) ;
#19390=CARTESIAN_POINT ( 'NONE',  ( 0.2819296736111110979, 4.398000000075866112, -0.1167790944451423396 ) ) ;
#19396=CARTESIAN_POINT ( 'NONE',  ( -0.2819296736111110979, 0.5249999999241332649, 0.1167790944451422425 ) ) ;
#19397=CARTESIAN_POINT ( 'NONE',  ( -0.2206173157302028787, 0.1083333333333329901, 0.2206173157302027954 ) ) ;
#19398=CARTESIAN_POINT ( 'NONE',  ( 1.910449006669871087E-17, 0.2541666666666663188, -0.3119999999999999996 ) ) ;
#19403=CARTESIAN_POINT ( 'NONE',  ( -0.2819296736111110979, 0.5631944443685777957, -3.452642723725051716E-17 ) ) ;
#19404=CARTESIAN_POINT ( 'NONE',  ( 0.2819296736111110424, 0.4208333332574666352, 0.1167790944451424923 ) ) ;
#19405=VERTEX_POINT ( 'NONE', #7796 ) ;
#19406=CARTESIAN_POINT ( 'NONE',  ( -1.726321361862525858E-17, 4.019527777853643791, -0.2819296736111110979 ) ) ;
#19409=CARTESIAN_POINT ( 'NONE',  ( 5.178964085587577574E-17, 4.602861111186976828, 0.2819296736111110979 ) ) ;
#19412=CARTESIAN_POINT ( 'NONE',  ( 0.2206173157302028787, 3.800777777929510215, 0.2206173157302027954 ) ) ;
#19417=VECTOR ( 'NONE', #23098, 39.37007874015748143 ) ;
#19419=EDGE_CURVE ( 'NONE', #6543, #23182, #7159, .T. ) ;
#19423=CARTESIAN_POINT ( 'NONE',  ( 0.2819296736111110979, 0.1604166665908000333, 0.000000000000000000 ) ) ;
#19426=CARTESIAN_POINT ( 'NONE',  ( -0.3112102497767363363, 4.723343425208045510, -0.03524716832280518769 ) ) ;
#19433=CARTESIAN_POINT ( 'NONE',  ( 0.1167790944451424368, 3.759111111186976828, 0.2819296736111110424 ) ) ;
#19435=CARTESIAN_POINT ( 'NONE',  ( -0.2209942451922433382, 5.187717628303036399, 0.1882505735780611034 ) ) ;
#19436=DIRECTION ( 'NONE',  ( -0.000000000000000000, -1.000000000000000000, -0.000000000000000000 ) ) ;
#19437=CARTESIAN_POINT ( 'NONE',  ( -0.1292346314604057023, 4.623694444596176290, 0.3119999999999998885 ) ) ;
#19438=CARTESIAN_POINT ( 'NONE',  ( -0.2819296736111110979, 4.755638888964754507, 0.000000000000000000 ) ) ;
#19440=CARTESIAN_POINT ( 'NONE',  ( -0.1167790944451423257, 4.064666666742532186, -0.2819296736111110424 ) ) ;
#19443=VERTEX_POINT ( 'NONE', #11343 ) ;
#19444=ORIENTED_EDGE ( 'NONE', *, *, #7562, .T. ) ;
#19449=CARTESIAN_POINT ( 'NONE',  ( 0.2206173157302028232, 0.3027777777777774237, -0.2206173157302028232 ) ) ;
#19451=VECTOR ( 'NONE', #8884, 39.37007874015748143 ) ;
#19452=CARTESIAN_POINT ( 'NONE',  ( 1.910449006669871087E-17, 0.5805555554038225319, -0.3119999999999999996 ) ) ;
#19456=CARTESIAN_POINT ( 'NONE',  ( -0.1167790944451424506, 0.07361111103524446697, 0.2819296736111110424 ) ) ;
#19460=CARTESIAN_POINT ( 'NONE',  ( 0.1993543840281267465, 4.540361111186976828, 0.1993543840281266633 ) ) ;
#19464=DIRECTION ( 'NONE',  ( 0.000000000000000000, 0.000000000000000000, -1.000000000000000000 ) ) ;
#19465=CARTESIAN_POINT ( 'NONE',  ( -0.3119999999999999996, 4.217444444444443441, 0.000000000000000000 ) ) ;
#19466=CARTESIAN_POINT ( 'NONE',  ( 0.1292346314604056190, 5.151472222373953969, -0.3119999999999999996 ) ) ;
#19467=CARTESIAN_POINT ( 'NONE',  ( 0.1754988631321229564, 4.983003950203682031, -0.2618203274534778857 ) ) ;
#19468=EDGE_LOOP ( 'NONE', ( #23611, #19002, #8195, #9265 ) ) ;
#19469=CARTESIAN_POINT ( 'NONE',  ( 0.03717937511614839707, 4.572701828437388372, 0.3120000032059407902 ) ) ;
#19470=B_SPLINE_CURVE_WITH_KNOTS ( 'NONE', 3,
 ( #5105, #11212, #8895, #23870, #1932, #16696, #18163, #9133, #5477, #5225, #5351, #16578, #11091, #18403, #18520, #23999, #1810, #12818, #19992, #7190 ),
 .UNSPECIFIED., .F., .F.,
 ( 4, 2, 2, 2, 2, 2, 2, 2, 2, 4 ),
 ( 0.5025725185951905871, 0.5048557457206661603, 0.5071389728461416224, 0.5094221999716171956, 0.5117054270970926577, 0.5139886542225682309, 0.5162718813480438040, 0.5185551084735192662, 0.5196967220362570528, 0.5208383355989948393 ),
 .UNSPECIFIED. ) ;
#19472=CARTESIAN_POINT ( 'NONE',  ( 0.003051384878943240540, 4.710417945387369798, -0.3119872305879987651 ) ) ;
#19477=CARTESIAN_POINT ( 'NONE',  ( 0.1571283475654022266, 3.798372783338246794, 0.2726217976190928871 ) ) ;
#19478=ORIENTED_EDGE ( 'NONE', *, *, #13462, .T. ) ;
#19482=CARTESIAN_POINT ( 'NONE',  ( 0.2819296736111110979, 0.1638888888130222432, -0.1167790944451422980 ) ) ;
#19484=CARTESIAN_POINT ( 'NONE',  ( 0.000000000000000000, 5.384999999999999787, 0.000000000000000000 ) ) ;
#19488=CARTESIAN_POINT ( 'NONE',  ( -0.008647338669235882930, 4.293587880010775848, 0.3118972423166174179 ) ) ;
#19490=CARTESIAN_POINT ( 'NONE',  ( -0.3119999999999999996, 0.4347222222222218435, -3.820898013339742174E-17 ) ) ;
#19491=CARTESIAN_POINT ( 'NONE',  ( -0.3119999999999999996, 5.047305555555555046, -0.1292346314604056468 ) ) ;
#19492=CARTESIAN_POINT ( 'NONE',  ( -0.2819296736111110424, 4.085500000075865223, -0.1167790944451423119 ) ) ;
#19493=CARTESIAN_POINT ( 'NONE',  ( -0.3119999999999999996, 0.5909722220704892726, -0.1292346314604056745 ) ) ;
#19499=CARTESIAN_POINT ( 'NONE',  ( -0.1167790944451423257, 4.731333333409198261, -0.2819296736111110424 ) ) ;
#19500=CARTESIAN_POINT ( 'NONE',  ( -0.02182715984130906631, 4.515461111269364558, 0.3112388426647295647 ) ) ;
#19507=CARTESIAN_POINT ( 'NONE',  ( -0.2819296736111110424, 4.036888888964755395, 0.1167790944451424923 ) ) ;
#19513=CARTESIAN_POINT ( 'NONE',  ( -0.2819296736111110979, 0.01111111103524447911, 0.1167790944451422425 ) ) ;
#19515=CARTESIAN_POINT ( 'NONE',  ( -0.2206173157302027954, 0.4277777777777774237, -0.2206173157302028232 ) ) ;
#19519=CYLINDRICAL_SURFACE ( 'NONE', #17668, 0.3119999999999999996 ) ;
#19521=CARTESIAN_POINT ( 'NONE',  ( -0.04084097786787917184, 3.848291582050888948, 0.3120000000000027196 ) ) ;
#19523=CARTESIAN_POINT ( 'NONE',  ( 1.726321361862525858E-17, 0.5493055554796888451, -0.2819296736111110979 ) ) ;
#19524=CARTESIAN_POINT ( 'NONE',  ( -0.1167790944451423535, 4.099388888964754507, 0.2819296736111110424 ) ) ;
#19526=CARTESIAN_POINT ( 'NONE',  ( -0.2819296736111110424, 4.641055555631422358, -0.1167790944451423119 ) ) ;
#19527=LINE ( 'NONE', #17701, #20556 ) ;
#19528=CARTESIAN_POINT ( 'NONE',  ( 0.02852117301596229088, 5.091364893910177436, -0.3114599212108494775 ) ) ;
#19529=ORIENTED_EDGE ( 'NONE', *, *, #23811, .T. ) ;
#19531=DIRECTION ( 'NONE',  ( -0.000000000000000000, -1.000000000000000000, -0.000000000000000000 ) ) ;
#19532=CARTESIAN_POINT ( 'NONE',  ( 0.3119999999999999996, 3.752166666818398610, -3.820898013339742174E-17 ) ) ;
#19536=CARTESIAN_POINT ( 'NONE',  ( 0.08563601764371561731, 5.206640035683671286, 0.2691675127473932005 ) ) ;
#19540=CARTESIAN_POINT ( 'NONE',  ( -0.1742296017712379186, 4.566445403052646235, 0.2618687473997388104 ) ) ;
#19542=CARTESIAN_POINT ( 'NONE',  ( 0.2819296736111110979, -0.006250000075866628431, 0.000000000000000000 ) ) ;
#19543=ORIENTED_EDGE ( 'NONE', *, *, #5151, .T. ) ;
#19544=CARTESIAN_POINT ( 'NONE',  ( -5.178964085587577574E-17, 0.09097222214635558579, 0.2819296736111110979 ) ) ;
#19545=CARTESIAN_POINT ( 'NONE',  ( -0.2616638558779200707, 4.719215415244865319, -0.1714447087179424845 ) ) ;
#19548=CARTESIAN_POINT ( 'NONE',  ( -0.2283086233831378709, 5.064367125495646604, 0.2126500461812922682 ) ) ;
#19549=EDGE_CURVE ( 'NONE', #18946, #9548, #19897, .T. ) ;
#19553=CARTESIAN_POINT ( 'NONE',  ( 0.2819296736111110424, 5.231333333409200037, -0.1167790944451423396 ) ) ;
#19554=CARTESIAN_POINT ( 'NONE',  ( 0.2719403539735216757, 5.025290946412584780, 0.1583353228916592748 ) ) ;
#19556=CARTESIAN_POINT ( 'NONE',  ( -0.2683823245555305159, 4.775102343486963719, -0.1640186721127107061 ) ) ;
#19557=CARTESIAN_POINT ( 'NONE',  ( -0.1292346314604057023, 4.568138889040620931, 0.3119999999999998885 ) ) ;
#19559=CARTESIAN_POINT ( 'NONE',  ( -0.1167790944451423119, 4.689666666742532186, -0.2819296736111110979 ) ) ;
#19560=VERTEX_POINT ( 'NONE', #20840 ) ;
#19561=CARTESIAN_POINT ( 'NONE',  ( 0.1993543840281267465, 3.984805555631421470, 0.1993543840281266633 ) ) ;
#19562=VERTEX_POINT ( 'NONE', #19372 ) ;
#19564=ORIENTED_EDGE ( 'NONE', *, *, #21712, .F. ) ;
#19568=CARTESIAN_POINT ( 'NONE',  ( -0.2206173157302027954, 0.08749999984826707655, -0.2206173157302028232 ) ) ;
#19572=CARTESIAN_POINT ( 'NONE',  ( 0.05068837741648516554, 5.073009555618063438, 0.3078549794868774558 ) ) ;
#19578=CARTESIAN_POINT ( 'NONE',  ( -1.726321361862525858E-17, 4.338972222298087544, -0.2819296736111110979 ) ) ;
#19581=CARTESIAN_POINT ( 'NONE',  ( -1.910449006669871087E-17, 4.870222222222222008, -0.3119999999999999996 ) ) ;
#19582=CARTESIAN_POINT ( 'NONE',  ( -1.910449006669871087E-17, 4.314666666666665762, -0.3119999999999999996 ) ) ;
#19583=CARTESIAN_POINT ( 'NONE',  ( -0.3119999999999999996, 5.220916666818399499, -0.1292346314604056468 ) ) ;
#19585=CARTESIAN_POINT ( 'NONE',  ( 0.2616181931105792668, 4.969273229293068361, 0.1714232944442920237 ) ) ;
#19587=CARTESIAN_POINT ( 'NONE',  ( 0.2852966298538977541, 4.581816164709135109, 0.1277710420903920563 ) ) ;
#19589=( BOUNDED_CURVE ( )  B_SPLINE_CURVE ( 2, ( #14266, #21703, #15854, #8767, #23632, #23271, #21224, #4513, #15742 ),
 .UNSPECIFIED., .F., .F. ) 
 B_SPLINE_CURVE_WITH_KNOTS ( ( 3, 2, 2, 2, 3 ),
 ( 0.2410714285714287142, 0.2455357142857143293, 0.2499999999999999445, 0.2544642857142855874, 0.2589285714285712303 ),
 .UNSPECIFIED. ) 
 CURVE ( )  GEOMETRIC_REPRESENTATION_ITEM ( )  RATIONAL_B_SPLINE_CURVE ( ( 0.9999999999999976685, 0.9238795325112890700, 1.000000000000000000, 0.9238795325112867385, 1.000000000000000000, 0.9238795325112867385, 1.000000000000000000, 0.9238795325112905132, 0.9999999999999962252 ) ) 
 REPRESENTATION_ITEM ( '' )  );
#19591=CARTESIAN_POINT ( 'NONE',  ( 0.2932484408783123109, 4.137880752413645169, 0.1097999344016974271 ) ) ;
#19593=CARTESIAN_POINT ( 'NONE',  ( 1.059513921322799533E-10, 3.821611107313654720, -0.3119999999999999996 ) ) ;
#19594=EDGE_CURVE ( 'NONE', #19238, #5827, #9138, .T. ) ;
#19596=ADVANCED_FACE ( 'NONE', ( #6680 ), #7052, .T. ) ;
#19597=ADVANCED_FACE ( 'NONE', ( #6927 ), #21554, .T. ) ;
#19598=CARTESIAN_POINT ( 'NONE',  ( 0.1993543840281266910, 0.5979166665908001166, -0.1993543840281266910 ) ) ;
#19605=CARTESIAN_POINT ( 'NONE',  ( -0.07708971822763990844, 4.291625973313240472, 0.3029365359921079581 ) ) ;
#19607=CARTESIAN_POINT ( 'NONE',  ( -5.731347020009612645E-17, 0.3930555555555551583, 0.3119999999999999996 ) ) ;
#19608=CARTESIAN_POINT ( 'NONE',  ( 0.1292346314604056190, 4.922305555555555046, -0.3119999999999999996 ) ) ;
#19609=CARTESIAN_POINT ( 'NONE',  ( -0.2819296736111110979, 4.241750000075865223, 0.000000000000000000 ) ) ;
#19611=CARTESIAN_POINT ( 'NONE',  ( -0.1167790944451423535, 4.043833333409200037, 0.2819296736111110424 ) ) ;
#19612=ADVANCED_FACE ( 'NONE', ( #10357 ), #21795, .T. ) ;
#19613=CARTESIAN_POINT ( 'NONE',  ( -5.731347020009612645E-17, 0.6083333331816004330, 0.3119999999999999996 ) ) ;
#19614=CARTESIAN_POINT ( 'NONE',  ( -1.910449006669871087E-17, 3.870222222222221564, -0.3119999999999999996 ) ) ;
#19615=CARTESIAN_POINT ( 'NONE',  ( 0.3115568539166290729, 4.807258945525052951, 0.01709936015787908575 ) ) ;
#19618=CARTESIAN_POINT ( 'NONE',  ( 0.1167790944451422702, 4.502166666742532186, -0.2819296736111110424 ) ) ;
#19619=CARTESIAN_POINT ( 'NONE',  ( -0.02692592971120469358, 4.515319170270573501, 0.3108360067888585876 ) ) ;
#19624=CARTESIAN_POINT ( 'NONE',  ( -1.726321361862525858E-17, 4.130638888964754507, -0.2819296736111110979 ) ) ;
#19630=CARTESIAN_POINT ( 'NONE',  ( -0.1167790944451422702, 0.05277777770191114520, -0.2819296736111110424 ) ) ;
#19640=CARTESIAN_POINT ( 'NONE',  ( 0.2819296736111110424, 0.4833333332574667462, -0.1167790944451423119 ) ) ;
#19641=CARTESIAN_POINT ( 'NONE',  ( -0.1993543840281266910, 4.026472222298087544, -0.1993543840281266910 ) ) ;
#19644=ORIENTED_EDGE ( 'NONE', *, *, #15276, .F. ) ;
#19645=CARTESIAN_POINT ( 'NONE',  ( 0.1993543840281267465, 4.609805555631421470, 0.1993543840281266633 ) ) ;
#19646=PRODUCT ( 'Aloris-BXA-Center-Rod', 'Aloris-BXA-Center-Rod', '', ( #4863 ) ) ;
#19648=CARTESIAN_POINT ( 'NONE',  ( 0.2991168607796587109, 5.081043917475041027, -0.08951420082251353161 ) ) ;
#19649=ORIENTED_EDGE ( 'NONE', *, *, #17286, .T. ) ;
#19651=CARTESIAN_POINT ( 'NONE',  ( 0.1167790944451422702, 5.224388888964754507, -0.2819296736111110424 ) ) ;
#19654=FACE_OUTER_BOUND ( 'NONE', #22185, .T. ) ;
#19656=CARTESIAN_POINT ( 'NONE',  ( -0.1993543840281266355, 4.859805555631421470, 0.1993543840281267465 ) ) ;
#19659=CARTESIAN_POINT ( 'NONE',  ( -0.1885148968005289083, 5.106211064497114371, -0.2472071745827196798 ) ) ;
#19660=CARTESIAN_POINT ( 'NONE',  ( -0.04622711050593557303, 4.570331327651010689, 0.3085716787575049636 ) ) ;
#19662=CARTESIAN_POINT ( 'NONE',  ( -0.2819296736111110979, 0.3583333332574666907, 0.1167790944451422425 ) ) ;
#19665=CARTESIAN_POINT ( 'NONE',  ( -0.1292346314604058410, 0.3340277777777773682, 0.3119999999999998885 ) ) ;
#19667=VECTOR ( 'NONE', #12941, 39.37007874015748143 ) ;
#19669=CARTESIAN_POINT ( 'NONE',  ( -0.1292346314604020385, 4.505638888888888083, 0.3120000000000036078 ) ) ;
#19672=CARTESIAN_POINT ( 'NONE',  ( 0.2819296736111110979, 3.769527777853642903, -3.452642723725051716E-17 ) ) ;
#19673=CARTESIAN_POINT ( 'NONE',  ( -0.2978458783688814338, 0.05116650193037295541, -0.04224598531790686035 ) ) ;
#19676=CARTESIAN_POINT ( 'NONE',  ( 4.589422455927707524E-07, 4.793851445074613693, 0.3119999999992840167 ) ) ;
#19677=CARTESIAN_POINT ( 'NONE',  ( -0.3119999999999999996, 4.609805555707287006, -0.1292346314604056468 ) ) ;
#19678=CARTESIAN_POINT ( 'NONE',  ( 0.2819296736111110979, 4.783416666742532186, -3.452642723725051716E-17 ) ) ;
#19680=CARTESIAN_POINT ( 'NONE',  ( -1.726321361862525858E-17, 4.061194444520309865, -0.2819296736111110979 ) ) ;
#19683=EDGE_CURVE ( 'NONE', #23806, #11205, #15681, .T. ) ;
#19690=CARTESIAN_POINT ( 'NONE',  ( -0.2206173157302027954, 0.03194444429271151714, -0.2206173157302028232 ) ) ;
#19691=CARTESIAN_POINT ( 'NONE',  ( -0.2337193498271271375, 4.384649860946254307, -0.2067694730596380537 ) ) ;
#19693=CARTESIAN_POINT ( 'NONE',  ( 0.2206173157302028232, 0.1847222220704893003, -0.2206173157302028232 ) ) ;
#19700=CARTESIAN_POINT ( 'NONE',  ( -0.2819296736111110424, 4.356333333409198261, 0.1167790944451424923 ) ) ;
#19702=CARTESIAN_POINT ( 'NONE',  ( -7.331754493858430024E-07, 4.349360015129621004, 0.3119999999981767358 ) ) ;
#19705=CARTESIAN_POINT ( 'NONE',  ( -0.1292346314604057023, 4.005638888888888971, 0.3119999999999998885 ) ) ;
#19706=CARTESIAN_POINT ( 'NONE',  ( -0.3119999999999999996, 5.109805555707287894, -0.1292346314604056468 ) ) ;
#19716=CARTESIAN_POINT ( 'NONE',  ( -0.1292346314604008173, 4.450083333333332725, 0.3120000000000048845 ) ) ;
#19719=CARTESIAN_POINT ( 'NONE',  ( 0.1993543840281266910, 0.05624999992413336897, -0.1993543840281266910 ) ) ;
#19722=CARTESIAN_POINT ( 'NONE',  ( 0.1993543840281266633, 5.179250000075866112, -0.1993543840281266910 ) ) ;
#19725=CARTESIAN_POINT ( 'NONE',  ( 2.802071455580988509E-07, 4.599388881221821990, -0.3119999999998741003 ) ) ;
#19726=CARTESIAN_POINT ( 'NONE',  ( -0.002160124341594215833, 4.293772033077872585, 0.3119935960890014570 ) ) ;
#19728=CARTESIAN_POINT ( 'NONE',  ( 0.3119999999999999996, 0.5215277777777774793, -0.1292346314604056468 ) ) ;
#19729=CARTESIAN_POINT ( 'NONE',  ( 0.2206173157302028787, 4.904944444444443441, 0.2206173157302027954 ) ) ;
#19730=VECTOR ( 'NONE', #10617, 39.37007874015748143 ) ;
#19731=CARTESIAN_POINT ( 'NONE',  ( 0.2819296736111110979, 4.328555555631421470, -0.1167790944451423396 ) ) ;
#19732=CARTESIAN_POINT ( 'NONE',  ( -0.1167790944451423535, 3.932722222298087544, 0.2819296736111110424 ) ) ;
#19733=( BOUNDED_CURVE ( )  B_SPLINE_CURVE ( 2, ( #18329, #1741, #16264, #20037, #3207, #24045, #5154, #16140, #23797 ),
 .UNSPECIFIED., .F., .T. ) 
 B_SPLINE_CURVE_WITH_KNOTS ( ( 3, 2, 2, 2, 3 ),
 ( 0.3541666666666666852, 0.3645833333333333148, 0.3750000000000000000, 0.3854166666666666852, 0.3958333333333333148 ),
 .UNSPECIFIED. ) 
 CURVE ( )  GEOMETRIC_REPRESENTATION_ITEM ( )  RATIONAL_B_SPLINE_CURVE ( ( 1.000000000000000000, 0.9238795325112867385, 1.000000000000000000, 0.9238795325112867385, 1.000000000000000000, 0.9238795325112867385, 1.000000000000000000, 0.9238795325112867385, 1.000000000000000000 ) ) 
 REPRESENTATION_ITEM ( '' )  );
#19734=CARTESIAN_POINT ( 'NONE',  ( -0.3120000000000000551, 0.5979166665149336923, 0.1292346314604056190 ) ) ;
#19736=CARTESIAN_POINT ( 'NONE',  ( 1.312321497832610059E-07, 4.821611112096344520, -0.3119999999999724105 ) ) ;
#19737=( BOUNDED_CURVE ( )  B_SPLINE_CURVE ( 2, ( #14061, #19904, #1250, #17957, #3083, #10640, #6735, #1372, #16006 ),
 .UNSPECIFIED., .F., .F. ) 
 B_SPLINE_CURVE_WITH_KNOTS ( ( 3, 2, 2, 2, 3 ),
 ( 0.2708333333333333148, 0.2812500000000000000, 0.2916666666666666852, 0.3020833333333333148, 0.3125000000000000000 ),
 .UNSPECIFIED. ) 
 CURVE ( )  GEOMETRIC_REPRESENTATION_ITEM ( )  RATIONAL_B_SPLINE_CURVE ( ( 1.000000000000000000, 0.9238795325112867385, 1.000000000000000000, 0.9238795325112867385, 1.000000000000000000, 0.9238795325112867385, 1.000000000000000000, 0.9238795325112867385, 1.000000000000000000 ) ) 
 REPRESENTATION_ITEM ( '' )  );
#19739=CARTESIAN_POINT ( 'NONE',  ( -0.2726213665948679643, 4.006868641008068721, 0.1571290981393282105 ) ) ;
#19740=CARTESIAN_POINT ( 'NONE',  ( -0.1167790944451423257, 4.398000000075866112, -0.2819296736111110424 ) ) ;
#19741=CARTESIAN_POINT ( 'NONE',  ( -0.2999751848458688253, 4.499730033197880452, -0.08647106361988687873 ) ) ;
#19748=DIMENSIONAL_EXPONENTS ( 1.000000000000000000, 0.000000000000000000, 0.000000000000000000, 0.000000000000000000, 0.000000000000000000, 0.000000000000000000, 0.000000000000000000 ) ;
#19749=CARTESIAN_POINT ( 'NONE',  ( -0.2819296736111110979, 4.141055555631421470, -0.1167790944451422980 ) ) ;
#19751=CARTESIAN_POINT ( 'NONE',  ( -0.3119999999999999996, 0.3791666666666663188, -3.820898013339742174E-17 ) ) ;
#19753=DIRECTION ( 'NONE',  ( 0.000000000000000000, 0.000000000000000000, -1.000000000000000000 ) ) ;
#19756=CARTESIAN_POINT ( 'NONE',  ( 0.1167790944451423535, 0.5944444443685777957, 0.2819296736111110424 ) ) ;
#19763=DIRECTION ( 'NONE',  ( -0.000000000000000000, -1.000000000000000000, -0.000000000000000000 ) ) ;
#19765=CARTESIAN_POINT ( 'NONE',  ( 0.1167790944451423257, 0.4902777777019112215, -0.2819296736111110424 ) ) ;
#19766=CARTESIAN_POINT ( 'NONE',  ( -0.1993543840281266355, 3.984805555631421470, 0.1993543840281267465 ) ) ;
#19769=CARTESIAN_POINT ( 'NONE',  ( -0.2819296736111110979, 4.588972222298088433, 0.000000000000000000 ) ) ;
#19770=CARTESIAN_POINT ( 'NONE',  ( 0.2491934408984518567, 5.125924046562484016, 0.1804089006109781124 ) ) ;
#19775=CARTESIAN_POINT ( 'NONE',  ( 0.3119999999999999996, 4.026472222222221120, -0.1292346314604056745 ) ) ;
#19776=CARTESIAN_POINT ( 'NONE',  ( 5.178964085587577574E-17, 5.088972222298087544, 0.2819296736111110979 ) ) ;
#19777=CARTESIAN_POINT ( 'NONE',  ( 0.2646253146636260434, 4.191643205751345747, 0.1652801019260927984 ) ) ;
#19778=CARTESIAN_POINT ( 'NONE',  ( 0.09911565489844109678, 0.03242967361111059182, 0.2643245622819848095 ) ) ;
#19779=CARTESIAN_POINT ( 'NONE',  ( 0.2819296736111111534, 4.988277777853643791, 0.1167790944451422563 ) ) ;
#19782=CARTESIAN_POINT ( 'NONE',  ( -0.09954347264555452046, 5.103090623246006707, -0.2948505828934365747 ) ) ;
#19785=CARTESIAN_POINT ( 'NONE',  ( 0.1993543840281266910, 0.2229166665908000333, -0.1993543840281266910 ) ) ;
#19789=FACE_OUTER_BOUND ( 'NONE', #15787, .T. ) ;
#19790=CARTESIAN_POINT ( 'NONE',  ( 0.04216970674995203922, 4.098166857964845811, -0.3119999999999987228 ) ) ;
#19792=CARTESIAN_POINT ( 'NONE',  ( -0.2930162582832894214, 5.060969273910194133, 0.1096452931246931495 ) ) ;
#19795=CARTESIAN_POINT ( 'NONE',  ( 0.1993543840281266633, 4.623694444520309865, -0.1993543840281266910 ) ) ;
#19798=CARTESIAN_POINT ( 'NONE',  ( -0.1167790944451423257, 3.731333333409198261, -0.2819296736111110424 ) ) ;
#19799=CARTESIAN_POINT ( 'NONE',  ( -0.2207274099297822922, 0.04780226632771114592, -0.1994142295682237720 ) ) ;
#19800=CARTESIAN_POINT ( 'NONE',  ( -0.3119999999999999996, 0.09444444429271151020, -3.820898013339742174E-17 ) ) ;
#19801=DIRECTION ( 'NONE',  ( -0.000000000000000000, -1.000000000000000000, -0.000000000000000000 ) ) ;
#19802=CARTESIAN_POINT ( 'NONE',  ( -0.05023616953324346046, 4.792438398584838666, 0.3079329440659664963 ) ) ;
#19803=CARTESIAN_POINT ( 'NONE',  ( 0.3119999999999999996, 4.363277777929510215, -3.820898013339742174E-17 ) ) ;
#19804=CARTESIAN_POINT ( 'NONE',  ( -0.1167790944451423535, 4.766055555631421470, 0.2819296736111110979 ) ) ;
#19805=ORIENTED_EDGE ( 'NONE', *, *, #17380, .T. ) ;
#19806=CARTESIAN_POINT ( 'NONE',  ( -0.1993543840281266355, 3.859805555631421026, 0.1993543840281267465 ) ) ;
#19807=VECTOR ( 'NONE', #9567, 39.37007874015748143 ) ;
#19809=ORIENTED_EDGE ( 'NONE', *, *, #16976, .T. ) ;
#19815=CARTESIAN_POINT ( 'NONE',  ( -0.3119999999999999996, 0.3722222220704893281, -3.820898013339742174E-17 ) ) ;
#19816=CARTESIAN_POINT ( 'NONE',  ( -0.2804777715993982956, 4.387060150774842349, -0.1381842819380600940 ) ) ;
#19822=DIRECTION ( 'NONE',  ( -0.000000000000000000, -1.000000000000000000, -0.000000000000000000 ) ) ;
#19825=CARTESIAN_POINT ( 'NONE',  ( -0.1993543840281266910, 4.457027777853642903, -0.1993543840281266910 ) ) ;
#19828=CARTESIAN_POINT ( 'NONE',  ( -3.345742422185251127E-06, 4.766055647721512578, -0.3119999999820609049 ) ) ;
#19829=CARTESIAN_POINT ( 'NONE',  ( -0.1568911027456994511, 4.215120699763493128, -0.2727482857155890117 ) ) ;
#19830=CARTESIAN_POINT ( 'NONE',  ( -1.910449006669871087E-17, 4.036888888888888083, -0.3119999999999999996 ) ) ;
#19831=CARTESIAN_POINT ( 'NONE',  ( -0.1292346314604057023, 4.901472222373953969, 0.3119999999999998885 ) ) ;
#19833=CARTESIAN_POINT ( 'NONE',  ( -0.03213320543484096681, 4.878081089662273939, -0.3105925309973510684 ) ) ;
#19835=CARTESIAN_POINT ( 'NONE',  ( 0.1167790944451422702, 5.224388888964754507, -0.2819296736111110424 ) ) ;
#19836=CARTESIAN_POINT ( 'NONE',  ( 0.1917385266880204386, 3.799560276120441227, 0.2494960911888102484 ) ) ;
#19841=CARTESIAN_POINT ( 'NONE',  ( 0.1167790944451424368, 5.217444444520309865, 0.2819296736111110424 ) ) ;
#19843=ORIENTED_EDGE ( 'NONE', *, *, #5875, .F. ) ;
#19844=CARTESIAN_POINT ( 'NONE',  ( -0.02506413332034217525, 4.600113615547450685, -0.3110320965815868144 ) ) ;
#19848=CARTESIAN_POINT ( 'NONE',  ( 1.910449006669871087E-17, 0.4763888888888885287, -0.3119999999999999996 ) ) ;
#19849=CARTESIAN_POINT ( 'NONE',  ( -0.2206173157302027676, 4.668833333333332725, 0.2206173157302028787 ) ) ;
#19852=CARTESIAN_POINT ( 'NONE',  ( -0.2819296736111110979, 4.127166666742532186, -0.1167790944451422980 ) ) ;
#19853=CARTESIAN_POINT ( 'NONE',  ( 0.1993543840281267465, 3.832027777853643791, 0.1993543840281266633 ) ) ;
#19857=CARTESIAN_POINT ( 'NONE',  ( 8.375559671162349491E-15, 3.988277777929486678, -0.3119999999999999996 ) ) ;
#19858=CARTESIAN_POINT ( 'NONE',  ( 0.2819296736111110979, 4.488277777853643791, 0.1167790944451422425 ) ) ;
#19859=ADVANCED_FACE ( 'NONE', ( #12923 ), #11195, .T. ) ;
#19860=CARTESIAN_POINT ( 'NONE',  ( -0.3100117717788872240, 4.501197505690473832, -0.03525460809166135884 ) ) ;
#19862=CARTESIAN_POINT ( 'NONE',  ( 0.000000000000000000, 5.384999999999999787, -0.3119999999999999996 ) ) ;
#19868=CARTESIAN_POINT ( 'NONE',  ( -0.1993543840281266355, 4.151472222298088433, 0.1993543840281267465 ) ) ;
#19869=CARTESIAN_POINT ( 'NONE',  ( -0.09821183740504324522, 4.824495949122511895, -0.2968094086098724271 ) ) ;
#19873=CARTESIAN_POINT ( 'NONE',  ( 0.1993543840281266910, 0.6118055554796889561, -0.1993543840281266910 ) ) ;
#19881=( BOUNDED_CURVE ( )  B_SPLINE_CURVE ( 2, ( #3320, #19669, #10777, #18203, #1499, #21382, #2840, #1017, #8447 ),
 .UNSPECIFIED., .F., .F. ) 
 B_SPLINE_CURVE_WITH_KNOTS ( ( 3, 2, 2, 2, 3 ),
 ( 0.4910714285714283811, 0.4955357142857142461, 0.5000000000000000000, 0.5044642857142858094, 0.5089285714285716189 ),
 .UNSPECIFIED. ) 
 CURVE ( )  GEOMETRIC_REPRESENTATION_ITEM ( )  RATIONAL_B_SPLINE_CURVE ( ( 1.000000000000002887, 0.9238795325112838519, 1.000000000000000000, 0.9238795325112867385, 1.000000000000000000, 0.9238795325112867385, 1.000000000000000000, 0.9238795325112829637, 1.000000000000003775 ) ) 
 REPRESENTATION_ITEM ( '' )  );
#19883=CARTESIAN_POINT ( 'NONE',  ( 0.2819296736111110979, 0.4243055554796889006, 0.000000000000000000 ) ) ;
#19884=ADVANCED_FACE ( 'NONE', ( #3873 ), #18624, .T. ) ;
#19885=CARTESIAN_POINT ( 'NONE',  ( 0.1993543840281267465, 3.832027777853643791, 0.1993543840281266633 ) ) ;
#19887=ORIENTED_EDGE ( 'NONE', *, *, #16922, .F. ) ;
#19888=CARTESIAN_POINT ( 'NONE',  ( 0.1167790944451424368, 4.439666666742532186, 0.2819296736111110424 ) ) ;
#19889=CARTESIAN_POINT ( 'NONE',  ( 0.2026171589331097200, 5.137660913757319037, -0.2291522707572892226 ) ) ;
#19893=CARTESIAN_POINT ( 'NONE',  ( 0.1292346314604009005, 4.012583333333331836, 0.3120000000000048845 ) ) ;
#19894=CARTESIAN_POINT ( 'NONE',  ( -0.3119999999999998885, 3.727861111262843252, 0.1292346314604058410 ) ) ;
#19896=CARTESIAN_POINT ( 'NONE',  ( 0.2604525334828327598, 4.191421240092715550, 0.1717991962690550156 ) ) ;
#19897=B_SPLINE_CURVE_WITH_KNOTS ( 'NONE', 3,
 ( #1944, #5729, #5362, #24011, #20364, #13188, #9390, #24124, #20247, #12828, #1707, #9144, #16707, #7321, #16941, #20602, #7439, #12952, #240, #7675, #18898, #15125, #22551, #16589, #14772, #22187, #11466, #5487, #3655, #1822, #19129, #21200, #8028, #4132, #6200, #2551, #23020, #11957, #12074, #2781, #20961, #17424, #17544, #22786, #2433, #9751, #6440 ),
 .UNSPECIFIED., .F., .F.,
 ( 4, 2, 2, 2, 2, 2, 2, 2, 2, 2, 2, 2, 2, 2, 2, 2, 2, 2, 2, 2, 2, 1, 2, 4 ),
 ( 0.01742734353126568214, 0.01820292306817463193, 0.01897850260508358519, 0.02052966167890148130, 0.02208082075271938088, 0.02285640028962833067, 0.02363197982653728046, 0.02518313890035518005, 0.02673429797417307963, 0.02828545704799098268, 0.02906103658489993247, 0.02983661612180887879, 0.03138777519562677837, 0.03293893426944467795, 0.03371451380635362427, 0.03449009334326257059, 0.03604125241708047711, 0.03681683195398942343, 0.03759241149089836975, 0.03914357056471626933, 0.03991915010162521565, 0.04069472963853416891, 0.04147030917544311523, 0.04224588871235206156 ),
 .UNSPECIFIED. ) ;
#19899=CARTESIAN_POINT ( 'NONE',  ( -0.1993543840281266355, 4.970916666742532186, 0.1993543840281267465 ) ) ;
#19902=CARTESIAN_POINT ( 'NONE',  ( -0.3119999999999999996, 0.3166666665149337478, -3.820898013339742174E-17 ) ) ;
#19903=EDGE_CURVE ( 'NONE', #18582, #23659, #10320, .T. ) ;
#19904=CARTESIAN_POINT ( 'NONE',  ( -0.1292346314604056190, 0.1951388887371559577, -0.3119999999999999996 ) ) ;
#19906=CARTESIAN_POINT ( 'NONE',  ( 0.1993543840281266355, 0.3201388888130222710, 0.1993543840281267465 ) ) ;
#19908=VERTEX_POINT ( 'NONE', #5935 ) ;
#19913=CARTESIAN_POINT ( 'NONE',  ( -0.03602220318626091905, 5.044808164693691310, -0.3105944775966490434 ) ) ;
#19914=CARTESIAN_POINT ( 'NONE',  ( 0.3120000000000000551, 4.186194444444444329, 0.1292346314604056190 ) ) ;
#19915=EDGE_CURVE ( 'NONE', #19560, #8097, #6054, .T. ) ;
#19916=CARTESIAN_POINT ( 'NONE',  ( -0.2703837395707749391, 3.895695782031614929, 0.1575116891411247888 ) ) ;
#19920=CARTESIAN_POINT ( 'NONE',  ( 0.1993543840281267465, 4.609805555631421470, 0.1993543840281266633 ) ) ;
#19922=CARTESIAN_POINT ( 'NONE',  ( 0.2819296736111110424, 3.828555555631421026, -0.1167790944451423396 ) ) ;
#19925=CARTESIAN_POINT ( 'NONE',  ( 0.09085534873164523295, 5.072999999999999510, 0.3012414626474842483 ) ) ;
#19926=CARTESIAN_POINT ( 'NONE',  ( -0.05310794838523746897, 4.792355782325940616, 0.3074473702546657305 ) ) ;
#19927=CARTESIAN_POINT ( 'NONE',  ( 5.731347020009612645E-17, 4.349388889040620931, 0.3119999999999999996 ) ) ;
#19929=CARTESIAN_POINT ( 'NONE',  ( -0.1993543840281266355, 4.651472222298087544, 0.1993543840281267465 ) ) ;
#19930=B_SPLINE_CURVE_WITH_KNOTS ( 'NONE', 3,
 ( #8874, #3029, #12313, #10711, #14009, #19726, #18022, #19488, #3260, #23130, #17906, #10594, #19605, #21682, #15947, #4613, #1201, #16077, #6805, #12432, #6442, #13895, #23373, #14246, #1319, #23249, #2900, #949, #12075, #12198, #4726, #4965, #8744, #10358, #16199, #17782, #16681, #7413, #7171 ),
 .UNSPECIFIED., .F., .F.,
 ( 4, 2, 1, 1, 1, 1, 1, 2, 2, 2, 2, 2, 2, 2, 2, 2, 2, 2, 2, 2, 2, 4 ),
 ( 0.6122134677491346544, 0.6122179294325030829, 0.6122223911158716225, 0.6122313144826084796, 0.6122491612160823049, 0.6122848546830299554, 0.6123562416169253675, 0.6124990154847160806, 0.6127845632202973958, 0.6133556586914602482, 0.6144978496337858420, 0.6156400405761114358, 0.6167822315184370296, 0.6179244224607626235, 0.6190666134030882173, 0.6202088043454138111, 0.6213509952877394049, 0.6224931862300648877, 0.6236353771723904815, 0.6259197590570416692, 0.6282041409416928568, 0.6304885228263440444 ),
 .UNSPECIFIED. ) ;
#19931=CARTESIAN_POINT ( 'NONE',  ( 0.1993543840281266633, 3.776472222298087988, -0.1993543840281266910 ) ) ;
#19938=CARTESIAN_POINT ( 'NONE',  ( -0.2206173157302028787, 0.2680555554038226429, 0.2206173157302027954 ) ) ;
#19939=CARTESIAN_POINT ( 'NONE',  ( -0.02010730444239897108, 4.377710753833683910, -0.3113796951532629143 ) ) ;
#19940=CARTESIAN_POINT ( 'NONE',  ( -0.2094265943819361708, 3.717041492013063220, -0.2313614939596641551 ) ) ;
#19941=CARTESIAN_POINT ( 'NONE',  ( -1.858121103377620624E-07, 4.877166671810766019, -0.3119999999999446549 ) ) ;
#19946=CARTESIAN_POINT ( 'NONE',  ( 0.2819296736111110979, 0.2611111110352444808, -0.1167790944451422980 ) ) ;
#19948=CARTESIAN_POINT ( 'NONE',  ( -0.2819296736111110424, 4.411888888964753619, 0.1167790944451424923 ) ) ;
#19949=CARTESIAN_POINT ( 'NONE',  ( 0.3119999999999999996, 0.1847222222222218990, 0.000000000000000000 ) ) ;
#19951=CARTESIAN_POINT ( 'NONE',  ( -0.02037115866045762641, 4.237742989552504724, 0.3115008212664499010 ) ) ;
#19952=CARTESIAN_POINT ( 'NONE',  ( -0.2206173157302028232, 3.988277777777776922, -0.2206173157302028232 ) ) ;
#19953=EDGE_CURVE ( 'NONE', #12009, #16668, #16469, .T. ) ;
#19954=CARTESIAN_POINT ( 'NONE',  ( -0.1292346314604056745, 4.991750000151732536, -0.3119999999999999996 ) ) ;
#19966=CARTESIAN_POINT ( 'NONE',  ( -0.2819296736111110979, 0.2993055554796889561, -3.452642723725051716E-17 ) ) ;
#19968=CARTESIAN_POINT ( 'NONE',  ( 0.1167790944451422702, 5.238277777853643791, -0.2819296736111110424 ) ) ;
#19969=CARTESIAN_POINT ( 'NONE',  ( 0.3049278984963029182, 4.472535498897220130, 0.06605302570197388312 ) ) ;
#19971=CARTESIAN_POINT ( 'NONE',  ( -0.1539092610705375952, 4.603981316102501609, -0.2721373798033744906 ) ) ;
#19975=CARTESIAN_POINT ( 'NONE',  ( 0.1292346314604057300, 0.5562499998482671737, 0.3119999999999998885 ) ) ;
#19976=CARTESIAN_POINT ( 'NONE',  ( -0.3119999999999999996, 4.717444444444443441, 0.000000000000000000 ) ) ;
#19977=CARTESIAN_POINT ( 'NONE',  ( 0.2819296736111111534, 4.099388888964754507, 0.1167790944451422563 ) ) ;
#19980=CARTESIAN_POINT ( 'NONE',  ( 1.910449006669871087E-17, 0.5249999998482670627, -0.3119999999999999996 ) ) ;
#19983=CARTESIAN_POINT ( 'NONE',  ( 0.1167790944451424368, 4.481333333409199149, 0.2819296736111110424 ) ) ;
#19984=AXIS2_PLACEMENT_3D ( 'NONE', #1863, #9062, #14442 ) ;
#19985=CARTESIAN_POINT ( 'NONE',  ( -0.2371201309373563992, 4.508458841826880281, 0.2028076677489544510 ) ) ;
#19989=CARTESIAN_POINT ( 'NONE',  ( 5.178964085587577574E-17, 4.102861111186976828, 0.2819296736111110979 ) ) ;
#19991=CARTESIAN_POINT ( 'NONE',  ( -0.3109883961989257095, 4.834813968162577247, -0.02511538183358531101 ) ) ;
#19992=CARTESIAN_POINT ( 'NONE',  ( -0.02037388374998021570, 4.433306081093942197, -0.3120000000000003326 ) ) ;
#19995=CARTESIAN_POINT ( 'NONE',  ( -0.1993543840281266633, 0.5701388888130222155, -0.1993543840281266910 ) ) ;
#20004=ORIENTED_EDGE ( 'NONE', *, *, #5591, .T. ) ;
#20006=CARTESIAN_POINT ( 'NONE',  ( 0.1167790944451423119, 0.6013888888130222155, -0.2819296736111110979 ) ) ;
#20007=CARTESIAN_POINT ( 'NONE',  ( -0.1993543840281267465, 0.5701388888130222155, 0.1993543840281266633 ) ) ;
#20008=CARTESIAN_POINT ( 'NONE',  ( 5.178964085587577574E-17, 3.769527777853644235, 0.2819296736111110979 ) ) ;
#20010=CARTESIAN_POINT ( 'NONE',  ( -0.1993543840281266355, 4.318138888964754507, 0.1993543840281267465 ) ) ;
#20012=CARTESIAN_POINT ( 'NONE',  ( -0.3119999999999999996, 4.384111111111110404, 0.000000000000000000 ) ) ;
#20014=CARTESIAN_POINT ( 'NONE',  ( 0.3090122127097978399, 4.364796073349109129, -0.05326403159567110607 ) ) ;
#20015=CARTESIAN_POINT ( 'NONE',  ( 0.1993543840281266633, 5.220916666742532186, -0.1993543840281266910 ) ) ;
#20016=CARTESIAN_POINT ( 'NONE',  ( 0.2252836021529972255, 4.203383026810429079, -0.2159527458307812231 ) ) ;
#20018=CARTESIAN_POINT ( 'NONE',  ( -1.726321361862525858E-17, 4.838972222298088433, -0.2819296736111110979 ) ) ;
#20020=ADVANCED_FACE ( 'NONE', ( #17757 ), #23706, .T. ) ;
#20025=CARTESIAN_POINT ( 'NONE',  ( -5.178964085587577574E-17, 0.2020833332574667185, 0.2819296736111110979 ) ) ;
#20033=CARTESIAN_POINT ( 'NONE',  ( -0.2933312968388447906, 3.887856832897826909, -0.1097277311388216714 ) ) ;
#20035=CARTESIAN_POINT ( 'NONE',  ( 0.1167790944451422702, 4.404944444520309865, -0.2819296736111110424 ) ) ;
#20037=CARTESIAN_POINT ( 'NONE',  ( -0.3119999999999999996, 0.2576388887371560132, -0.1292346314604056745 ) ) ;
#20039=CARTESIAN_POINT ( 'NONE',  ( -0.2819296736111110424, 5.141055555631421470, -0.1167790944451423119 ) ) ;
#20040=CARTESIAN_POINT ( 'NONE',  ( -0.2909984631779261588, 0.05351298515340481565, 0.08506003772084960723 ) ) ;
#20041=CARTESIAN_POINT ( 'NONE',  ( 0.3071603949907269482, 3.750640993411230362, 0.05477998771989885801 ) ) ;
#20044=CARTESIAN_POINT ( 'NONE',  ( -0.1292346314604056745, 4.325083333485065573, -0.3119999999999999996 ) ) ;
#20045=CARTESIAN_POINT ( 'NONE',  ( 0.2819296736111110979, 4.509111111186976828, -0.1167790944451423396 ) ) ;
#20046=CARTESIAN_POINT ( 'NONE',  ( 5.178964085587577574E-17, 3.922305555631421026, 0.2819296736111110979 ) ) ;
#20049=EDGE_CURVE ( 'NONE', #16613, #7560, #14771, .T. ) ;
#20050=ADVANCED_FACE ( 'NONE', ( #3004 ), #925, .T. ) ;
#20051=EDGE_CURVE ( 'NONE', #22245, #14830, #12966, .T. ) ;
#20055=CARTESIAN_POINT ( 'NONE',  ( 7.699581739047377146E-15, 4.099388889040679551, -0.3119999999999999996 ) ) ;
#20056=DIRECTION ( 'NONE',  ( 0.000000000000000000, 0.000000000000000000, -1.000000000000000000 ) ) ;
#20058=CARTESIAN_POINT ( 'NONE',  ( 0.3119999999999998885, 0.3409722220704892726, 0.1292346314604058410 ) ) ;
#20060=CARTESIAN_POINT ( 'NONE',  ( -0.1410631782541221235, 3.714607375173814230, -0.2794366395611496690 ) ) ;
#20070=CARTESIAN_POINT ( 'NONE',  ( 0.2819296736111110979, 4.158416666742532186, -3.452642723725051716E-17 ) ) ;
#20071=CARTESIAN_POINT ( 'NONE',  ( -0.2819296736111110979, 5.019527777853642903, 0.000000000000000000 ) ) ;
#20072=CARTESIAN_POINT ( 'NONE',  ( 0.000000000000000000, 5.384999999999999787, -0.3119999999999999996 ) ) ;
#20074=CARTESIAN_POINT ( 'NONE',  ( -0.3119999999999999996, 3.995222222222221120, 0.000000000000000000 ) ) ;
#20075=CARTESIAN_POINT ( 'NONE',  ( 5.731347020009612645E-17, 5.016055555707287894, 0.3119999999999999996 ) ) ;
#20079=CARTESIAN_POINT ( 'NONE',  ( 0.03900027537438015973, 4.683786655857547387, 0.3095907352979412885 ) ) ;
#20081=DIRECTION ( 'NONE',  ( -0.000000000000000000, -1.000000000000000000, -0.000000000000000000 ) ) ;
#20083=ORIENTED_EDGE ( 'NONE', *, *, #21933, .T. ) ;
#20086=EDGE_CURVE ( 'NONE', #9562, #20417, #21931, .T. ) ;
#20088=CARTESIAN_POINT ( 'NONE',  ( 0.1167790944451423119, 0.2819444443685777957, -0.2819296736111110979 ) ) ;
#20090=CARTESIAN_POINT ( 'NONE',  ( 5.178964085587577574E-17, 5.213972222298088433, 0.2819296736111110979 ) ) ;
#20091=CARTESIAN_POINT ( 'NONE',  ( 0.05308315351926259917, 4.486801226741740756, -0.3074512618920948182 ) ) ;
#20094=CARTESIAN_POINT ( 'NONE',  ( -0.002508478379659685818, 4.599461472648869176, -0.3119924374546728663 ) ) ;
#20097=CARTESIAN_POINT ( 'NONE',  ( 0.000000000000000000, 5.072999999999999510, 0.000000000000000000 ) ) ;
#20098=CARTESIAN_POINT ( 'NONE',  ( 0.1292346314604056745, 0.5770833331816004330, -0.3119999999999999996 ) ) ;
#20099=CARTESIAN_POINT ( 'NONE',  ( 0.2206173157302028787, 4.793833333333332725, 0.2206173157302027954 ) ) ;
#20100=CARTESIAN_POINT ( 'NONE',  ( -0.1167790944451423119, 3.953555555631421470, -0.2819296736111110979 ) ) ;
#20101=CARTESIAN_POINT ( 'NONE',  ( 0.2819296736111110979, 3.838972222298087544, -3.452642723725051716E-17 ) ) ;
#20102=CARTESIAN_POINT ( 'NONE',  ( 0.2944344138913315145, 4.032913573979330479, -0.1032379509715019711 ) ) ;
#20107=CARTESIAN_POINT ( 'NONE',  ( 0.1993543840281266633, 4.443138888964754507, -0.1993543840281266910 ) ) ;
#20108=CARTESIAN_POINT ( 'NONE',  ( 0.3119999999999999996, 3.804249999999999243, -0.1292346314604056745 ) ) ;
#20109=CARTESIAN_POINT ( 'NONE',  ( 0.1678627478218750191, 0.06466217769286664030, 0.2733718836385306550 ) ) ;
#20111=CARTESIAN_POINT ( 'NONE',  ( -1.726321361862525858E-17, 3.797305555631421470, -0.2819296736111110979 ) ) ;
#20117=CARTESIAN_POINT ( 'NONE',  ( 0.1993543840281266355, 0.3618055554796889006, 0.1993543840281267465 ) ) ;
#20118=CARTESIAN_POINT ( 'NONE',  ( 0.004465723772902090855, 3.877046577749164502, -0.3119726078432636940 ) ) ;
#20125=CARTESIAN_POINT ( 'NONE',  ( -0.1292346314604056745, 4.707027777777776478, -0.3119999999999999996 ) ) ;
#20126=CARTESIAN_POINT ( 'NONE',  ( 0.3119999999999999996, 0.1326388888888885287, -0.1292346314604056468 ) ) ;
#20127=CARTESIAN_POINT ( 'NONE',  ( 0.1993543840281267465, 3.776472222298087988, 0.1993543840281266633 ) ) ;
#20130=CARTESIAN_POINT ( 'NONE',  ( 0.2819296736111110979, 4.502166666742532186, 0.1167790944451422425 ) ) ;
#20131=CARTESIAN_POINT ( 'NONE',  ( 0.1292346314603994850, 4.977861111111109516, -0.3120000000000061058 ) ) ;
#20132=ADVANCED_FACE ( 'NONE', ( #8243 ), #12783, .T. ) ;
#20135=CARTESIAN_POINT ( 'NONE',  ( 0.2984505573353404273, 4.360600408414049056, 0.09256242935286859708 ) ) ;
#20137=CARTESIAN_POINT ( 'NONE',  ( 0.1167790944451424368, 5.148000000075865223, 0.2819296736111110424 ) ) ;
#20138=CARTESIAN_POINT ( 'NONE',  ( 0.2318695005579780033, 4.203111999684435496, -0.2087629577079343768 ) ) ;
#20139=VECTOR ( 'NONE', #13574, 39.37007874015748143 ) ;
#20144=CARTESIAN_POINT ( 'NONE',  ( -0.1993543840281266910, 4.845916666742532186, -0.1993543840281266910 ) ) ;
#20145=CARTESIAN_POINT ( 'NONE',  ( -0.1873832016899178166, 4.065874456094106471, 0.2496566584368918318 ) ) ;
#20146=CARTESIAN_POINT ( 'NONE',  ( -0.1292346314604058410, 0.4381944442927114824, 0.3119999999999998885 ) ) ;
#20147=ORIENTED_EDGE ( 'NONE', *, *, #17351, .F. ) ;
#20148=CARTESIAN_POINT ( 'NONE',  ( 0.1993543840281266910, 0.3340277777019111660, -0.1993543840281266910 ) ) ;
#20149=CARTESIAN_POINT ( 'NONE',  ( 0.1167790944451423535, 0.2055555554796889006, 0.2819296736111110424 ) ) ;
#20151=CARTESIAN_POINT ( 'NONE',  ( -0.2081355123581232758, 5.196100638220133128, -0.1976311321815438227 ) ) ;
#20155=CARTESIAN_POINT ( 'NONE',  ( -0.2841659888207613283, 3.887232178795674287, -0.1299132057024031117 ) ) ;
#20157=CARTESIAN_POINT ( 'NONE',  ( 0.1993543840281267465, 4.498694444520309865, 0.1993543840281266633 ) ) ;
#20160=CARTESIAN_POINT ( 'NONE',  ( 0.3084280012298056262, 4.528428812793057645, 0.05274586746176852803 ) ) ;
#20161=CARTESIAN_POINT ( 'NONE',  ( -0.1167790944451423535, 5.099388888964754507, 0.2819296736111110424 ) ) ;
#20164=CARTESIAN_POINT ( 'NONE',  ( 0.3039537214805487775, 4.921172874434618372, -0.08137803535339727112 ) ) ;
#20167=EDGE_CURVE ( 'NONE', #9441, #3702, #13113, .T. ) ;
#20168=CARTESIAN_POINT ( 'NONE',  ( 0.2206173157302027954, 4.259111111262843252, -0.2206173157302028232 ) ) ;
#20169=CARTESIAN_POINT ( 'NONE',  ( 0.1993543840281267465, 4.554250000075866112, 0.1993543840281266633 ) ) ;
#20170=CARTESIAN_POINT ( 'NONE',  ( -0.2819296736111110424, 3.856333333409198705, 0.1167790944451424923 ) ) ;
#20171=ORIENTED_EDGE ( 'NONE', *, *, #9517, .F. ) ;
#20175=EDGE_LOOP ( 'NONE', ( #889, #9721, #2267, #4812 ) ) ;
#20177=CARTESIAN_POINT ( 'NONE',  ( -0.2491417453393007519, 4.952411878662227096, 0.1921816384585380566 ) ) ;
#20180=CARTESIAN_POINT ( 'NONE',  ( 0.3119999999999999996, 0.1777777776260448250, 0.000000000000000000 ) ) ;
#20182=CARTESIAN_POINT ( 'NONE',  ( -0.2147042302794207880, 3.717251267640226065, -0.2264494125071482844 ) ) ;
#20187=ORIENTED_EDGE ( 'NONE', *, *, #4151, .T. ) ;
#20188=CARTESIAN_POINT ( 'NONE',  ( 0.2385176312641979768, 5.092063675167946002, -0.2011546486555612634 ) ) ;
#20190=CARTESIAN_POINT ( 'NONE',  ( -0.1993543840281266910, 4.290361111186976828, -0.1993543840281266910 ) ) ;
#20191=CARTESIAN_POINT ( 'NONE',  ( 0.2819296736111110979, 5.050777777853643791, -0.1167790944451423396 ) ) ;
#20193=CARTESIAN_POINT ( 'NONE',  ( -0.3119999999999999996, 0.3722222220704893281, -3.820898013339742174E-17 ) ) ;
#20195=CARTESIAN_POINT ( 'NONE',  ( 0.2206173157302027954, 3.974388888888888083, -0.2206173157302028232 ) ) ;
#20197=CARTESIAN_POINT ( 'NONE',  ( -0.2206173157302028232, 4.939666666818398610, -0.2206173157302028232 ) ) ;
#20198=CARTESIAN_POINT ( 'NONE',  ( 0.1993543840281266633, 5.068138888964754507, -0.1993543840281266910 ) ) ;
#20203=CARTESIAN_POINT ( 'NONE',  ( -0.1504393870195933902, 0.05786178725312922377, 0.2687619224414409813 ) ) ;
#20204=ORIENTED_EDGE ( 'NONE', *, *, #12033, .F. ) ;
#20206=CARTESIAN_POINT ( 'NONE',  ( -0.2819296736111110424, 5.023000000075864335, 0.1167790944451424923 ) ) ;
#20209=EDGE_CURVE ( 'NONE', #11982, #11042, #5881, .T. ) ;
#20211=CARTESIAN_POINT ( 'NONE',  ( 0.2819296736111110979, 0.2159722221463555858, 0.000000000000000000 ) ) ;
#20215=ORIENTED_EDGE ( 'NONE', *, *, #23553, .F. ) ;
#20216=CARTESIAN_POINT ( 'NONE',  ( 0.1993543840281266633, 4.887583333409199149, -0.1993543840281266910 ) ) ;
#20217=CARTESIAN_POINT ( 'NONE',  ( -0.3120384249108475450, 4.169999822687207036, 0.04055185888031334618 ) ) ;
#20218=CARTESIAN_POINT ( 'NONE',  ( -0.3119999999999998885, 5.054249999999998799, 0.1292346314604058410 ) ) ;
#20220=CARTESIAN_POINT ( 'NONE',  ( 0.2340640474074713873, 0.06249999999999967387, 0.2102997499711236618 ) ) ;
#20221=CARTESIAN_POINT ( 'NONE',  ( -0.1292346314604056745, 4.651472222222221120, -0.3119999999999999996 ) ) ;
#20222=CARTESIAN_POINT ( 'NONE',  ( -0.1167790944451423119, 4.064666666742532186, -0.2819296736111110979 ) ) ;
#20223=CARTESIAN_POINT ( 'NONE',  ( -0.1167790944451423257, 3.745222222298088433, -0.2819296736111110424 ) ) ;
#20224=CARTESIAN_POINT ( 'NONE',  ( 0.3026829317664078700, 4.027635661132299205, 0.08109514562084400857 ) ) ;
#20227=VECTOR ( 'NONE', #12929, 39.37007874015748143 ) ;
#20230=CARTESIAN_POINT ( 'NONE',  ( 5.178964085587577574E-17, 4.200083333409199149, 0.2819296736111110979 ) ) ;
#20231=CARTESIAN_POINT ( 'NONE',  ( -0.3142628774615948695, 4.113298624980298968, 0.0008691249496092882118 ) ) ;
#20234=CARTESIAN_POINT ( 'NONE',  ( -0.2726213901831366915, 3.951241869235229576, 0.1571290601157238898 ) ) ;
#20239=AXIS2_PLACEMENT_3D ( 'NONE', #17315, #8040, #16951 ) ;
#20240=CARTESIAN_POINT ( 'NONE',  ( 0.2819296736111110424, 0.1986111110352444253, 0.1167790944451424923 ) ) ;
#20242=CARTESIAN_POINT ( 'NONE',  ( 0.2206173157302027676, 0.5666666666666663188, 0.2206173157302028787 ) ) ;
#20247=CARTESIAN_POINT ( 'NONE',  ( -0.1555525600596525115, 5.096577603750602314, -0.2701852920847304662 ) ) ;
#20249=CARTESIAN_POINT ( 'NONE',  ( 0.1292346314604056745, 0.02847222222222188515, -0.3119999999999999996 ) ) ;
#20250=CARTESIAN_POINT ( 'NONE',  ( -0.2819296736111110979, 3.755638888964754951, 0.000000000000000000 ) ) ;
#20253=CARTESIAN_POINT ( 'NONE',  ( 5.178964085587577574E-17, 4.436194444520310753, 0.2819296736111110979 ) ) ;
#20256=CARTESIAN_POINT ( 'NONE',  ( 5.731347020009612645E-17, 4.620222222222221120, 0.3119999999999999996 ) ) ;
#20258=CARTESIAN_POINT ( 'NONE',  ( 0.2927819169943106647, 4.360098288153534618, 0.1093008224459383754 ) ) ;
#20259=CARTESIAN_POINT ( 'NONE',  ( 0.2819296736111110979, 4.932722222298088433, 0.1167790944451422425 ) ) ;
#20260=EDGE_CURVE ( 'NONE', #20423, #7667, #21017, .T. ) ;
#20261=AXIS2_PLACEMENT_3D ( 'NONE', #4065, #18591, #16763 ) ;
#20262=CARTESIAN_POINT ( 'NONE',  ( 0.003964402099250808643, 4.210387593481760504, -0.3119783974053816911 ) ) ;
#20264=CARTESIAN_POINT ( 'NONE',  ( -0.2206173157302028787, 0.2194444444444441089, 0.2206173157302027954 ) ) ;
#20265=CARTESIAN_POINT ( 'NONE',  ( -0.1993543840281266910, 4.568138888964754507, -0.1993543840281266910 ) ) ;
#20268=CARTESIAN_POINT ( 'NONE',  ( -0.1167790944451424368, 0.4763888888130221599, 0.2819296736111110424 ) ) ;
#20270=CARTESIAN_POINT ( 'NONE',  ( -0.2819296736111110979, 0.3027777777019111660, 0.1167790944451422425 ) ) ;
#20271=CARTESIAN_POINT ( 'NONE',  ( -1.910449006669871087E-17, 4.203555555555555046, -0.3119999999999999996 ) ) ;
#20277=CARTESIAN_POINT ( 'NONE',  ( -0.2491303024454969428, 3.885307312177345818, -0.1878477653712340434 ) ) ;
#20278=CARTESIAN_POINT ( 'NONE',  ( 0.2819296736111110424, -0.01666666674253329886, -0.1167790944451423119 ) ) ;
#20280=CARTESIAN_POINT ( 'NONE',  ( 0.2819296736111110979, 4.561194444520310753, -3.452642723725051716E-17 ) ) ;
#20282=CARTESIAN_POINT ( 'NONE',  ( 0.2494586801225501804, 4.524212161881605354, 0.1883225769997851351 ) ) ;
#20283=CARTESIAN_POINT ( 'NONE',  ( 0.2819296736111110979, 5.168833333409199149, 0.1167790944451422425 ) ) ;
#20285=CARTESIAN_POINT ( 'NONE',  ( -0.2819296736111110979, 4.460500000075867000, -0.1167790944451422980 ) ) ;
#20286=FACE_OUTER_BOUND ( 'NONE', #11915, .T. ) ;
#20287=CARTESIAN_POINT ( 'NONE',  ( 1.910449006669871087E-17, 0.4694444442927115380, -0.3119999999999999996 ) ) ;
#20289=CARTESIAN_POINT ( 'NONE',  ( -0.3119999999999998885, 4.338972222373953969, 0.1292346314604058410 ) ) ;
#20290=CARTESIAN_POINT ( 'NONE',  ( -0.2819296736111110979, 4.474388888964753619, -0.1167790944451422980 ) ) ;
#20291=CARTESIAN_POINT ( 'NONE',  ( 0.1167790944451422702, 3.835500000075866556, -0.2819296736111110424 ) ) ;
#20293=VECTOR ( 'NONE', #19801, 39.37007874015748143 ) ;
#20297=CARTESIAN_POINT ( 'NONE',  ( 0.3119999999999999996, 4.248694444444443441, -0.1292346314604056745 ) ) ;
#20300=CARTESIAN_POINT ( 'NONE',  ( 0.3119999999999999996, 0.2888888887371559577, 0.000000000000000000 ) ) ;
#20302=CARTESIAN_POINT ( 'NONE',  ( -0.1658153428128203155, 3.715415045890231749, -0.2660418640364478615 ) ) ;
#20304=CARTESIAN_POINT ( 'NONE',  ( -0.3120000000000000551, 0.4937499999999996336, 0.1292346314604056190 ) ) ;
#20306=EDGE_LOOP ( 'NONE', ( #22170, #11222, #7250, #21260, #15885, #6758, #15536, #22633, #19543, #1010, #20622, #11691, #6745, #23771, #15687, #3679, #2626, #9846, #4931, #23260, #11909, #7970, #2550, #2418 ) ) ;
#20312=CARTESIAN_POINT ( 'NONE',  ( 0.1167790944451424368, 4.259111111186975940, 0.2819296736111110424 ) ) ;
#20313=CARTESIAN_POINT ( 'NONE',  ( 5.178964085587577574E-17, 5.088972222298087544, 0.2819296736111110979 ) ) ;
#20315=CARTESIAN_POINT ( 'NONE',  ( -0.1914634726864894720, 4.216274578790281780, -0.2496961836083926023 ) ) ;
#20316=CARTESIAN_POINT ( 'NONE',  ( 0.3119999999999999996, 3.856333333333332281, -3.820898013339742174E-17 ) ) ;
#20317=CARTESIAN_POINT ( 'NONE',  ( 0.2206173157302027954, 4.925777777929509327, -0.2206173157302028232 ) ) ;
#20318=CARTESIAN_POINT ( 'NONE',  ( 0.2672777582604971558, 4.802940054489442723, 0.1621179023351098369 ) ) ;
#20323=CARTESIAN_POINT ( 'NONE',  ( -0.1993543840281266910, 5.179250000075866112, -0.1993543840281266910 ) ) ;
#20327=ORIENTED_EDGE ( 'NONE', *, *, #15134, .F. ) ;
#20328=CARTESIAN_POINT ( 'NONE',  ( -0.1993543840281267465, 0.3062499999241333759, 0.1993543840281266633 ) ) ;
#20330=CARTESIAN_POINT ( 'NONE',  ( 0.1993543840281266633, 5.012583333409199149, -0.1993543840281266910 ) ) ;
#20331=CARTESIAN_POINT ( 'NONE',  ( 0.3131742759023632416, 4.473813942010830047, 0.02214152731887029241 ) ) ;
#20333=CARTESIAN_POINT ( 'NONE',  ( 5.178964085587577574E-17, 4.922305555631420582, 0.2819296736111110979 ) ) ;
#20335=( BOUNDED_CURVE ( )  B_SPLINE_CURVE ( 2, ( #13921, #21467, #19515, #6349, #15625, #17689, #2808, #6588, #14037 ),
 .UNSPECIFIED., .F., .F. ) 
 B_SPLINE_CURVE_WITH_KNOTS ( ( 3, 2, 2, 2, 3 ),
 ( 0.6875000000000000000, 0.6979166666666666297, 0.7083333333333333703, 0.7187500000000000000, 0.7291666666666666297 ),
 .UNSPECIFIED. ) 
 CURVE ( )  GEOMETRIC_REPRESENTATION_ITEM ( )  RATIONAL_B_SPLINE_CURVE ( ( 1.000000000000000000, 0.9238795325112867385, 1.000000000000000000, 0.9238795325112867385, 1.000000000000000000, 0.9238795325112867385, 1.000000000000000000, 0.9238795325112867385, 1.000000000000000000 ) ) 
 REPRESENTATION_ITEM ( '' )  );
#20336=CARTESIAN_POINT ( 'NONE',  ( -0.1292346314604124191, 5.040361111111109516, -0.3119999999999932272 ) ) ;
#20339=CARTESIAN_POINT ( 'NONE',  ( 0.3119999999999999996, 4.415361111111110404, -0.1292346314604056745 ) ) ;
#20340=CARTESIAN_POINT ( 'NONE',  ( 0.1167790944451424506, 4.036888888964753619, 0.2819296736111110424 ) ) ;
#20342=CARTESIAN_POINT ( 'NONE',  ( 0.1862751262687404319, 4.021747071989843825, 0.2502911891028875568 ) ) ;
#20345=CARTESIAN_POINT ( 'NONE',  ( 0.2206173157302028787, 3.904944444444443885, 0.2206173157302027954 ) ) ;
#20347=CARTESIAN_POINT ( 'NONE',  ( -0.1709082777654523100, 4.122007486075570881, 0.2610300066267514096 ) ) ;
#20349=DIRECTION ( 'NONE',  ( -0.000000000000000000, -1.000000000000000000, -0.000000000000000000 ) ) ;
#20357=CARTESIAN_POINT ( 'NONE',  ( 0.1167790944451423535, 0.1916666665908000333, 0.2819296736111110424 ) ) ;
#20358=CARTESIAN_POINT ( 'NONE',  ( -5.731347020009612645E-17, 0.2819444444444441089, 0.3119999999999999996 ) ) ;
#20359=CARTESIAN_POINT ( 'NONE',  ( 0.000000000000000000, 0.000000000000000000, 0.000000000000000000 ) ) ;
#20362=ORIENTED_EDGE ( 'NONE', *, *, #15967, .T. ) ;
#20364=CARTESIAN_POINT ( 'NONE',  ( -0.05073967362410713305, 5.093467254518128762, -0.3073318483525642741 ) ) ;
#20366=CARTESIAN_POINT ( 'NONE',  ( 0.1167790944451423535, 0.5805555554796888451, 0.2819296736111110424 ) ) ;
#20367=CARTESIAN_POINT ( 'NONE',  ( 0.2819296736111110979, 3.946611111186976384, 0.1167790944451422425 ) ) ;
#20371=CARTESIAN_POINT ( 'NONE',  ( 0.1993543840281267465, 4.332027777853642903, 0.1993543840281266633 ) ) ;
#20372=FACE_OUTER_BOUND ( 'NONE', #2992, .T. ) ;
#20373=LINE ( 'NONE', #1601, #20383 ) ;
#20375=DIRECTION ( 'NONE',  ( 1.000000000000000000, -0.000000000000000000, 1.224646799147353207E-16 ) ) ;
#20376=CARTESIAN_POINT ( 'NONE',  ( 0.1993543840281267465, 5.040361111186975940, 0.1993543840281266633 ) ) ;
#20378=( BOUNDED_CURVE ( )  B_SPLINE_CURVE ( 2, ( #17504, #10446, #13858 ),
 .UNSPECIFIED., .F., .F. ) 
 B_SPLINE_CURVE_WITH_KNOTS ( ( 3, 3 ),
 ( 0.9732142857142858094, 0.9771335280684947389 ),
 .UNSPECIFIED. ) 
 CURVE ( )  GEOMETRIC_REPRESENTATION_ITEM ( )  RATIONAL_B_SPLINE_CURVE ( ( 0.9999999999999981126, 0.9331730585143147572, 0.9836822358325096882 ) ) 
 REPRESENTATION_ITEM ( '' )  );
#20380=FACE_OUTER_BOUND ( 'NONE', #16412, .T. ) ;
#20381=CARTESIAN_POINT ( 'NONE',  ( 0.1167790944451424506, 4.703555555631420582, 0.2819296736111110424 ) ) ;
#20383=VECTOR ( 'NONE', #14287, 39.37007874015748143 ) ;
#20384=CARTESIAN_POINT ( 'NONE',  ( -0.04741907581679727368, 4.070294630609375908, 0.3093645555771465383 ) ) ;
#20386=CARTESIAN_POINT ( 'NONE',  ( -5.178964085587577574E-17, 0.5909722221463555858, 0.2819296736111110979 ) ) ;
#20388=CARTESIAN_POINT ( 'NONE',  ( -0.1167790944451424368, 0.1986111110352444808, 0.2819296736111110424 ) ) ;
#20396=CARTESIAN_POINT ( 'NONE',  ( -0.2558214270178758021, 3.885631657198463706, -0.1786047227777496083 ) ) ;
#20397=CARTESIAN_POINT ( 'NONE',  ( -5.178964085587577574E-17, 0.1881944443685778512, 0.2819296736111110979 ) ) ;
#20398=CARTESIAN_POINT ( 'NONE',  ( -0.1167790944451424368, 0.01805555547968892838, 0.2819296736111110424 ) ) ;
#20399=CARTESIAN_POINT ( 'NONE',  ( 0.1167790944451422702, 4.516055555631421470, -0.2819296736111110424 ) ) ;
#20401=CARTESIAN_POINT ( 'NONE',  ( 0.1993543840281267465, 5.054250000075865223, 0.1993543840281266633 ) ) ;
#20402=CARTESIAN_POINT ( 'NONE',  ( -0.1993543840281266910, 4.512583333409199149, -0.1993543840281266910 ) ) ;
#20403=CARTESIAN_POINT ( 'NONE',  ( 0.1521196438571344733, 3.742789775738293301, 0.2735830517299060460 ) ) ;
#20405=CARTESIAN_POINT ( 'NONE',  ( 0.3143848286800483005, 3.918459697589230739, 0.01319625459807933707 ) ) ;
#20406=CARTESIAN_POINT ( 'NONE',  ( -0.1292346314604057023, 4.068138889040620931, 0.3119999999999998885 ) ) ;
#20408=CARTESIAN_POINT ( 'NONE',  ( -0.1993543840281266355, 4.429250000075866112, 0.1993543840281267465 ) ) ;
#20413=CARTESIAN_POINT ( 'NONE',  ( -0.04527543151830683288, 4.848148877423151148, 0.3096339228700176749 ) ) ;
#20416=CARTESIAN_POINT ( 'NONE',  ( 0.2206173157302027676, 0.5041666665149336923, 0.2206173157302028787 ) ) ;
#20417=VERTEX_POINT ( 'NONE', #14054 ) ;
#20419=CARTESIAN_POINT ( 'NONE',  ( -0.1342463367781699390, 3.734338305776751188, 0.2818767121370694961 ) ) ;
#20423=VERTEX_POINT ( 'NONE', #11752 ) ;
#20426=CARTESIAN_POINT ( 'NONE',  ( 0.3116113683979374605, 5.085271449707127189, 0.01361995752066778517 ) ) ;
#20429=CARTESIAN_POINT ( 'NONE',  ( -0.2819296736111110424, 4.245222222298087544, 0.1167790944451424923 ) ) ;
#20430=CARTESIAN_POINT ( 'NONE',  ( -1.726321361862525858E-17, 5.172305555631420582, -0.2819296736111110979 ) ) ;
#20433=CARTESIAN_POINT ( 'NONE',  ( 0.1123264932791805809, 3.756093169699425083, -0.3119999999999999996 ) ) ;
#20434=CARTESIAN_POINT ( 'NONE',  ( -0.3119999999999999996, 4.665361111262842364, -0.1292346314604056468 ) ) ;
#20435=CARTESIAN_POINT ( 'NONE',  ( 0.2819296736111110979, 5.116750000075866112, -3.452642723725051716E-17 ) ) ;
#20436=B_SPLINE_CURVE_WITH_KNOTS ( 'NONE', 3,
 ( #4625, #10251, #12090, #19500, #2796, #965, #14025, #6093, #19619, #9767, #489, #11720, #19143, #9890, #17318, #1573, #10849, #22051, #3155, #19985, #8642, #14628, #5217, #6693, #21808, #10725, #17918, #18035, #14380, #23740, #6940, #7065, #5097, #14504, #1331, #1090, #19860, #12811, #12327, #16452, #8757, #18157, #23625, #18278, #19741, #23866, #2916, #9009, #16330, #8522, #14138, #12564, #16213, #1454, #3272, #7186, #8887, #5347 ),
 .UNSPECIFIED., .F., .F.,
 ( 4, 2, 1, 2, 2, 1, 1, 1, 1, 2, 2, 2, 1, 1, 1, 2, 2, 2, 2, 2, 2, 2, 1, 2, 2, 1, 2, 2, 2, 2, 2, 2, 2, 4 ),
 ( 0.4648409156512180451, 0.4660563802132510758, 0.4663602463537592779, 0.4665121794240134068, 0.4665216752409043210, 0.4665311710577951798, 0.4665501626915769529, 0.4665881459591404989, 0.4666641124942675911, 0.4672718447752841620, 0.4697027738993504453, 0.4709182384613835870, 0.4710701715316377158, 0.4711461380667647525, 0.4711841213343282986, 0.4712031129681100716, 0.4712221046018918447, 0.4715259707424001023, 0.4721337030234166732, 0.4733491675854497038, 0.4745646321474827900, 0.4757800967095158762, 0.4758560632446429128, 0.4758940465122064589, 0.4759320297797700050, 0.4760839628500241338, 0.4763878289905323915, 0.4769955612715489068, 0.4794264903956150792, 0.4818574195196811960, 0.4830728840817142822, 0.4836806163627308530, 0.4839844825032391107, 0.4842883486437473683 ),
 .UNSPECIFIED. ) ;
#20437=ORIENTED_EDGE ( 'NONE', *, *, #19318, .F. ) ;
#20439=AXIS2_PLACEMENT_3D ( 'NONE', #11424, #22749, #2397 ) ;
#20440=CARTESIAN_POINT ( 'NONE',  ( 0.2195746668131363655, 0.03828721274327267360, -0.1863886668264715940 ) ) ;
#20444=CARTESIAN_POINT ( 'NONE',  ( -0.2819296736111110979, 5.186194444520309865, 0.000000000000000000 ) ) ;
#20450=CARTESIAN_POINT ( 'NONE',  ( 0.2819296736111110424, 0.2680555554796889561, 0.1167790944451424923 ) ) ;
#20452=CARTESIAN_POINT ( 'NONE',  ( -0.2819296736111110424, 5.036888888964754507, 0.1167790944451424923 ) ) ;
#20453=CARTESIAN_POINT ( 'NONE',  ( 0.08714812177476737032, 4.485845587538219270, -0.2997357158451462444 ) ) ;
#20455=CARTESIAN_POINT ( 'NONE',  ( 0.2819296736111110979, 4.991750000075866112, -3.452642723725051716E-17 ) ) ;
#20458=CARTESIAN_POINT ( 'NONE',  ( 0.1292346314604068680, 4.588972222222221120, -0.3119999999999987228 ) ) ;
#20460=CARTESIAN_POINT ( 'NONE',  ( 0.2206173157302028787, 4.571611111111110404, 0.2206173157302027954 ) ) ;
#20461=CARTESIAN_POINT ( 'NONE',  ( 0.2819296736111110979, 3.936194444520309865, -3.452642723725051716E-17 ) ) ;
#20463=CARTESIAN_POINT ( 'NONE',  ( 0.2348144578000487537, 4.023596968965510889, 0.2061937808865371424 ) ) ;
#20464=CARTESIAN_POINT ( 'NONE',  ( 0.000000000000000000, 5.384999999999999787, 0.000000000000000000 ) ) ;
#20467=VERTEX_POINT ( 'NONE', #22944 ) ;
#20469=CARTESIAN_POINT ( 'NONE',  ( -0.1756959055429883343, 4.121843226292245532, 0.2578300476179096190 ) ) ;
#20472=CARTESIAN_POINT ( 'NONE',  ( 0.2562267853273828555, 4.635683002082432225, 0.1824161936367395542 ) ) ;
#20475=CARTESIAN_POINT ( 'NONE',  ( 8.984713656453739555E-13, 5.162518060853549251, -0.2988821118451543968 ) ) ;
#20478=CARTESIAN_POINT ( 'NONE',  ( 0.2819296736111110424, 0.2055555554796889006, -0.1167790944451423119 ) ) ;
#20479=CARTESIAN_POINT ( 'NONE',  ( 0.1005328971134487603, 3.874363271045468071, -0.2960644379690948180 ) ) ;
#20485=CARTESIAN_POINT ( 'NONE',  ( 0.3119999999999999996, 0.07708333333333300397, -0.1292346314604056468 ) ) ;
#20486=CARTESIAN_POINT ( 'NONE',  ( 0.3119999999999999996, 5.137583333333332725, -0.1292346314604056745 ) ) ;
#20488=ORIENTED_EDGE ( 'NONE', *, *, #1089, .F. ) ;
#20489=CARTESIAN_POINT ( 'NONE',  ( 0.1993543840281266633, 4.123694444520309865, -0.1993543840281266910 ) ) ;
#20494=CARTESIAN_POINT ( 'NONE',  ( 0.2479582629286654072, 4.357447403414685283, 0.1904730091441463047 ) ) ;
#20495=CARTESIAN_POINT ( 'NONE',  ( -0.2819296736111110424, 4.967444444520310753, 0.1167790944451424923 ) ) ;
#20499=CARTESIAN_POINT ( 'NONE',  ( 0.007859944718908516703, 3.710288412741159725, -0.3119151351536944006 ) ) ;
#20500=CARTESIAN_POINT ( 'NONE',  ( -0.2206173157302027954, 0.2055555555555551861, -0.2206173157302028232 ) ) ;
#20502=CARTESIAN_POINT ( 'NONE',  ( 0.1993543840281266633, 4.776472222298087544, -0.1993543840281266910 ) ) ;
#20504=CARTESIAN_POINT ( 'NONE',  ( -0.1492905759043549330, 4.067176878490561975, 0.2739898953200897158 ) ) ;
#20506=CARTESIAN_POINT ( 'NONE',  ( 0.1993543840281266355, 0.4312499999241333759, 0.1993543840281267465 ) ) ;
#20509=CARTESIAN_POINT ( 'NONE',  ( 1.726321361862525858E-17, 0.2298611110352444531, -0.2819296736111110979 ) ) ;
#20516=CARTESIAN_POINT ( 'NONE',  ( 0.1167790944451423119, 0.1569444443685777679, -0.2819296736111110979 ) ) ;
#20517=CARTESIAN_POINT ( 'NONE',  ( 0.2819296736111110424, 0.03888888881302225708, -0.1167790944451423119 ) ) ;
#20518=CARTESIAN_POINT ( 'NONE',  ( -0.2819296736111110424, 4.196611111186976828, -0.1167790944451423119 ) ) ;
#20520=CARTESIAN_POINT ( 'NONE',  ( -0.2819296736111110979, 5.088972222298087544, 0.000000000000000000 ) ) ;
#20521=CARTESIAN_POINT ( 'NONE',  ( -0.2819296736111110979, 4.408416666742532186, 0.000000000000000000 ) ) ;
#20522=CARTESIAN_POINT ( 'NONE',  ( 0.000000000000000000, 5.384999999999999787, 0.000000000000000000 ) ) ;
#20524=VECTOR ( 'NONE', #7195, 39.37007874015748143 ) ;
#20526=CARTESIAN_POINT ( 'NONE',  ( -0.2206173157302027676, 4.120222222373954857, 0.2206173157302028787 ) ) ;
#20535=DIRECTION ( 'NONE',  ( -0.000000000000000000, -1.000000000000000000, -0.000000000000000000 ) ) ;
#20539=CARTESIAN_POINT ( 'NONE',  ( 0.3119999999999998885, 0.5631944442927114824, 0.1292346314604058410 ) ) ;
#20543=CARTESIAN_POINT ( 'NONE',  ( 9.326145492192990669E-05, 4.766052907303594210, -0.3120000010180138394 ) ) ;
#20545=VERTEX_POINT ( 'NONE', #9917 ) ;
#20547=CARTESIAN_POINT ( 'NONE',  ( -1.903245722532910002E-17, 5.100068075568266579, -0.3108236144263021861 ) ) ;
#20549=CARTESIAN_POINT ( 'NONE',  ( 0.1167790944451424368, 4.203555555631420582, 0.2819296736111110424 ) ) ;
#20550=CARTESIAN_POINT ( 'NONE',  ( -0.1993543840281266355, 5.026472222298088433, 0.1993543840281267465 ) ) ;
#20553=CARTESIAN_POINT ( 'NONE',  ( 0.2206173157302027954, 3.863277777777777366, -0.2206173157302028232 ) ) ;
#20554=CARTESIAN_POINT ( 'NONE',  ( -1.910449006669871087E-17, 4.654944444596176290, -0.3119999999999999996 ) ) ;
#20555=CARTESIAN_POINT ( 'NONE',  ( -0.1993543840281266910, 5.137583333409199149, -0.1993543840281266910 ) ) ;
#20556=VECTOR ( 'NONE', #994, 39.37007874015748143 ) ;
#20564=CARTESIAN_POINT ( 'NONE',  ( 0.2819296736111110424, 5.050777777853643791, -0.1167790944451423396 ) ) ;
#20565=CARTESIAN_POINT ( 'NONE',  ( -0.1167790944451423535, 3.766055555631421470, 0.2819296736111110979 ) ) ;
#20567=CARTESIAN_POINT ( 'NONE',  ( -2.266361716303445225E-16, 4.432722222374099630, -0.3119999999999999996 ) ) ;
#20571=CARTESIAN_POINT ( 'NONE',  ( -0.1167790944451422702, 0.3999999999241333204, -0.2819296736111110979 ) ) ;
#20573=CARTESIAN_POINT ( 'NONE',  ( -0.1167790944451423535, 4.932722222298088433, 0.2819296736111110424 ) ) ;
#20574=CARTESIAN_POINT ( 'NONE',  ( 0.08172087692283847016, 4.462815503623632551, 0.3038682820922922190 ) ) ;
#20575=CARTESIAN_POINT ( 'NONE',  ( 0.2819296736111110424, 4.828555555631420582, -0.1167790944451423396 ) ) ;
#20577=CARTESIAN_POINT ( 'NONE',  ( 0.0007453629615518840784, 4.877146636198903984, -0.3119992385510536037 ) ) ;
#20580=CARTESIAN_POINT ( 'NONE',  ( 5.731347020009612645E-17, 4.509111111111110404, 0.3119999999999999996 ) ) ;
#20581=CARTESIAN_POINT ( 'NONE',  ( 5.178964085587577574E-17, 3.755638888964754951, 0.2819296736111110979 ) ) ;
#20582=CARTESIAN_POINT ( 'NONE',  ( 0.2206173157302027676, 0.3374999998482670627, 0.2206173157302028787 ) ) ;
#20584=CARTESIAN_POINT ( 'NONE',  ( -0.1049254751525411922, 3.735256410060579846, 0.2938276733034849153 ) ) ;
#20585=CARTESIAN_POINT ( 'NONE',  ( 0.3111759409473714988, 4.584880126860398697, 0.02273571722973519171 ) ) ;
#20586=ORIENTED_EDGE ( 'NONE', *, *, #15134, .T. ) ;
#20591=LINE ( 'NONE', #11332, #19667 ) ;
#20596=CARTESIAN_POINT ( 'NONE',  ( -0.1167790944451422702, 0.3305555554796889561, -0.2819296736111110424 ) ) ;
#20602=CARTESIAN_POINT ( 'NONE',  ( -0.2691620460978288443, 5.100921413008813410, -0.1566095457824691894 ) ) ;
#20603=CARTESIAN_POINT ( 'NONE',  ( -0.2206173157302028232, 4.710499999999999687, -0.2206173157302028232 ) ) ;
#20604=CARTESIAN_POINT ( 'NONE',  ( -0.2206173157302028787, 0.1638888888888885287, 0.2206173157302027954 ) ) ;
#20605=CARTESIAN_POINT ( 'NONE',  ( 0.3646812958242482416, 3.728225405753418098, -0.06420867857498598064 ) ) ;
#20608=CARTESIAN_POINT ( 'NONE',  ( 0.2819296736111110424, 4.231333333409199149, -0.1167790944451423396 ) ) ;
#20609=CARTESIAN_POINT ( 'NONE',  ( 0.3119999999999999996, 0.1256944442927115102, -0.1292346314604056468 ) ) ;
#20613=CARTESIAN_POINT ( 'NONE',  ( 0.2819296736111110979, 4.988277777853642903, 0.1167790944451422425 ) ) ;
#20614=CARTESIAN_POINT ( 'NONE',  ( 0.1913604482712364940, 4.188439349523841670, 0.2497711034849461054 ) ) ;
#20617=CARTESIAN_POINT ( 'NONE',  ( 0.2819296736111110979, 4.602861111186975940, -3.452642723725051716E-17 ) ) ;
#20621=CARTESIAN_POINT ( 'NONE',  ( 0.2819296736111110424, 0.5458333332574666352, 0.1167790944451424923 ) ) ;
#20622=ORIENTED_EDGE ( 'NONE', *, *, #8548, .T. ) ;
#20623=CARTESIAN_POINT ( 'NONE',  ( 0.2819296736111110424, 0.3236111110352444253, 0.1167790944451424923 ) ) ;
#20624=CYLINDRICAL_SURFACE ( 'NONE', #11977, 0.3119999999999999996 ) ;
#20630=DIRECTION ( 'NONE',  ( -0.000000000000000000, -1.000000000000000000, -0.000000000000000000 ) ) ;
#20631=CARTESIAN_POINT ( 'NONE',  ( -0.2819296736111111534, 0.1777777777019111938, 0.1167790944451422563 ) ) ;
#20632=CARTESIAN_POINT ( 'NONE',  ( 0.2819296736111110424, 0.09444444436857780956, -0.1167790944451423119 ) ) ;
#20633=CARTESIAN_POINT ( 'NONE',  ( -0.2819296736111110979, 4.200083333409199149, 0.000000000000000000 ) ) ;
#20635=EDGE_CURVE ( 'NONE', #12983, #18582, #9977, .T. ) ;
#20636=CARTESIAN_POINT ( 'NONE',  ( 0.2819296736111110424, 4.953555555631421470, -0.1167790944451423396 ) ) ;
#20637=CARTESIAN_POINT ( 'NONE',  ( 0.1993543840281266633, 4.554250000075866112, -0.1993543840281266910 ) ) ;
#20642=CARTESIAN_POINT ( 'NONE',  ( -0.2206173157302028232, 4.161888889040620931, -0.2206173157302028232 ) ) ;
#20644=LINE ( 'NONE', #2242, #21210 ) ;
#20646=EDGE_CURVE ( 'NONE', #10582, #3466, #3669, .T. ) ;
#20649=CARTESIAN_POINT ( 'NONE',  ( 0.000000000000000000, 0.06249999999999967387, 0.3119999999999999996 ) ) ;
#20653=CARTESIAN_POINT ( 'NONE',  ( -0.3119999999999999996, 0.5388888887371559022, -3.820898013339742174E-17 ) ) ;
#20655=VECTOR ( 'NONE', #11860, 39.37007874015748143 ) ;
#20661=ORIENTED_EDGE ( 'NONE', *, *, #8461, .T. ) ;
#20665=CARTESIAN_POINT ( 'NONE',  ( -0.1292346314604106428, 4.061194444444443441, 0.3119999999999950036 ) ) ;
#20667=CARTESIAN_POINT ( 'NONE',  ( -0.1167790944451423257, 4.064666666742532186, -0.2819296736111110424 ) ) ;
#20670=CARTESIAN_POINT ( 'NONE',  ( 0.1129719973630488317, 5.040650656955687481, -0.2914126276313158126 ) ) ;
#20672=CARTESIAN_POINT ( 'NONE',  ( 0.1292346314604058410, 3.790361111111110404, 0.3119999999999998885 ) ) ;
#20673=CARTESIAN_POINT ( 'NONE',  ( -0.2206173157302027676, 4.675777777929510215, 0.2206173157302028787 ) ) ;
#20674=CARTESIAN_POINT ( 'NONE',  ( -0.1167790944451423535, 5.099388888964754507, 0.2819296736111110979 ) ) ;
#20676=CARTESIAN_POINT ( 'NONE',  ( -0.1993543840281266910, 4.345916666742532186, -0.1993543840281266910 ) ) ;
#20677=CARTESIAN_POINT ( 'NONE',  ( -0.1274622673633111769, 3.901219489371187343, 0.2865353922227728556 ) ) ;
#20684=CARTESIAN_POINT ( 'NONE',  ( 0.1993543840281266633, 5.165361111186976828, -0.1993543840281266910 ) ) ;
#20685=CARTESIAN_POINT ( 'NONE',  ( 0.2819296736111110979, 3.786888888964754507, -0.1167790944451423396 ) ) ;
#20690=CARTESIAN_POINT ( 'NONE',  ( -0.1993543840281266633, 0.5145833332574666352, -0.1993543840281266910 ) ) ;
#20693=CARTESIAN_POINT ( 'NONE',  ( 0.1993543840281267465, 4.998694444520309865, 0.1993543840281266633 ) ) ;
#20695=EDGE_CURVE ( 'NONE', #6543, #8220, #20733, .T. ) ;
#20696=CARTESIAN_POINT ( 'NONE',  ( -0.1993543840281266910, 4.901472222298087544, -0.1993543840281266910 ) ) ;
#20697=CARTESIAN_POINT ( 'NONE',  ( -0.08067706695034009001, 4.180438756533890299, 0.3020759868123111813 ) ) ;
#20698=CARTESIAN_POINT ( 'NONE',  ( 0.1567781121482516860, 4.854100146818556283, 0.2702798039214149295 ) ) ;
#20699=CARTESIAN_POINT ( 'NONE',  ( 5.731347020009612645E-17, 4.175777777777776478, 0.3119999999999999996 ) ) ;
#20701=CARTESIAN_POINT ( 'NONE',  ( 0.3119999999999999996, 4.411888888888888083, -3.820898013339742174E-17 ) ) ;
#20702=CARTESIAN_POINT ( 'NONE',  ( -0.2819296736111110979, 3.741750000075865668, 0.000000000000000000 ) ) ;
#20703=CARTESIAN_POINT ( 'NONE',  ( -0.1292346314604032043, 4.207027777777776478, -0.3120000000000024420 ) ) ;
#20710=CARTESIAN_POINT ( 'NONE',  ( -0.2726212802448290673, 3.941984754839822802, -0.1571292508600286020 ) ) ;
#20711=CARTESIAN_POINT ( 'NONE',  ( 0.3033563106615940752, 5.146283422524257745, -0.006787276862509872624 ) ) ;
#20715=CARTESIAN_POINT ( 'NONE',  ( -0.1993543840281266633, 0.5562499999241333759, -0.1993543840281266910 ) ) ;
#20716=DIRECTION ( 'NONE',  ( 0.000000000000000000, 0.000000000000000000, 1.000000000000000000 ) ) ;
#20718=CARTESIAN_POINT ( 'NONE',  ( -0.3119999999999999996, 0.1534722222222218990, -0.1292346314604056745 ) ) ;
#20722=CARTESIAN_POINT ( 'NONE',  ( 0.1292346314604057023, 0.3409722222222218435, 0.3119999999999998885 ) ) ;
#20723=CARTESIAN_POINT ( 'NONE',  ( -0.2206173157302027676, 5.113277777777777366, 0.2206173157302028787 ) ) ;
#20724=CARTESIAN_POINT ( 'NONE',  ( 5.178964085587577574E-17, 4.158416666742532186, 0.2819296736111110979 ) ) ;
#20730=CARTESIAN_POINT ( 'NONE',  ( 0.1993543840281266633, 4.943138888964754507, -0.1993543840281266910 ) ) ;
#20733=B_SPLINE_CURVE_WITH_KNOTS ( 'NONE', 3,
 ( #2080, #15251, #1834, #4148, #24022, #22682, #5855, #22200, #11116, #7687, #22564, #11477, #18912, #5972, #2213, #14784, #5500, #9402, #18663, #16841, #12963, #9643, #17077, #18545, #368, #16720, #1425, #7450, #14897, #22317, #5617, #23033, #8396, #15847, #17679, #4738, #10015, #2684, #15492, #7920, #21095, #13562, #4507, #17559, #613 ),
 .UNSPECIFIED., .F., .F.,
 ( 4, 2, 2, 2, 2, 2, 2, 1, 2, 2, 2, 2, 2, 2, 2, 2, 2, 2, 2, 2, 2, 2, 4 ),
 ( 0.06676172314147620079, 0.06751374342960875241, 0.06826576371774129015, 0.06976980429400639339, 0.07127384487027149662, 0.07277788544653658598, 0.07352990573466913760, 0.07428192602280167534, 0.07503394631093422695, 0.07578596659906677857, 0.07729000717533186793, 0.07804202746346441955, 0.07879404775159697116, 0.08029808832786206052, 0.08105010861599461214, 0.08180212890412716376, 0.08330616948039225311, 0.08481021005665734247, 0.08556223034478989409, 0.08631425063292244571, 0.08781829120918754894, 0.08932233178545265218, 0.09082637236171775541 ),
 .UNSPECIFIED. ) ;
#20734=CARTESIAN_POINT ( 'NONE',  ( 0.1568014993035689308, 4.187283761971905882, 0.2727961053911494571 ) ) ;
#20738=CARTESIAN_POINT ( 'NONE',  ( 0.1993543840281266633, 4.401472222298088433, -0.1993543840281266910 ) ) ;
#20741=CARTESIAN_POINT ( 'NONE',  ( -1.910449006669871087E-17, 4.314666666666665762, -0.3119999999999999996 ) ) ;
#20743=CARTESIAN_POINT ( 'NONE',  ( 0.2819296736111110424, 0.6083333332574668573, -0.1167790944451423119 ) ) ;
#20745=CARTESIAN_POINT ( 'NONE',  ( 0.1993543840281266355, 0.5423611110352445364, 0.1993543840281267465 ) ) ;
#20746=CARTESIAN_POINT ( 'NONE',  ( 0.3120000000000000551, 4.130638888888888083, 0.1292346314604056190 ) ) ;
#20753=CARTESIAN_POINT ( 'NONE',  ( -0.1993543840281267465, 0.2368055554796889561, 0.1993543840281266633 ) ) ;
#20754=CARTESIAN_POINT ( 'NONE',  ( 0.2819296736111110424, 0.3166666665908000056, -0.1167790944451423119 ) ) ;
#20756=CARTESIAN_POINT ( 'NONE',  ( -0.2819296736111110424, 4.307722222298088433, -0.1167790944451423119 ) ) ;
#20758=CARTESIAN_POINT ( 'NONE',  ( -0.1993543840281266910, 4.970916666742532186, -0.1993543840281266910 ) ) ;
#20759=CARTESIAN_POINT ( 'NONE',  ( -0.1167790944451423535, 4.529944444520309865, 0.2819296736111110979 ) ) ;
#20760=CARTESIAN_POINT ( 'NONE',  ( 0.2615470475763201352, 5.073407320188289660, 0.1707168293479552346 ) ) ;
#20761=CARTESIAN_POINT ( 'NONE',  ( -8.964115882027956832E-07, 3.710500024236165206, -0.3119999999987121964 ) ) ;
#20762=CARTESIAN_POINT ( 'NONE',  ( -0.3119999999999999996, 4.109805555707288782, -0.1292346314604056468 ) ) ;
#20764=EDGE_CURVE ( 'NONE', #1879, #2780, #19312, .T. ) ;
#20772=CARTESIAN_POINT ( 'NONE',  ( -0.04066036887665752664, 4.989443942244452757, -0.3119999862560016712 ) ) ;
#20774=CARTESIAN_POINT ( 'NONE',  ( -0.2206173157302028787, 0.6013888887371559022, 0.2206173157302027954 ) ) ;
#20775=CYLINDRICAL_SURFACE ( 'NONE', #20261, 0.3119999999999999996 ) ;
#20777=CARTESIAN_POINT ( 'NONE',  ( -3.345742422185251127E-06, 4.766055647721512578, -0.3119999999820609049 ) ) ;
#20779=CARTESIAN_POINT ( 'NONE',  ( 0.009615703107365407981, 5.190106621824546629, -0.2891886902264009795 ) ) ;
#20780=ORIENTED_EDGE ( 'NONE', *, *, #1230, .T. ) ;
#20783=CARTESIAN_POINT ( 'NONE',  ( -0.2228749573452438737, 4.675693542979938222, 0.2183525872440850724 ) ) ;
#20785=CARTESIAN_POINT ( 'NONE',  ( 5.178964085587577574E-17, 4.033416666742532186, 0.2819296736111110979 ) ) ;
#20787=CARTESIAN_POINT ( 'NONE',  ( -1.910449006669871087E-17, 4.814666666666665762, -0.3119999999999999996 ) ) ;
#20788=CARTESIAN_POINT ( 'NONE',  ( -1.910449006669871087E-17, 3.925777777777776922, -0.3119999999999999996 ) ) ;
#20789=CARTESIAN_POINT ( 'NONE',  ( 0.3119999999999999996, 4.755638889040620043, -0.1292346314604056745 ) ) ;
#20790=CARTESIAN_POINT ( 'NONE',  ( -0.1993543840281266910, 4.859805555631421470, -0.1993543840281266910 ) ) ;
#20791=EDGE_LOOP ( 'NONE', ( #9744, #21400, #3257, #19326 ) ) ;
#20793=EDGE_CURVE ( 'NONE', #9670, #3584, #20436, .T. ) ;
#20794=CARTESIAN_POINT ( 'NONE',  ( -0.1993543840281266355, 4.248694444520309865, 0.1993543840281267465 ) ) ;
#20795=EDGE_CURVE ( 'NONE', #23206, #11776, #23633, .T. ) ;
#20800=AXIS2_PLACEMENT_3D ( 'NONE', #12287, #23343, #4817 ) ;
#20804=CARTESIAN_POINT ( 'NONE',  ( -0.2819296736111110979, 3.918833333409198705, -0.1167790944451422980 ) ) ;
#20805=CARTESIAN_POINT ( 'NONE',  ( 0.02037670883466128138, 4.432138282695498255, -0.3119999999999997220 ) ) ;
#20810=CARTESIAN_POINT ( 'NONE',  ( 0.1167790944451423119, 0.3930555554796889561, -0.2819296736111110979 ) ) ;
#20812=CARTESIAN_POINT ( 'NONE',  ( 0.2819296736111110424, 4.953555555631421470, -0.1167790944451423396 ) ) ;
#20813=CARTESIAN_POINT ( 'NONE',  ( 0.1918522775149521797, 4.466287634334791257, 0.2494131876992732866 ) ) ;
#20814=CARTESIAN_POINT ( 'NONE',  ( -0.2819296736111110424, 4.634111111186976828, 0.1167790944451424923 ) ) ;
#20817=CARTESIAN_POINT ( 'NONE',  ( 0.2903586046000930510, 4.866586313092618354, -0.1141781630894242727 ) ) ;
#20820=CARTESIAN_POINT ( 'NONE',  ( -1.910449006669871087E-17, 4.536888888888888083, -0.3119999999999999996 ) ) ;
#20823=CARTESIAN_POINT ( 'NONE',  ( -0.1292346314604057300, 4.227861111111110404, 0.3119999999999998885 ) ) ;
#20825=CARTESIAN_POINT ( 'NONE',  ( 0.3108980883051527533, 4.584783822353920790, 0.02619940625674591766 ) ) ;
#20828=CARTESIAN_POINT ( 'NONE',  ( 0.0003785305096514256316, 4.710489828778345434, -0.3119998034525927055 ) ) ;
#20829=CARTESIAN_POINT ( 'NONE',  ( 0.09510778779462622512, 4.652184472055949094, -0.2980982098042628814 ) ) ;
#20835=CARTESIAN_POINT ( 'NONE',  ( -0.1993543840281266633, 0.5006944443685777957, -0.1993543840281266910 ) ) ;
#20840=CARTESIAN_POINT ( 'NONE',  ( 2.064578755398029967E-15, 5.043833333485014947, -0.3119999999999999996 ) ) ;
#20843=CARTESIAN_POINT ( 'NONE',  ( 0.3120000000000000551, 4.741749999999998799, 0.1292346314604056190 ) ) ;
#20844=CARTESIAN_POINT ( 'NONE',  ( 0.2206173157302028232, 0.1916666666666663466, -0.2206173157302028232 ) ) ;
#20845=CARTESIAN_POINT ( 'NONE',  ( 0.3119999999999999996, 5.130638888888888083, 0.1292346314604056190 ) ) ;
#20846=CARTESIAN_POINT ( 'NONE',  ( 0.2819296736111110979, 4.224388888964755395, 0.1167790944451422425 ) ) ;
#20849=DIRECTION ( 'NONE',  ( -0.000000000000000000, -1.000000000000000000, -0.000000000000000000 ) ) ;
#20850=ORIENTED_EDGE ( 'NONE', *, *, #17960, .F. ) ;
#20853=CARTESIAN_POINT ( 'NONE',  ( 0.2819296736111110979, 4.769527777853642903, -3.452642723725051716E-17 ) ) ;
#20859=CARTESIAN_POINT ( 'NONE',  ( 0.1993543840281267465, 4.220916666742532186, 0.1993543840281266633 ) ) ;
#20861=CARTESIAN_POINT ( 'NONE',  ( 7.459700445346810805E-07, 4.043833313442511290, -0.3119999999991081574 ) ) ;
#20863=CARTESIAN_POINT ( 'NONE',  ( 0.000000000000000000, 5.384999999999999787, -0.3119999999999999996 ) ) ;
#20866=CARTESIAN_POINT ( 'NONE',  ( -0.1993543840281267465, 0.3618055554796889561, 0.1993543840281266633 ) ) ;
#20867=CARTESIAN_POINT ( 'NONE',  ( -0.2663696356376525909, 5.203905143399228272, 0.09717633342841931754 ) ) ;
#20872=CARTESIAN_POINT ( 'NONE',  ( -0.1167790944451424506, 0.5180555554796888451, 0.2819296736111110424 ) ) ;
#20873=CARTESIAN_POINT ( 'NONE',  ( -0.2819296736111110979, 0.1777777777019111383, 0.1167790944451422425 ) ) ;
#20875=CARTESIAN_POINT ( 'NONE',  ( 0.2819296736111110424, 4.286888888964754507, -0.1167790944451423396 ) ) ;
#20877=CARTESIAN_POINT ( 'NONE',  ( 5.178964085587577574E-17, 4.880638888964754507, 0.2819296736111110979 ) ) ;
#20878=CARTESIAN_POINT ( 'NONE',  ( 0.2819296736111110979, 4.273000000075865223, -0.1167790944451423396 ) ) ;
#20881=CARTESIAN_POINT ( 'NONE',  ( -0.1292346314604056745, 4.047305555707287894, -0.3119999999999999996 ) ) ;
#20890=CARTESIAN_POINT ( 'NONE',  ( -0.06305314479216488077, 0.03242967361111057795, 0.2752503750687063100 ) ) ;
#20893=CARTESIAN_POINT ( 'NONE',  ( -0.3119999999999999996, 0.5423611109593782231, 0.1292346314604056190 ) ) ;
#20904=EDGE_CURVE ( 'NONE', #6065, #21824, #2119, .T. ) ;
#20905=CARTESIAN_POINT ( 'NONE',  ( -0.1993543840281266910, 4.068138888964754507, -0.1993543840281266910 ) ) ;
#20907=CARTESIAN_POINT ( 'NONE',  ( 0.1357040439698322387, 5.122023438247767402, 0.2773560592096749877 ) ) ;
#20908=CARTESIAN_POINT ( 'NONE',  ( -0.2380092882192336723, 5.172599870306766157, -0.1756940437445040915 ) ) ;
#20909=CARTESIAN_POINT ( 'NONE',  ( 0.3119999999999999996, 4.807722222373953969, -3.820898013339742174E-17 ) ) ;
#20911=CARTESIAN_POINT ( 'NONE',  ( -0.2819296736111110424, 4.981333333409200037, 0.1167790944451424923 ) ) ;
#20913=CARTESIAN_POINT ( 'NONE',  ( 0.2819296736111110979, 4.213972222298087544, -3.452642723725051716E-17 ) ) ;
#20919=ORIENTED_EDGE ( 'NONE', *, *, #12330, .F. ) ;
#20921=CARTESIAN_POINT ( 'NONE',  ( 0.1292346314604057300, 0.2854166666666662633, 0.3119999999999998885 ) ) ;
#20922=CARTESIAN_POINT ( 'NONE',  ( 0.1993543840281267465, 3.832027777853643791, 0.1993543840281266633 ) ) ;
#20923=DIRECTION ( 'NONE',  ( -0.000000000000000000, -1.000000000000000000, -0.000000000000000000 ) ) ;
#20924=CARTESIAN_POINT ( 'NONE',  ( 0.2206173157302028787, 4.627166666666665762, 0.2206173157302027954 ) ) ;
#20929=CARTESIAN_POINT ( 'NONE',  ( -5.178964085587577574E-17, 0.4243055554796889006, 0.2819296736111110979 ) ) ;
#20933=CARTESIAN_POINT ( 'NONE',  ( 5.178964085587577574E-17, 4.713972222298088433, 0.2819296736111110979 ) ) ;
#20934=CARTESIAN_POINT ( 'NONE',  ( 0.2956865686883918820, 4.471526487522247351, 0.1000891740342018943 ) ) ;
#20935=CARTESIAN_POINT ( 'NONE',  ( -0.1993543840281266355, 4.693138888964754507, 0.1993543840281267465 ) ) ;
#20936=DIRECTION ( 'NONE',  ( -0.000000000000000000, -1.000000000000000000, -0.000000000000000000 ) ) ;
#20937=CARTESIAN_POINT ( 'NONE',  ( 0.2218613123050385549, 4.870266018951173947, -0.2206117788904509158 ) ) ;
#20940=CARTESIAN_POINT ( 'NONE',  ( 5.731347020009612645E-17, 4.342444444444443441, 0.3119999999999999996 ) ) ;
#20942=CARTESIAN_POINT ( 'NONE',  ( 0.2819296736111111534, 3.766055555631421026, 0.1167790944451422563 ) ) ;
#20946=CARTESIAN_POINT ( 'NONE',  ( 0.3115085581940752468, 4.585014881649954965, 0.01788609438656960440 ) ) ;
#20948=CARTESIAN_POINT ( 'NONE',  ( 0.06090392925245493444, 4.708829327785332808, -0.3064243836155239320 ) ) ;
#20951=CARTESIAN_POINT ( 'NONE',  ( 0.3120466542833977841, 4.308815547343077590, -0.04051276955858209433 ) ) ;
#20955=EDGE_CURVE ( 'NONE', #606, #20467, #7350, .T. ) ;
#20956=CARTESIAN_POINT ( 'NONE',  ( -0.1167790944451422702, 0.4972222221463556413, -0.2819296736111110424 ) ) ;
#20957=CARTESIAN_POINT ( 'NONE',  ( -0.009764748067830458442, 5.206640035683669510, 0.2819296736110837309 ) ) ;
#20959=CARTESIAN_POINT ( 'NONE',  ( 0.1292346314604056745, 0.5284722222222218990, -0.3119999999999999996 ) ) ;
#20961=CARTESIAN_POINT ( 'NONE',  ( -0.09977969951898062184, 5.115641765141615949, 0.2926989633898121057 ) ) ;
#20964=CARTESIAN_POINT ( 'NONE',  ( -5.731347020009612645E-17, 0.2263888888888885564, 0.3119999999999999996 ) ) ;
#20965=CARTESIAN_POINT ( 'NONE',  ( 0.2206173157302027954, 5.085499999999998799, -0.2206173157302028232 ) ) ;
#20966=CARTESIAN_POINT ( 'NONE',  ( -0.2819296736111110424, 4.141055555631421470, -0.1167790944451423119 ) ) ;
#20967=CARTESIAN_POINT ( 'NONE',  ( -1.910449006669871087E-17, 3.814666666666665762, -0.3119999999999999996 ) ) ;
#20971=CARTESIAN_POINT ( 'NONE',  ( -0.1167790944451423535, 4.807722222298087544, 0.2819296736111110424 ) ) ;
#20975=CARTESIAN_POINT ( 'NONE',  ( 0.02244429927890741541, 3.709892914452737500, -0.3112240927256947898 ) ) ;
#20976=CARTESIAN_POINT ( 'NONE',  ( -1.726321361862525858E-17, 4.297305555631421470, -0.2819296736111110979 ) ) ;
#20978=CARTESIAN_POINT ( 'NONE',  ( -0.01914896636169877847, 4.044354364280504655, -0.3114118915433974344 ) ) ;
#20982=CARTESIAN_POINT ( 'NONE',  ( -0.2819296736111110424, 0.3513888888130222155, -0.1167790944451423396 ) ) ;
#20987=LINE ( 'NONE', #9786, #5600 ) ;
#20988=CARTESIAN_POINT ( 'NONE',  ( 0.2206173157302027954, 5.029944444444443441, -0.2206173157302028232 ) ) ;
#20989=CARTESIAN_POINT ( 'NONE',  ( 0.1993543840281266910, 0.5423611110352445364, -0.1993543840281266910 ) ) ;
#20990=CARTESIAN_POINT ( 'NONE',  ( 0.1167790944451423535, 0.1361111110352444808, 0.2819296736111110424 ) ) ;
#20992=CARTESIAN_POINT ( 'NONE',  ( 0.2819296736111110979, 4.227861111186976828, -3.452642723725051716E-17 ) ) ;
#20995=CARTESIAN_POINT ( 'NONE',  ( -1.726321361862525858E-17, 4.908416666742532186, -0.2819296736111110979 ) ) ;
#20997=CARTESIAN_POINT ( 'NONE',  ( 5.178964085587577574E-17, 4.255638888964754507, 0.2819296736111110979 ) ) ;
#20998=CYLINDRICAL_SURFACE ( 'NONE', #11411, 0.3119999999999999996 ) ;
#21000=CARTESIAN_POINT ( 'NONE',  ( 0.2206173157302028787, 4.516055555555555046, 0.2206173157302027954 ) ) ;
#21001=CARTESIAN_POINT ( 'NONE',  ( 0.3119999999999999996, 3.807722222373953969, -3.820898013339742174E-17 ) ) ;
#21008=CARTESIAN_POINT ( 'NONE',  ( -0.2368311528898977558, 5.008462562740330526, 0.2031552041900300254 ) ) ;
#21010=CARTESIAN_POINT ( 'NONE',  ( 0.3119999999999998885, 0.6187499998482670627, 0.1292346314604058410 ) ) ;
#21012=CARTESIAN_POINT ( 'NONE',  ( 0.1915112473476633104, 4.244112575941767496, 0.2496615136355418429 ) ) ;
#21016=CARTESIAN_POINT ( 'NONE',  ( 0.2640909437941768578, 5.182232675516351250, -0.1266275688248941766 ) ) ;
#21017=( BOUNDED_CURVE ( )  B_SPLINE_CURVE ( 2, ( #9552, #22710, #2361, #15405, #9309, #4176, #13466, #7717, #400 ),
 .UNSPECIFIED., .F., .T. ) 
 B_SPLINE_CURVE_WITH_KNOTS ( ( 3, 2, 2, 2, 3 ),
 ( 0.2291666666666666574, 0.2395833333333333426, 0.2500000000000000000, 0.2604166666666666852, 0.2708333333333333148 ),
 .UNSPECIFIED. ) 
 CURVE ( )  GEOMETRIC_REPRESENTATION_ITEM ( )  RATIONAL_B_SPLINE_CURVE ( ( 1.000000000000000000, 0.9238795325112867385, 1.000000000000000000, 0.9238795325112867385, 1.000000000000000000, 0.9238795325112867385, 1.000000000000000000, 0.9238795325112867385, 1.000000000000000000 ) ) 
 REPRESENTATION_ITEM ( '' )  );
#21024=CARTESIAN_POINT ( 'NONE',  ( -0.1993543840281266910, 3.957027777853642903, -0.1993543840281266910 ) ) ;
#21026=CARTESIAN_POINT ( 'NONE',  ( -0.2928190810534017641, 5.180208114765485483, 0.01414289444493066483 ) ) ;
#21027=CARTESIAN_POINT ( 'NONE',  ( 0.1292346314604058410, 4.630638889040620931, 0.3119999999999998885 ) ) ;
#21028=CARTESIAN_POINT ( 'NONE',  ( -0.1993543840281266355, 5.040361111186977716, 0.1993543840281267465 ) ) ;
#21030=CARTESIAN_POINT ( 'NONE',  ( -0.2819296736111110424, 4.349388888964754507, -0.1167790944451423119 ) ) ;
#21035=EDGE_CURVE ( 'NONE', #789, #23019, #12592, .T. ) ;
#21041=CARTESIAN_POINT ( 'NONE',  ( 0.000000000000000000, 5.384999999999999787, 0.000000000000000000 ) ) ;
#21042=CARTESIAN_POINT ( 'NONE',  ( -0.1292346314604056190, 0.1395833331816004053, -0.3119999999999999996 ) ) ;
#21043=CARTESIAN_POINT ( 'NONE',  ( 0.08947733366648276399, 4.407491422679668425, 0.2989658942065363534 ) ) ;
#21046=CARTESIAN_POINT ( 'NONE',  ( -1.910449006669871087E-17, 4.925777777777777366, -0.3119999999999999996 ) ) ;
#21048=CARTESIAN_POINT ( 'NONE',  ( 1.726321361862525858E-17, 0.5631944443685776847, -0.2819296736111110979 ) ) ;
#21051=CARTESIAN_POINT ( 'NONE',  ( 0.2819296736111110424, 4.731333333409200925, -0.1167790944451423396 ) ) ;
#21053=CARTESIAN_POINT ( 'NONE',  ( 0.1993543840281267465, 4.707027777853643791, 0.1993543840281266633 ) ) ;
#21054=CARTESIAN_POINT ( 'NONE',  ( -5.731347020009612645E-17, 0.2749999998482670627, 0.3119999999999999996 ) ) ;
#21056=CARTESIAN_POINT ( 'NONE',  ( 0.2853224037306363869, 4.866967269276749164, -0.1262817630124163093 ) ) ;
#21057=CARTESIAN_POINT ( 'NONE',  ( 3.820898013339742174E-17, 5.384999999999999787, 0.3119999999999999996 ) ) ;
#21059=CARTESIAN_POINT ( 'NONE',  ( 0.1292346314604058410, 4.179249999999998799, 0.3119999999999998885 ) ) ;
#21061=CARTESIAN_POINT ( 'NONE',  ( 0.1015006192750689679, 3.724843167714382286, -0.2819296736111111534 ) ) ;
#21062=CARTESIAN_POINT ( 'NONE',  ( -1.054647954922321762E-07, 4.988277780858759947, -0.3119999999999820695 ) ) ;
#21065=ORIENTED_EDGE ( 'NONE', *, *, #14087, .F. ) ;
#21066=CARTESIAN_POINT ( 'NONE',  ( 0.1554048093938449615, 4.687324857274296264, 0.2736299092323108972 ) ) ;
#21069=CIRCLE ( 'NONE', #13699, 0.3119999999999999996 ) ;
#21070=CARTESIAN_POINT ( 'NONE',  ( 0.04078035003190004504, 4.294990863552893501, 0.3120001095418362125 ) ) ;
#21074=CARTESIAN_POINT ( 'NONE',  ( 1.726321361862525858E-17, 0.5493055554796888451, -0.2819296736111110979 ) ) ;
#21075=CARTESIAN_POINT ( 'NONE',  ( -0.1317548836793264455, 5.206640035683668621, 0.2500202773221226193 ) ) ;
#21083=CARTESIAN_POINT ( 'NONE',  ( -5.731347020009612645E-17, 0.2819444444444441089, 0.3119999999999999996 ) ) ;
#21084=CARTESIAN_POINT ( 'NONE',  ( -0.1292346314604056745, 4.873694444444444329, -0.3119999999999999996 ) ) ;
#21085=CARTESIAN_POINT ( 'NONE',  ( -0.2819296736111110424, 3.981333333409199593, 0.1167790944451424923 ) ) ;
#21086=CARTESIAN_POINT ( 'NONE',  ( -0.04085484144393203287, 4.322780934022267374, -0.3119999999289135850 ) ) ;
#21087=DIRECTION ( 'NONE',  ( 0.000000000000000000, 0.000000000000000000, 1.000000000000000000 ) ) ;
#21088=CARTESIAN_POINT ( 'NONE',  ( 0.3013753051098548297, 4.810095209863023413, -0.08402212184464949440 ) ) ;
#21092=CARTESIAN_POINT ( 'NONE',  ( 0.2819296736111110979, 4.710500000075865223, 0.1167790944451422425 ) ) ;
#21095=CARTESIAN_POINT ( 'NONE',  ( -0.09708543963280202860, 5.164879205389378392, 0.2826001691826344753 ) ) ;
#21096=EDGE_CURVE ( 'NONE', #3466, #12593, #3276, .T. ) ;
#21100=CARTESIAN_POINT ( 'NONE',  ( 0.000000000000000000, 5.384999999999999787, 0.000000000000000000 ) ) ;
#21101=CARTESIAN_POINT ( 'NONE',  ( -0.2819296736111110979, 4.307722222298088433, -0.1167790944451422980 ) ) ;
#21102=EDGE_CURVE ( 'NONE', #14570, #3466, #8497, .T. ) ;
#21107=CARTESIAN_POINT ( 'NONE',  ( 0.2819296736111110424, 0.3791666665908000611, 0.1167790944451424923 ) ) ;
#21108=CARTESIAN_POINT ( 'NONE',  ( 0.000000000000000000, 5.384999999999999787, 0.000000000000000000 ) ) ;
#21109=CARTESIAN_POINT ( 'NONE',  ( -1.910449006669871087E-17, 4.481333333333331836, -0.3119999999999999996 ) ) ;
#21114=CARTESIAN_POINT ( 'NONE',  ( 0.1167790944451423119, 0.3791666665908000611, -0.2819296736111110979 ) ) ;
#21115=CARTESIAN_POINT ( 'NONE',  ( 1.726321361862525858E-17, 0.1604166665908000333, -0.2819296736111110979 ) ) ;
#21117=CARTESIAN_POINT ( 'NONE',  ( -1.726321361862525858E-17, 3.963972222298087988, -0.2819296736111110979 ) ) ;
#21119=CARTESIAN_POINT ( 'NONE',  ( 0.2819296736111110424, 4.786888888964755395, -0.1167790944451423396 ) ) ;
#21120=( BOUNDED_CURVE ( )  B_SPLINE_CURVE ( 2, ( #21952, #10872, #14779, #120, #18658, #20609, #9152, #22312, #9035 ),
 .UNSPECIFIED., .F., .F. ) 
 B_SPLINE_CURVE_WITH_KNOTS ( ( 3, 2, 2, 2, 3 ),
 ( 0.1458333333333333426, 0.1562500000000000000, 0.1666666666666666574, 0.1770833333333333426, 0.1875000000000000000 ),
 .UNSPECIFIED. ) 
 CURVE ( )  GEOMETRIC_REPRESENTATION_ITEM ( )  RATIONAL_B_SPLINE_CURVE ( ( 1.000000000000000000, 0.9238795325112867385, 1.000000000000000000, 0.9238795325112867385, 1.000000000000000000, 0.9238795325112867385, 1.000000000000000000, 0.9238795325112867385, 1.000000000000000000 ) ) 
 REPRESENTATION_ITEM ( '' )  );
#21121=CARTESIAN_POINT ( 'NONE',  ( 0.3122281832482405317, 5.078663991669950306, -0.005250876328984169575 ) ) ;
#21122=ORIENTED_EDGE ( 'NONE', *, *, #19683, .F. ) ;
#21124=CARTESIAN_POINT ( 'NONE',  ( 5.731347020009612645E-17, 3.793833333485065573, 0.3119999999999999996 ) ) ;
#21134=CARTESIAN_POINT ( 'NONE',  ( 0.2819296736111110979, 0.04930555547968892144, 0.000000000000000000 ) ) ;
#21136=CARTESIAN_POINT ( 'NONE',  ( 0.2659125765915840711, 4.257081166359744984, -0.1637272094895568519 ) ) ;
#21137=CARTESIAN_POINT ( 'NONE',  ( 0.000000000000000000, 5.384999999999999787, 0.000000000000000000 ) ) ;
#21138=CARTESIAN_POINT ( 'NONE',  ( 0.2552298690385793600, 4.090937613976504572, -0.1843366434591496850 ) ) ;
#21145=CARTESIAN_POINT ( 'NONE',  ( 0.1993543840281267465, 4.095916666742532186, 0.1993543840281266633 ) ) ;
#21146=B_SPLINE_CURVE_WITH_KNOTS ( 'NONE', 3,
 ( #8640, #962, #15728, #12088, #8277, #4504, #19739, #1087, #17434, #8156, #3038, #8519, #23142, #14022, #21213, #15610, #2912, #19857 ),
 .UNSPECIFIED., .F., .F.,
 ( 4, 2, 2, 2, 2, 2, 2, 2, 4 ),
 ( 0.7949730820619140825, 0.7972563070159356391, 0.7995395319699570846, 0.8018227569239786412, 0.8041059818780001978, 0.8063892068320216433, 0.8086724317860431999, 0.8109556567400646454, 0.8132388816940862020 ),
 .UNSPECIFIED. ) ;
#21147=CARTESIAN_POINT ( 'NONE',  ( -0.09380593400082881672, 0.03242967361111052244, 0.2658661084243340578 ) ) ;
#21148=CARTESIAN_POINT ( 'NONE',  ( -0.2548359695741092557, 5.185457950352025946, 0.1418493590379871494 ) ) ;
#21149=CARTESIAN_POINT ( 'NONE',  ( 0.2206173157302027954, 4.592444444596176290, -0.2206173157302028232 ) ) ;
#21151=CARTESIAN_POINT ( 'NONE',  ( 0.2819296736111110979, 4.838972222298088433, -3.452642723725051716E-17 ) ) ;
#21152=ORIENTED_EDGE ( 'NONE', *, *, #21842, .T. ) ;
#21153=CARTESIAN_POINT ( 'NONE',  ( -0.1167790944451423535, 3.974388888964754063, 0.2819296736111110424 ) ) ;
#21160=CARTESIAN_POINT ( 'NONE',  ( 1.910449006669871087E-17, 0.3097222222222218435, -0.3119999999999999996 ) ) ;
#21161=CARTESIAN_POINT ( 'NONE',  ( 0.2206173157302027676, 0.05972222207048929338, 0.2206173157302028787 ) ) ;
#21162=CARTESIAN_POINT ( 'NONE',  ( 0.3033084913416829176, 5.145647145552547208, 0.01295876866797208288 ) ) ;
#21164=CARTESIAN_POINT ( 'NONE',  ( -5.731347020009612645E-17, 0.1638888887371559577, 0.3119999999999999996 ) ) ;
#21165=CARTESIAN_POINT ( 'NONE',  ( -5.731347020009612645E-17, 0.3305555554038226429, 0.3119999999999999996 ) ) ;
#21169=CARTESIAN_POINT ( 'NONE',  ( -0.2819296736111110979, 0.1187499999241333620, -3.452642723725051716E-17 ) ) ;
#21171=CARTESIAN_POINT ( 'NONE',  ( -1.726321361862525858E-17, 4.686194444520309865, -0.2819296736111110979 ) ) ;
#21173=CARTESIAN_POINT ( 'NONE',  ( -0.1993543840281266910, 4.623694444520309865, -0.1993543840281266910 ) ) ;
#21174=CARTESIAN_POINT ( 'NONE',  ( -0.001112167594266136794, 4.154976392104846816, -0.3119983012180029269 ) ) ;
#21179=CARTESIAN_POINT ( 'NONE',  ( -0.2206173157302027676, 4.224388888888888083, 0.2206173157302028787 ) ) ;
#21180=CARTESIAN_POINT ( 'NONE',  ( 0.2206173157302027954, 5.148000000151732536, -0.2206173157302028232 ) ) ;
#21181=CARTESIAN_POINT ( 'NONE',  ( 0.2828693099792405352, 4.978340185095941450, -0.1368988876663677356 ) ) ;
#21183=CARTESIAN_POINT ( 'NONE',  ( 0.1337988207375339911, 4.575549332303573635, 0.2837483186149677983 ) ) ;
#21186=AXIS2_PLACEMENT_3D ( 'NONE', #4016, #18532, #15240 ) ;
#21189=CARTESIAN_POINT ( 'NONE',  ( 0.3110870456949443863, 4.140046527910736351, 0.03488342758349934764 ) ) ;
#21193=CARTESIAN_POINT ( 'NONE',  ( 0.1993543840281266355, 0.4729166665908000611, 0.1993543840281267465 ) ) ;
#21194=CARTESIAN_POINT ( 'NONE',  ( -0.03908633756214337229, 5.206640035683666845, 0.2793782410116296688 ) ) ;
#21196=CARTESIAN_POINT ( 'NONE',  ( 0.3119999999999999996, 0.5215277777777775903, -0.1292346314604056468 ) ) ;
#21200=CARTESIAN_POINT ( 'NONE',  ( -0.2467709493912808305, 5.110806576942171553, 0.1882333731734037174 ) ) ;
#21202=DIRECTION ( 'NONE',  ( 1.000000000000000000, -0.000000000000000000, 1.224646799147353207E-16 ) ) ;
#21203=CARTESIAN_POINT ( 'NONE',  ( -0.3119999999999999996, 0.3756944444444441089, -0.1292346314604056745 ) ) ;
#21204=CARTESIAN_POINT ( 'NONE',  ( 5.731347020009612645E-17, 5.009111111111110404, 0.3119999999999999996 ) ) ;
#21206=CARTESIAN_POINT ( 'NONE',  ( -0.1167790944451423535, 3.877166666742531742, 0.2819296736111110424 ) ) ;
#21207=CARTESIAN_POINT ( 'NONE',  ( -0.2206173157302027676, 3.835499999999998799, 0.2206173157302028787 ) ) ;
#21209=CARTESIAN_POINT ( 'NONE',  ( 0.07179678270565797993, 4.819533739383511595, -0.3060367993099030737 ) ) ;
#21210=VECTOR ( 'NONE', #5882, 39.37007874015748143 ) ;
#21213=CARTESIAN_POINT ( 'NONE',  ( -0.1571291158571934687, 3.992938027066821771, -0.2726213563812835972 ) ) ;
#21214=CARTESIAN_POINT ( 'NONE',  ( 0.1167790944451422702, 4.724388888964754507, -0.2819296736111110424 ) ) ;
#21222=CARTESIAN_POINT ( 'NONE',  ( 0.1993543840281267465, 4.276472222298088433, 0.1993543840281266633 ) ) ;
#21224=CARTESIAN_POINT ( 'NONE',  ( -0.2206173157302028232, 4.877166666666665762, -0.2206173157302028232 ) ) ;
#21227=DIRECTION ( 'NONE',  ( -0.000000000000000000, -1.000000000000000000, -0.000000000000000000 ) ) ;
#21229=CARTESIAN_POINT ( 'NONE',  ( -0.1167790944451422702, 0.5111111110352446474, -0.2819296736111110424 ) ) ;
#21231=CARTESIAN_POINT ( 'NONE',  ( 0.3120000000000000551, 4.463972222222222008, 0.1292346314604056190 ) ) ;
#21237=CARTESIAN_POINT ( 'NONE',  ( -0.02548689453205812278, 3.766744744258326172, -0.3109991600399485412 ) ) ;
#21238=CARTESIAN_POINT ( 'NONE',  ( 1.726321361862525858E-17, 0.4381944443685778512, -0.2819296736111110979 ) ) ;
#21239=CARTESIAN_POINT ( 'NONE',  ( -0.2819296736111110979, 0.2888888888130223265, 0.1167790944451422425 ) ) ;
#21242=CARTESIAN_POINT ( 'NONE',  ( 0.2819296736111110979, 4.061194444520309865, -3.452642723725051716E-17 ) ) ;
#21245=CARTESIAN_POINT ( 'NONE',  ( -0.1167790944451423535, 4.543833333409199149, 0.2819296736111110424 ) ) ;
#21246=CARTESIAN_POINT ( 'NONE',  ( 0.2710853860383645730, 5.083076204145490884, -0.1547793690661009858 ) ) ;
#21247=VERTEX_POINT ( 'NONE', #13792 ) ;
#21248=CARTESIAN_POINT ( 'NONE',  ( 0.1292346314604031765, 4.033416666666667538, -0.3120000000000024420 ) ) ;
#21249=CARTESIAN_POINT ( 'NONE',  ( 0.3119999999999999996, 3.863277777929509771, -3.820898013339742174E-17 ) ) ;
#21253=CARTESIAN_POINT ( 'NONE',  ( 0.1125312330130331800, 0.03242967361111057795, 0.2589088460590495688 ) ) ;
#21257=CARTESIAN_POINT ( 'NONE',  ( -0.2919173025508979280, 4.998982188319265774, -0.1102035603291813132 ) ) ;
#21258=ORIENTED_EDGE ( 'NONE', *, *, #4587, .T. ) ;
#21259=CARTESIAN_POINT ( 'NONE',  ( 1.910449006669871087E-17, 0.6361111109593781121, -0.3119999999999999996 ) ) ;
#21260=ORIENTED_EDGE ( 'NONE', *, *, #11057, .T. ) ;
#21267=CARTESIAN_POINT ( 'NONE',  ( -0.2491085460084383196, 4.662980843054849167, -0.1922337267564872276 ) ) ;
#21268=CARTESIAN_POINT ( 'NONE',  ( -0.1993543840281266910, 3.845916666742532186, -0.1993543840281266910 ) ) ;
#21269=CARTESIAN_POINT ( 'NONE',  ( 0.2596226291738499281, 5.035194357586231462, -0.1734927606623648810 ) ) ;
#21271=CARTESIAN_POINT ( 'NONE',  ( -5.731347020009612645E-17, 0.3305555554038226429, 0.3119999999999999996 ) ) ;
#21272=CARTESIAN_POINT ( 'NONE',  ( -0.1292346314604057023, 4.512583333485064685, 0.3119999999999998885 ) ) ;
#21273=EDGE_CURVE ( 'NONE', #7634, #19443, #15252, .T. ) ;
#21274=CARTESIAN_POINT ( 'NONE',  ( -1.726321361862525858E-17, 4.686194444520309865, -0.2819296736111110979 ) ) ;
#21276=CARTESIAN_POINT ( 'NONE',  ( 0.2819296736111110979, 4.158416666742532186, -3.452642723725051716E-17 ) ) ;
#21281=ORIENTED_EDGE ( 'NONE', *, *, #17202, .T. ) ;
#21287=CARTESIAN_POINT ( 'NONE',  ( 0.1844455389852084348, 5.136728975353069160, 0.2436424482298817917 ) ) ;
#21290=CARTESIAN_POINT ( 'NONE',  ( 0.1167790944451423119, 0.1013888888130222571, -0.2819296736111110979 ) ) ;
#21294=CARTESIAN_POINT ( 'NONE',  ( 0.1167790944451422702, 4.668833333409200037, -0.2819296736111110424 ) ) ;
#21297=CARTESIAN_POINT ( 'NONE',  ( 0.1940838408004180171, 3.748630699786517528, -0.2346081964820543042 ) ) ;
#21300=CARTESIAN_POINT ( 'NONE',  ( -0.3119999999999998885, 4.220916666666665762, 0.1292346314604058410 ) ) ;
#21302=CARTESIAN_POINT ( 'NONE',  ( 0.3119999999999999996, 5.200083333485065573, -0.1292346314604056745 ) ) ;
#21303=CARTESIAN_POINT ( 'NONE',  ( 0.09556577126599200001, 4.963224787294483242, 0.2971471245525674210 ) ) ;
#21308=( BOUNDED_CURVE ( )  B_SPLINE_CURVE ( 2, ( #20256, #12469, #10631, #18303, #12718, #5370, #16479, #12959, #12837 ),
 .UNSPECIFIED., .F., .T. ) 
 B_SPLINE_CURVE_WITH_KNOTS ( ( 3, 2, 2, 2, 3 ),
 ( 0.4196428571428572063, 0.4241071428571429047, 0.4285714285714286031, 0.4330357142857143571, 0.4375000000000000555 ),
 .UNSPECIFIED. ) 
 CURVE ( )  GEOMETRIC_REPRESENTATION_ITEM ( )  RATIONAL_B_SPLINE_CURVE ( ( 0.9999999999999990008, 0.9238795325112877377, 1.000000000000000000, 0.9238795325112867385, 1.000000000000000000, 0.9238795325112867385, 1.000000000000000000, 0.9238795325112857393, 1.000000000000000888 ) ) 
 REPRESENTATION_ITEM ( '' )  );
#21310=CARTESIAN_POINT ( 'NONE',  ( 0.04847343760161313547, 4.684065114164263299, 0.3082221411203268646 ) ) ;
#21320=CARTESIAN_POINT ( 'NONE',  ( 0.000000000000000000, 5.384999999999999787, 0.000000000000000000 ) ) ;
#21322=CARTESIAN_POINT ( 'NONE',  ( -0.1379734605153020432, 4.623101557285290042, 0.2798964025940948175 ) ) ;
#21325=DIRECTION ( 'NONE',  ( -0.000000000000000000, -1.000000000000000000, -0.000000000000000000 ) ) ;
#21326=CARTESIAN_POINT ( 'NONE',  ( 0.3119999999999998885, 0.5701388888888886397, 0.1292346314604058410 ) ) ;
#21327=CARTESIAN_POINT ( 'NONE',  ( -0.1292346314604056745, 5.040361111111110404, -0.3119999999999999996 ) ) ;
#21328=CARTESIAN_POINT ( 'NONE',  ( -0.1993543840281266355, 3.984805555631421470, 0.1993543840281267465 ) ) ;
#21329=DIRECTION ( 'NONE',  ( -0.000000000000000000, -1.000000000000000000, -0.000000000000000000 ) ) ;
#21335=CARTESIAN_POINT ( 'NONE',  ( 5.178964085587577574E-17, 4.644527777853642903, 0.2819296736111110979 ) ) ;
#21340=ADVANCED_FACE ( 'NONE', ( #9892 ), #18915, .T. ) ;
#21342=CARTESIAN_POINT ( 'NONE',  ( 0.1167790944451422702, 4.016055555631422358, -0.2819296736111110979 ) ) ;
#21348=CARTESIAN_POINT ( 'NONE',  ( -0.1993543840281267465, 0.07013888881302225708, 0.1993543840281266633 ) ) ;
#21357=CARTESIAN_POINT ( 'NONE',  ( -0.1993543840281267465, 0.5145833332574667462, 0.1993543840281266633 ) ) ;
#21358=CARTESIAN_POINT ( 'NONE',  ( 0.2819296736111110424, 0.5319444443685777957, 0.1167790944451424923 ) ) ;
#21359=CARTESIAN_POINT ( 'NONE',  ( 0.2819296736111110979, 4.168833333409199149, 0.1167790944451422425 ) ) ;
#21362=CARTESIAN_POINT ( 'NONE',  ( 0.2819296736111110979, 4.668833333409200037, 0.1167790944451422425 ) ) ;
#21365=VERTEX_POINT ( 'NONE', #7692 ) ;
#21366=VERTEX_POINT ( 'NONE', #15140 ) ;
#21368=CARTESIAN_POINT ( 'NONE',  ( -0.3119999999999999996, 3.776472222373954413, -0.1292346314604056468 ) ) ;
#21373=ORIENTED_EDGE ( 'NONE', *, *, #21697, .F. ) ;
#21376=CARTESIAN_POINT ( 'NONE',  ( 0.2819296736111110424, 0.1638888888130222432, -0.1167790944451423119 ) ) ;
#21378=CARTESIAN_POINT ( 'NONE',  ( 0.0007571358743316145218, 4.266035208878255602, -0.3119992139512273166 ) ) ;
#21380=CARTESIAN_POINT ( 'NONE',  ( 0.3137470792316710555, 4.086203903373451851, -0.02617354482465570481 ) ) ;
#21382=CARTESIAN_POINT ( 'NONE',  ( -0.3119999999999999996, 4.491749999999999687, -0.1292346314604056468 ) ) ;
#21387=CARTESIAN_POINT ( 'NONE',  ( -0.1167790944451423535, 5.210500000075866112, 0.2819296736111110424 ) ) ;
#21388=SPHERICAL_SURFACE ( 'NONE', #8676, 0.3119999999999999996 ) ;
#21391=CARTESIAN_POINT ( 'NONE',  ( -0.3133020153825915033, 4.780755246673074055, 0.02780367048916862482 ) ) ;
#21392=CARTESIAN_POINT ( 'NONE',  ( -0.2206173157302027676, 4.564666666818398610, 0.2206173157302028787 ) ) ;
#21393=CARTESIAN_POINT ( 'NONE',  ( 0.1993543840281267465, 4.720916666742533074, 0.1993543840281266633 ) ) ;
#21396=CARTESIAN_POINT ( 'NONE',  ( -0.2819296736111110424, 4.071611111186976828, -0.1167790944451423119 ) ) ;
#21400=ORIENTED_EDGE ( 'NONE', *, *, #10756, .T. ) ;
#21402=CARTESIAN_POINT ( 'NONE',  ( 0.3119999999999998885, 0.4590277777777774237, 0.1292346314604058410 ) ) ;
#21404=DIRECTION ( 'NONE',  ( -0.000000000000000000, -1.000000000000000000, -0.000000000000000000 ) ) ;
#21405=DIRECTION ( 'NONE',  ( -0.000000000000000000, -1.000000000000000000, -0.000000000000000000 ) ) ;
#21408=DIRECTION ( 'NONE',  ( 0.000000000000000000, 0.000000000000000000, -1.000000000000000000 ) ) ;
#21409=CARTESIAN_POINT ( 'NONE',  ( 0.2819296736111110424, 0.1430555554796889284, 0.1167790944451424923 ) ) ;
#21412=CARTESIAN_POINT ( 'NONE',  ( -0.1167790944451423257, 4.509111111186976828, -0.2819296736111110424 ) ) ;
#21413=CARTESIAN_POINT ( 'NONE',  ( -0.1167790944451423535, 5.196611111186976828, 0.2819296736111110979 ) ) ;
#21416=CARTESIAN_POINT ( 'NONE',  ( 0.3119999999999999996, 0.4590277776260448528, -0.1292346314604056468 ) ) ;
#21417=CARTESIAN_POINT ( 'NONE',  ( -0.1292346314604057023, 4.172305555555555046, 0.3119999999999998885 ) ) ;
#21418=CARTESIAN_POINT ( 'NONE',  ( 0.2383741534419201169, 5.072285808806758389, 0.2028604780184855572 ) ) ;
#21424=CARTESIAN_POINT ( 'NONE',  ( -0.3120460406368502637, 4.889979835822584775, -0.04045770392581769098 ) ) ;
#21429=ADVANCED_FACE ( 'NONE', ( #552 ), #316, .T. ) ;
#21430=CARTESIAN_POINT ( 'NONE',  ( 0.04084074131989445106, 3.820513810923966691, -0.3119999999999996110 ) ) ;
#21439=CARTESIAN_POINT ( 'NONE',  ( -0.04998852818392456737, 4.600835773807371964, -0.3081328456724486964 ) ) ;
#21442=CARTESIAN_POINT ( 'NONE',  ( 0.2206173157302028232, 0.3583333333333329485, -0.2206173157302028232 ) ) ;
#21443=CARTESIAN_POINT ( 'NONE',  ( 0.3119999999999999996, 5.019527777777777366, 0.1292346314604056190 ) ) ;
#21444=CARTESIAN_POINT ( 'NONE',  ( 0.1993543840281266633, 4.220916666742532186, -0.1993543840281266910 ) ) ;
#21445=CARTESIAN_POINT ( 'NONE',  ( 0.2819296736111110979, 3.950083333409199149, -3.452642723725051716E-17 ) ) ;
#21446=( BOUNDED_CURVE ( )  B_SPLINE_CURVE ( 2, ( #10867, #13189, #1945, #18414, #16831, #14647, #20603, #20125, #18296 ),
 .UNSPECIFIED., .F., .T. ) 
 B_SPLINE_CURVE_WITH_KNOTS ( ( 3, 2, 2, 2, 3 ),
 ( 0.3482142857142856429, 0.3526785714285713969, 0.3571428571428570953, 0.3616071428571428492, 0.3660714285714285476 ),
 .UNSPECIFIED. ) 
 CURVE ( )  GEOMETRIC_REPRESENTATION_ITEM ( )  RATIONAL_B_SPLINE_CURVE ( ( 1.000000000000000888, 0.9238795325112857393, 1.000000000000000000, 0.9238795325112867385, 1.000000000000000000, 0.9238795325112867385, 1.000000000000000000, 0.9238795325112867385, 1.000000000000000000 ) ) 
 REPRESENTATION_ITEM ( '' )  );
#21452=ORIENTED_EDGE ( 'NONE', *, *, #20904, .T. ) ;
#21454=CARTESIAN_POINT ( 'NONE',  ( 0.2819296736111110424, 4.439666666742532186, -0.1167790944451423396 ) ) ;
#21456=VECTOR ( 'NONE', #17790, 39.37007874015748143 ) ;
#21460=CARTESIAN_POINT ( 'NONE',  ( 0.2819296736111111534, 4.002166666742532186, 0.1167790944451422563 ) ) ;
#21461=CARTESIAN_POINT ( 'NONE',  ( -0.3119999999999999996, 0.3756944444444441089, -0.1292346314604056745 ) ) ;
#21465=CARTESIAN_POINT ( 'NONE',  ( -5.178964085587577574E-17, 0.1326388888130222710, 0.2819296736111110979 ) ) ;
#21467=CARTESIAN_POINT ( 'NONE',  ( -0.1292346314604056190, 0.4243055555555552139, -0.3119999999999999996 ) ) ;
#21469=DIRECTION ( 'NONE',  ( -0.000000000000000000, -1.000000000000000000, -0.000000000000000000 ) ) ;
#21474=CARTESIAN_POINT ( 'NONE',  ( 1.910449006669871087E-17, 0.4138888887371559577, -0.3119999999999999996 ) ) ;
#21475=CARTESIAN_POINT ( 'NONE',  ( -0.2819296736111110979, 0.4555555554796890116, 0.1167790944451422425 ) ) ;
#21476=CARTESIAN_POINT ( 'NONE',  ( 0.2819296736111110424, 4.064666666742532186, -0.1167790944451423396 ) ) ;
#21478=CARTESIAN_POINT ( 'NONE',  ( -0.1167790944451423257, 4.689666666742532186, -0.2819296736111110424 ) ) ;
#21479=CARTESIAN_POINT ( 'NONE',  ( 0.2755744112216236830, 5.134589151667465323, -0.1342242742989331605 ) ) ;
#21483=CARTESIAN_POINT ( 'NONE',  ( 0.2206173157302027954, 3.925777777929509771, -0.2206173157302028232 ) ) ;
#21486=ORIENTED_EDGE ( 'NONE', *, *, #20086, .F. ) ;
#21487=CARTESIAN_POINT ( 'NONE',  ( -0.2819296736111110424, 4.856333333409198261, 0.1167790944451424923 ) ) ;
#21489=ORIENTED_EDGE ( 'NONE', *, *, #20955, .T. ) ;
#21490=CARTESIAN_POINT ( 'NONE',  ( -0.3091906612878179694, 5.115463718648684655, 0.01877637416671624343 ) ) ;
#21492=CARTESIAN_POINT ( 'NONE',  ( -0.2819296736111110979, 0.2437499999241333759, -3.452642723725051716E-17 ) ) ;
#21493=CARTESIAN_POINT ( 'NONE',  ( 0.1993543840281266910, 0.1118055554796889145, -0.1993543840281266910 ) ) ;
#21494=CARTESIAN_POINT ( 'NONE',  ( -0.3119999999999999996, 0.3236111111111107941, -3.820898013339742174E-17 ) ) ;
#21495=CARTESIAN_POINT ( 'NONE',  ( 0.3072960869570707798, 4.083864392164723967, 0.05794554327026871926 ) ) ;
#21497=CARTESIAN_POINT ( 'NONE',  ( -0.2087850922559471578, 5.050207145506960593, -0.2334572881547273548 ) ) ;
#21499=CARTESIAN_POINT ( 'NONE',  ( -0.04066006786217810781, 4.656110604545615317, -0.3119999479932474840 ) ) ;
#21501=CARTESIAN_POINT ( 'NONE',  ( -0.2819296736111110979, 3.852861111186976828, 0.000000000000000000 ) ) ;
#21503=CARTESIAN_POINT ( 'NONE',  ( 0.05604226080982818020, 5.017622031331995913, 0.3069361942873307658 ) ) ;
#21506=CARTESIAN_POINT ( 'NONE',  ( -0.1292346314604056745, 4.491750000151731648, -0.3119999999999999996 ) ) ;
#21507=CARTESIAN_POINT ( 'NONE',  ( -1.726321361862525858E-17, 4.741750000075866112, -0.2819296736111110979 ) ) ;
#21509=CARTESIAN_POINT ( 'NONE',  ( 0.2819296736111110424, 4.050777777853642903, -0.1167790944451423396 ) ) ;
#21514=ORIENTED_EDGE ( 'NONE', *, *, #1277, .T. ) ;
#21517=CARTESIAN_POINT ( 'NONE',  ( 0.3119999999999999996, 0.01111111095937818323, 0.000000000000000000 ) ) ;
#21521=ORIENTED_EDGE ( 'NONE', *, *, #11086, .T. ) ;
#21527=CARTESIAN_POINT ( 'NONE',  ( -0.1167790944451423535, 4.363277777853642903, 0.2819296736111110424 ) ) ;
#21532=CARTESIAN_POINT ( 'NONE',  ( 0.3119999999999999996, 0.4555555554038225874, 0.000000000000000000 ) ) ;
#21534=CARTESIAN_POINT ( 'NONE',  ( -0.3119999999999999996, 4.161888888888888083, 0.000000000000000000 ) ) ;
#21537=CARTESIAN_POINT ( 'NONE',  ( 0.3085230613478114892, 4.973060968630374390, 0.04778564154238736789 ) ) ;
#21541=CARTESIAN_POINT ( 'NONE',  ( -0.1907560547815114194, 4.883016371272789868, -0.2468929990473206493 ) ) ;
#21546=CARTESIAN_POINT ( 'NONE',  ( 0.1917387269100320757, 3.815884185560293851, -0.2494959453317835418 ) ) ;
#21554=CYLINDRICAL_SURFACE ( 'NONE', #11878, 0.3119999999999999996 ) ;
#21557=CARTESIAN_POINT ( 'NONE',  ( -0.1292346314604058410, 0.4451388888888885287, 0.3119999999999998885 ) ) ;
#21558=CARTESIAN_POINT ( 'NONE',  ( 0.2206173157302028787, 4.960499999999998799, 0.2206173157302027954 ) ) ;
#21559=CARTESIAN_POINT ( 'NONE',  ( 0.1993543840281266633, 4.165361111186975940, -0.1993543840281266910 ) ) ;
#21561=CARTESIAN_POINT ( 'NONE',  ( 0.1993543840281266633, 4.012583333409199149, -0.1993543840281266910 ) ) ;
#21562=CARTESIAN_POINT ( 'NONE',  ( 5.731347020009612645E-17, 4.620222222222221120, 0.3119999999999999996 ) ) ;
#21564=CARTESIAN_POINT ( 'NONE',  ( 0.3108819030004250084, 4.807000738355847069, 0.02639019689791599274 ) ) ;
#21565=DIRECTION ( 'NONE',  ( -0.000000000000000000, -1.000000000000000000, -0.000000000000000000 ) ) ;
#21566=CARTESIAN_POINT ( 'NONE',  ( 0.1167790944451424368, 4.592444444520309865, 0.2819296736111110424 ) ) ;
#21568=CARTESIAN_POINT ( 'NONE',  ( 0.1292346314604080892, 3.811194444444443885, -0.3119999999999975016 ) ) ;
#21572=CARTESIAN_POINT ( 'NONE',  ( 0.1167790944451422702, 4.127166666742532186, -0.2819296736111110979 ) ) ;
#21574=CARTESIAN_POINT ( 'NONE',  ( -0.03977763657374241979, 4.822768489001279413, -0.3096144168800403773 ) ) ;
#21575=FACE_OUTER_BOUND ( 'NONE', #4439, .T. ) ;
#21578=CARTESIAN_POINT ( 'NONE',  ( 0.1167790944451423257, 0.1013888888130222432, -0.2819296736111110424 ) ) ;
#21580=CARTESIAN_POINT ( 'NONE',  ( -0.3120000000000000551, 0.1048611111111107663, 0.1292346314604056190 ) ) ;
#21584=ORIENTED_EDGE ( 'NONE', *, *, #11057, .F. ) ;
#21590=CARTESIAN_POINT ( 'NONE',  ( -0.1167790944451422702, 0.4972222221463556413, -0.2819296736111110424 ) ) ;
#21591=CARTESIAN_POINT ( 'NONE',  ( 0.2819296736111110979, 4.002166666742532186, 0.1167790944451422425 ) ) ;
#21594=CARTESIAN_POINT ( 'NONE',  ( 0.2819296736111110979, 4.727861111186976828, -3.452642723725051716E-17 ) ) ;
#21595=CARTESIAN_POINT ( 'NONE',  ( 0.3060896505723387229, 5.131432179253541115, -0.01842300014300301755 ) ) ;
#21596=CARTESIAN_POINT ( 'NONE',  ( 0.2206173157302027676, 0.3930555554038225874, 0.2206173157302028787 ) ) ;
#21600=CARTESIAN_POINT ( 'NONE',  ( -0.2819296736111110979, 5.130638888964754507, 0.000000000000000000 ) ) ;
#21602=CARTESIAN_POINT ( 'NONE',  ( 0.2730120068861431881, 4.201137816707454675, -0.1516840408520623573 ) ) ;
#21604=CARTESIAN_POINT ( 'NONE',  ( 0.1510366717642406820, 0.03242967361111057795, 0.2384937495143246711 ) ) ;
#21606=CARTESIAN_POINT ( 'NONE',  ( 0.1993543840281267465, 4.984805555631420582, 0.1993543840281266633 ) ) ;
#21610=CARTESIAN_POINT ( 'NONE',  ( -5.731347020009612645E-17, 0.2263888888888885564, 0.3119999999999999996 ) ) ;
#21612=CARTESIAN_POINT ( 'NONE',  ( -0.1167790944451424368, 0.2541666665908000056, 0.2819296736111110424 ) ) ;
#21614=CARTESIAN_POINT ( 'NONE',  ( 0.1167790944451423535, 0.03888888881302225708, 0.2819296736111110424 ) ) ;
#21617=AXIS2_PLACEMENT_3D ( 'NONE', #5104, #12570, #10257 ) ;
#21619=CARTESIAN_POINT ( 'NONE',  ( -0.2265706608393805443, 5.064436836433479527, 0.2145077285249635812 ) ) ;
#21622=CARTESIAN_POINT ( 'NONE',  ( 0.1993543840281267465, 4.832027777853643791, 0.1993543840281266633 ) ) ;
#21623=ORIENTED_EDGE ( 'NONE', *, *, #20086, .T. ) ;
#21625=CARTESIAN_POINT ( 'NONE',  ( 0.2819296736111110979, 3.821611111186975940, 0.1167790944451422425 ) ) ;
#21626=CARTESIAN_POINT ( 'NONE',  ( -0.2704407926385273275, 0.05463348271415230384, 0.1405181078658110927 ) ) ;
#21627=CARTESIAN_POINT ( 'NONE',  ( 0.2829377148481755366, 5.033800763418417645, -0.1314924907175452073 ) ) ;
#21629=CARTESIAN_POINT ( 'NONE',  ( 0.2063516445293624157, 0.05509720184852035657, 0.2244782525227043135 ) ) ;
#21631=CARTESIAN_POINT ( 'NONE',  ( 0.3119999999999999996, 4.200083333485066461, -0.1292346314604056745 ) ) ;
#21632=CARTESIAN_POINT ( 'NONE',  ( -0.1167790944451423535, 4.821611111186976828, 0.2819296736111110979 ) ) ;
#21633=ORIENTED_EDGE ( 'NONE', *, *, #369, .T. ) ;
#21634=CARTESIAN_POINT ( 'NONE',  ( 0.1167790944451424368, 4.148000000075866112, 0.2819296736111110424 ) ) ;
#21643=CARTESIAN_POINT ( 'NONE',  ( 0.3119999999999999996, 0.2923611109593781676, -0.1292346314604056468 ) ) ;
#21644=CARTESIAN_POINT ( 'NONE',  ( -0.2476358783382842099, 4.385282689055078009, -0.1900661484681659408 ) ) ;
#21649=VECTOR ( 'NONE', #4864, 39.37007874015748143 ) ;
#21651=CARTESIAN_POINT ( 'NONE',  ( 0.000000000000000000, 5.384999999999999787, -0.3119999999999999996 ) ) ;
#21652=CARTESIAN_POINT ( 'NONE',  ( -0.1993543840281266633, 0.05624999992413336897, -0.1993543840281266910 ) ) ;
#21655=CARTESIAN_POINT ( 'NONE',  ( -1.726321361862525858E-17, 4.450083333409198261, -0.2819296736111110979 ) ) ;
#21658=CYLINDRICAL_SURFACE ( 'NONE', #697, 0.3119999999999999996 ) ;
#21659=CARTESIAN_POINT ( 'NONE',  ( 0.3119999999999999996, 4.130638888888888971, 0.1292346314604056190 ) ) ;
#21660=CARTESIAN_POINT ( 'NONE',  ( -0.2206173157302028232, 5.217444444596177178, -0.2206173157302028232 ) ) ;
#21661=CARTESIAN_POINT ( 'NONE',  ( 0.06250759245605955194, 4.962249824674097809, 0.3056744829715940526 ) ) ;
#21671=CARTESIAN_POINT ( 'NONE',  ( 0.2726213023189543172, 3.803182761333917750, 0.1571292069147020298 ) ) ;
#21672=EDGE_LOOP ( 'NONE', ( #21735, #16950, #5201, #2999, #20780, #20204 ) ) ;
#21674=CARTESIAN_POINT ( 'NONE',  ( 1.726321361862525858E-17, 0.1187499999241333620, -0.2819296736111110979 ) ) ;
#21681=CARTESIAN_POINT ( 'NONE',  ( -0.1913234629623414007, 4.605258746665392700, -0.2464539925195264325 ) ) ;
#21682=CARTESIAN_POINT ( 'NONE',  ( -0.09533899702212705884, 4.291089024194236323, 0.2976594037573775942 ) ) ;
#21684=CARTESIAN_POINT ( 'NONE',  ( 0.3119999999999999996, 0.4624999999999996336, 0.000000000000000000 ) ) ;
#21685=CARTESIAN_POINT ( 'NONE',  ( -0.3119999999999999996, 4.828555555555555046, 0.000000000000000000 ) ) ;
#21686=CARTESIAN_POINT ( 'NONE',  ( -0.1167790944451423119, 4.231333333409199149, -0.2819296736111110979 ) ) ;
#21687=CARTESIAN_POINT ( 'NONE',  ( 0.1993543840281266633, 3.790361111186977272, -0.1993543840281266910 ) ) ;
#21692=CARTESIAN_POINT ( 'NONE',  ( 0.2819296736111110979, 4.602861111186975940, -3.452642723725051716E-17 ) ) ;
#21696=DIRECTION ( 'NONE',  ( -0.000000000000000000, -1.000000000000000000, -0.000000000000000000 ) ) ;
#21697=EDGE_CURVE ( 'NONE', #848, #12392, #2075, .T. ) ;
#21701=CARTESIAN_POINT ( 'NONE',  ( 0.2819296736111111534, 4.113277777853643791, 0.1167790944451422563 ) ) ;
#21702=CARTESIAN_POINT ( 'NONE',  ( -0.3112736230039412910, 4.834918082158893959, -0.02136994806237297803 ) ) ;
#21703=CARTESIAN_POINT ( 'NONE',  ( -0.1292346314604088386, 4.894527777777777366, 0.3119999999999968909 ) ) ;
#21706=CARTESIAN_POINT ( 'NONE',  ( -0.2819296736111110424, 0.004166666590800034188, -0.1167790944451423396 ) ) ;
#21708=CARTESIAN_POINT ( 'NONE',  ( -0.3119999999999999996, 0.09791666666666633267, -0.1292346314604056745 ) ) ;
#21712=EDGE_CURVE ( 'NONE', #7667, #14283, #24060, .T. ) ;
#21717=CARTESIAN_POINT ( 'NONE',  ( 0.1167790944451423535, 0.4138888888130222155, 0.2819296736111110424 ) ) ;
#21718=CARTESIAN_POINT ( 'NONE',  ( 0.2819296736111110979, 3.838972222298087544, -3.452642723725051716E-17 ) ) ;
#21720=ORIENTED_EDGE ( 'NONE', *, *, #239, .T. ) ;
#21721=CARTESIAN_POINT ( 'NONE',  ( 0.1167790944451422702, 4.571611111186976828, -0.2819296736111110424 ) ) ;
#21723=CARTESIAN_POINT ( 'NONE',  ( -1.910449006669871087E-17, 4.370222222222221120, -0.3119999999999999996 ) ) ;
#21726=CARTESIAN_POINT ( 'NONE',  ( 0.3120000000000000551, 4.019527777777777366, 0.1292346314604056190 ) ) ;
#21727=CARTESIAN_POINT ( 'NONE',  ( -0.1292346314604057023, 3.734805555707287450, 0.3119999999999998885 ) ) ;
#21728=CARTESIAN_POINT ( 'NONE',  ( 0.2329872879727148405, 4.203065777311293161, -0.2075117620790080109 ) ) ;
#21730=CARTESIAN_POINT ( 'NONE',  ( -0.2819296736111110979, 4.963972222298087544, 0.000000000000000000 ) ) ;
#21732=EDGE_LOOP ( 'NONE', ( #14850, #13123, #10722, #3719, #21720, #21633, #18587, #23323 ) ) ;
#21734=CARTESIAN_POINT ( 'NONE',  ( -0.2594808896536389686, 4.563054605363555893, 0.1777663154329622852 ) ) ;
#21735=ORIENTED_EDGE ( 'NONE', *, *, #6776, .T. ) ;
#21736=CARTESIAN_POINT ( 'NONE',  ( 0.1167790944451423535, 0.3166666665908000056, 0.2819296736111110424 ) ) ;
#21738=CARTESIAN_POINT ( 'NONE',  ( -0.2819296736111110424, 0.07361111103524449473, -0.1167790944451423396 ) ) ;
#21739=CARTESIAN_POINT ( 'NONE',  ( -0.2284438653877429726, 4.731022001090376072, 0.2152624247096975307 ) ) ;
#21740=CARTESIAN_POINT ( 'NONE',  ( -0.1669986196823105007, 5.194782195289050719, -0.2341252263734615313 ) ) ;
#21742=CARTESIAN_POINT ( 'NONE',  ( -0.07645976968530923679, 5.045943673328737056, -0.3031838258476152181 ) ) ;
#21744=CARTESIAN_POINT ( 'NONE',  ( -2.307748244742446386E-07, 4.182713274783838919, 0.3119999999998222528 ) ) ;
#21746=CARTESIAN_POINT ( 'NONE',  ( -0.2819296736111110424, 4.752166666742533074, -0.1167790944451423119 ) ) ;
#21747=CARTESIAN_POINT ( 'NONE',  ( 0.1457644982981150250, 4.520328994860446592, 0.2772101093080964196 ) ) ;
#21748=CARTESIAN_POINT ( 'NONE',  ( 0.1993543840281266633, 5.234805555631421470, -0.1993543840281266910 ) ) ;
#21750=DIRECTION ( 'NONE',  ( 1.000000000000000000, 0.000000000000000000, 0.000000000000000000 ) ) ;
#21753=CARTESIAN_POINT ( 'NONE',  ( 0.2206173157302028787, 4.356333333485065573, 0.2206173157302027954 ) ) ;
#21754=CARTESIAN_POINT ( 'NONE',  ( 0.2819296736111111534, 4.779944444520310753, 0.1167790944451422563 ) ) ;
#21755=CARTESIAN_POINT ( 'NONE',  ( 0.2819296736111110979, 3.769527777853642903, -3.452642723725051716E-17 ) ) ;
#21758=( BOUNDED_CURVE ( )  B_SPLINE_CURVE ( 2, ( #1773, #24079, #1297, #22256, #20193, #3482, #23708, #22014, #14471 ),
 .UNSPECIFIED., .F., .T. ) 
 B_SPLINE_CURVE_WITH_KNOTS ( ( 3, 2, 2, 2, 3 ),
 ( 0.5208333333333333703, 0.5312500000000000000, 0.5416666666666666297, 0.5520833333333333703, 0.5625000000000000000 ),
 .UNSPECIFIED. ) 
 CURVE ( )  GEOMETRIC_REPRESENTATION_ITEM ( )  RATIONAL_B_SPLINE_CURVE ( ( 1.000000000000000000, 0.9238795325112867385, 1.000000000000000000, 0.9238795325112867385, 1.000000000000000000, 0.9238795325112867385, 1.000000000000000000, 0.9238795325112867385, 1.000000000000000000 ) ) 
 REPRESENTATION_ITEM ( '' )  );
#21764=CARTESIAN_POINT ( 'NONE',  ( 0.1292346314604056745, 0.2437499998482670627, -0.3119999999999999996 ) ) ;
#21765=CARTESIAN_POINT ( 'NONE',  ( -0.04129347423352384971, 4.378292985746897514, -0.3093854606850361399 ) ) ;
#21770=CARTESIAN_POINT ( 'NONE',  ( 0.2819296736111110424, 0.3652777777019111105, 0.1167790944451424923 ) ) ;
#21773=CARTESIAN_POINT ( 'NONE',  ( 0.2819296736111110979, 4.377166666742532186, 0.1167790944451422425 ) ) ;
#21777=CARTESIAN_POINT ( 'NONE',  ( -0.3119999999999998885, 4.165361111111110404, 0.1292346314604058410 ) ) ;
#21778=CARTESIAN_POINT ( 'NONE',  ( 0.2206173157302027954, 4.981333333485065573, -0.2206173157302028232 ) ) ;
#21780=CARTESIAN_POINT ( 'NONE',  ( -0.1292346314604032043, 4.151472222222222008, -0.3120000000000024420 ) ) ;
#21782=CARTESIAN_POINT ( 'NONE',  ( -0.1939026278979700812, 4.883130061274394862, -0.2444469480974038600 ) ) ;
#21787=CARTESIAN_POINT ( 'NONE',  ( -0.2206173157302028232, 4.432722222222222008, -0.2206173157302028232 ) ) ;
#21791=CARTESIAN_POINT ( 'NONE',  ( 5.178964085587577574E-17, 5.158416666742532186, 0.2819296736111110979 ) ) ;
#21792=CARTESIAN_POINT ( 'NONE',  ( 0.1366576343437972407, 4.484363875748784700, -0.2809856522123292955 ) ) ;
#21794=( BOUNDED_CURVE ( )  B_SPLINE_CURVE ( 2, ( #5415, #10557, #12882, #20297, #3582, #17989, #11034, #18464, #9199 ),
 .UNSPECIFIED., .F., .F. ) 
 B_SPLINE_CURVE_WITH_KNOTS ( ( 3, 2, 2, 2, 3 ),
 ( 0.6517857142857143016, 0.6562500000000000000, 0.6607142857142856984, 0.6651785714285713969, 0.6696428571428570953 ),
 .UNSPECIFIED. ) 
 CURVE ( )  GEOMETRIC_REPRESENTATION_ITEM ( )  RATIONAL_B_SPLINE_CURVE ( ( 1.000000000000000000, 0.9238795325112867385, 1.000000000000000000, 0.9238795325112867385, 1.000000000000000000, 0.9238795325112867385, 1.000000000000000000, 0.9238795325112867385, 1.000000000000000000 ) ) 
 REPRESENTATION_ITEM ( '' )  );
#21795=CYLINDRICAL_SURFACE ( 'NONE', #10303, 0.3119999999999999996 ) ;
#21796=VECTOR ( 'NONE', #21404, 39.37007874015748143 ) ;
#21800=CARTESIAN_POINT ( 'NONE',  ( 0.3119999999999999996, 4.800777777777776478, -3.820898013339742174E-17 ) ) ;
#21802=B_SPLINE_CURVE_WITH_KNOTS ( 'NONE', 3,
 ( #23152, #4632, #12100, #1581 ),
 .UNSPECIFIED., .F., .F.,
 ( 4, 4 ),
 ( 0.09513879656923393546, 0.09617319050982510442 ),
 .UNSPECIFIED. ) ;
#21803=CARTESIAN_POINT ( 'NONE',  ( -0.1993543840281266355, 3.915361111186976384, 0.1993543840281267465 ) ) ;
#21806=CARTESIAN_POINT ( 'NONE',  ( -0.3119999999999998885, 4.554249999999997911, 0.1292346314604058410 ) ) ;
#21807=CARTESIAN_POINT ( 'NONE',  ( -0.2819296736111110979, 4.575083333409199149, 0.000000000000000000 ) ) ;
#21808=CARTESIAN_POINT ( 'NONE',  ( -0.2428671054993716272, 4.508197984795457636, 0.1958561003821059909 ) ) ;
#21814=CARTESIAN_POINT ( 'NONE',  ( 0.2819296736111111534, 4.057722222298088433, 0.1167790944451422563 ) ) ;
#21815=CARTESIAN_POINT ( 'NONE',  ( 0.009921425828668055391, 5.162181618341242562, -0.2989828796063835337 ) ) ;
#21818=CARTESIAN_POINT ( 'NONE',  ( -0.2819296736111110424, 0.05972222214635559273, -0.1167790944451423396 ) ) ;
#21821=CARTESIAN_POINT ( 'NONE',  ( 0.000000000000000000, 5.384999999999999787, 0.000000000000000000 ) ) ;
#21824=VERTEX_POINT ( 'NONE', #20055 ) ;
#21825=ORIENTED_EDGE ( 'NONE', *, *, #3851, .T. ) ;
#21828=CARTESIAN_POINT ( 'NONE',  ( 0.2819296736111110979, 0.5354166665908000056, 0.000000000000000000 ) ) ;
#21829=CARTESIAN_POINT ( 'NONE',  ( -0.2819296736111110424, 3.759111111186976828, 0.1167790944451424923 ) ) ;
#21831=CARTESIAN_POINT ( 'NONE',  ( -0.2819296736111110424, 4.418833333409199149, -0.1167790944451423119 ) ) ;
#21835=CARTESIAN_POINT ( 'NONE',  ( -5.731347020009612645E-17, 0.1638888887371559577, 0.3119999999999999996 ) ) ;
#21840=CARTESIAN_POINT ( 'NONE',  ( -0.1993543840281266910, 5.179250000075866112, -0.1993543840281266910 ) ) ;
#21841=CARTESIAN_POINT ( 'NONE',  ( 0.2181460042443824077, 4.203673976828415704, -0.2235058125270818763 ) ) ;
#21842=EDGE_CURVE ( 'NONE', #12796, #10917, #21794, .T. ) ;
#21845=CARTESIAN_POINT ( 'NONE',  ( 0.1993543840281266633, 4.943138888964754507, -0.1993543840281266910 ) ) ;
#21847=ORIENTED_EDGE ( 'NONE', *, *, #6670, .F. ) ;
#21851=CARTESIAN_POINT ( 'NONE',  ( -5.178964085587577574E-17, 0.3687499999241333204, 0.2819296736111110979 ) ) ;
#21853=CARTESIAN_POINT ( 'NONE',  ( 0.1167790944451423535, 0.09444444436857780956, 0.2819296736111110424 ) ) ;
#21855=CARTESIAN_POINT ( 'NONE',  ( -0.05462043248617448610, 5.191653777754733134, -0.2846966416326855986 ) ) ;
#21860=CARTESIAN_POINT ( 'NONE',  ( -0.2573147180782621724, 3.885706225055585161, -0.1764478447289662133 ) ) ;
#21862=CARTESIAN_POINT ( 'NONE',  ( -0.2819296736111110424, 4.418833333409199149, -0.1167790944451423119 ) ) ;
#21864=CARTESIAN_POINT ( 'NONE',  ( -0.2819296736111110979, 5.144527777853643791, 0.000000000000000000 ) ) ;
#21866=CARTESIAN_POINT ( 'NONE',  ( 0.3038219221730117936, 4.916572523495020164, 0.08186873057857177449 ) ) ;
#21870=CARTESIAN_POINT ( 'NONE',  ( -0.3119999999999999996, 4.332027777929510215, -0.1292346314604056468 ) ) ;
#21871=CARTESIAN_POINT ( 'NONE',  ( 0.2819296736111111534, 4.502166666742532186, 0.1167790944451422563 ) ) ;
#21872=CARTESIAN_POINT ( 'NONE',  ( 0.1993543840281267465, 3.762583333409198705, 0.1993543840281266633 ) ) ;
#21881=CARTESIAN_POINT ( 'NONE',  ( 0.1292346314604057023, 0.1673611109593781676, 0.3119999999999998885 ) ) ;
#21882=CARTESIAN_POINT ( 'NONE',  ( -0.06786238497518067014, 4.379037417340335914, -0.3050586073130007736 ) ) ;
#21883=CARTESIAN_POINT ( 'NONE',  ( -0.2921947132138422165, 3.721047735574461335, -0.1187172976513048844 ) ) ;
#21890=CARTESIAN_POINT ( 'NONE',  ( -0.1167790944451424506, 0.1847222221463556413, 0.2819296736111110424 ) ) ;
#21892=CARTESIAN_POINT ( 'NONE',  ( -0.2819296736111110979, 4.463972222298087544, 0.000000000000000000 ) ) ;
#21895=CARTESIAN_POINT ( 'NONE',  ( -0.04062695888593492732, 4.237158410735314185, 0.3093461996519432100 ) ) ;
#21896=CARTESIAN_POINT ( 'NONE',  ( -0.3119999999999998885, 4.054249999999998799, 0.1292346314604058410 ) ) ;
#21897=CARTESIAN_POINT ( 'NONE',  ( 5.731347020009612645E-17, 5.071611111262843252, 0.3119999999999999996 ) ) ;
#21902=CARTESIAN_POINT ( 'NONE',  ( 0.009844691510165828885, 4.682939453713771627, 0.3119999979940254464 ) ) ;
#21907=CARTESIAN_POINT ( 'NONE',  ( -0.1993543840281266633, 0.2368055554796889006, -0.1993543840281266910 ) ) ;
#21909=EDGE_CURVE ( 'NONE', #2426, #14570, #5888, .T. ) ;
#21910=CARTESIAN_POINT ( 'NONE',  ( -0.2819296736111110424, 5.196611111186976828, -0.1167790944451423119 ) ) ;
#21911=CARTESIAN_POINT ( 'NONE',  ( 0.3040713822389952137, 4.472421292987645458, 0.06995111167926036655 ) ) ;
#21912=CARTESIAN_POINT ( 'NONE',  ( 0.000000000000000000, 5.384999999999999787, 0.000000000000000000 ) ) ;
#21913=CARTESIAN_POINT ( 'NONE',  ( 0.02885018458022743301, 4.876384086389262684, -0.3107525876215130878 ) ) ;
#21916=CARTESIAN_POINT ( 'NONE',  ( 0.3119999999999999996, 4.693138888888888971, -0.1292346314604056745 ) ) ;
#21919=CARTESIAN_POINT ( 'NONE',  ( -0.2819296736111110979, 3.908416666742532630, 0.000000000000000000 ) ) ;
#21920=CARTESIAN_POINT ( 'NONE',  ( -0.2819296736111110424, 3.807722222298089321, -0.1167790944451423119 ) ) ;
#21924=CARTESIAN_POINT ( 'NONE',  ( -0.2819296736111110979, 4.463972222298087544, 0.000000000000000000 ) ) ;
#21926=CARTESIAN_POINT ( 'NONE',  ( 0.3119999999999999996, 0.07361111111111078020, 0.000000000000000000 ) ) ;
#21928=CARTESIAN_POINT ( 'NONE',  ( 0.1167790944451422702, 3.849388888964754951, -0.2819296736111110979 ) ) ;
#21930=CARTESIAN_POINT ( 'NONE',  ( 0.09770977851924383950, 5.159011269489411688, -0.2842526675492763055 ) ) ;
#21931=( BOUNDED_CURVE ( )  B_SPLINE_CURVE ( 2, ( #17641, #21418, #14106, #10216, #12292 ),
 .UNSPECIFIED., .F., .T. ) 
 B_SPLINE_CURVE_WITH_KNOTS ( ( 3, 2, 3 ),
 ( 0.1285401400649176518, 0.1294642857142857262, 0.1339285714285714246 ),
 .UNSPECIFIED. ) 
 CURVE ( )  GEOMETRIC_REPRESENTATION_ITEM ( )  RATIONAL_B_SPLINE_CURVE ( ( 0.9750087287892017507, 0.9842424066559070095, 1.000000000000000000, 0.9238795325112867385, 1.000000000000000000 ) ) 
 REPRESENTATION_ITEM ( '' )  );
#21933=EDGE_CURVE ( 'NONE', #3702, #6119, #4096, .T. ) ;
#21935=CARTESIAN_POINT ( 'NONE',  ( 0.1167790944451423535, 0.3583333332574666907, 0.2819296736111110424 ) ) ;
#21944=ORIENTED_EDGE ( 'NONE', *, *, #16067, .F. ) ;
#21945=CARTESIAN_POINT ( 'NONE',  ( 0.000000000000000000, 5.384999999999999787, 0.000000000000000000 ) ) ;
#21946=CARTESIAN_POINT ( 'NONE',  ( -0.2494959280049152961, 3.829773069302058630, -0.1917387442425347033 ) ) ;
#21947=CARTESIAN_POINT ( 'NONE',  ( 0.3119999999999999996, 0.1291666666666663188, 0.000000000000000000 ) ) ;
#21948=CARTESIAN_POINT ( 'NONE',  ( -0.1993543840281266910, 3.804250000075865668, -0.1993543840281266910 ) ) ;
#21951=CARTESIAN_POINT ( 'NONE',  ( -0.1993543840281266910, 4.415361111186976828, -0.1993543840281266910 ) ) ;
#21952=CARTESIAN_POINT ( 'NONE',  ( -5.731347020009612645E-17, 0.1083333331816004053, 0.3119999999999999996 ) ) ;
#21956=CARTESIAN_POINT ( 'NONE',  ( 5.178964085587577574E-17, 5.144527777853643791, 0.2819296736111110979 ) ) ;
#21961=CYLINDRICAL_SURFACE ( 'NONE', #6794, 0.3119999999999999996 ) ;
#21962=CARTESIAN_POINT ( 'NONE',  ( -0.2819296736111110424, 4.800777777853643791, 0.1167790944451424923 ) ) ;
#21965=CARTESIAN_POINT ( 'NONE',  ( -0.3119999999999999996, 0.4243055554038226429, -0.1292346314604056745 ) ) ;
#21967=CARTESIAN_POINT ( 'NONE',  ( -0.2819296736111110424, 0.2402777777019111938, -0.1167790944451423396 ) ) ;
#21971=CARTESIAN_POINT ( 'NONE',  ( -0.1993543840281266633, 0.2923611110352444808, -0.1993543840281266910 ) ) ;
#21973=CARTESIAN_POINT ( 'NONE',  ( -0.1076999173815676586, 5.193055214671070452, -0.2685177118993510859 ) ) ;
#21977=CARTESIAN_POINT ( 'NONE',  ( -5.731347020009612645E-17, 0.1083333331816004053, 0.3119999999999999996 ) ) ;
#21979=CARTESIAN_POINT ( 'NONE',  ( 0.2819296736111110979, 4.557722222298087544, 0.1167790944451422425 ) ) ;
#21981=CARTESIAN_POINT ( 'NONE',  ( 0.3051448587956195890, 4.531920635835558819, -0.06985392631230002980 ) ) ;
#21983=EDGE_CURVE ( 'NONE', #23019, #3616, #7841, .T. ) ;
#21984=CARTESIAN_POINT ( 'NONE',  ( 0.2819296736111110979, 5.113277777853642903, 0.1167790944451422425 ) ) ;
#21986=CARTESIAN_POINT ( 'NONE',  ( 0.1570546580433174466, 4.909658102729531848, 0.2726611153537367715 ) ) ;
#21987=CARTESIAN_POINT ( 'NONE',  ( 0.2170440708343631397, 0.05599619865938067903, 0.2154300401225580364 ) ) ;
#21988=CARTESIAN_POINT ( 'NONE',  ( -0.03984298593500181646, 4.767186640188652902, -0.3119995727676234121 ) ) ;
#21989=CARTESIAN_POINT ( 'NONE',  ( -0.3119999999999999996, 4.276472222373953969, -0.1292346314604056468 ) ) ;
#21990=CARTESIAN_POINT ( 'NONE',  ( 0.2819296736111110979, 4.561194444520310753, -3.452642723725051716E-17 ) ) ;
#21991=CARTESIAN_POINT ( 'NONE',  ( -1.726321361862525858E-17, 3.783416666742532186, -0.2819296736111110979 ) ) ;
#21992=VERTEX_POINT ( 'NONE', #11637 ) ;
#21993=EDGE_CURVE ( 'NONE', #10368, #18493, #13455, .T. ) ;
#21997=CARTESIAN_POINT ( 'NONE',  ( -5.488040394358968970E-07, 4.960478275469978549, 0.3119999999989728212 ) ) ;
#21999=ORIENTED_EDGE ( 'NONE', *, *, #3343, .T. ) ;
#22000=CARTESIAN_POINT ( 'NONE',  ( -0.3119999999999999996, 0.2020833331816004053, -0.1292346314604056745 ) ) ;
#22001=CARTESIAN_POINT ( 'NONE',  ( -0.08148921683276161287, 4.402575570918881631, 0.3039149224628344692 ) ) ;
#22002=CARTESIAN_POINT ( 'NONE',  ( -0.02028168178945650296, 5.129600928296707885, 0.3068236208125575404 ) ) ;
#22011=CARTESIAN_POINT ( 'NONE',  ( -0.2819296736111110424, 4.300777777853642903, 0.1167790944451424923 ) ) ;
#22012=CARTESIAN_POINT ( 'NONE',  ( -0.1167790944451423119, 5.009111111186976828, -0.2819296736111110979 ) ) ;
#22014=CARTESIAN_POINT ( 'NONE',  ( -0.1292346314604058410, 0.3826388887371559022, 0.3119999999999998885 ) ) ;
#22015=CARTESIAN_POINT ( 'NONE',  ( 0.3119999999999999996, 4.078555555555555046, -3.820898013339742174E-17 ) ) ;
#22016=CARTESIAN_POINT ( 'NONE',  ( -0.3119999999999998885, 4.950083333485066461, 0.1292346314604058410 ) ) ;
#22018=CARTESIAN_POINT ( 'NONE',  ( -0.1167790944451423119, 5.078555555631421470, -0.2819296736111110979 ) ) ;
#22022=CARTESIAN_POINT ( 'NONE',  ( 0.2832806843015959197, 0.03401755210715768502, 0.01622507305669601205 ) ) ;
#22030=CARTESIAN_POINT ( 'NONE',  ( -0.1993543840281267465, 0.2506944443685777957, 0.1993543840281266633 ) ) ;
#22034=CARTESIAN_POINT ( 'NONE',  ( 0.1228621477648789984, 4.484786867006959277, -0.2870958250574380255 ) ) ;
#22036=CARTESIAN_POINT ( 'NONE',  ( -0.1993543840281266355, 4.970916666742532186, 0.1993543840281267465 ) ) ;
#22037=CARTESIAN_POINT ( 'NONE',  ( -0.2726727406394559017, 4.173537243704723565, 0.1570538247964039513 ) ) ;
#22038=CARTESIAN_POINT ( 'NONE',  ( 0.0002098633495959924473, 4.877161027885005495, -0.3119999340045161440 ) ) ;
#22040=CARTESIAN_POINT ( 'NONE',  ( 0.3119999999999999996, 4.082027777777776478, -0.1292346314604056745 ) ) ;
#22041=CARTESIAN_POINT ( 'NONE',  ( 0.3119999999999998885, 0.5631944442927114824, 0.1292346314604058410 ) ) ;
#22042=CARTESIAN_POINT ( 'NONE',  ( 0.3119999999999999996, 4.741749999999998799, 0.1292346314604056190 ) ) ;
#22043=CARTESIAN_POINT ( 'NONE',  ( -1.726321361862525858E-17, 4.005638888964754507, -0.2819296736111110979 ) ) ;
#22045=CARTESIAN_POINT ( 'NONE',  ( 0.2734898064461412370, 4.034470968406938418, -0.1527495561689310444 ) ) ;
#22046=CARTESIAN_POINT ( 'NONE',  ( 0.1292346314604057300, 0.5006944442927115935, 0.3119999999999998885 ) ) ;
#22049=ORIENTED_EDGE ( 'NONE', *, *, #10701, .F. ) ;
#22050=CARTESIAN_POINT ( 'NONE',  ( 0.2819296736111110979, 4.210500000075865223, 0.1167790944451422425 ) ) ;
#22051=CARTESIAN_POINT ( 'NONE',  ( -0.2181590239592449132, 4.509281914422427207, 0.2241040346535229100 ) ) ;
#22061=CARTESIAN_POINT ( 'NONE',  ( -0.2819296736111110979, 0.2333333332574667185, 0.1167790944451422425 ) ) ;
#22062=CARTESIAN_POINT ( 'NONE',  ( 0.2494946377407150639, 3.857550799961272592, 0.1917403518701246146 ) ) ;
#22068=CARTESIAN_POINT ( 'NONE',  ( 0.3119999999999999996, 4.356333333333332725, -3.820898013339742174E-17 ) ) ;
#22069=CARTESIAN_POINT ( 'NONE',  ( -0.2206173157302028787, -0.002777777777778111818, 0.2206173157302027954 ) ) ;
#22070=CARTESIAN_POINT ( 'NONE',  ( -0.1993543840281266355, 3.818138888964754507, 0.1993543840281267465 ) ) ;
#22072=ORIENTED_EDGE ( 'NONE', *, *, #9762, .T. ) ;
#22073=CARTESIAN_POINT ( 'NONE',  ( 0.1993543840281266633, 4.401472222298088433, -0.1993543840281266910 ) ) ;
#22077=CARTESIAN_POINT ( 'NONE',  ( 0.1426520719866612441, 4.373010559984535917, -0.2781209046996724332 ) ) ;
#22078=CARTESIAN_POINT ( 'NONE',  ( 0.2819296736111110979, 5.102861111186976828, -3.452642723725051716E-17 ) ) ;
#22079=CARTESIAN_POINT ( 'NONE',  ( 0.2510418245647489388, 4.202275339918530861, -0.1855358740567382703 ) ) ;
#22082=CARTESIAN_POINT ( 'NONE',  ( 0.000000000000000000, 5.384999999999999787, 0.000000000000000000 ) ) ;
#22084=CARTESIAN_POINT ( 'NONE',  ( -0.2819296736111110979, 4.575083333409199149, 0.000000000000000000 ) ) ;
#22088=CARTESIAN_POINT ( 'NONE',  ( -0.2206173157302028787, 0.4347222220704892726, 0.2206173157302027954 ) ) ;
#22089=CARTESIAN_POINT ( 'NONE',  ( -0.1167790944451422702, 0.5666666665908001166, -0.2819296736111110424 ) ) ;
#22092=CARTESIAN_POINT ( 'NONE',  ( 0.2819296736111110424, 0.2749999999241333204, -0.1167790944451423119 ) ) ;
#22093=DIRECTION ( 'NONE',  ( -0.000000000000000000, -1.000000000000000000, -0.000000000000000000 ) ) ;
#22097=CARTESIAN_POINT ( 'NONE',  ( -1.910449006669871087E-17, 4.203555555555555046, -0.3119999999999999996 ) ) ;
#22098=CARTESIAN_POINT ( 'NONE',  ( -0.2563606228057540570, 3.885658506346372665, -0.1778292439628233468 ) ) ;
#22099=CARTESIAN_POINT ( 'NONE',  ( 0.1167790944451423257, 0.04583333325746669074, -0.2819296736111110424 ) ) ;
#22100=CARTESIAN_POINT ( 'NONE',  ( 0.2819296736111110979, 4.613277777853643791, 0.1167790944451422425 ) ) ;
#22103=CARTESIAN_POINT ( 'NONE',  ( 0.0002615309095209263448, 4.543825908977736638, -0.3119999184752035859 ) ) ;
#22104=CARTESIAN_POINT ( 'NONE',  ( -0.1167790944451423257, 5.134111111186976828, -0.2819296736111110424 ) ) ;
#22105=CARTESIAN_POINT ( 'NONE',  ( 0.2819296736111111534, 4.432722222298088433, 0.1167790944451422563 ) ) ;
#22106=CARTESIAN_POINT ( 'NONE',  ( 0.1262412304268583363, 3.762410328379145685, -0.2858544259516618835 ) ) ;
#22107=CARTESIAN_POINT ( 'NONE',  ( -0.2206173157302028787, 0.4902777776260447973, 0.2206173157302027954 ) ) ;
#22108=B_SPLINE_CURVE_WITH_KNOTS ( 'NONE', 3,
 ( #23901, #10768, #20384, #7454, #3432, #22324, #20504, #5748, #18194, #1611, #7220, #23781, #7103, #14541, #5258, #12729, #20145, #10885, #18314, #22809, #13570, #15381, #2219, #11607, #4392, #9896, #2457, #11729, #19268, #6100, #10023, #494, #13442, #15259, #738, #18791, #17210, #2573, #17445, #11854, #23039, #8167, #22572, #22689, #19037, #5979, #11484, #20978, #4275, #15621, #6343, #2340, #7696, #2086, #15142, #9775, #13796, #22926, #3919, #20861 ),
 .UNSPECIFIED., .F., .F.,
 ( 4, 2, 2, 1, 1, 2, 2, 1, 1, 2, 2, 2, 2, 2, 2, 2, 2, 2, 2, 1, 2, 2, 2, 2, 2, 1, 1, 2, 2, 1, 1, 1, 1, 1, 2, 4 ),
 ( 0.7590242753740639170, 0.7601283167772955318, 0.7612323581805270356, 0.7613703633559310013, 0.7614048646497819650, 0.7614134899732447614, 0.7614221152967074469, 0.7614393659436329287, 0.7615083685313349671, 0.7617843788821428985, 0.7623363995837586504, 0.7634404409869903763, 0.7656485237934537169, 0.7678566065999170576, 0.7689606480031487834, 0.7700646894063803982, 0.7722727722128437389, 0.7725487825636516703, 0.7726177851513537087, 0.7726867877390556361, 0.7728247929144596018, 0.7733768136160754647, 0.7744808550193070795, 0.7755848964225388054, 0.7761369171241545573, 0.7762749222995585230, 0.7763094235934094867, 0.7763266742403350795, 0.7763439248872605614, 0.7764129274749624887, 0.7765509326503664544, 0.7766199352380684928, 0.7766544365319194565, 0.7766716871788449383, 0.7766803125023076237, 0.7766889378257704202 ),
 .UNSPECIFIED. ) ;
#22109=CARTESIAN_POINT ( 'NONE',  ( 0.2856353109896033193, 3.915016894130901814, 0.1313266209029238241 ) ) ;
#22110=CARTESIAN_POINT ( 'NONE',  ( -0.2206173157302028232, 4.217444444596176290, -0.2206173157302028232 ) ) ;
#22111=CARTESIAN_POINT ( 'NONE',  ( -0.2819296736111110424, 4.481333333409199149, 0.1167790944451424923 ) ) ;
#22112=CARTESIAN_POINT ( 'NONE',  ( -0.1167790944451423257, 3.842444444520309865, -0.2819296736111110424 ) ) ;
#22113=ADVANCED_FACE ( 'NONE', ( #16219 ), #6582, .T. ) ;
#22118=EDGE_CURVE ( 'NONE', #5409, #11982, #3766, .T. ) ;
#22120=CARTESIAN_POINT ( 'NONE',  ( 0.3119999999999999996, 0.2368055554038226151, -0.1292346314604056468 ) ) ;
#22122=CARTESIAN_POINT ( 'NONE',  ( 1.910449006669871087E-17, 0.2541666666666663188, -0.3119999999999999996 ) ) ;
#22127=CARTESIAN_POINT ( 'NONE',  ( 0.2980859225763422549, 5.088325808746541057, -0.09136059965523930793 ) ) ;
#22129=CARTESIAN_POINT ( 'NONE',  ( -0.1167790944451423257, 4.286888888964754507, -0.2819296736111110424 ) ) ;
#22130=CARTESIAN_POINT ( 'NONE',  ( -0.1993543840281266355, 5.082027777853643791, 0.1993543840281267465 ) ) ;
#22133=CARTESIAN_POINT ( 'NONE',  ( -0.3086600503652839889, 4.225649461085167147, 0.04553437359818874458 ) ) ;
#22134=CARTESIAN_POINT ( 'NONE',  ( -0.3119999999999998885, 3.943138888888888527, 0.1292346314604058410 ) ) ;
#22135=AXIS2_PLACEMENT_3D ( 'NONE', #5170, #12636, #20056 ) ;
#22136=CARTESIAN_POINT ( 'NONE',  ( -0.1292346314604056745, 4.880638889040620931, -0.3119999999999999996 ) ) ;
#22137=CARTESIAN_POINT ( 'NONE',  ( -0.2819296736111110979, 5.200083333409199149, 0.000000000000000000 ) ) ;
#22143=CARTESIAN_POINT ( 'NONE',  ( -0.2260933988346537915, 0.05608587455741884109, 0.2058197434722169872 ) ) ;
#22147=CARTESIAN_POINT ( 'NONE',  ( -1.726321361862525858E-17, 5.005638888964754507, -0.2819296736111110979 ) ) ;
#22152=CARTESIAN_POINT ( 'NONE',  ( -0.2819296736111111534, 0.1916666665908000056, 0.1167790944451422563 ) ) ;
#22154=CARTESIAN_POINT ( 'NONE',  ( -0.1993543840281266910, 4.915361111186976828, -0.1993543840281266910 ) ) ;
#22155=CARTESIAN_POINT ( 'NONE',  ( 0.3001226394952070664, 4.471964646715294478, 0.08541954505744529802 ) ) ;
#22157=CARTESIAN_POINT ( 'NONE',  ( 0.2819296736111110979, 4.821611111186976828, 0.1167790944451422425 ) ) ;
#22160=CARTESIAN_POINT ( 'NONE',  ( 0.2206173157302028787, 4.571611111111110404, 0.2206173157302027954 ) ) ;
#22162=CARTESIAN_POINT ( 'NONE',  ( -0.2206173157302028232, 4.766055555555554157, -0.2206173157302028232 ) ) ;
#22163=CARTESIAN_POINT ( 'NONE',  ( 0.1167790944451424506, 4.092444444520309865, 0.2819296736111110424 ) ) ;
#22165=CARTESIAN_POINT ( 'NONE',  ( 0.2963340753493131641, 4.032741672258961074, -0.09762241780008150405 ) ) ;
#22166=FACE_OUTER_BOUND ( 'NONE', #7061, .T. ) ;
#22170=ORIENTED_EDGE ( 'NONE', *, *, #525, .T. ) ;
#22172=EDGE_CURVE ( 'NONE', #20467, #6926, #20591, .T. ) ;
#22180=CARTESIAN_POINT ( 'NONE',  ( 0.1993543840281266355, 0.3062499999241333759, 0.1993543840281267465 ) ) ;
#22185=EDGE_LOOP ( 'NONE', ( #17181, #1783, #3834, #9005, #2722, #21258 ) ) ;
#22187=CARTESIAN_POINT ( 'NONE',  ( -0.3004112128421244088, 5.107488232101096592, 0.07954157393797596509 ) ) ;
#22188=CYLINDRICAL_SURFACE ( 'NONE', #3911, 0.3119999999999999996 ) ;
#22189=CARTESIAN_POINT ( 'NONE',  ( 0.2206173157302027676, 0.01111111111111077500, 0.2206173157302028787 ) ) ;
#22190=CARTESIAN_POINT ( 'NONE',  ( 0.1167790944451422702, 3.904944444520310753, -0.2819296736111110424 ) ) ;
#22193=CARTESIAN_POINT ( 'NONE',  ( -1.726321361862525858E-17, 4.408416666742533074, -0.2819296736111110979 ) ) ;
#22195=DIRECTION ( 'NONE',  ( -0.000000000000000000, -1.000000000000000000, -0.000000000000000000 ) ) ;
#22197=CARTESIAN_POINT ( 'NONE',  ( 0.3110112520880878306, 4.362073312222188193, 0.04245179714123451659 ) ) ;
#22198=CARTESIAN_POINT ( 'NONE',  ( -0.1167790944451423535, 5.029944444520310753, 0.2819296736111110424 ) ) ;
#22200=CARTESIAN_POINT ( 'NONE',  ( -0.1331303419516291220, 5.146900442876030546, -0.2730306959456248461 ) ) ;
#22203=DIRECTION ( 'NONE',  ( -0.000000000000000000, -1.000000000000000000, -0.000000000000000000 ) ) ;
#22204=CARTESIAN_POINT ( 'NONE',  ( -0.1993543840281266355, 4.748694444520309865, 0.1993543840281267465 ) ) ;
#22206=CARTESIAN_POINT ( 'NONE',  ( -0.2206173157302027676, 4.779944444444443441, 0.2206173157302028787 ) ) ;
#22207=CARTESIAN_POINT ( 'NONE',  ( 0.3120000000000000551, 4.908416666666665762, 0.1292346314604056190 ) ) ;
#22208=CARTESIAN_POINT ( 'NONE',  ( -0.2819296736111110979, 0.4104166665908000056, -3.452642723725051716E-17 ) ) ;
#22210=CARTESIAN_POINT ( 'NONE',  ( -0.1167790944451424368, 0.2541666665908000056, 0.2819296736111110424 ) ) ;
#22211=CARTESIAN_POINT ( 'NONE',  ( -1.910449006669871087E-17, 4.314666666666665762, -0.3119999999999999996 ) ) ;
#22212=CARTESIAN_POINT ( 'NONE',  ( -0.2845704250721091122, 5.201214412163930767, -0.01070544790218683727 ) ) ;
#22218=CARTESIAN_POINT ( 'NONE',  ( 0.2819296736111110979, -0.02013888896475552262, 0.000000000000000000 ) ) ;
#22220=CARTESIAN_POINT ( 'NONE',  ( 0.1167790944451424368, 4.439666666742532186, 0.2819296736111110424 ) ) ;
#22222=CARTESIAN_POINT ( 'NONE',  ( 0.1728547196185014345, 4.521197801589692311, 0.2619698204964887034 ) ) ;
#22223=CARTESIAN_POINT ( 'NONE',  ( 0.1167790944451422702, 5.127166666742532186, -0.2819296736111110424 ) ) ;
#22224=CARTESIAN_POINT ( 'NONE',  ( 0.2819296736111110979, 4.384111111186976828, -0.1167790944451423396 ) ) ;
#22225=CARTESIAN_POINT ( 'NONE',  ( 0.1007954511899375599, 4.929790153955178056, -0.2959789403773529504 ) ) ;
#22228=CARTESIAN_POINT ( 'NONE',  ( 0.1292346314604058410, 4.019527777929511103, 0.3119999999999998885 ) ) ;
#22230=CARTESIAN_POINT ( 'NONE',  ( 0.1167790944451422702, 4.516055555631421470, -0.2819296736111110979 ) ) ;
#22233=CARTESIAN_POINT ( 'NONE',  ( 5.178964085587577574E-17, 3.866750000075865668, 0.2819296736111110979 ) ) ;
#22238=CARTESIAN_POINT ( 'NONE',  ( 0.000000000000000000, 0.06249999999999967387, 0.000000000000000000 ) ) ;
#22240=CARTESIAN_POINT ( 'NONE',  ( 0.2206173157302027676, 0.4486111109593781676, 0.2206173157302028787 ) ) ;
#22242=CARTESIAN_POINT ( 'NONE',  ( -0.2270342100380514649, 3.717753562207886997, -0.2143185460272691856 ) ) ;
#22245=VERTEX_POINT ( 'NONE', #5719 ) ;
#22246=EDGE_LOOP ( 'NONE', ( #1767, #1974, #18779, #19809 ) ) ;
#22248=ORIENTED_EDGE ( 'NONE', *, *, #239, .F. ) ;
#22249=CARTESIAN_POINT ( 'NONE',  ( 0.2716150497474701941, 5.090361019658427466, -0.1537593218455965693 ) ) ;
#22253=CARTESIAN_POINT ( 'NONE',  ( -0.1167790944451423257, 4.175777777853643791, -0.2819296736111110424 ) ) ;
#22254=CARTESIAN_POINT ( 'NONE',  ( 0.2819296736111111534, 5.043833333409199149, 0.1167790944451422563 ) ) ;
#22256=CARTESIAN_POINT ( 'NONE',  ( -0.3119999999999999996, 0.3687499998482670627, -0.1292346314604056745 ) ) ;
#22258=CARTESIAN_POINT ( 'NONE',  ( 0.1292346314604056190, 4.818138889040620931, -0.3119999999999999996 ) ) ;
#22259=EDGE_CURVE ( 'NONE', #14703, #2366, #9255, .T. ) ;
#22260=CARTESIAN_POINT ( 'NONE',  ( 0.1993543840281266633, 5.123694444520309865, -0.1993543840281266910 ) ) ;
#22267=CARTESIAN_POINT ( 'NONE',  ( -0.1167790944451423535, 5.085500000075866112, 0.2819296736111110424 ) ) ;
#22274=CARTESIAN_POINT ( 'NONE',  ( 0.2819296736111110424, 0.3791666665908000611, 0.1167790944451424923 ) ) ;
#22276=CARTESIAN_POINT ( 'NONE',  ( -0.2819296736111110979, 5.033416666742532186, 0.000000000000000000 ) ) ;
#22278=CARTESIAN_POINT ( 'NONE',  ( -1.726321361862525858E-17, 4.894527777853642903, -0.2819296736111110979 ) ) ;
#22280=CARTESIAN_POINT ( 'NONE',  ( -0.2082794372640225100, 5.206640035683668621, 0.1900105704308308607 ) ) ;
#22283=CARTESIAN_POINT ( 'NONE',  ( -0.3119999999999999996, 4.439666666666665762, 0.000000000000000000 ) ) ;
#22284=CARTESIAN_POINT ( 'NONE',  ( -1.726321361862525858E-17, 3.950083333409199149, -0.2819296736111110979 ) ) ;
#22285=CARTESIAN_POINT ( 'NONE',  ( -0.3119999999999999996, 4.213972222222222008, -0.1292346314604056468 ) ) ;
#22287=CARTESIAN_POINT ( 'NONE',  ( 0.1203817380124382053, 4.040418582577093076, -0.2885312214009505549 ) ) ;
#22288=CARTESIAN_POINT ( 'NONE',  ( -0.1061085311203168874, 3.735219933786901425, 0.2934028053144311921 ) ) ;
#22289=DIRECTION ( 'NONE',  ( -0.000000000000000000, -1.000000000000000000, -0.000000000000000000 ) ) ;
#22293=CARTESIAN_POINT ( 'NONE',  ( 0.01077313864395416584, 4.654635478660750891, -0.3118404384345617175 ) ) ;
#22298=CARTESIAN_POINT ( 'NONE',  ( -0.2819296736111110979, 0.1777777777019111383, 0.1167790944451422425 ) ) ;
#22299=CARTESIAN_POINT ( 'NONE',  ( 0.0005571238342427710811, 3.877151696567567196, -0.3119995739661102774 ) ) ;
#22304=ORIENTED_EDGE ( 'NONE', *, *, #9965, .T. ) ;
#22306=DIRECTION ( 'NONE',  ( 0.000000000000000000, 0.000000000000000000, -1.000000000000000000 ) ) ;
#22307=CARTESIAN_POINT ( 'NONE',  ( 0.2206173157302027676, 0.06666666666666633267, 0.2206173157302028787 ) ) ;
#22308=CARTESIAN_POINT ( 'NONE',  ( -0.1292346314604056745, 5.095916666666666650, -0.3119999999999999996 ) ) ;
#22311=CARTESIAN_POINT ( 'NONE',  ( 0.2819296736111110979, 4.446611111186976828, 0.1167790944451422425 ) ) ;
#22312=CARTESIAN_POINT ( 'NONE',  ( 0.1292346314604056745, 0.1326388887371559577, -0.3119999999999999996 ) ) ;
#22315=CARTESIAN_POINT ( 'NONE',  ( 0.1268833284183610299, 4.373501793580047092, -0.2854709177596411185 ) ) ;
#22316=CARTESIAN_POINT ( 'NONE',  ( 0.2819296736111110979, 4.991750000075866112, -3.452642723725051716E-17 ) ) ;
#22317=CARTESIAN_POINT ( 'NONE',  ( -0.2818813690555227458, 5.158154447605131310, 0.1035947188507469058 ) ) ;
#22321=CARTESIAN_POINT ( 'NONE',  ( -0.1993543840281266910, 4.679250000075866112, -0.1993543840281266910 ) ) ;
#22324=CARTESIAN_POINT ( 'NONE',  ( -0.1456855345975412996, 4.067294776256560773, 0.2759172852803205567 ) ) ;
#22326=CARTESIAN_POINT ( 'NONE',  ( 0.2819296736111110979, 0.4937499999241333759, 0.000000000000000000 ) ) ;
#22327=ORIENTED_EDGE ( 'NONE', *, *, #22555, .F. ) ;
#22328=CARTESIAN_POINT ( 'NONE',  ( -0.2819296736111110424, 0.1847222221463555858, -0.1167790944451423396 ) ) ;
#22329=CARTESIAN_POINT ( 'NONE',  ( -1.296004783052830448E-07, 4.710500003633881327, -0.3119999999999730766 ) ) ;
#22330=CARTESIAN_POINT ( 'NONE',  ( -0.2611278098349356092, 5.204257314301414361, 0.1100826262484129597 ) ) ;
#22335=CARTESIAN_POINT ( 'NONE',  ( -0.1993543840281267465, 0.3479166665908000611, 0.1993543840281266633 ) ) ;
#22336=CARTESIAN_POINT ( 'NONE',  ( -5.178964085587577574E-17, 0.02152777770191114173, 0.2819296736111110979 ) ) ;
#22337=CARTESIAN_POINT ( 'NONE',  ( 0.1993543840281266633, 4.568138888964755395, -0.1993543840281266910 ) ) ;
#22340=CARTESIAN_POINT ( 'NONE',  ( -0.1993543840281266355, 5.151472222298088433, 0.1993543840281267465 ) ) ;
#22341=EDGE_CURVE ( 'NONE', #9981, #1934, #4555, .T. ) ;
#22342=CARTESIAN_POINT ( 'NONE',  ( 0.1993543840281267465, 4.429250000075865223, 0.1993543840281266633 ) ) ;
#22343=CARTESIAN_POINT ( 'NONE',  ( 0.04081965062135220479, 4.906194639886546582, 0.3120000089134554178 ) ) ;
#22345=CARTESIAN_POINT ( 'NONE',  ( -0.2206173157302027676, 4.064666666818398610, 0.2206173157302028787 ) ) ;
#22347=CARTESIAN_POINT ( 'NONE',  ( 0.1167790944451422702, 4.571611111186976828, -0.2819296736111110979 ) ) ;
#22350=ORIENTED_EDGE ( 'NONE', *, *, #7665, .F. ) ;
#22353=CARTESIAN_POINT ( 'NONE',  ( -0.1290798622871512646, 4.845609795294118172, 0.2840783873375067881 ) ) ;
#22356=CARTESIAN_POINT ( 'NONE',  ( -0.3119999999999999996, 0.4243055554038226429, -0.1292346314604056745 ) ) ;
#22357=ORIENTED_EDGE ( 'NONE', *, *, #17520, .T. ) ;
#22362=CARTESIAN_POINT ( 'NONE',  ( 0.2724977880658804863, 3.969733213627001156, 0.1573355931994520895 ) ) ;
#22367=CARTESIAN_POINT ( 'NONE',  ( 0.01924054892003582498, 5.099521701092943893, -0.3108711954494297602 ) ) ;
#22369=CARTESIAN_POINT ( 'NONE',  ( 0.2819296736111110979, 4.154944444520309865, 0.1167790944451422425 ) ) ;
#22370=CARTESIAN_POINT ( 'NONE',  ( -0.1167790944451423535, 5.029944444520308977, 0.2819296736111110979 ) ) ;
#22371=( BOUNDED_CURVE ( )  B_SPLINE_CURVE ( 2, ( #18671, #18552, #9165, #16372, #23782, #22207, #7455, #23903, #5259 ),
 .UNSPECIFIED., .F., .F. ) 
 B_SPLINE_CURVE_WITH_KNOTS ( ( 3, 2, 2, 2, 3 ),
 ( 0.2232142857142854764, 0.2276785714285712858, 0.2321428571428570953, 0.2366071428571429047, 0.2410714285714287142 ),
 .UNSPECIFIED. ) 
 CURVE ( )  GEOMETRIC_REPRESENTATION_ITEM ( )  RATIONAL_B_SPLINE_CURVE ( ( 1.000000000000004219, 0.9238795325112825196, 1.000000000000000000, 0.9238795325112867385, 1.000000000000000000, 0.9238795325112867385, 1.000000000000000000, 0.9238795325112844070, 1.000000000000002442 ) ) 
 REPRESENTATION_ITEM ( '' )  );
#22373=CARTESIAN_POINT ( 'NONE',  ( 5.731347020009612645E-17, 4.842444444444443441, 0.3119999999999999996 ) ) ;
#22374=CARTESIAN_POINT ( 'NONE',  ( 0.3119999999999999996, 3.852861111111110404, 0.1292346314604056190 ) ) ;
#22375=CARTESIAN_POINT ( 'NONE',  ( -0.2206173157302028232, 4.661888889040620931, -0.2206173157302028232 ) ) ;
#22376=CARTESIAN_POINT ( 'NONE',  ( 0.2819296736111110979, 5.172305555631421470, -3.452642723725051716E-17 ) ) ;
#22380=CARTESIAN_POINT ( 'NONE',  ( 0.2732760442592158667, 0.03601662800317857738, -0.08586055624119162677 ) ) ;
#22386=CARTESIAN_POINT ( 'NONE',  ( 0.2819296736111110979, 5.210500000075865223, 0.1167790944451422425 ) ) ;
#22388=CARTESIAN_POINT ( 'NONE',  ( 0.1993543840281266633, 3.957027777853643791, -0.1993543840281266910 ) ) ;
#22393=CARTESIAN_POINT ( 'NONE',  ( -0.2819296736111110979, 0.5180555554796888451, -0.1167790944451423396 ) ) ;
#22395=CARTESIAN_POINT ( 'NONE',  ( -0.1993543840281266355, 4.873694444520310753, 0.1993543840281267465 ) ) ;
#22398=CARTESIAN_POINT ( 'NONE',  ( 5.178964085587577574E-17, 4.866750000075865223, 0.2819296736111110979 ) ) ;
#22403=CARTESIAN_POINT ( 'NONE',  ( 0.3119999999999999996, 4.463972222222222008, 0.1292346314604056190 ) ) ;
#22404=CARTESIAN_POINT ( 'NONE',  ( 0.1167790944451424506, 3.814666666742532630, 0.2819296736111110424 ) ) ;
#22405=CARTESIAN_POINT ( 'NONE',  ( 0.3119999999999999996, 0.3479166665149338589, -0.1292346314604056468 ) ) ;
#22406=CARTESIAN_POINT ( 'NONE',  ( 0.2045172001623904168, 4.022406176792101107, 0.2356682906421939394 ) ) ;
#22407=CARTESIAN_POINT ( 'NONE',  ( -0.09399142304410415538, 3.735586886565314124, 0.2976376820043376004 ) ) ;
#22414=CARTESIAN_POINT ( 'NONE',  ( 0.06359797816605802789, 4.153123496935264392, -0.3074626295701026191 ) ) ;
#22422=CARTESIAN_POINT ( 'NONE',  ( -0.2819296736111110424, 0.2263888888130222710, -0.1167790944451423396 ) ) ;
#22423=CARTESIAN_POINT ( 'NONE',  ( 0.3038785920422452658, 3.861053045795140193, 0.08166846456136669929 ) ) ;
#22425=CARTESIAN_POINT ( 'NONE',  ( -0.1292346314604056190, 0.1465277777777774515, -0.3119999999999999996 ) ) ;
#22429=CARTESIAN_POINT ( 'NONE',  ( 0.1292346314604058410, 4.345916666666665762, 0.3119999999999998885 ) ) ;
#22430=CARTESIAN_POINT ( 'NONE',  ( 0.1993543840281266355, 0.5840277777019111660, 0.1993543840281267465 ) ) ;
#22431=CARTESIAN_POINT ( 'NONE',  ( -0.2206173157302028232, 5.266055555555555046, -0.2206173157302028232 ) ) ;
#22435=CARTESIAN_POINT ( 'NONE',  ( 0.1993543840281266633, 4.179250000075865223, -0.1993543840281266910 ) ) ;
#22436=CARTESIAN_POINT ( 'NONE',  ( 5.731347020009612645E-17, 4.286888888888888083, 0.3119999999999999996 ) ) ;
#22440=CARTESIAN_POINT ( 'NONE',  ( -0.2819296736111110979, 4.963972222298087544, 0.000000000000000000 ) ) ;
#22444=CARTESIAN_POINT ( 'NONE',  ( -0.1292346314604058410, 0.2229166666666663466, 0.3119999999999998885 ) ) ;
#22446=CARTESIAN_POINT ( 'NONE',  ( -0.1167790944451423119, 4.675777777853642903, -0.2819296736111110979 ) ) ;
#22448=EDGE_CURVE ( 'NONE', #10770, #16112, #10955, .T. ) ;
#22449=CARTESIAN_POINT ( 'NONE',  ( -0.2206173157302028232, 4.766055555555554157, -0.2206173157302028232 ) ) ;
#22451=CARTESIAN_POINT ( 'NONE',  ( 0.1993543840281266355, 0.4868055554796889561, 0.1993543840281267465 ) ) ;
#22454=CARTESIAN_POINT ( 'NONE',  ( -0.1167790944451422702, 0.1222222221463555858, -0.2819296736111110424 ) ) ;
#22461=CARTESIAN_POINT ( 'NONE',  ( -0.2819296736111110979, 0.1708333332574666907, -0.1167790944451423396 ) ) ;
#22462=CARTESIAN_POINT ( 'NONE',  ( 0.1167790944451423535, 0.08055555547968892838, 0.2819296736111110424 ) ) ;
#22463=CARTESIAN_POINT ( 'NONE',  ( 0.1167790944451422702, 4.182722222298087544, -0.2819296736111110424 ) ) ;
#22465=CARTESIAN_POINT ( 'NONE',  ( -0.2819296736111110424, 4.807722222298088433, -0.1167790944451423119 ) ) ;
#22466=CARTESIAN_POINT ( 'NONE',  ( 0.2819296736111110979, 4.495222222298087544, -0.1167790944451423396 ) ) ;
#22468=ORIENTED_EDGE ( 'NONE', *, *, #7039, .T. ) ;
#22472=CARTESIAN_POINT ( 'NONE',  ( -0.3119999999999999996, 4.057722222373953969, 0.000000000000000000 ) ) ;
#22482=CARTESIAN_POINT ( 'NONE',  ( -0.3119999999999999996, 0.4798611109593782231, -0.1292346314604056745 ) ) ;
#22483=VERTEX_POINT ( 'NONE', #12543 ) ;
#22485=CARTESIAN_POINT ( 'NONE',  ( -4.974594353761572974E-07, 4.738258141874186258, 0.3119999999991586170 ) ) ;
#22492=CARTESIAN_POINT ( 'NONE',  ( -0.2919176283147316697, 4.665648881694019146, -0.1102027081678718656 ) ) ;
#22493=CARTESIAN_POINT ( 'NONE',  ( -0.1993543840281266355, 4.137583333409199149, 0.1993543840281267465 ) ) ;
#22496=CARTESIAN_POINT ( 'NONE',  ( 0.2206173157302027954, 3.918833333333332281, -0.2206173157302028232 ) ) ;
#22497=CARTESIAN_POINT ( 'NONE',  ( 0.1292346314604058410, 4.852861111262844140, 0.3119999999999998885 ) ) ;
#22498=CARTESIAN_POINT ( 'NONE',  ( -0.2819296736111110424, 4.189666666742533074, 0.1167790944451424923 ) ) ;
#22509=CARTESIAN_POINT ( 'NONE',  ( 0.1993543840281266633, 5.054250000075865223, -0.1993543840281266910 ) ) ;
#22510=CARTESIAN_POINT ( 'NONE',  ( -1.726321361862525858E-17, 3.852861111186976828, -0.2819296736111110979 ) ) ;
#22511=DIRECTION ( 'NONE',  ( -0.000000000000000000, -1.000000000000000000, -0.000000000000000000 ) ) ;
#22516=CARTESIAN_POINT ( 'NONE',  ( -0.2819296736111110979, 0.4659722221463555303, -3.452642723725051716E-17 ) ) ;
#22518=CARTESIAN_POINT ( 'NONE',  ( 0.1993543840281267465, 4.943138888964754507, 0.1993543840281266633 ) ) ;
#22520=CARTESIAN_POINT ( 'NONE',  ( -0.1167790944451423257, 4.842444444520309865, -0.2819296736111110424 ) ) ;
#22525=FACE_OUTER_BOUND ( 'NONE', #16036, .T. ) ;
#22526=CARTESIAN_POINT ( 'NONE',  ( -0.1292346314604057023, 4.450083333333333613, 0.3119999999999998885 ) ) ;
#22527=CARTESIAN_POINT ( 'NONE',  ( 0.1167790944451422702, 3.779944444520309865, -0.2819296736111110979 ) ) ;
#22528=CARTESIAN_POINT ( 'NONE',  ( -0.2206173157302028232, 4.210499999999999687, -0.2206173157302028232 ) ) ;
#22532=CARTESIAN_POINT ( 'NONE',  ( 0.3080688034448511026, 4.584097653652008830, 0.05047243502379121505 ) ) ;
#22538=CARTESIAN_POINT ( 'NONE',  ( 0.2764557534944322437, 4.636758977684069194, 0.1492039665729707199 ) ) ;
#22539=( BOUNDED_CURVE ( )  B_SPLINE_CURVE ( 2, ( #14104, #2762, #10213, #15923, #21532, #21416, #4705, #4820, #12173 ),
 .UNSPECIFIED., .F., .F. ) 
 B_SPLINE_CURVE_WITH_KNOTS ( ( 3, 2, 2, 2, 3 ),
 ( 0.6458333333333333703, 0.6562500000000000000, 0.6666666666666666297, 0.6770833333333333703, 0.6875000000000000000 ),
 .UNSPECIFIED. ) 
 CURVE ( )  GEOMETRIC_REPRESENTATION_ITEM ( )  RATIONAL_B_SPLINE_CURVE ( ( 1.000000000000000000, 0.9238795325112867385, 1.000000000000000000, 0.9238795325112867385, 1.000000000000000000, 0.9238795325112867385, 1.000000000000000000, 0.9238795325112867385, 1.000000000000000000 ) ) 
 REPRESENTATION_ITEM ( '' )  );
#22542=CARTESIAN_POINT ( 'NONE',  ( -0.008932914564021687126, 3.932975559310150526, -0.3118903747639839574 ) ) ;
#22543=CARTESIAN_POINT ( 'NONE',  ( 0.3028983722527614497, 5.146603643761612723, -0.01666118118391866215 ) ) ;
#22546=CARTESIAN_POINT ( 'NONE',  ( 0.2819296736111110424, 0.4208333332574666352, 0.1167790944451424923 ) ) ;
#22547=CARTESIAN_POINT ( 'NONE',  ( -0.05830577631245405928, 5.206640035683668621, 0.2763456444142127766 ) ) ;
#22551=CARTESIAN_POINT ( 'NONE',  ( -0.3103109364157903838, 5.105077227193183909, -0.01115075287914376635 ) ) ;
#22553=CARTESIAN_POINT ( 'NONE',  ( 0.2206173157302027676, 0.1777777777777774515, 0.2206173157302028787 ) ) ;
#22554=CARTESIAN_POINT ( 'NONE',  ( 0.2206173157302028787, 5.238277777777776478, 0.2206173157302027954 ) ) ;
#22555=EDGE_CURVE ( 'NONE', #9589, #19562, #9226, .T. ) ;
#22556=CARTESIAN_POINT ( 'NONE',  ( 0.1993543840281266633, 4.234805555631421470, -0.1993543840281266910 ) ) ;
#22558=B_SPLINE_CURVE_WITH_KNOTS ( 'NONE', 3,
 ( #6020, #13607, #19190, #9938, #11405, #20783, #4315, #4074, #18837, #18961, #7855, #17369, #9694, #15303, #660, #8087, #9452, #2133, #5670, #177, #13135, #11288, #18717, #2016, #7619, #13251, #22732, #15070, #22492, #8328, #4676, #4789, #10302, #21267, #6508, #23436, #12256, #21499, #6624 ),
 .UNSPECIFIED., .F., .F.,
 ( 4, 2, 2, 1, 2, 2, 1, 2, 2, 2, 2, 2, 2, 2, 2, 1, 2, 2, 2, 2, 4 ),
 ( 0.3563978319476573398, 0.3586778708967638396, 0.3609579098458703950, 0.3611004122801895200, 0.3611716634973491380, 0.3612072891059289192, 0.3612429147145087005, 0.3615279195831470060, 0.3620979293204236171, 0.3632379487949767838, 0.3643779682695300060, 0.3655179877440832281, 0.3666580072186363948, 0.3672280169559130059, 0.3675130218245513114, 0.3676555242588704364, 0.3677267754760300544, 0.3677980266931896169, 0.3700780656422960058, 0.3723581045914023391, 0.3746381435405087279 ),
 .UNSPECIFIED. ) ;
#22561=CARTESIAN_POINT ( 'NONE',  ( -1.910449006669871087E-17, 4.314666666666665762, -0.3119999999999999996 ) ) ;
#22562=CARTESIAN_POINT ( 'NONE',  ( 0.2819296736111110424, 4.939666666742532186, -0.1167790944451423396 ) ) ;
#22563=ADVANCED_FACE ( 'NONE', ( #939 ), #23602, .T. ) ;
#22564=CARTESIAN_POINT ( 'NONE',  ( -0.1985484582051802449, 5.148926605952134139, -0.2292351911855036173 ) ) ;
#22568=CARTESIAN_POINT ( 'NONE',  ( 0.1292346314604057300, 0.6118055554038226429, 0.3119999999999998885 ) ) ;
#22570=CARTESIAN_POINT ( 'NONE',  ( -0.2819296736111110979, 4.738277777853642903, -0.1167790944451422980 ) ) ;
#22572=CARTESIAN_POINT ( 'NONE',  ( -0.04147181628195097114, 4.044975027077821750, -0.3093406118436980434 ) ) ;
#22574=CARTESIAN_POINT ( 'NONE',  ( -0.1993543840281266633, 0.5145833332574666352, -0.1993543840281266910 ) ) ;
#22575=ORIENTED_EDGE ( 'NONE', *, *, #9829, .F. ) ;
#22576=CARTESIAN_POINT ( 'NONE',  ( 0.1167790944451423535, 0.5388888888130222155, 0.2819296736111110424 ) ) ;
#22582=EDGE_CURVE ( 'NONE', #6423, #6354, #7776, .T. ) ;
#22584=CARTESIAN_POINT ( 'NONE',  ( -0.2819296736111110979, 0.3374999999241333759, -0.1167790944451423396 ) ) ;
#22585=CARTESIAN_POINT ( 'NONE',  ( 0.2819296736111110979, 0.3131944443685777957, 0.000000000000000000 ) ) ;
#22588=CARTESIAN_POINT ( 'NONE',  ( 0.2819296736111110979, 4.391055555631421470, 0.1167790944451422425 ) ) ;
#22590=CARTESIAN_POINT ( 'NONE',  ( -0.1167790944451423535, 4.877166666742533963, 0.2819296736111110424 ) ) ;
#22591=CARTESIAN_POINT ( 'NONE',  ( -0.1993543840281266355, 4.526472222298087544, 0.1993543840281267465 ) ) ;
#22592=AXIS2_PLACEMENT_3D ( 'NONE', #5541, #15175, #9077 ) ;
#22595=CARTESIAN_POINT ( 'NONE',  ( 5.731347020009612645E-17, 4.509111111111110404, 0.3119999999999999996 ) ) ;
#22596=CARTESIAN_POINT ( 'NONE',  ( -0.3119999999999998885, 4.172305555707287894, 0.1292346314604058410 ) ) ;
#22599=CARTESIAN_POINT ( 'NONE',  ( 0.000000000000000000, 5.384999999999999787, -0.3119999999999999996 ) ) ;
#22606=CARTESIAN_POINT ( 'NONE',  ( -0.2965161282126838049, 4.999381080173537661, -0.09725926298535028658 ) ) ;
#22608=CARTESIAN_POINT ( 'NONE',  ( 0.2206173157302028232, 0.4624999998482670627, -0.2206173157302028232 ) ) ;
#22612=LINE ( 'NONE', #13355, #7330 ) ;
#22613=CARTESIAN_POINT ( 'NONE',  ( 0.04740204007499370514, 4.764705480950462757, -0.3086056850508328009 ) ) ;
#22619=CARTESIAN_POINT ( 'NONE',  ( 3.820898013339742174E-17, 5.384999999999999787, 0.3119999999999999996 ) ) ;
#22621=CARTESIAN_POINT ( 'NONE',  ( 0.2819296736111110424, 4.106333333409199149, -0.1167790944451423396 ) ) ;
#22623=CARTESIAN_POINT ( 'NONE',  ( -0.2206173157302028232, 4.821611111111110404, -0.2206173157302028232 ) ) ;
#22624=CARTESIAN_POINT ( 'NONE',  ( -0.2206173157302028232, 3.766055555555554601, -0.2206173157302028232 ) ) ;
#22625=CARTESIAN_POINT ( 'NONE',  ( 0.3119999999999999996, 4.700083333485065573, -0.1292346314604056745 ) ) ;
#22627=CARTESIAN_POINT ( 'NONE',  ( 0.1993543840281266633, 5.012583333409199149, -0.1993543840281266910 ) ) ;
#22628=ORIENTED_EDGE ( 'NONE', *, *, #8915, .F. ) ;
#22629=CARTESIAN_POINT ( 'NONE',  ( -0.1993543840281266910, 4.290361111186976828, -0.1993543840281266910 ) ) ;
#22630=ORIENTED_EDGE ( 'NONE', *, *, #8536, .F. ) ;
#22633=ORIENTED_EDGE ( 'NONE', *, *, #23018, .T. ) ;
#22637=CARTESIAN_POINT ( 'NONE',  ( 0.1167790944451422702, 3.960500000075866112, -0.2819296736111110979 ) ) ;
#22640=CARTESIAN_POINT ( 'NONE',  ( 7.256325792998745354E-13, 0.06073895945496885634, 0.3102389594549692098 ) ) ;
#22642=CARTESIAN_POINT ( 'NONE',  ( -0.1167790944451422702, 0.4555555554796890116, -0.2819296736111110979 ) ) ;
#22644=CARTESIAN_POINT ( 'NONE',  ( -0.2819296736111110424, 4.974388888964754507, -0.1167790944451423119 ) ) ;
#22645=CARTESIAN_POINT ( 'NONE',  ( -0.2206173157302028232, 3.932722222222221120, -0.2206173157302028232 ) ) ;
#22646=CARTESIAN_POINT ( 'NONE',  ( -1.726321361862525858E-17, 4.561194444520309865, -0.2819296736111110979 ) ) ;
#22648=CARTESIAN_POINT ( 'NONE',  ( 0.2893869579258043223, 4.866662948179751425, -0.1166288015440531262 ) ) ;
#22651=CARTESIAN_POINT ( 'NONE',  ( 0.1292346314604056190, 4.533416666666664874, -0.3119999999999999996 ) ) ;
#22652=CARTESIAN_POINT ( 'NONE',  ( 0.2819296736111110979, 3.884111111186976384, -0.1167790944451423396 ) ) ;
#22653=CARTESIAN_POINT ( 'NONE',  ( -0.3119999999999998885, 4.220916666666665762, 0.1292346314604058410 ) ) ;
#22654=CARTESIAN_POINT ( 'NONE',  ( -0.3119999999999999996, 0.5354166665149336923, -0.1292346314604056745 ) ) ;
#22656=CARTESIAN_POINT ( 'NONE',  ( 0.2487385569593157653, 4.591261249557366142, -0.1929159009956799564 ) ) ;
#22658=CARTESIAN_POINT ( 'NONE',  ( -0.1735004431958599436, 4.121918744418447744, 0.2593098876758328508 ) ) ;
#22661=CARTESIAN_POINT ( 'NONE',  ( -0.1917384371582980807, 3.938511949306523707, -0.2494961635661361310 ) ) ;
#22664=CARTESIAN_POINT ( 'NONE',  ( -0.2819296736111110979, 0.4555555554796890116, 0.1167790944451422425 ) ) ;
#22665=CARTESIAN_POINT ( 'NONE',  ( -0.07707608760941696280, 5.206640035683669510, 0.2713641110486283980 ) ) ;
#22669=CARTESIAN_POINT ( 'NONE',  ( -0.3111413042013332908, 4.614172690785681930, 0.03290619045792032848 ) ) ;
#22671=CARTESIAN_POINT ( 'NONE',  ( -0.3119999999999999996, 0.2680555555555552139, -3.820898013339742174E-17 ) ) ;
#22672=CARTESIAN_POINT ( 'NONE',  ( -0.2206173157302028232, 5.210499999999999687, -0.2206173157302028232 ) ) ;
#22673=CARTESIAN_POINT ( 'NONE',  ( 0.2819296736111110424, 4.286888888964754507, -0.1167790944451423396 ) ) ;
#22677=ORIENTED_EDGE ( 'NONE', *, *, #14198, .F. ) ;
#22678=CARTESIAN_POINT ( 'NONE',  ( 0.3119999999999998885, 0.3479166666666662633, 0.1292346314604058410 ) ) ;
#22679=CARTESIAN_POINT ( 'NONE',  ( -0.1993543840281266355, 4.693138888964754507, 0.1993543840281267465 ) ) ;
#22682=CARTESIAN_POINT ( 'NONE',  ( -0.07811407312994299301, 5.145356041543204029, -0.2939319536219872631 ) ) ;
#22684=CARTESIAN_POINT ( 'NONE',  ( 0.0002793920057309124327, 3.710492493090175259, -0.3119999064896394336 ) ) ;
#22686=CARTESIAN_POINT ( 'NONE',  ( 5.178964085587577574E-17, 4.325083333409199149, 0.2819296736111110979 ) ) ;
#22689=CARTESIAN_POINT ( 'NONE',  ( -0.03372224778004788426, 4.044757933730085853, -0.3102599952880983336 ) ) ;
#22692=CARTESIAN_POINT ( 'NONE',  ( 1.726321361862525858E-17, 0.5631944443685776847, -0.2819296736111110979 ) ) ;
#22694=LINE ( 'NONE', #7933, #15995 ) ;
#22700=CARTESIAN_POINT ( 'NONE',  ( -0.1167790944451422702, 0.4416666665908000611, -0.2819296736111110979 ) ) ;
#22701=CARTESIAN_POINT ( 'NONE',  ( -0.1993543840281266633, 0.3340277777019111660, -0.1993543840281266910 ) ) ;
#22702=CARTESIAN_POINT ( 'NONE',  ( -0.1167790944451423535, 4.266055555631421470, 0.2819296736111110424 ) ) ;
#22704=CARTESIAN_POINT ( 'NONE',  ( -0.1993543840281266355, 4.873694444520310753, 0.1993543840281267465 ) ) ;
#22705=CARTESIAN_POINT ( 'NONE',  ( 0.1993543840281267465, 4.318138888964754507, 0.1993543840281266633 ) ) ;
#22709=CARTESIAN_POINT ( 'NONE',  ( -0.3119999999999998885, 4.005638889040620931, 0.1292346314604058410 ) ) ;
#22710=CARTESIAN_POINT ( 'NONE',  ( 0.1292346314604057300, 0.1187499999999996614, 0.3119999999999998885 ) ) ;
#22712=ORIENTED_EDGE ( 'NONE', *, *, #6893, .F. ) ;
#22717=CARTESIAN_POINT ( 'NONE',  ( -0.02214754980521025859, 4.848813742978035357, 0.3119999961461823457 ) ) ;
#22718=CARTESIAN_POINT ( 'NONE',  ( -0.2884719277531277437, 4.998711128422118399, -0.1188678792519748117 ) ) ;
#22720=CARTESIAN_POINT ( 'NONE',  ( 0.3119999999999999996, 0.5145833331816003220, -0.1292346314604056468 ) ) ;
#22722=CARTESIAN_POINT ( 'NONE',  ( 0.07773895667863905956, 4.263908277548741133, -0.3027182936550676384 ) ) ;
#22723=CARTESIAN_POINT ( 'NONE',  ( -0.1292346314604068958, 4.651472222222221120, -0.3119999999999987228 ) ) ;
#22726=CARTESIAN_POINT ( 'NONE',  ( 0.2543668527069268270, 5.175014549981658440, 0.1503412913315801680 ) ) ;
#22732=CARTESIAN_POINT ( 'NONE',  ( -0.2965167191063861618, 4.666047801639679804, -0.09725748803006217802 ) ) ;
#22734=CARTESIAN_POINT ( 'NONE',  ( 0.1993543840281266633, 3.998694444520309865, -0.1993543840281266910 ) ) ;
#22737=CARTESIAN_POINT ( 'NONE',  ( -0.2144645408843714462, 5.188090166419283555, 0.1954364597099001455 ) ) ;
#22738=CARTESIAN_POINT ( 'NONE',  ( 0.1292346314604056190, 4.651472222373953969, -0.3119999999999999996 ) ) ;
#22739=CARTESIAN_POINT ( 'NONE',  ( -0.2819296736111110979, 4.974388888964754507, -0.1167790944451422980 ) ) ;
#22741=ADVANCED_FACE ( 'NONE', ( #17151 ), #19093, .T. ) ;
#22742=CARTESIAN_POINT ( 'NONE',  ( 0.1167790944451424368, 4.259111111186975940, 0.2819296736111110424 ) ) ;
#22745=ORIENTED_EDGE ( 'NONE', *, *, #12285, .T. ) ;
#22749=DIRECTION ( 'NONE',  ( 1.000000000000000000, 0.000000000000000000, 0.000000000000000000 ) ) ;
#22751=CARTESIAN_POINT ( 'NONE',  ( 0.2819296736111111534, 3.891055555631421470, 0.1167790944451422563 ) ) ;
#22752=CARTESIAN_POINT ( 'NONE',  ( 0.1000962206091226825, 4.429843089621714469, -0.2955515137184793195 ) ) ;
#22753=CARTESIAN_POINT ( 'NONE',  ( 0.3120000000000000551, 4.630638888888888083, 0.1292346314604056190 ) ) ;
#22754=CARTESIAN_POINT ( 'NONE',  ( 0.06525658555531335669, 0.06189869434473758980, 0.3049238613443945312 ) ) ;
#22756=CARTESIAN_POINT ( 'NONE',  ( 0.1167790944451423119, 0.4486111110352445364, -0.2819296736111110979 ) ) ;
#22759=CARTESIAN_POINT ( 'NONE',  ( 0.1167790944451424368, 4.828555555631421470, 0.2819296736111110424 ) ) ;
#22761=CARTESIAN_POINT ( 'NONE',  ( 0.2819296736111110424, 4.773000000075865223, -0.1167790944451423396 ) ) ;
#22763=CARTESIAN_POINT ( 'NONE',  ( 7.256325792998745354E-13, 0.06073895945496885634, 0.3102389594549692098 ) ) ;
#22764=LINE ( 'NONE', #21057, #1275 ) ;
#22766=CARTESIAN_POINT ( 'NONE',  ( -0.2206173157302028232, 4.599388888888888083, -0.2206173157302028232 ) ) ;
#22767=CARTESIAN_POINT ( 'NONE',  ( 0.2819296736111110979, 3.880638888964754063, -3.452642723725051716E-17 ) ) ;
#22768=CARTESIAN_POINT ( 'NONE',  ( 0.0003180184531269840040, 4.988268656965369807, -0.3120000001075144969 ) ) ;
#22769=ORIENTED_EDGE ( 'NONE', *, *, #1453, .F. ) ;
#22773=CARTESIAN_POINT ( 'NONE',  ( 0.3086474089601525805, 4.639775044814750338, 0.04641666148907084427 ) ) ;
#22775=EDGE_CURVE ( 'NONE', #8952, #5177, #5099, .T. ) ;
#22777=CARTESIAN_POINT ( 'NONE',  ( -0.01786144021398791693, 3.933228899117950927, -0.3115615334367522471 ) ) ;
#22778=EDGE_CURVE ( 'NONE', #5409, #1715, #2034, .T. ) ;
#22781=CARTESIAN_POINT ( 'NONE',  ( -0.2819296736111110424, 0.3930555554796889561, -0.1167790944451423396 ) ) ;
#22784=CARTESIAN_POINT ( 'NONE',  ( 0.3119999999999999996, 0.5180555555555551583, 0.000000000000000000 ) ) ;
#22786=CARTESIAN_POINT ( 'NONE',  ( -0.04069169679679301294, 5.117267119184975677, 0.3063199299893399896 ) ) ;
#22789=CARTESIAN_POINT ( 'NONE',  ( 0.2206173157302028787, 4.738277777777777366, 0.2206173157302027954 ) ) ;
#22790=CARTESIAN_POINT ( 'NONE',  ( 0.3119999999999999996, 0.1881944444444441089, -0.1292346314604056468 ) ) ;
#22791=CARTESIAN_POINT ( 'NONE',  ( -0.3119999999999999996, 5.102861111111111292, -0.1292346314604056468 ) ) ;
#22792=CARTESIAN_POINT ( 'NONE',  ( 0.1167790944451424368, 4.273000000075865223, 0.2819296736111110424 ) ) ;
#22793=CARTESIAN_POINT ( 'NONE',  ( -0.3039181560427893225, 4.333230708440404477, -0.08152835368557848073 ) ) ;
#22798=CARTESIAN_POINT ( 'NONE',  ( -0.1993543840281266910, 4.679250000075866112, -0.1993543840281266910 ) ) ;
#22803=CARTESIAN_POINT ( 'NONE',  ( -8.964115882027956832E-07, 3.710500024236165206, -0.3119999999987121964 ) ) ;
#22807=CARTESIAN_POINT ( 'NONE',  ( 0.1993543840281266633, 4.345916666742532186, -0.1993543840281266910 ) ) ;
#22809=CARTESIAN_POINT ( 'NONE',  ( -0.2629549181022274862, 4.062781045653800938, 0.1724798338529683339 ) ) ;
#22813=CARTESIAN_POINT ( 'NONE',  ( -0.2819296736111110424, 0.5180555554796888451, -0.1167790944451423396 ) ) ;
#22814=LINE ( 'NONE', #6104, #20139 ) ;
#22820=CARTESIAN_POINT ( 'NONE',  ( 0.2819296736111110979, 0.5944444443685777957, -0.1167790944451422980 ) ) ;
#22821=CARTESIAN_POINT ( 'NONE',  ( -0.1167790944451422702, 0.1638888888130222432, -0.2819296736111110424 ) ) ;
#22822=CARTESIAN_POINT ( 'NONE',  ( -0.1993543840281266355, 4.318138888964754507, 0.1993543840281267465 ) ) ;
#22824=CARTESIAN_POINT ( 'NONE',  ( 0.1167790944451424368, 4.884111111186977716, 0.2819296736111110424 ) ) ;
#22825=( BOUNDED_CURVE ( )  B_SPLINE_CURVE ( 2, ( #1081, #6448, #15838, #19493, #1207, #19734, #12559, #17550, #19613 ),
 .UNSPECIFIED., .F., .F. ) 
 B_SPLINE_CURVE_WITH_KNOTS ( ( 3, 2, 2, 2, 3 ),
 ( 0.8541666666666666297, 0.8645833333333333703, 0.8750000000000000000, 0.8854166666666666297, 0.8958333333333333703 ),
 .UNSPECIFIED. ) 
 CURVE ( )  GEOMETRIC_REPRESENTATION_ITEM ( )  RATIONAL_B_SPLINE_CURVE ( ( 1.000000000000000000, 0.9238795325112867385, 1.000000000000000000, 0.9238795325112867385, 1.000000000000000000, 0.9238795325112867385, 1.000000000000000000, 0.9238795325112867385, 1.000000000000000000 ) ) 
 REPRESENTATION_ITEM ( '' )  );
#22826=CARTESIAN_POINT ( 'NONE',  ( 0.1167790944451422702, 4.335500000075866112, -0.2819296736111110979 ) ) ;
#22831=CARTESIAN_POINT ( 'NONE',  ( 0.3119999999999999996, 3.866750000151731648, -0.1292346314604056745 ) ) ;
#22833=AXIS2_PLACEMENT_3D ( 'NONE', #23430, #23309, #6986 ) ;
#22838=CARTESIAN_POINT ( 'NONE',  ( 5.574357792518489764E-07, 4.071633398088104094, 0.3119999999989289674 ) ) ;
#22841=CARTESIAN_POINT ( 'NONE',  ( -0.1993543840281266633, 0.1256944443685777957, -0.1993543840281266910 ) ) ;
#22843=CARTESIAN_POINT ( 'NONE',  ( 0.001519364365302375416, 4.266014716456939304, -0.3119968335204331700 ) ) ;
#22845=CARTESIAN_POINT ( 'NONE',  ( 0.2897599955979855979, 4.755713818965608297, -0.1232763402910086042 ) ) ;
#22847=CARTESIAN_POINT ( 'NONE',  ( 0.2209006037727569149, 5.173586066099031378, 0.1969744680321389718 ) ) ;
#22848=VERTEX_POINT ( 'NONE', #1164 ) ;
#22853=CARTESIAN_POINT ( 'NONE',  ( 0.1167790944451424368, 3.925777777853643347, 0.2819296736111110424 ) ) ;
#22855=CARTESIAN_POINT ( 'NONE',  ( -0.2389227046462522874, 5.186592499910797294, 0.1656744875650611459 ) ) ;
#22856=CARTESIAN_POINT ( 'NONE',  ( 0.1292346314604056190, 4.540361111262843252, -0.3119999999999999996 ) ) ;
#22857=CARTESIAN_POINT ( 'NONE',  ( 0.1167790944451424506, 4.884111111186975940, 0.2819296736111110424 ) ) ;
#22859=CARTESIAN_POINT ( 'NONE',  ( 0.1993543840281267465, 4.318138888964754507, 0.1993543840281266633 ) ) ;
#22862=EDGE_CURVE ( 'NONE', #8952, #6354, #800, .T. ) ;
#22866=( BOUNDED_CURVE ( )  B_SPLINE_CURVE ( 2, ( #22122, #9079, #13007, #5421, #12522, #3715, #16410, #3351, #23818 ),
 .UNSPECIFIED., .F., .F. ) 
 B_SPLINE_CURVE_WITH_KNOTS ( ( 3, 2, 2, 2, 3 ),
 ( 0.4375000000000000000, 0.4479166666666666852, 0.4583333333333333148, 0.4687500000000000000, 0.4791666666666666852 ),
 .UNSPECIFIED. ) 
 CURVE ( )  GEOMETRIC_REPRESENTATION_ITEM ( )  RATIONAL_B_SPLINE_CURVE ( ( 1.000000000000000000, 0.9238795325112867385, 1.000000000000000000, 0.9238795325112867385, 1.000000000000000000, 0.9238795325112867385, 1.000000000000000000, 0.9238795325112867385, 1.000000000000000000 ) ) 
 REPRESENTATION_ITEM ( '' )  );
#22869=CARTESIAN_POINT ( 'NONE',  ( -0.2206173157302028787, 0.04583333318160039832, 0.2206173157302027954 ) ) ;
#22870=CARTESIAN_POINT ( 'NONE',  ( 0.2736220506547213938, 4.414403590476274175, 0.1516610675028668143 ) ) ;
#22872=CARTESIAN_POINT ( 'NONE',  ( -0.2819296736111110979, 0.4104166665908000056, -3.452642723725051716E-17 ) ) ;
#22875=CARTESIAN_POINT ( 'NONE',  ( -0.2819296736111110979, 4.811194444520309865, 0.000000000000000000 ) ) ;
#22877=CARTESIAN_POINT ( 'NONE',  ( 5.178964085587577574E-17, 4.700083333409199149, 0.2819296736111110979 ) ) ;
#22879=CARTESIAN_POINT ( 'NONE',  ( 0.2779722363314617861, 4.867466925649863718, -0.1418491738069263541 ) ) ;
#22882=CARTESIAN_POINT ( 'NONE',  ( -0.3119999999999999996, 4.384111111111110404, 0.000000000000000000 ) ) ;
#22885=CARTESIAN_POINT ( 'NONE',  ( 0.1167790944451422702, 3.891055555631421470, -0.2819296736111110979 ) ) ;
#22886=CARTESIAN_POINT ( 'NONE',  ( -1.910449006669871087E-17, 4.703555555555555046, -0.3119999999999999996 ) ) ;
#22887=ORIENTED_EDGE ( 'NONE', *, *, #23237, .T. ) ;
#22888=CARTESIAN_POINT ( 'NONE',  ( 2.802071455580988509E-07, 4.599388881221821990, -0.3119999999998741003 ) ) ;
#22890=EDGE_CURVE ( 'NONE', #5468, #14944, #16037, .T. ) ;
#22891=CARTESIAN_POINT ( 'NONE',  ( 0.2666049204415198437, 4.701487312746555958, -0.1626043098652351082 ) ) ;
#22899=CARTESIAN_POINT ( 'NONE',  ( -0.2819296736111110979, 0.5076388888130222155, -3.452642723725051716E-17 ) ) ;
#22905=CARTESIAN_POINT ( 'NONE',  ( -0.1497743226700191388, 4.622716354764487612, 0.2736999939638214974 ) ) ;
#22906=PLANE ( 'NONE',  #23362 ) ;
#22907=CYLINDRICAL_SURFACE ( 'NONE', #6333, 0.3119999999999999996 ) ;
#22908=CARTESIAN_POINT ( 'NONE',  ( 0.3119999999999999996, 0.2993055555555552139, -0.1292346314604056468 ) ) ;
#22909=CARTESIAN_POINT ( 'NONE',  ( 0.3119999999999999996, 4.856333333333332725, -3.820898013339742174E-17 ) ) ;
#22910=CARTESIAN_POINT ( 'NONE',  ( -0.2819296736111110424, 4.314666666742533074, 0.1167790944451424923 ) ) ;
#22911=CARTESIAN_POINT ( 'NONE',  ( -0.3038293207672896901, 4.337833751873854560, 0.08185879226206393966 ) ) ;
#22913=B_SPLINE_CURVE_WITH_KNOTS ( 'NONE', 3,
 ( #5283, #18575, #1866, #7245, #5527, #18692, #9428, #7596, #8946, #5768, #20405, #3698, #22109, #14811, #5404, #13228, #7360, #18452, #15048, #18335 ),
 .UNSPECIFIED., .F., .F.,
 ( 4, 2, 2, 2, 2, 2, 2, 2, 2, 4 ),
 ( 0.8497888536353912503, 0.8505139355485479280, 0.8512390174617047167, 0.8526891812880181831, 0.8541393451143315385, 0.8555895089406450049, 0.8570396727669584713, 0.8584898365932718267, 0.8599400004195852931, 0.8613901642458987595 ),
 .UNSPECIFIED. ) ;
#22918=EDGE_CURVE ( 'NONE', #2004, #19258, #20378, .T. ) ;
#22919=CARTESIAN_POINT ( 'NONE',  ( -0.2819296736111110979, 4.741750000075865223, 0.000000000000000000 ) ) ;
#22925=CARTESIAN_POINT ( 'NONE',  ( -0.2819296736111110979, 4.366750000075866112, 0.000000000000000000 ) ) ;
#22926=CARTESIAN_POINT ( 'NONE',  ( -0.0002931826408786237289, 4.043841211789635182, -0.3119998970421027362 ) ) ;
#22930=CARTESIAN_POINT ( 'NONE',  ( 0.1993543840281266355, 0.3756944443685777402, 0.1993543840281267465 ) ) ;
#22931=FACE_OUTER_BOUND ( 'NONE', #10405, .T. ) ;
#22932=CARTESIAN_POINT ( 'NONE',  ( 0.000000000000000000, 0.06249999999999967387, 0.000000000000000000 ) ) ;
#22935=CARTESIAN_POINT ( 'NONE',  ( -0.3119984077913639520, 3.778846792292107182, -0.04085387950071681790 ) ) ;
#22936=CARTESIAN_POINT ( 'NONE',  ( -0.1167790944451422702, 0.4972222221463556413, -0.2819296736111110979 ) ) ;
#22937=CARTESIAN_POINT ( 'NONE',  ( -0.1993543840281267465, 0.1256944443685777957, 0.1993543840281266633 ) ) ;
#22938=CARTESIAN_POINT ( 'NONE',  ( 5.178964085587577574E-17, 4.325083333409199149, 0.2819296736111110979 ) ) ;
#22940=CARTESIAN_POINT ( 'NONE',  ( 0.1993543840281266633, 4.790361111186976828, -0.1993543840281266910 ) ) ;
#22943=CARTESIAN_POINT ( 'NONE',  ( -0.3119999999999999996, 3.832027777929509771, -0.1292346314604056468 ) ) ;
#22944=CARTESIAN_POINT ( 'NONE',  ( -8.252060436089559755E-07, 4.682689096385127314, 0.3119999999976427185 ) ) ;
#22951=CARTESIAN_POINT ( 'NONE',  ( 0.1993543840281266355, 0.09791666659080004720, 0.1993543840281267465 ) ) ;
#22953=CARTESIAN_POINT ( 'NONE',  ( 0.1569321314460191408, 4.242963909200604178, 0.2727264845398821858 ) ) ;
#22956=CARTESIAN_POINT ( 'NONE',  ( 0.2754387896051087581, 4.081160839835338727, 0.1498674073576002908 ) ) ;
#22965=CARTESIAN_POINT ( 'NONE',  ( -0.2819296736111110424, 4.071611111186976828, -0.1167790944451423119 ) ) ;
#22966=CARTESIAN_POINT ( 'NONE',  ( 0.06090617276557083043, 5.042162600288494723, -0.3064239527462913615 ) ) ;
#22968=CARTESIAN_POINT ( 'NONE',  ( 0.1292346314604058410, 4.463972222373954857, 0.3119999999999998885 ) ) ;
#22969=CARTESIAN_POINT ( 'NONE',  ( 0.1993543840281267465, 4.943138888964754507, 0.1993543840281266633 ) ) ;
#22971=CARTESIAN_POINT ( 'NONE',  ( 5.178964085587577574E-17, 4.144527777853642903, 0.2819296736111110979 ) ) ;
#22974=VECTOR ( 'NONE', #10120, 39.37007874015748143 ) ;
#22975=VERTEX_POINT ( 'NONE', #10922 ) ;
#22980=CARTESIAN_POINT ( 'NONE',  ( 0.03975918008867412173, 5.131473312690730815, 0.3040444178253544072 ) ) ;
#22982=CARTESIAN_POINT ( 'NONE',  ( 0.06319114465426710348, 4.406713632401503489, 0.3055443619506773012 ) ) ;
#22983=CARTESIAN_POINT ( 'NONE',  ( 1.910449006669871087E-17, 0.08055555540382261515, -0.3119999999999999996 ) ) ;
#22986=CARTESIAN_POINT ( 'NONE',  ( 1.726321361862525858E-17, 0.1048611110352444808, -0.2819296736111110979 ) ) ;
#22989=CARTESIAN_POINT ( 'NONE',  ( 0.2819296736111110979, 4.779944444520310753, 0.1167790944451422425 ) ) ;
#22992=CARTESIAN_POINT ( 'NONE',  ( 0.1993543840281267465, 4.762583333409199149, 0.1993543840281266633 ) ) ;
#22993=CARTESIAN_POINT ( 'NONE',  ( -0.002224882015017722817, 4.155008342873060201, -0.3119932009208763457 ) ) ;
#22997=CARTESIAN_POINT ( 'NONE',  ( -0.1292346314604057023, 4.283416666666666650, 0.3119999999999998885 ) ) ;
#22998=AXIS2_PLACEMENT_3D ( 'NONE', #13289, #16924, #5582 ) ;
#22999=CARTESIAN_POINT ( 'NONE',  ( 0.3119999999999999996, 5.088972222373954857, -0.1292346314604056745 ) ) ;
#23006=CARTESIAN_POINT ( 'NONE',  ( 0.001521130329658632301, 4.710459113145087251, -0.3119968249152551554 ) ) ;
#23007=CARTESIAN_POINT ( 'NONE',  ( -2.918002456435568987E-09, 4.127166543308980806, 0.3119999999999999996 ) ) ;
#23010=ADVANCED_FACE ( 'NONE', ( #5303 ), #23696, .T. ) ;
#23013=CARTESIAN_POINT ( 'NONE',  ( -0.2819296736111110424, 0.4486111110352445364, -0.1167790944451423396 ) ) ;
#23018=EDGE_CURVE ( 'NONE', #10793, #14891, #22866, .T. ) ;
#23019=VERTEX_POINT ( 'NONE', #19941 ) ;
#23020=CARTESIAN_POINT ( 'NONE',  ( -0.1808653720604334325, 5.113170069492856129, 0.2512378506988575122 ) ) ;
#23023=CARTESIAN_POINT ( 'NONE',  ( -0.2206173157302028787, 0.5527777777777773682, 0.2206173157302027954 ) ) ;
#23024=CARTESIAN_POINT ( 'NONE',  ( 0.1292346314604058410, 5.012583333333332725, 0.3119999999999998885 ) ) ;
#23025=CARTESIAN_POINT ( 'NONE',  ( -0.1167790944451423257, 4.023000000075866112, -0.2819296736111110424 ) ) ;
#23031=CARTESIAN_POINT ( 'NONE',  ( -0.1167790944451423535, 4.696611111186976828, 0.2819296736111110424 ) ) ;
#23033=CARTESIAN_POINT ( 'NONE',  ( -0.2614063550833075067, 5.159425771521426896, 0.1481041763251536303 ) ) ;
#23037=CARTESIAN_POINT ( 'NONE',  ( 0.1167790944451422702, 4.293833333409199149, -0.2819296736111110979 ) ) ;
#23039=CARTESIAN_POINT ( 'NONE',  ( -0.08351110729652544418, 4.046178605385413185, -0.3012663639467730858 ) ) ;
#23043=CARTESIAN_POINT ( 'NONE',  ( 1.726321361862525858E-17, 0.5076388888130222155, -0.2819296736111110979 ) ) ;
#23048=CARTESIAN_POINT ( 'NONE',  ( -0.2495005081859424656, 3.785671182798638235, 0.1917329975044681778 ) ) ;
#23049=CARTESIAN_POINT ( 'NONE',  ( 0.2819296736111110979, 0.5388888888130223265, -0.1167790944451422980 ) ) ;
#23050=CARTESIAN_POINT ( 'NONE',  ( -5.178964085587577574E-17, 0.2993055554796889561, 0.2819296736111110979 ) ) ;
#23051=CARTESIAN_POINT ( 'NONE',  ( -0.1167790944451423257, 4.078555555631421470, -0.2819296736111110424 ) ) ;
#23054=CARTESIAN_POINT ( 'NONE',  ( 0.2819296736111110979, 4.724388888964754507, 0.1167790944451422425 ) ) ;
#23055=CARTESIAN_POINT ( 'NONE',  ( -0.1292346314604056190, 0.1395833331816004053, -0.3119999999999999996 ) ) ;
#23059=CARTESIAN_POINT ( 'NONE',  ( -0.3119999999999999996, 3.779944444596176734, 0.000000000000000000 ) ) ;
#23067=CARTESIAN_POINT ( 'NONE',  ( -0.2983450752461472288, 4.999556594882858640, -0.09148912044693334467 ) ) ;
#23068=CARTESIAN_POINT ( 'NONE',  ( 0.2206173157302028232, 0.6291666665149338034, -0.2206173157302028232 ) ) ;
#23070=CARTESIAN_POINT ( 'NONE',  ( 0.1127385644800980580, 4.262880112112297226, -0.2914991025335854635 ) ) ;
#23072=CARTESIAN_POINT ( 'NONE',  ( 0.2058003546260330774, 4.078051603074912101, 0.2353791526578999371 ) ) ;
#23078=CARTESIAN_POINT ( 'NONE',  ( 0.1993543840281267465, 3.762583333409198705, 0.1993543840281266633 ) ) ;
#23079=DIRECTION ( 'NONE',  ( 0.000000000000000000, 0.000000000000000000, 1.000000000000000000 ) ) ;
#23080=CARTESIAN_POINT ( 'NONE',  ( -0.2932553954330455737, 5.179855157894580842, 0.004433361297087813797 ) ) ;
#23082=CARTESIAN_POINT ( 'NONE',  ( 5.731347020009612645E-17, 4.627166666818398610, 0.3119999999999999996 ) ) ;
#23084=CARTESIAN_POINT ( 'NONE',  ( 5.178964085587577574E-17, 5.047305555631421470, 0.2819296736111110979 ) ) ;
#23086=CARTESIAN_POINT ( 'NONE',  ( -0.2819296736111110424, 4.127166666742532186, -0.1167790944451423119 ) ) ;
#23094=CARTESIAN_POINT ( 'NONE',  ( 0.3119999999999998885, 0.06319444429271152408, 0.1292346314604058410 ) ) ;
#23098=DIRECTION ( 'NONE',  ( -0.000000000000000000, -1.000000000000000000, -0.000000000000000000 ) ) ;
#23101=CARTESIAN_POINT ( 'NONE',  ( -0.1993543840281267465, 0.07013888881302225708, 0.1993543840281266633 ) ) ;
#23104=CARTESIAN_POINT ( 'NONE',  ( -0.2819296736111110424, 4.689666666742532186, 0.1167790944451424923 ) ) ;
#23109=CARTESIAN_POINT ( 'NONE',  ( 5.731347020009612645E-17, 4.286888888888888083, 0.3119999999999999996 ) ) ;
#23111=CARTESIAN_POINT ( 'NONE',  ( 0.3105037589794399921, 4.973547786746206789, 0.03065709337648704624 ) ) ;
#23117=CARTESIAN_POINT ( 'NONE',  ( 0.2485617479699924470, 4.690811910894372438, 0.1929793757338557625 ) ) ;
#23123=CARTESIAN_POINT ( 'NONE',  ( -0.1993543840281267465, 0.1395833332574666907, 0.1993543840281266633 ) ) ;
#23127=AXIS2_PLACEMENT_3D ( 'NONE', #1918, #18747, #16804 ) ;
#23129=CARTESIAN_POINT ( 'NONE',  ( -0.2975325615348068942, 4.615999354583628644, 0.09627391117643818719 ) ) ;
#23130=CARTESIAN_POINT ( 'NONE',  ( -0.02459558260538192292, 4.293134600018148284, 0.3110673077616819548 ) ) ;
#23132=CARTESIAN_POINT ( 'NONE',  ( 0.2206173157302027676, 0.4555555555555552139, 0.2206173157302028787 ) ) ;
#23133=CARTESIAN_POINT ( 'NONE',  ( -0.3119999999999999996, 4.939666666666665762, 0.000000000000000000 ) ) ;
#23134=CARTESIAN_POINT ( 'NONE',  ( -0.1993543840281266355, 4.040361111186976828, 0.1993543840281267465 ) ) ;
#23137=CARTESIAN_POINT ( 'NONE',  ( 5.731347020009612645E-17, 3.897999999999999243, 0.3119999999999999996 ) ) ;
#23142=CARTESIAN_POINT ( 'NONE',  ( -0.2494960473753227714, 3.996427622109653299, -0.1917385859694114847 ) ) ;
#23143=CARTESIAN_POINT ( 'NONE',  ( -0.2819296736111110424, 4.634111111186976828, 0.1167790944451424923 ) ) ;
#23150=CARTESIAN_POINT ( 'NONE',  ( -0.2819296736111110979, 4.363277777853643791, -0.1167790944451422980 ) ) ;
#23151=CARTESIAN_POINT ( 'NONE',  ( -0.3104415801607898762, 4.834635239992220335, -0.03154143600449414719 ) ) ;
#23152=CARTESIAN_POINT ( 'NONE',  ( 0.04820796449995154442, 5.072973651020436847, 0.3082531300064171864 ) ) ;
#23156=CARTESIAN_POINT ( 'NONE',  ( 0.2819296736111110424, 0.09444444436857780956, -0.1167790944451423119 ) ) ;
#23157=CARTESIAN_POINT ( 'NONE',  ( -5.731347020009612645E-17, 0.1152777777777774515, 0.3119999999999999996 ) ) ;
#23158=CARTESIAN_POINT ( 'NONE',  ( 0.2206173157302027954, 4.474388888888888083, -0.2206173157302028232 ) ) ;
#23164=CARTESIAN_POINT ( 'NONE',  ( -0.2819296736111110979, 0.4520833332574666907, -3.452642723725051716E-17 ) ) ;
#23165=CARTESIAN_POINT ( 'NONE',  ( -0.1167790944451422702, 0.4416666665908000611, -0.2819296736111110424 ) ) ;
#23166=CARTESIAN_POINT ( 'NONE',  ( -0.1993543840281266910, 4.137583333409199149, -0.1993543840281266910 ) ) ;
#23168=B_SPLINE_CURVE_WITH_KNOTS ( 'NONE', 3,
 ( #16745, #7475, #8944, #7121, #24048, #14561, #16392, #10903, #22106, #1745, #5279, #3451, #12989, #7358, #6998, #23800, #3211, #12623, #27, #8818, #3696, #18333, #20041, #16267, #1628, #16509, #7242, #14688, #3571, #9185, #16629, #14808, #20403, #11142, #18572, #9304, #14924, #23678, #3329 ),
 .UNSPECIFIED., .F., .F.,
 ( 4, 2, 2, 2, 2, 2, 2, 2, 2, 2, 1, 2, 2, 2, 2, 2, 2, 2, 2, 4 ),
 ( 0.9594394450162125887, 0.9614297162944156483, 0.9624248519335172336, 0.9634199875726187079, 0.9644151232117202932, 0.9654102588508217675, 0.9664053944899233528, 0.9674005301290248271, 0.9683956657681264124, 0.9693908014072278867, 0.9695151933621155571, 0.9695773893395593923, 0.9696395853170033385, 0.9698883692267786794, 0.9703859370463294720, 0.9713810726854309463, 0.9723762083245325316, 0.9733713439636340059, 0.9743664796027355912, 0.9753616152418370655 ),
 .UNSPECIFIED. ) ;
#23170=CARTESIAN_POINT ( 'NONE',  ( -0.1993543840281266355, 4.707027777853643791, 0.1993543840281267465 ) ) ;
#23174=EDGE_LOOP ( 'NONE', ( #14726, #23783, #8593, #13093 ) ) ;
#23176=CARTESIAN_POINT ( 'NONE',  ( 0.1292346314604056190, 4.700083333333332725, -0.3119999999999999996 ) ) ;
#23177=CARTESIAN_POINT ( 'NONE',  ( -0.2206173157302028232, 3.939666666818398610, -0.2206173157302028232 ) ) ;
#23180=ADVANCED_FACE ( 'NONE', ( #4641 ), #17755, .T. ) ;
#23181=DIRECTION ( 'NONE',  ( 0.000000000000000000, 0.000000000000000000, 1.000000000000000000 ) ) ;
#23182=VERTEX_POINT ( 'NONE', #2810 ) ;
#23185=VECTOR ( 'NONE', #19822, 39.37007874015748143 ) ;
#23186=CARTESIAN_POINT ( 'NONE',  ( 5.731347020009612645E-17, 4.786888888888888083, 0.3119999999999999996 ) ) ;
#23187=CARTESIAN_POINT ( 'NONE',  ( -0.2683814352459896746, 4.552880090615864184, -0.1640201213671886316 ) ) ;
#23188=ORIENTED_EDGE ( 'NONE', *, *, #21993, .T. ) ;
#23189=CARTESIAN_POINT ( 'NONE',  ( -0.1167790944451422702, 0.06666666659080003332, -0.2819296736111110424 ) ) ;
#23191=CARTESIAN_POINT ( 'NONE',  ( 6.089848770316828444E-07, 4.238302053322364316, 0.3119999999987258521 ) ) ;
#23199=CARTESIAN_POINT ( 'NONE',  ( 0.1993543840281266633, 3.776472222298087988, -0.1993543840281266910 ) ) ;
#23200=CARTESIAN_POINT ( 'NONE',  ( 0.2761986883776191282, 5.034245972029707694, -0.1452648408779728950 ) ) ;
#23201=CARTESIAN_POINT ( 'NONE',  ( -0.2835900173929711277, 5.176626687221649092, -0.08093004039994856902 ) ) ;
#23203=CARTESIAN_POINT ( 'NONE',  ( 0.2206173157302027954, 4.536888889040620931, -0.2206173157302028232 ) ) ;
#23204=CARTESIAN_POINT ( 'NONE',  ( 0.1993543840281266633, 4.623694444520309865, -0.1993543840281266910 ) ) ;
#23205=CARTESIAN_POINT ( 'NONE',  ( 0.1167790944451422702, 4.002166666742532186, -0.2819296736111110424 ) ) ;
#23206=VERTEX_POINT ( 'NONE', #17691 ) ;
#23208=EDGE_CURVE ( 'NONE', #14891, #12009, #14039, .T. ) ;
#23215=CARTESIAN_POINT ( 'NONE',  ( 0.3119999999999998885, 0.1187499998482670627, 0.1292346314604058410 ) ) ;
#23217=CARTESIAN_POINT ( 'NONE',  ( 1.145733547534701715E-12, 5.130222168000691418, 0.3067077167097377322 ) ) ;
#23220=CARTESIAN_POINT ( 'NONE',  ( 0.2819296736111110979, 0.03398119426037962687, 0.04827834974809540325 ) ) ;
#23223=CARTESIAN_POINT ( 'NONE',  ( -0.1993543840281266355, 4.526472222298087544, 0.1993543840281267465 ) ) ;
#23224=CARTESIAN_POINT ( 'NONE',  ( 0.1900105704308386045, 5.206640035683666845, 0.2082794372640154323 ) ) ;
#23227=FACE_OUTER_BOUND ( 'NONE', #16350, .T. ) ;
#23228=CARTESIAN_POINT ( 'NONE',  ( 0.3119999999999999996, 4.193138888888888083, -0.1292346314604056745 ) ) ;
#23229=CARTESIAN_POINT ( 'NONE',  ( 5.731347020009612645E-17, 4.564666666666665762, 0.3119999999999999996 ) ) ;
#23231=CARTESIAN_POINT ( 'NONE',  ( 0.1290452976441722188, 4.964245088727332167, 0.2846185331919179329 ) ) ;
#23235=CARTESIAN_POINT ( 'NONE',  ( 0.0001071248759953418567, 4.710497121865020453, -0.3119999863294411480 ) ) ;
#23236=CARTESIAN_POINT ( 'NONE',  ( 0.2557079804836105974, 4.135622660786435922, 0.1809013949627109874 ) ) ;
#23237=EDGE_CURVE ( 'NONE', #789, #16124, #2463, .T. ) ;
#23242=CARTESIAN_POINT ( 'NONE',  ( 0.2819296736111110979, 0.5909722221463555858, 0.000000000000000000 ) ) ;
#23249=CARTESIAN_POINT ( 'NONE',  ( -0.2805582969777798974, 4.275873129557496100, -0.1383904727280197144 ) ) ;
#23251=CARTESIAN_POINT ( 'NONE',  ( -0.3119999999999999996, 0.4381944444444440534, 0.1292346314604056190 ) ) ;
#23252=CARTESIAN_POINT ( 'NONE',  ( -1.910449006669871087E-17, 5.036888888888888971, -0.3119999999999999996 ) ) ;
#23254=CARTESIAN_POINT ( 'NONE',  ( 0.2819296736111111534, 4.210500000075865223, 0.1167790944451422563 ) ) ;
#23255=EDGE_CURVE ( 'NONE', #20423, #9842, #4399, .T. ) ;
#23256=CARTESIAN_POINT ( 'NONE',  ( 0.1167790944451422702, 3.960500000075866556, -0.2819296736111110424 ) ) ;
#23258=DIRECTION ( 'NONE',  ( -0.000000000000000000, -1.000000000000000000, -0.000000000000000000 ) ) ;
#23260=ORIENTED_EDGE ( 'NONE', *, *, #1036, .T. ) ;
#23263=CARTESIAN_POINT ( 'NONE',  ( -1.726321361862525858E-17, 4.616750000075865223, -0.2819296736111110979 ) ) ;
#23264=CARTESIAN_POINT ( 'NONE',  ( -0.1292346314604057300, 4.116749999999998799, 0.3119999999999998885 ) ) ;
#23269=CARTESIAN_POINT ( 'NONE',  ( -0.2819296736111110424, 3.981333333409199593, 0.1167790944451424923 ) ) ;
#23270=CARTESIAN_POINT ( 'NONE',  ( -0.07900779940945044932, 4.823921452132610810, -0.3024882769266306615 ) ) ;
#23271=CARTESIAN_POINT ( 'NONE',  ( -0.3119999999999999996, 4.880638888888888083, -0.1292346314604056468 ) ) ;
#23274=CARTESIAN_POINT ( 'NONE',  ( -0.1167790944451424368, 0.5874999999241333759, 0.2819296736111110424 ) ) ;
#23279=CARTESIAN_POINT ( 'NONE',  ( 0.3119999999999999996, 3.967444444444443441, -3.820898013339742174E-17 ) ) ;
#23280=CARTESIAN_POINT ( 'NONE',  ( -0.3038822597986416407, 3.782168817998234456, 0.08165548423408781897 ) ) ;
#23282=CARTESIAN_POINT ( 'NONE',  ( 0.1993543840281266910, 0.4868055554796889561, -0.1993543840281266910 ) ) ;
#23283=CARTESIAN_POINT ( 'NONE',  ( -0.2819296736111110424, 4.029944444520309865, -0.1167790944451423119 ) ) ;
#23287=CARTESIAN_POINT ( 'NONE',  ( 0.1993543840281266633, 4.623694444520309865, -0.1993543840281266910 ) ) ;
#23288=CARTESIAN_POINT ( 'NONE',  ( 0.3065460696617670067, 5.130431554589877763, 0.02195525653071019045 ) ) ;
#23289=CARTESIAN_POINT ( 'NONE',  ( 0.2637416282169243176, 5.083478233281141456, -0.1669753523072903256 ) ) ;
#23291=CARTESIAN_POINT ( 'NONE',  ( 0.3119999999999999996, 4.800777777777776478, -3.820898013339742174E-17 ) ) ;
#23292=CARTESIAN_POINT ( 'NONE',  ( -0.3119999999999999996, 3.946611111262843252, 0.000000000000000000 ) ) ;
#23294=DIRECTION ( 'NONE',  ( 1.000000000000000000, 0.000000000000000000, 0.000000000000000000 ) ) ;
#23295=CARTESIAN_POINT ( 'NONE',  ( 0.2550676506477509431, 0.03242967361111052244, 0.1209729261660745098 ) ) ;
#23297=CARTESIAN_POINT ( 'NONE',  ( -0.2819296736111110979, 4.797305555631420582, 0.000000000000000000 ) ) ;
#23299=ORIENTED_EDGE ( 'NONE', *, *, #14552, .F. ) ;
#23300=CARTESIAN_POINT ( 'NONE',  ( -0.2681623976265802289, 5.109836857663620613, -0.1564668307319910245 ) ) ;
#23302=CARTESIAN_POINT ( 'NONE',  ( -0.2064849667589426785, 4.565315176446661738, 0.2372659973544750944 ) ) ;
#23304=CARTESIAN_POINT ( 'NONE',  ( 0.1993543840281266355, 0.04236111103524448085, 0.1993543840281267465 ) ) ;
#23305=EDGE_CURVE ( 'NONE', #3503, #23698, #3717, .T. ) ;
#23307=ORIENTED_EDGE ( 'NONE', *, *, #13462, .F. ) ;
#23309=DIRECTION ( 'NONE',  ( 1.000000000000000000, 0.000000000000000000, 6.123233995736811642E-17 ) ) ;
#23312=CARTESIAN_POINT ( 'NONE',  ( -0.2578690707795402992, 5.052376359289721286, -0.1763080320115959498 ) ) ;
#23316=ADVANCED_FACE ( 'NONE', ( #4939 ), #3231, .T. ) ;
#23317=CARTESIAN_POINT ( 'NONE',  ( -0.2819296736111110979, 3.797305555631421470, 0.000000000000000000 ) ) ;
#23318=CARTESIAN_POINT ( 'NONE',  ( 0.09843671724995897709, 5.018886197857182374, 0.2967729835320978005 ) ) ;
#23319=CARTESIAN_POINT ( 'NONE',  ( 0.09694982473845883963, 0.06249891840240667101, 0.2965547697865978938 ) ) ;
#23321=CARTESIAN_POINT ( 'NONE',  ( -0.3119999999999998885, 4.561194444596177178, 0.1292346314604058410 ) ) ;
#23322=CARTESIAN_POINT ( 'NONE',  ( -0.1993543840281266355, 4.707027777853643791, 0.1993543840281267465 ) ) ;
#23323=ORIENTED_EDGE ( 'NONE', *, *, #7809, .F. ) ;
#23324=CARTESIAN_POINT ( 'NONE',  ( -0.1167790944451423535, 4.085500000075865223, 0.2819296736111110424 ) ) ;
#23330=CARTESIAN_POINT ( 'NONE',  ( 0.1292346314604056745, 0.02152777762604484585, -0.3119999999999999996 ) ) ;
#23332=CARTESIAN_POINT ( 'NONE',  ( -0.3039450333671691595, 4.388825253606679411, -0.08146239154257989279 ) ) ;
#23333=CARTESIAN_POINT ( 'NONE',  ( 0.000000000000000000, 5.384999999999999787, -0.3119999999999999996 ) ) ;
#23340=CYLINDRICAL_SURFACE ( 'NONE', #13995, 0.3119999999999999996 ) ;
#23342=CARTESIAN_POINT ( 'NONE',  ( 0.1993543840281267465, 4.484805555631420582, 0.1993543840281266633 ) ) ;
#23343=DIRECTION ( 'NONE',  ( -0.000000000000000000, -1.000000000000000000, -0.000000000000000000 ) ) ;
#23347=CARTESIAN_POINT ( 'NONE',  ( 0.3119999999999999996, 4.300777777777777366, -3.820898013339742174E-17 ) ) ;
#23348=CARTESIAN_POINT ( 'NONE',  ( -0.3119999999999999996, 4.658416666666666650, -0.1292346314604056468 ) ) ;
#23354=CARTESIAN_POINT ( 'NONE',  ( -0.1916180747362854764, 4.899256411840736014, 0.2495837949844624815 ) ) ;
#23360=CARTESIAN_POINT ( 'NONE',  ( 0.08166450070216819956, 3.796057964755177760, 0.3038796990105872564 ) ) ;
#23361=VERTEX_POINT ( 'NONE', #8349 ) ;
#23362=AXIS2_PLACEMENT_3D ( 'NONE', #2434, #11958, #13774 ) ;
#23368=CARTESIAN_POINT ( 'NONE',  ( -0.1993543840281266355, 5.095916666742533074, 0.1993543840281267465 ) ) ;
#23371=EDGE_CURVE ( 'NONE', #8265, #19443, #8231, .T. ) ;
#23372=CARTESIAN_POINT ( 'NONE',  ( -0.2507716889269062666, 4.607602545532474281, -0.1880287605004705154 ) ) ;
#23373=CARTESIAN_POINT ( 'NONE',  ( -0.3103924686884816375, 4.278734377591210780, -0.04199753653605552139 ) ) ;
#23375=CARTESIAN_POINT ( 'NONE',  ( 0.3119999999999999996, 0.5180555555555551583, 0.000000000000000000 ) ) ;
#23376=CARTESIAN_POINT ( 'NONE',  ( -0.2206173157302027676, 4.891055555555555046, 0.2206173157302028787 ) ) ;
#23377=CARTESIAN_POINT ( 'NONE',  ( 5.178964085587577574E-17, 4.311194444520309865, 0.2819296736111110979 ) ) ;
#23378=CARTESIAN_POINT ( 'NONE',  ( -0.1167790944451423535, 3.988277777853643347, 0.2819296736111110424 ) ) ;
#23383=CARTESIAN_POINT ( 'NONE',  ( -0.2819296736111110424, 4.404944444520309865, -0.1167790944451423119 ) ) ;
#23391=CARTESIAN_POINT ( 'NONE',  ( -0.1167790944451423535, 4.154944444520310753, 0.2819296736111110979 ) ) ;
#23397=CARTESIAN_POINT ( 'NONE',  ( -5.178964085587577574E-17, 0.5909722221463555858, 0.2819296736111110979 ) ) ;
#23399=CARTESIAN_POINT ( 'NONE',  ( -0.1292346314604056190, 0.09097222222222188515, -0.3119999999999999996 ) ) ;
#23403=ORIENTED_EDGE ( 'NONE', *, *, #1428, .T. ) ;
#23405=CARTESIAN_POINT ( 'NONE',  ( -0.004454008101752859362, 3.766175329530188076, -0.3119727745386958184 ) ) ;
#23407=CARTESIAN_POINT ( 'NONE',  ( -5.178964085587577574E-17, 0.3548611110352444808, 0.2819296736111110979 ) ) ;
#23408=CARTESIAN_POINT ( 'NONE',  ( 0.1993543840281266633, 4.012583333409199149, -0.1993543840281266910 ) ) ;
#23411=CARTESIAN_POINT ( 'NONE',  ( 0.1993543840281267465, 4.665361111186976828, 0.1993543840281266633 ) ) ;
#23412=CARTESIAN_POINT ( 'NONE',  ( 0.2020813919255678437, 5.124140614773011748, 0.2323642223043996258 ) ) ;
#23414=ORIENTED_EDGE ( 'NONE', *, *, #23894, .T. ) ;
#23415=CARTESIAN_POINT ( 'NONE',  ( 0.3120000000000000551, 4.797305555555555046, 0.1292346314604056190 ) ) ;
#23416=CARTESIAN_POINT ( 'NONE',  ( 0.1167790944451424368, 5.092444444520309865, 0.2819296736111110424 ) ) ;
#23417=CARTESIAN_POINT ( 'NONE',  ( 0.2664282082089008408, 4.191741270665894525, 0.1623755266555968191 ) ) ;
#23420=CARTESIAN_POINT ( 'NONE',  ( 0.2819296736111110979, 4.936194444520309865, -3.452642723725051716E-17 ) ) ;
#23422=ORIENTED_EDGE ( 'NONE', *, *, #666, .T. ) ;
#23424=CARTESIAN_POINT ( 'NONE',  ( -0.3066395854341782967, 5.113642974739954106, -0.04204093653351399090 ) ) ;
#23425=CARTESIAN_POINT ( 'NONE',  ( 2.802071455580988509E-07, 4.599388881221821990, -0.3119999999998741003 ) ) ;
#23427=CARTESIAN_POINT ( 'NONE',  ( 0.1167790944451423257, 0.3930555554796889561, -0.2819296736111110424 ) ) ;
#23430=CARTESIAN_POINT ( 'NONE',  ( 1.864417095468034626E-17, 0.5918402777588108732, -0.3044824184027777880 ) ) ;
#23433=CARTESIAN_POINT ( 'NONE',  ( -6.528214817076446933E-07, 5.071585437816050757, 0.3119999999985565986 ) ) ;
#23435=CARTESIAN_POINT ( 'NONE',  ( -1.726321361862525858E-17, 4.630638888964754507, -0.2819296736111110979 ) ) ;
#23436=CARTESIAN_POINT ( 'NONE',  ( -0.1566809303765275552, 4.659511855693362570, -0.2728735228218804321 ) ) ;
#23437=CARTESIAN_POINT ( 'NONE',  ( -0.1167790944451423535, 3.863277777853643791, 0.2819296736111110424 ) ) ;
#23439=CARTESIAN_POINT ( 'NONE',  ( 0.2485560646891840364, 5.024144980645338876, 0.1929866496405842624 ) ) ;
#23441=CARTESIAN_POINT ( 'NONE',  ( -0.1292346314604056745, 4.213972222373954857, -0.3119999999999999996 ) ) ;
#23442=CARTESIAN_POINT ( 'NONE',  ( 5.178964085587577574E-17, 4.713972222298088433, 0.2819296736111110979 ) ) ;
#23445=CARTESIAN_POINT ( 'NONE',  ( 0.2819296736111110979, 4.099388888964754507, 0.1167790944451422425 ) ) ;
#23451=ADVANCED_FACE ( 'NONE', ( #803 ), #919, .T. ) ;
#23454=VERTEX_POINT ( 'NONE', #19572 ) ;
#23455=CARTESIAN_POINT ( 'NONE',  ( -0.1292346314604058410, 0.2159722220704893003, 0.3119999999999998885 ) ) ;
#23456=CARTESIAN_POINT ( 'NONE',  ( -0.01598815013341712762, 4.377598596822689814, -0.3116164386091518912 ) ) ;
#23458=CARTESIAN_POINT ( 'NONE',  ( -1.861236469537744314E-17, 5.143359825938298435, -0.3039629827691722741 ) ) ;
#23459=ORIENTED_EDGE ( 'NONE', *, *, #16976, .F. ) ;
#23460=CARTESIAN_POINT ( 'NONE',  ( 1.910449006669871087E-17, 0.2472222220704892726, -0.3119999999999999996 ) ) ;
#23461=CARTESIAN_POINT ( 'NONE',  ( 0.1167790944451423535, 0.08055555547968892838, 0.2819296736111110979 ) ) ;
#23463=ORIENTED_EDGE ( 'NONE', *, *, #4520, .T. ) ;
#23465=CARTESIAN_POINT ( 'NONE',  ( 0.2819296736111110424, 4.439666666742532186, -0.1167790944451423396 ) ) ;
#23466=CARTESIAN_POINT ( 'NONE',  ( 0.000000000000000000, 5.384999999999999787, 0.000000000000000000 ) ) ;
#23470=CARTESIAN_POINT ( 'NONE',  ( 5.731347020009612645E-17, 3.953555555555555046, 0.3119999999999999996 ) ) ;
#23471=CARTESIAN_POINT ( 'NONE',  ( -1.910449006669871087E-17, 5.154944444596176290, -0.3119999999999999996 ) ) ;
#23472=CARTESIAN_POINT ( 'NONE',  ( 0.3117034358253052972, 4.973992755114602815, 0.01468513461878798859 ) ) ;
#23474=ORIENTED_EDGE ( 'NONE', *, *, #5129, .T. ) ;
#23476=AXIS2_PLACEMENT_3D ( 'NONE', #4515, #19152, #13572 ) ;
#23485=CARTESIAN_POINT ( 'NONE',  ( 0.1167790944451422702, 5.071611111186976828, -0.2819296736111110424 ) ) ;
#23488=CARTESIAN_POINT ( 'NONE',  ( -0.04004678673780891901, 4.600547297044312423, -0.3095819090388297057 ) ) ;
#23491=CARTESIAN_POINT ( 'NONE',  ( 0.1292346314604056745, 0.5284722222222218990, -0.3119999999999999996 ) ) ;
#23492=CARTESIAN_POINT ( 'NONE',  ( -0.3119999999999999996, 4.713972222222221120, -0.1292346314604056468 ) ) ;
#23493=CARTESIAN_POINT ( 'NONE',  ( -0.1167790944451423535, 4.141055555631421470, 0.2819296736111110979 ) ) ;
#23495=CARTESIAN_POINT ( 'NONE',  ( 0.2819296736111110979, 3.835500000075866556, 0.1167790944451422425 ) ) ;
#23498=ORIENTED_EDGE ( 'NONE', *, *, #5798, .F. ) ;
#23500=CARTESIAN_POINT ( 'NONE',  ( 0.2819296736111110979, 4.436194444520309865, -3.452642723725051716E-17 ) ) ;
#23502=B_SPLINE_CURVE_WITH_KNOTS ( 'NONE', 3,
 ( #9207, #12890, #16648, #2727, #8325, #11766, #17128, #11524, #417, #4310, #13832, #8206, #10181, #22847, #11896, #22726, #19187, #18957, #6136, #2255, #17482, #17604, #894, #11646, #17248, #10058, #532, #19071, #15777, #21016, #19311, #7850, #7968, #15655, #774, #15299, #13484, #2496, #9935, #15419, #13603, #17364, #656, #9689, #20779, #8084 ),
 .UNSPECIFIED., .F., .F.,
 ( 4, 2, 2, 2, 2, 2, 2, 2, 2, 2, 2, 2, 2, 2, 2, 2, 2, 2, 2, 2, 2, 2, 4 ),
 ( 0.09082637236171775541, 0.09155946950567490916, 0.09229256664963206291, 0.09375876093754638430, 0.09522495522546070568, 0.09595805236941785943, 0.09669114951337501318, 0.09815734380128933456, 0.09962353808920364207, 0.1010897323771179634, 0.1018228295210751172, 0.1025559266650322848, 0.1032890238089894386, 0.1040221209529466062, 0.1054883152408609276, 0.1069545095287752490, 0.1084207038166895565, 0.1091538009606467241, 0.1098868981046038779, 0.1113530923925181854, 0.1128192866804325067, 0.1135523838243896605, 0.1142854809683468142 ),
 .UNSPECIFIED. ) ;
#23508=CARTESIAN_POINT ( 'NONE',  ( -0.2819296736111110979, 4.029944444520310753, -0.1167790944451422980 ) ) ;
#23510=CYLINDRICAL_SURFACE ( 'NONE', #11298, 0.3119999999999999996 ) ;
#23513=CARTESIAN_POINT ( 'NONE',  ( 0.2819296736111110979, -0.02013888896475552262, 0.000000000000000000 ) ) ;
#23521=CARTESIAN_POINT ( 'NONE',  ( 1.337745543335387199E-07, 4.460505239618372642, 0.3119999999999396589 ) ) ;
#23522=CARTESIAN_POINT ( 'NONE',  ( 0.1167790944451423535, 0.3583333332574666907, 0.2819296736111110424 ) ) ;
#23523=CARTESIAN_POINT ( 'NONE',  ( -1.726321361862525858E-17, 3.908416666742532630, -0.2819296736111110979 ) ) ;
#23526=CARTESIAN_POINT ( 'NONE',  ( -0.1167790944451423535, 4.654944444520310753, 0.2819296736111110424 ) ) ;
#23529=CARTESIAN_POINT ( 'NONE',  ( 0.3119999999999998885, 0.3965277776260449083, 0.1292346314604058410 ) ) ;
#23530=ORIENTED_EDGE ( 'NONE', *, *, #15276, .T. ) ;
#23531=CARTESIAN_POINT ( 'NONE',  ( 0.3119999999999999996, 4.022999999999998799, -3.820898013339742174E-17 ) ) ;
#23532=CARTESIAN_POINT ( 'NONE',  ( -0.1167790944451423535, 5.085500000075866112, 0.2819296736111110424 ) ) ;
#23535=CARTESIAN_POINT ( 'NONE',  ( 0.2644034564220129058, 4.191631208498491468, 0.1656346508680236751 ) ) ;
#23536=CARTESIAN_POINT ( 'NONE',  ( 0.1856355564575103978, 0.03242967361111056407, 0.2126852203547632825 ) ) ;
#23537=CARTESIAN_POINT ( 'NONE',  ( 0.1179581865186765804, 5.206640035683670398, 0.2566525738614713892 ) ) ;
#23539=CARTESIAN_POINT ( 'NONE',  ( -0.1993543840281266355, 4.915361111186976828, 0.1993543840281267465 ) ) ;
#23542=CARTESIAN_POINT ( 'NONE',  ( -0.3091666942010690144, 5.114568388431837143, -0.01160475953834872766 ) ) ;
#23543=CARTESIAN_POINT ( 'NONE',  ( -0.05196600641818320543, 4.570166421312822358, 0.3076424449429943642 ) ) ;
#23545=CARTESIAN_POINT ( 'NONE',  ( 0.2819296736111110424, 0.2124999999241334314, 0.1167790944451424923 ) ) ;
#23546=DIRECTION ( 'NONE',  ( 0.000000000000000000, 0.000000000000000000, -1.000000000000000000 ) ) ;
#23553=EDGE_CURVE ( 'NONE', #13418, #23454, #12078, .T. ) ;
#23555=CARTESIAN_POINT ( 'NONE',  ( 5.178964085587577574E-17, 4.769527777853643791, 0.2819296736111110979 ) ) ;
#23556=CARTESIAN_POINT ( 'NONE',  ( 0.08220319591558655770, 4.541475605104787761, -0.3014068057065943940 ) ) ;
#23557=CARTESIAN_POINT ( 'NONE',  ( 0.1167790944451422702, 3.835500000075866556, -0.2819296736111110424 ) ) ;
#23558=CARTESIAN_POINT ( 'NONE',  ( -0.1997126322592100711, 0.04726736168861581100, -0.2204034460251000083 ) ) ;
#23559=CARTESIAN_POINT ( 'NONE',  ( 0.2841435314273037527, 5.033717116179627915, -0.1288771532856403945 ) ) ;
#23561=CARTESIAN_POINT ( 'NONE',  ( 0.1296959877176626363, 5.072999999999997733, 0.2866706542028402693 ) ) ;
#23562=CARTESIAN_POINT ( 'NONE',  ( -0.008837736642443364682, 4.793618865691314568, 0.3119999992354540175 ) ) ;
#23564=CARTESIAN_POINT ( 'NONE',  ( -1.910449006669871087E-17, 4.321611111262843252, -0.3119999999999999996 ) ) ;
#23565=CARTESIAN_POINT ( 'NONE',  ( 0.1167790944451422702, 4.793833333409199149, -0.2819296736111110979 ) ) ;
#23567=CARTESIAN_POINT ( 'NONE',  ( -0.2819296736111110979, 3.741750000075865668, 0.000000000000000000 ) ) ;
#23568=ORIENTED_EDGE ( 'NONE', *, *, #4689, .T. ) ;
#23572=CARTESIAN_POINT ( 'NONE',  ( 0.000000000000000000, 5.384999999999999787, -0.3119999999999999996 ) ) ;
#23576=CARTESIAN_POINT ( 'NONE',  ( -0.2206173157302027954, 0.2541666665149337478, -0.2206173157302028232 ) ) ;
#23577=CARTESIAN_POINT ( 'NONE',  ( -0.2378982579381299922, 4.384836116680865814, -0.2019271802617891021 ) ) ;
#23582=CARTESIAN_POINT ( 'NONE',  ( -0.1993543840281266633, 0.2229166665908000333, -0.1993543840281266910 ) ) ;
#23585=CARTESIAN_POINT ( 'NONE',  ( -0.2819296736111110424, 4.404944444520309865, -0.1167790944451423119 ) ) ;
#23588=CARTESIAN_POINT ( 'NONE',  ( -0.01018560833394164394, 4.238034833529570555, 0.3119999986181690721 ) ) ;
#23589=CARTESIAN_POINT ( 'NONE',  ( -0.1292346314604056745, 4.095916666666666650, -0.3119999999999999996 ) ) ;
#23591=CARTESIAN_POINT ( 'NONE',  ( -1.910449006669871087E-17, 4.988277777929510215, -0.3119999999999999996 ) ) ;
#23601=EDGE_LOOP ( 'NONE', ( #13022, #5022, #15434, #6011, #10010 ) ) ;
#23602=CYLINDRICAL_SURFACE ( 'NONE', #18500, 0.3119999999999999996 ) ;
#23607=CARTESIAN_POINT ( 'NONE',  ( -0.1993543840281266633, 0.1256944443685777957, -0.1993543840281266910 ) ) ;
#23609=CARTESIAN_POINT ( 'NONE',  ( -1.726321361862525858E-17, 5.241750000075865223, -0.2819296736111110979 ) ) ;
#23611=ORIENTED_EDGE ( 'NONE', *, *, #5846, .F. ) ;
#23612=CARTESIAN_POINT ( 'NONE',  ( -0.01755531255181863592, 4.599896533210952931, -0.3115764429237145583 ) ) ;
#23614=CARTESIAN_POINT ( 'NONE',  ( 0.000000000000000000, 5.072999999999999510, 0.000000000000000000 ) ) ;
#23615=CARTESIAN_POINT ( 'NONE',  ( 0.09694982473845883963, 0.06249891840240667101, 0.2965547697865978938 ) ) ;
#23616=CARTESIAN_POINT ( 'NONE',  ( 0.3119999999999999996, 4.637583333333332725, -0.1292346314604056745 ) ) ;
#23618=CARTESIAN_POINT ( 'NONE',  ( 5.178964085587577574E-17, 4.033416666742532186, 0.2819296736111110979 ) ) ;
#23619=CARTESIAN_POINT ( 'NONE',  ( 0.1167790944451422702, 3.849388888964754951, -0.2819296736111110424 ) ) ;
#23621=LINE ( 'NONE', #3035, #4980 ) ;
#23623=ORIENTED_EDGE ( 'NONE', *, *, #20635, .T. ) ;
#23624=CARTESIAN_POINT ( 'NONE',  ( -0.2819296736111110424, 4.578555555631421470, 0.1167790944451424923 ) ) ;
#23625=CARTESIAN_POINT ( 'NONE',  ( -0.3062257137753721659, 4.500494688259138343, -0.05999501074661200278 ) ) ;
#23630=CARTESIAN_POINT ( 'NONE',  ( -0.1167790944451423535, 4.043833333409200037, 0.2819296736111110979 ) ) ;
#23631=CARTESIAN_POINT ( 'NONE',  ( -0.2451711420345534798, 4.829615264078582548, -0.1970397708553964233 ) ) ;
#23632=CARTESIAN_POINT ( 'NONE',  ( -0.3119999999999999996, 4.884111111111110404, 0.000000000000000000 ) ) ;
#23633=( BOUNDED_CURVE ( )  B_SPLINE_CURVE ( 2, ( #1213, #21568, #12690, #20108, #10373, #17797, #3398, #15963, #16090 ),
 .UNSPECIFIED., .F., .T. ) 
 B_SPLINE_CURVE_WITH_KNOTS ( ( 3, 2, 2, 2, 3 ),
 ( 0.9375000000000001110, 0.9419642857142856984, 0.9464285714285712858, 0.9508928571428568732, 0.9553571428571425717 ),
 .UNSPECIFIED. ) 
 CURVE ( )  GEOMETRIC_REPRESENTATION_ITEM ( )  RATIONAL_B_SPLINE_CURVE ( ( 0.9999999999999981126, 0.9238795325112886259, 1.000000000000000000, 0.9238795325112867385, 1.000000000000000000, 0.9238795325112867385, 1.000000000000000000, 0.9238795325112924006, 0.9999999999999943379 ) ) 
 REPRESENTATION_ITEM ( '' )  );
#23636=CARTESIAN_POINT ( 'NONE',  ( 0.1993543840281266910, -0.01319444452031107509, -0.1993543840281266910 ) ) ;
#23641=ORIENTED_EDGE ( 'NONE', *, *, #7113, .F. ) ;
#23644=CARTESIAN_POINT ( 'NONE',  ( -5.178964085587577574E-17, 0.4659722221463555858, 0.2819296736111110979 ) ) ;
#23645=CARTESIAN_POINT ( 'NONE',  ( 0.2819296736111110424, 3.786888888964754507, -0.1167790944451423396 ) ) ;
#23648=CARTESIAN_POINT ( 'NONE',  ( 0.1167790944451422702, 4.404944444520309865, -0.2819296736111110424 ) ) ;
#23654=CARTESIAN_POINT ( 'NONE',  ( -0.2819296736111110424, 5.189666666742532186, 0.1167790944451424923 ) ) ;
#23655=CARTESIAN_POINT ( 'NONE',  ( 0.1831843189501979052, 4.204970245508889093, -0.2534774667974905027 ) ) ;
#23658=CARTESIAN_POINT ( 'NONE',  ( -0.2819296736111110979, 4.960500000075865223, -0.1167790944451422980 ) ) ;
#23659=VERTEX_POINT ( 'NONE', #7854 ) ;
#23661=CARTESIAN_POINT ( 'NONE',  ( -0.07966684101420479225, 4.546095312717049808, -0.3042768302726782670 ) ) ;
#23663=CARTESIAN_POINT ( 'NONE',  ( -0.1993543840281267465, 0.3062499999241333759, 0.1993543840281266633 ) ) ;
#23667=CARTESIAN_POINT ( 'NONE',  ( -0.3125913837188149524, 4.724895613529112026, 0.01951433487545338810 ) ) ;
#23670=CARTESIAN_POINT ( 'NONE',  ( -0.3040973647138868752, 5.055585790322281170, -0.07619071978167928083 ) ) ;
#23671=CARTESIAN_POINT ( 'NONE',  ( 3.820898013339742174E-17, 5.384999999999999787, 0.3119999999999999996 ) ) ;
#23672=CARTESIAN_POINT ( 'NONE',  ( -0.2986281097515258720, 3.893695228114878226, 0.09285130349114770199 ) ) ;
#23674=CARTESIAN_POINT ( 'NONE',  ( -0.1993543840281266355, 4.429250000075866112, 0.1993543840281267465 ) ) ;
#23675=CARTESIAN_POINT ( 'NONE',  ( 0.06631022961668026072, 4.541938770673441539, -0.3053197120535988129 ) ) ;
#23676=CARTESIAN_POINT ( 'NONE',  ( -0.1167790944451423535, 5.154944444520309865, 0.2819296736111110424 ) ) ;
#23678=CARTESIAN_POINT ( 'NONE',  ( 0.01543252246473785644, 3.738736189315518210, 0.3120000007626770877 ) ) ;
#23681=B_SPLINE_CURVE_WITH_KNOTS ( 'NONE', 3,
 ( #13742, #10085, #22754, #7995, #4097, #22640 ),
 .UNSPECIFIED., .F., .F.,
 ( 4, 2, 4 ),
 ( 0.000000000000000000, 0.001246561431700771031, 0.002493122863401542495 ),
 .UNSPECIFIED. ) ;
#23682=CARTESIAN_POINT ( 'NONE',  ( -0.1292346314604057023, 4.345916666818399499, 0.3119999999999998885 ) ) ;
#23683=CARTESIAN_POINT ( 'NONE',  ( -0.2819296736111110979, 4.807722222298088433, -0.1167790944451422980 ) ) ;
#23684=CARTESIAN_POINT ( 'NONE',  ( 0.2819296736111110424, 3.773000000075866112, -0.1167790944451423396 ) ) ;
#23692=CARTESIAN_POINT ( 'NONE',  ( -0.3119999999999999996, 0.2576388887371560132, -0.1292346314604056745 ) ) ;
#23695=CARTESIAN_POINT ( 'NONE',  ( -0.2017922277526993935, 3.716746900542896359, -0.2379588540888969983 ) ) ;
#23696=CYLINDRICAL_SURFACE ( 'NONE', #13866, 0.3119999999999999996 ) ;
#23698=VERTEX_POINT ( 'NONE', #5904 ) ;
#23701=CARTESIAN_POINT ( 'NONE',  ( 0.1222830683586546147, 5.096320389118245586, -0.2862511053145868622 ) ) ;
#23702=CARTESIAN_POINT ( 'NONE',  ( 1.726321361862525858E-17, 0.2715277777019111660, -0.2819296736111110979 ) ) ;
#23705=CARTESIAN_POINT ( 'NONE',  ( -0.1993543840281266355, 4.470916666742532186, 0.1993543840281267465 ) ) ;
#23706=CYLINDRICAL_SURFACE ( 'NONE', #20800, 0.3119999999999999996 ) ;
#23708=CARTESIAN_POINT ( 'NONE',  ( -0.2206173157302028787, 0.3791666665149337478, 0.2206173157302027954 ) ) ;
#23709=CARTESIAN_POINT ( 'NONE',  ( 0.2206173157302027954, 4.029944444444443441, -0.2206173157302028232 ) ) ;
#23710=CARTESIAN_POINT ( 'NONE',  ( 0.3119999999999999996, 4.970916666818399499, 0.1292346314604056190 ) ) ;
#23711=CARTESIAN_POINT ( 'NONE',  ( -0.2206173157302028232, 4.154944444444443441, -0.2206173157302028232 ) ) ;
#23712=CARTESIAN_POINT ( 'NONE',  ( -0.3037986732609906926, 4.893462023975497566, 0.08195073769739492919 ) ) ;
#23717=B_SPLINE_CURVE_WITH_KNOTS ( 'NONE', 3,
 ( #7714, #20760, #4534, #15871, #10280, #8306, #4411, #8666, #21121, #1240, #876, #8183, #19648, #4651, #15759, #21246, #23289, #14049, #3069, #16116, #12120, #2822, #8552, #10039, #4892, #14166, #19528, #17826 ),
 .UNSPECIFIED., .F., .F.,
 ( 4, 2, 2, 2, 2, 2, 2, 2, 2, 2, 2, 2, 2, 4 ),
 ( 0.000000000000000000, 0.001089208970704103616, 0.002178417941408206365, 0.004356835882816414464, 0.005446044853520517863, 0.006535253824224622130, 0.007624462794928726396, 0.008713671765632828928, 0.009802880736336934062, 0.01089208970704103920, 0.01198129867774514606, 0.01307050764844925120, 0.01524892558985746667, 0.01742734353126568214 ),
 .UNSPECIFIED. ) ;
#23722=CARTESIAN_POINT ( 'NONE',  ( 0.2819296736111110979, 0.2194444443685778234, -0.1167790944451422980 ) ) ;
#23724=CARTESIAN_POINT ( 'NONE',  ( -0.1167790944451423535, 5.099388888964754507, 0.2819296736111110424 ) ) ;
#23725=CARTESIAN_POINT ( 'NONE',  ( 0.05028335205149757348, 4.486876821019038175, -0.3079317466717229612 ) ) ;
#23726=ORIENTED_EDGE ( 'NONE', *, *, #14552, .T. ) ;
#23727=CARTESIAN_POINT ( 'NONE',  ( 0.3120000000000000551, 3.852861111111110404, 0.1292346314604056190 ) ) ;
#23730=CARTESIAN_POINT ( 'NONE',  ( 0.2206173157302027676, 0.5597222220704892726, 0.2206173157302028787 ) ) ;
#23731=CARTESIAN_POINT ( 'NONE',  ( 0.2206173157302028787, 4.682722222222222008, 0.2206173157302027954 ) ) ;
#23733=CARTESIAN_POINT ( 'NONE',  ( -1.726321361862525858E-17, 4.061194444520309865, -0.2819296736111110979 ) ) ;
#23734=CARTESIAN_POINT ( 'NONE',  ( -0.2819296736111110424, 3.870222222298087988, 0.1167790944451424923 ) ) ;
#23738=CARTESIAN_POINT ( 'NONE',  ( 5.731347020009612645E-17, 4.564666666666665762, 0.3119999999999999996 ) ) ;
#23739=CARTESIAN_POINT ( 'NONE',  ( -0.1993543840281266355, 4.470916666742532186, 0.1993543840281267465 ) ) ;
#23740=CARTESIAN_POINT ( 'NONE',  ( -0.2715579528645996055, 4.506751968752040760, 0.1545152121325979455 ) ) ;
#23747=CARTESIAN_POINT ( 'NONE',  ( 0.1993543840281266633, 4.068138888964754507, -0.1993543840281266910 ) ) ;
#23750=CARTESIAN_POINT ( 'NONE',  ( 0.04962117880717522439, 5.160786044563907993, -0.2954202128566375540 ) ) ;
#23752=CARTESIAN_POINT ( 'NONE',  ( 0.3119999999999999996, 0.06666666651493373397, 0.000000000000000000 ) ) ;
#23754=CARTESIAN_POINT ( 'NONE',  ( -0.2819296736111110979, 0.3444444443685779067, 0.1167790944451422425 ) ) ;
#23763=CARTESIAN_POINT ( 'NONE',  ( 2.824051777240061223E-14, 3.849388889040854522, 0.3119999999999999996 ) ) ;
#23764=CARTESIAN_POINT ( 'NONE',  ( -5.731347020009612645E-17, 0.1152777777777774515, 0.3119999999999999996 ) ) ;
#23765=CARTESIAN_POINT ( 'NONE',  ( -0.2819296736111110424, 3.814666666742532630, 0.1167790944451424923 ) ) ;
#23767=CARTESIAN_POINT ( 'NONE',  ( 0.1167790944451424368, 4.328555555631420582, 0.2819296736111110424 ) ) ;
#23768=LINE ( 'NONE', #11230, #19387 ) ;
#23769=CARTESIAN_POINT ( 'NONE',  ( -0.3119999999999999996, 0.1499999998482670627, -3.820898013339742174E-17 ) ) ;
#23771=ORIENTED_EDGE ( 'NONE', *, *, #2023, .T. ) ;
#23772=CARTESIAN_POINT ( 'NONE',  ( 0.1292346314604070623, 4.679249999999999687, 0.3119999999999986673 ) ) ;
#23773=CARTESIAN_POINT ( 'NONE',  ( 0.1167790944451424368, 5.203555555631421470, 0.2819296736111110424 ) ) ;
#23774=CARTESIAN_POINT ( 'NONE',  ( 0.3011295810430658082, 4.199072593115692698, -0.08461153459480627581 ) ) ;
#23775=( BOUNDED_CURVE ( )  B_SPLINE_CURVE ( 2, ( #14531, #23890, #16715, #16239, #20012, #7209, #3423, #1478, #21723 ),
 .UNSPECIFIED., .F., .T. ) 
 B_SPLINE_CURVE_WITH_KNOTS ( ( 3, 2, 2, 2, 3 ),
 ( 0.5624999999999998890, 0.5669642857142855874, 0.5714285714285711748, 0.5758928571428568732, 0.5803571428571426827 ),
 .UNSPECIFIED. ) 
 CURVE ( )  GEOMETRIC_REPRESENTATION_ITEM ( )  RATIONAL_B_SPLINE_CURVE ( ( 1.000000000000001998, 0.9238795325112848511, 1.000000000000000000, 0.9238795325112867385, 1.000000000000000000, 0.9238795325112867385, 1.000000000000000000, 0.9238795325112905132, 0.9999999999999962252 ) ) 
 REPRESENTATION_ITEM ( '' )  );
#23777=( BOUNDED_CURVE ( )  B_SPLINE_CURVE ( 2, ( #8563, #10525, #1249, #12483, #19902, #3311, #12132, #3191, #10639 ),
 .UNSPECIFIED., .F., .T. ) 
 B_SPLINE_CURVE_WITH_KNOTS ( ( 3, 2, 2, 2, 3 ),
 ( 0.4375000000000000000, 0.4479166666666666852, 0.4583333333333333148, 0.4687500000000000000, 0.4791666666666666852 ),
 .UNSPECIFIED. ) 
 CURVE ( )  GEOMETRIC_REPRESENTATION_ITEM ( )  RATIONAL_B_SPLINE_CURVE ( ( 1.000000000000000000, 0.9238795325112867385, 1.000000000000000000, 0.9238795325112867385, 1.000000000000000000, 0.9238795325112867385, 1.000000000000000000, 0.9238795325112867385, 1.000000000000000000 ) ) 
 REPRESENTATION_ITEM ( '' )  );
#23778=CARTESIAN_POINT ( 'NONE',  ( 0.2819296736111110979, 4.880638888964754507, -3.452642723725051716E-17 ) ) ;
#23781=CARTESIAN_POINT ( 'NONE',  ( -0.1549220363945191525, 4.066990437257307356, 0.2708196028344186379 ) ) ;
#23782=CARTESIAN_POINT ( 'NONE',  ( 0.3119999999999999996, 4.911888888888888083, -3.820898013339742174E-17 ) ) ;
#23783=ORIENTED_EDGE ( 'NONE', *, *, #6893, .T. ) ;
#23784=CARTESIAN_POINT ( 'NONE',  ( -0.1993543840281266633, 0.2923611110352444808, -0.1993543840281266910 ) ) ;
#23787=CARTESIAN_POINT ( 'NONE',  ( -0.1167790944451424368, 0.03194444436857781650, 0.2819296736111110424 ) ) ;
#23795=CARTESIAN_POINT ( 'NONE',  ( -0.1993543840281266355, 4.595916666742532186, 0.1993543840281267465 ) ) ;
#23797=CARTESIAN_POINT ( 'NONE',  ( -5.731347020009612645E-17, 0.2749999998482670627, 0.3119999999999999996 ) ) ;
#23798=CARTESIAN_POINT ( 'NONE',  ( 0.1167790944451424368, 4.995222222298087544, 0.2819296736111110424 ) ) ;
#23800=CARTESIAN_POINT ( 'NONE',  ( 0.2911863994614913853, 3.755533081060165923, -0.1151799365104299866 ) ) ;
#23803=CARTESIAN_POINT ( 'NONE',  ( -0.1292346314604056745, 4.269527777929510215, -0.3119999999999999996 ) ) ;
#23804=CARTESIAN_POINT ( 'NONE',  ( -0.2819296736111110979, 4.585500000075865223, -0.1167790944451422980 ) ) ;
#23805=CARTESIAN_POINT ( 'NONE',  ( -0.1167790944451423257, 3.786888888964754063, -0.2819296736111110424 ) ) ;
#23806=VERTEX_POINT ( 'NONE', #6140 ) ;
#23811=EDGE_CURVE ( 'NONE', #2014, #17381, #9451, .T. ) ;
#23812=CARTESIAN_POINT ( 'NONE',  ( -0.08150439437264625497, 4.958142549569055646, 0.3039118706599210351 ) ) ;
#23815=CARTESIAN_POINT ( 'NONE',  ( -0.3119999999999999996, 0.2645833331816004330, 0.1292346314604056190 ) ) ;
#23816=CARTESIAN_POINT ( 'NONE',  ( -0.2346756888474252623, 4.397428374997647715, 0.2066071494487769222 ) ) ;
#23817=CARTESIAN_POINT ( 'NONE',  ( -0.2009661027989112503, 3.716715306565030019, -0.2386561446537507347 ) ) ;
#23818=CARTESIAN_POINT ( 'NONE',  ( -5.731347020009612645E-17, 0.2819444444444441089, 0.3119999999999999996 ) ) ;
#23824=CARTESIAN_POINT ( 'NONE',  ( 0.06994230879797320999, 5.073571722091643643, 0.3046847899301766138 ) ) ;
#23826=CARTESIAN_POINT ( 'NONE',  ( -0.1993543840281266910, 4.123694444520309865, -0.1993543840281266910 ) ) ;
#23827=CARTESIAN_POINT ( 'NONE',  ( -0.1993543840281266910, 5.012583333409199149, -0.1993543840281266910 ) ) ;
#23829=CARTESIAN_POINT ( 'NONE',  ( -0.3085935790486541430, 4.225662198787177637, 0.04598119064307899101 ) ) ;
#23830=CARTESIAN_POINT ( 'NONE',  ( -0.2206173157302027676, 4.168833333333332725, 0.2206173157302028787 ) ) ;
#23831=CARTESIAN_POINT ( 'NONE',  ( -0.1292346314604056745, 5.047305555707287894, -0.3119999999999999996 ) ) ;
#23833=CARTESIAN_POINT ( 'NONE',  ( -0.1993543840281266910, 5.082027777853643791, -0.1993543840281266910 ) ) ;
#23834=CARTESIAN_POINT ( 'NONE',  ( -1.910449006669871087E-17, 4.147999999999998799, -0.3119999999999999996 ) ) ;
#23836=CARTESIAN_POINT ( 'NONE',  ( -0.07783884650168826358, 0.05932970560135347043, 0.2990238257868908511 ) ) ;
#23844=CARTESIAN_POINT ( 'NONE',  ( -5.178964085587577574E-17, 0.2576388888130222155, 0.2819296736111110979 ) ) ;
#23846=CARTESIAN_POINT ( 'NONE',  ( 0.1993543840281266633, 5.123694444520309865, -0.1993543840281266910 ) ) ;
#23847=CARTESIAN_POINT ( 'NONE',  ( 0.05305093651153936635, 4.486802096876033374, -0.3074566729606528215 ) ) ;
#23849=CARTESIAN_POINT ( 'NONE',  ( -1.726321361862525858E-17, 4.783416666742532186, -0.2819296736111110979 ) ) ;
#23853=CARTESIAN_POINT ( 'NONE',  ( 0.2206173157302028787, 4.071611111111110404, 0.2206173157302027954 ) ) ;
#23855=CARTESIAN_POINT ( 'NONE',  ( -0.3119999999999998885, 4.665361111111110404, 0.1292346314604058410 ) ) ;
#23856=CARTESIAN_POINT ( 'NONE',  ( -0.1167790944451423119, 4.009111111186976828, -0.2819296736111110979 ) ) ;
#23857=CARTESIAN_POINT ( 'NONE',  ( -0.2819296736111110979, 3.866750000075866112, 0.000000000000000000 ) ) ;
#23858=CARTESIAN_POINT ( 'NONE',  ( 0.2904387420176882117, 4.033251672939094590, -0.1141962754506169742 ) ) ;
#23861=CARTESIAN_POINT ( 'NONE',  ( -1.910449006669871087E-17, 3.925777777777776922, -0.3119999999999999996 ) ) ;
#23863=CARTESIAN_POINT ( 'NONE',  ( -0.1993543840281266355, 4.359805555631421470, 0.1993543840281267465 ) ) ;
#23866=CARTESIAN_POINT ( 'NONE',  ( -0.2830962153688056371, 4.498198518508631949, -0.1381818899629860820 ) ) ;
#23869=CARTESIAN_POINT ( 'NONE',  ( -0.1571291514452808069, 3.955868408054724394, 0.2726213375442139708 ) ) ;
#23870=CARTESIAN_POINT ( 'NONE',  ( -0.1571085868019625187, 4.455918294536927782, 0.2726333643457281020 ) ) ;
#23871=CARTESIAN_POINT ( 'NONE',  ( 0.1292346314604056745, 0.07708333318160039138, -0.3119999999999999996 ) ) ;
#23873=CARTESIAN_POINT ( 'NONE',  ( -0.2819296736111110424, 0.1708333332574666907, -0.1167790944451423396 ) ) ;
#23874=CARTESIAN_POINT ( 'NONE',  ( 0.0001582775150950677980, 3.877162414149467828, -0.3119999700502704143 ) ) ;
#23875=CARTESIAN_POINT ( 'NONE',  ( 0.3119999999999999996, 0.5770833333333330595, -0.1292346314604056468 ) ) ;
#23879=ORIENTED_EDGE ( 'NONE', *, *, #12017, .T. ) ;
#23881=CARTESIAN_POINT ( 'NONE',  ( 6.388359114324787822E-07, 4.627192232271967853, 0.3119999999985919592 ) ) ;
#23883=CARTESIAN_POINT ( 'NONE',  ( -0.3119999999999999996, -0.01319444444444478094, -0.1292346314604056745 ) ) ;
#23885=CARTESIAN_POINT ( 'NONE',  ( 5.178964085587577574E-17, 3.825083333409199149, 0.2819296736111110979 ) ) ;
#23888=CARTESIAN_POINT ( 'NONE',  ( -0.1167790944451423535, 4.432722222298088433, 0.2819296736111110424 ) ) ;
#23890=CARTESIAN_POINT ( 'NONE',  ( -0.1292346314604032875, 4.394527777777778255, 0.3120000000000023865 ) ) ;
#23892=CARTESIAN_POINT ( 'NONE',  ( 1.364852645245658621E-07, 4.377166663151471404, -0.3119999999999701346 ) ) ;
#23893=CARTESIAN_POINT ( 'NONE',  ( -0.1167790944451423535, 5.141055555631421470, 0.2819296736111110424 ) ) ;
#23894=EDGE_CURVE ( 'NONE', #11233, #4444, #5130, .T. ) ;
#23895=CARTESIAN_POINT ( 'NONE',  ( 0.2345140992797901391, 4.203002459309779226, -0.2057879445052058498 ) ) ;
#23899=CARTESIAN_POINT ( 'NONE',  ( -0.1993543840281266910, 4.734805555631420582, -0.1993543840281266910 ) ) ;
#23901=CARTESIAN_POINT ( 'NONE',  ( 5.574357792518489764E-07, 4.071633398088104094, 0.3119999999989289674 ) ) ;
#23903=CARTESIAN_POINT ( 'NONE',  ( 0.1292346314604027324, 4.901472222222221120, 0.3120000000000029972 ) ) ;
#23905=CARTESIAN_POINT ( 'NONE',  ( 0.1167790944451423257, 0.2263888888130222710, -0.2819296736111110424 ) ) ;
#23906=ORIENTED_EDGE ( 'NONE', *, *, #22448, .F. ) ;
#23907=CARTESIAN_POINT ( 'NONE',  ( -5.178964085587577574E-17, 0.1465277777019111383, 0.2819296736111110979 ) ) ;
#23908=CARTESIAN_POINT ( 'NONE',  ( 5.731347020009612645E-17, 4.342444444444443441, 0.3119999999999999996 ) ) ;
#23909=CARTESIAN_POINT ( 'NONE',  ( -0.2705232885797667075, 5.199178293702563458, -0.09182951230709678059 ) ) ;
#23913=CARTESIAN_POINT ( 'NONE',  ( -0.3073899478517820305, 3.889436215408048625, -0.05583288564120540698 ) ) ;
#23914=CARTESIAN_POINT ( 'NONE',  ( 1.726321361862525858E-17, 0.1048611110352444808, -0.2819296736111110979 ) ) ;
#23915=EDGE_CURVE ( 'NONE', #7560, #21247, #14327, .T. ) ;
#23916=ADVANCED_FACE ( 'NONE', ( #20380 ), #21961, .T. ) ;
#23917=CARTESIAN_POINT ( 'NONE',  ( -0.1167790944451423535, 4.543833333409199149, 0.2819296736111110424 ) ) ;
#23919=CARTESIAN_POINT ( 'NONE',  ( 7.284403261834130553E-05, 4.543831265541522946, -0.3120000004383560732 ) ) ;
#23921=CARTESIAN_POINT ( 'NONE',  ( 0.2819296736111110424, 5.120222222298088433, -0.1167790944451423396 ) ) ;
#23923=CARTESIAN_POINT ( 'NONE',  ( 0.1916526620523836544, 4.910811664053455594, 0.2495586235085527904 ) ) ;
#23926=CARTESIAN_POINT ( 'NONE',  ( -0.3119999999999999996, 4.224388889040620931, 0.000000000000000000 ) ) ;
#23928=CARTESIAN_POINT ( 'NONE',  ( 0.2819296736111110979, 4.505638888964754507, -3.452642723725051716E-17 ) ) ;
#23929=( BOUNDED_CURVE ( )  B_SPLINE_CURVE ( 2, ( #13164, #23984, #3755, #22040, #7652, #5816, #23853, #7172, #5335 ),
 .UNSPECIFIED., .F., .T. ) 
 B_SPLINE_CURVE_WITH_KNOTS ( ( 3, 2, 2, 2, 3 ),
 ( 0.7589285714285712858, 0.7633928571428570953, 0.7678571428571430157, 0.7723214285714287142, 0.7767857142857145236 ),
 .UNSPECIFIED. ) 
 CURVE ( )  GEOMETRIC_REPRESENTATION_ITEM ( )  RATIONAL_B_SPLINE_CURVE ( ( 1.000000000000001998, 0.9238795325112848511, 1.000000000000000000, 0.9238795325112867385, 1.000000000000000000, 0.9238795325112867385, 1.000000000000000000, 0.9238795325112829637, 1.000000000000003775 ) ) 
 REPRESENTATION_ITEM ( '' )  );
#23932=CARTESIAN_POINT ( 'NONE',  ( 0.2819296736111110979, 3.880638888964754063, -3.452642723725051716E-17 ) ) ;
#23939=CARTESIAN_POINT ( 'NONE',  ( -0.3119332791068817889, 4.947851738477909045, 0.04138887372432151907 ) ) ;
#23942=CARTESIAN_POINT ( 'NONE',  ( -0.1292346314604058410, 0.3270833331816004330, 0.3119999999999998885 ) ) ;
#23944=CARTESIAN_POINT ( 'NONE',  ( -0.3148642296646037009, 3.724867759073636542, 0.01804088196266112956 ) ) ;
#23951=ORIENTED_EDGE ( 'NONE', *, *, #9831, .F. ) ;
#23952=CARTESIAN_POINT ( 'NONE',  ( 0.1756681423353473881, 5.076946340042797878, 0.2579994535246159515 ) ) ;
#23954=CARTESIAN_POINT ( 'NONE',  ( -0.1167790944451423535, 4.307722222298088433, 0.2819296736111110424 ) ) ;
#23955=CARTESIAN_POINT ( 'NONE',  ( -0.2819296736111110424, 5.189666666742532186, 0.1167790944451424923 ) ) ;
#23957=CARTESIAN_POINT ( 'NONE',  ( 6.089848770316828444E-07, 4.238302053322364316, 0.3119999999987258521 ) ) ;
#23958=CARTESIAN_POINT ( 'NONE',  ( 0.3119999999999999996, 3.859805555555555046, -0.1292346314604056745 ) ) ;
#23960=CARTESIAN_POINT ( 'NONE',  ( -1.910449006669871087E-17, 5.043833333485064685, -0.3119999999999999996 ) ) ;
#23962=ADVANCED_FACE ( 'NONE', ( #14662 ), #11240, .T. ) ;
#23963=CARTESIAN_POINT ( 'NONE',  ( 0.1993543840281267465, 5.165361111186976828, 0.1993543840281266633 ) ) ;
#23970=CARTESIAN_POINT ( 'NONE',  ( -0.2819296736111110424, 5.016055555631420582, -0.1167790944451423119 ) ) ;
#23971=ORIENTED_EDGE ( 'NONE', *, *, #4587, .F. ) ;
#23974=ORIENTED_EDGE ( 'NONE', *, *, #8701, .F. ) ;
#23975=CARTESIAN_POINT ( 'NONE',  ( -0.1167790944451422702, 0.3444444443685777402, -0.2819296736111110979 ) ) ;
#23977=CARTESIAN_POINT ( 'NONE',  ( -0.2819296736111110979, 4.922305555631420582, 0.000000000000000000 ) ) ;
#23978=CARTESIAN_POINT ( 'NONE',  ( 0.3051180496388954388, 4.472561363414810032, 0.06516940886235408903 ) ) ;
#23980=CARTESIAN_POINT ( 'NONE',  ( -0.1167790944451423257, 4.898000000075866112, -0.2819296736111110424 ) ) ;
#23981=CARTESIAN_POINT ( 'NONE',  ( -0.1568318157528670875, 4.159500745689967971, -0.2727933530271318130 ) ) ;
#23984=CARTESIAN_POINT ( 'NONE',  ( 0.1292346314604031765, 4.088972222222221120, -0.3120000000000024420 ) ) ;
#23985=CARTESIAN_POINT ( 'NONE',  ( 1.910449006669871087E-17, 0.5874999999999996891, -0.3119999999999999996 ) ) ;
#23986=CARTESIAN_POINT ( 'NONE',  ( 0.2206173157302028787, 4.738277777777777366, 0.2206173157302027954 ) ) ;
#23987=CARTESIAN_POINT ( 'NONE',  ( 0.2819296736111110979, 4.047305555631421470, -3.452642723725051716E-17 ) ) ;
#23988=CARTESIAN_POINT ( 'NONE',  ( 1.910449006669871087E-17, 0.1986111111111107386, -0.3119999999999999996 ) ) ;
#23989=CARTESIAN_POINT ( 'NONE',  ( 0.1819161012131308708, 4.021594027790507120, 0.2535283937084970574 ) ) ;
#23992=VECTOR ( 'NONE', #8444, 39.37007874015748143 ) ;
#23993=CARTESIAN_POINT ( 'NONE',  ( -2.266361716303445225E-16, 4.432722222374099630, -0.3119999999999999996 ) ) ;
#23999=CARTESIAN_POINT ( 'NONE',  ( -0.1005340957006147506, 4.435645067432016475, -0.2960640309988838981 ) ) ;
#24002=CARTESIAN_POINT ( 'NONE',  ( -0.1167790944451422702, 0.2749999999241333204, -0.2819296736111110424 ) ) ;
#24003=CARTESIAN_POINT ( 'NONE',  ( 0.0003178160707640876313, 3.877158127254288544, -0.3119998483270248202 ) ) ;
#24004=LINE ( 'NONE', #7316, #20524 ) ;
#24006=CYLINDRICAL_SURFACE ( 'NONE', #8977, 0.3119999999999999996 ) ;
#24011=CARTESIAN_POINT ( 'NONE',  ( -0.04071097728432398338, 5.093190941573745967, -0.3088414402879665066 ) ) ;
#24013=CARTESIAN_POINT ( 'NONE',  ( -5.731347020009612645E-17, 0.004166666666666329205, 0.3119999999999999996 ) ) ;
#24014=CARTESIAN_POINT ( 'NONE',  ( 0.2819296736111110979, 3.779944444520310309, 0.1167790944451422425 ) ) ;
#24016=CARTESIAN_POINT ( 'NONE',  ( 0.1167790944451422702, 4.460500000075867000, -0.2819296736111110424 ) ) ;
#24017=CARTESIAN_POINT ( 'NONE',  ( 0.3119999999999999996, 4.970916666666665762, -0.1292346314604056745 ) ) ;
#24020=CARTESIAN_POINT ( 'NONE',  ( 0.08156453417730161193, 4.351642364793766760, 0.3038997693205980899 ) ) ;
#24021=CARTESIAN_POINT ( 'NONE',  ( 0.1167790944451424368, 5.036888888964754507, 0.2819296736111110424 ) ) ;
#24022=CARTESIAN_POINT ( 'NONE',  ( -0.04912707777265164222, 5.144593440471582291, -0.2998369709411419781 ) ) ;
#24026=CARTESIAN_POINT ( 'NONE',  ( 0.2819296736111110979, 4.658416666742532186, -3.452642723725051716E-17 ) ) ;
#24029=CARTESIAN_POINT ( 'NONE',  ( -0.1292346314604056190, 0.4173611109593781676, -0.3119999999999999996 ) ) ;
#24030=CARTESIAN_POINT ( 'NONE',  ( -0.2819296736111110424, 0.4624999999241333759, -0.1167790944451423396 ) ) ;
#24033=CARTESIAN_POINT ( 'NONE',  ( -0.1167790944451422702, 0.1777777777019111383, -0.2819296736111110424 ) ) ;
#24040=CARTESIAN_POINT ( 'NONE',  ( -0.05856351884197068952, 3.878803041371024385, -0.3066960576329920696 ) ) ;
#24042=CARTESIAN_POINT ( 'NONE',  ( 0.2819296736111110424, 4.509111111186976828, -0.1167790944451423396 ) ) ;
#24045=CARTESIAN_POINT ( 'NONE',  ( -0.3120000000000000551, 0.2645833331816004330, 0.1292346314604056190 ) ) ;
#24046=CARTESIAN_POINT ( 'NONE',  ( 0.2819296736111110979, 5.172305555631421470, -3.452642723725051716E-17 ) ) ;
#24047=CARTESIAN_POINT ( 'NONE',  ( -0.1167790944451423535, 4.363277777853642903, 0.2819296736111110979 ) ) ;
#24048=CARTESIAN_POINT ( 'NONE',  ( 0.04921115518204333128, 3.764677272939175090, -0.3083034729010514785 ) ) ;
#24051=CARTESIAN_POINT ( 'NONE',  ( 0.1292346314604056190, 4.151472222373953969, -0.3119999999999999996 ) ) ;
#24052=CARTESIAN_POINT ( 'NONE',  ( 0.2819296736111110979, 4.450083333409199149, -3.452642723725051716E-17 ) ) ;
#24053=CARTESIAN_POINT ( 'NONE',  ( 0.1993543840281266633, 3.887583333409198705, -0.1993543840281266910 ) ) ;
#24060=LINE ( 'NONE', #23572, #4862 ) ;
#24061=DIRECTION ( 'NONE',  ( -0.000000000000000000, -1.000000000000000000, -0.000000000000000000 ) ) ;
#24063=CARTESIAN_POINT ( 'NONE',  ( -0.1292346314604058410, 0.5493055554038226429, 0.3119999999999998885 ) ) ;
#24067=CARTESIAN_POINT ( 'NONE',  ( -0.2206173157302028787, 0.4972222222222218435, 0.2206173157302027954 ) ) ;
#24072=ORIENTED_EDGE ( 'NONE', *, *, #23811, .F. ) ;
#24073=CARTESIAN_POINT ( 'NONE',  ( 0.07683745418995416299, 5.097786225156845319, -0.3020026545442724419 ) ) ;
#24075=CARTESIAN_POINT ( 'NONE',  ( 0.2819296736111110979, 4.266055555631421470, 0.1167790944451422425 ) ) ;
#24076=CARTESIAN_POINT ( 'NONE',  ( -0.1993543840281266910, 5.068138888964754507, -0.1993543840281266910 ) ) ;
#24079=CARTESIAN_POINT ( 'NONE',  ( -0.1292346314604056190, 0.3618055554038226429, -0.3119999999999999996 ) ) ;
#24080=CARTESIAN_POINT ( 'NONE',  ( -0.1292346314604056745, 3.873694444444442997, -0.3119999999999999996 ) ) ;
#24082=CARTESIAN_POINT ( 'NONE',  ( -0.2206173157302028232, 4.884111111262843252, -0.2206173157302028232 ) ) ;
#24083=CARTESIAN_POINT ( 'NONE',  ( 0.3107418214344630503, 4.806955620829070241, 0.02800764279169619744 ) ) ;
#24084=EDGE_CURVE ( 'NONE', #10770, #8566, #20644, .T. ) ;
#24085=CARTESIAN_POINT ( 'NONE',  ( 0.3119999999999999996, 4.856333333333332725, -3.820898013339742174E-17 ) ) ;
#24087=CARTESIAN_POINT ( 'NONE',  ( 0.2461656082887962727, 0.03739867468129062789, -0.1491120642768181681 ) ) ;
#24090=CARTESIAN_POINT ( 'NONE',  ( 0.1167790944451422702, 5.113277777853642903, -0.2819296736111110424 ) ) ;
#24094=EDGE_CURVE ( 'NONE', #606, #4893, #15283, .T. ) ;
#24097=CARTESIAN_POINT ( 'NONE',  ( -0.1167790944451422702, 0.2888888888130222710, -0.2819296736111110979 ) ) ;
#24099=CARTESIAN_POINT ( 'NONE',  ( 0.1167790944451424368, 4.884111111186977716, 0.2819296736111110424 ) ) ;
#24101=CARTESIAN_POINT ( 'NONE',  ( -0.2819296736111110424, 4.904944444520310753, -0.1167790944451423119 ) ) ;
#24103=CARTESIAN_POINT ( 'NONE',  ( -0.2206173157302027676, 5.057722222222222008, 0.2206173157302028787 ) ) ;
#24106=CARTESIAN_POINT ( 'NONE',  ( -0.3119999999999999996, 4.606333333333332725, 0.000000000000000000 ) ) ;
#24107=CARTESIAN_POINT ( 'NONE',  ( -0.1167790944451423535, 3.974388888964754063, 0.2819296736111110979 ) ) ;
#24108=CARTESIAN_POINT ( 'NONE',  ( 1.910449006669871087E-17, 0.1430555555555552139, -0.3119999999999999996 ) ) ;
#24109=CARTESIAN_POINT ( 'NONE',  ( 0.2954588070498663788, 4.032821911431771156, -0.1002473225235935156 ) ) ;
#24110=CARTESIAN_POINT ( 'NONE',  ( 0.3119999999999999996, 4.415361111111110404, -0.1292346314604056745 ) ) ;
#24113=CARTESIAN_POINT ( 'NONE',  ( -0.1724646555813178495, 4.121954259501087847, 0.2600007236767823415 ) ) ;
#24114=CARTESIAN_POINT ( 'NONE',  ( 0.02148743539037334394, 4.654328078246623868, -0.3113644187995892598 ) ) ;
#24119=CARTESIAN_POINT ( 'NONE',  ( 0.1993543840281266355, 0.1951388888130222155, 0.1993543840281267465 ) ) ;
#24121=CARTESIAN_POINT ( 'NONE',  ( 0.1292346314604056745, 0.5840277777777772572, -0.3119999999999999996 ) ) ;
#24124=CARTESIAN_POINT ( 'NONE',  ( -0.1376149012345692091, 5.096011253522892304, -0.2798126666846854627 ) ) ;
#24126=CARTESIAN_POINT ( 'NONE',  ( -0.3119999999999999996, 0.04236111111111078020, -0.1292346314604056745 ) ) ;
#24127=CARTESIAN_POINT ( 'NONE',  ( 0.2206173157302027954, 5.252166666666665762, -0.2206173157302028232 ) ) ;
#24128=AXIS2_PLACEMENT_3D ( 'NONE', #5727, #12948, #13186 ) ;
#24159=COLOUR_RGB('Slate Gray', 0.72549020, 0.75294118, 0.79215686);
#24160=FILL_AREA_STYLE_COLOUR('',#24159);
#24161=FILL_AREA_STYLE('',(#24160));
#24162=SURFACE_STYLE_FILL_AREA(#24161);
#24163=SURFACE_SIDE_STYLE('',(#24162));
#24164=SURFACE_STYLE_USAGE(.BOTH.,#24163);
#24165=PRESENTATION_STYLE_ASSIGNMENT((#24164));
#24188=STYLED_ITEM('',(#24165),#1448);
#24189=MECHANICAL_DESIGN_GEOMETRIC_PRESENTATION_REPRESENTATION('',(#24188),#15765);
ENDSEC;
END-ISO-10303-21;
